ISO-10303-21;
HEADER;
/* Generated by software containing ST-Developer
 * from STEP Tools, Inc. (www.steptools.com) 
 */

FILE_DESCRIPTION(
/* description */ (''),
/* implementation_level */ '2;1');

FILE_NAME(
/* name */ 'Screw_02.step',
/* time_stamp */ '2026-10-05T00:14:20-07:00',
/* author */ (''),
/* organization */ (''),
/* preprocessor_version */ 'ST-DEVELOPER v20.2',
/* originating_system */ 'Autodesk Translation Framework v15.15.0.0',
/* authorisation */ '');

FILE_SCHEMA (('AUTOMOTIVE_DESIGN { 1 0 10303 214 3 1 1 }'));
ENDSEC;

DATA;
#10=MECHANICAL_DESIGN_GEOMETRIC_PRESENTATION_REPRESENTATION('',(#3377),#75336);
#45=(
BOUNDED_SURFACE()
B_SPLINE_SURFACE(1,2,((#63743,#63744,#63745,#63746,#63747,#63748,#63749,
#63750,#63751,#63752,#63753,#63754,#63755,#63756,#63757,#63758,#63759,#63760,
#63761,#63762,#63763,#63764,#63765,#63766,#63767,#63768,#63769,#63770,#63771,
#63772,#63773,#63774,#63775,#63776,#63777,#63778,#63779,#63780,#63781,#63782,
#63783,#63784,#63785,#63786,#63787,#63788,#63789,#63790,#63791,#63792,#63793,
#63794,#63795,#63796,#63797,#63798,#63799,#63800,#63801,#63802,#63803,#63804,
#63805,#63806,#63807,#63808,#63809,#63810,#63811,#63812,#63813,#63814,#63815,
#63816,#63817,#63818,#63819,#63820,#63821,#63822,#63823,#63824,#63825,#63826,
#63827,#63828,#63829,#63830,#63831,#63832,#63833,#63834,#63835,#63836,#63837,
#63838,#63839,#63840,#63841,#63842,#63843,#63844,#63845,#63846,#63847,#63848,
#63849,#63850,#63851,#63852,#63853,#63854,#63855,#63856,#63857,#63858,#63859,
#63860,#63861,#63862,#63863,#63864,#63865,#63866,#63867,#63868,#63869,#63870,
#63871,#63872,#63873,#63874,#63875,#63876,#63877,#63878,#63879,#63880,#63881,
#63882,#63883,#63884,#63885,#63886,#63887,#63888,#63889,#63890,#63891,#63892,
#63893,#63894,#63895,#63896,#63897,#63898,#63899,#63900,#63901,#63902,#63903,
#63904,#63905,#63906,#63907,#63908,#63909,#63910,#63911,#63912,#63913,#63914,
#63915,#63916,#63917,#63918,#63919,#63920,#63921,#63922,#63923,#63924,#63925,
#63926,#63927,#63928,#63929,#63930,#63931,#63932,#63933,#63934,#63935,#63936,
#63937,#63938,#63939,#63940,#63941,#63942,#63943,#63944,#63945,#63946,#63947,
#63948,#63949,#63950,#63951,#63952,#63953,#63954,#63955,#63956,#63957,#63958,
#63959,#63960,#63961,#63962,#63963,#63964,#63965,#63966,#63967,#63968,#63969,
#63970,#63971,#63972,#63973,#63974,#63975,#63976,#63977,#63978,#63979,#63980,
#63981,#63982,#63983,#63984,#63985,#63986,#63987,#63988,#63989,#63990,#63991,
#63992,#63993,#63994,#63995,#63996,#63997,#63998,#63999,#64000,#64001,#64002,
#64003,#64004,#64005,#64006,#64007,#64008,#64009,#64010,#64011,#64012,#64013,
#64014,#64015,#64016,#64017,#64018,#64019,#64020,#64021,#64022,#64023,#64024,
#64025,#64026,#64027,#64028,#64029,#64030,#64031,#64032,#64033,#64034,#64035,
#64036,#64037,#64038,#64039,#64040,#64041,#64042,#64043,#64044,#64045,#64046,
#64047,#64048,#64049,#64050,#64051,#64052,#64053,#64054,#64055,#64056,#64057,
#64058,#64059,#64060,#64061,#64062,#64063,#64064,#64065,#64066,#64067,#64068,
#64069,#64070,#64071,#64072,#64073,#64074,#64075,#64076,#64077,#64078,#64079,
#64080,#64081,#64082,#64083,#64084,#64085,#64086,#64087,#64088,#64089,#64090,
#64091,#64092,#64093,#64094,#64095,#64096,#64097,#64098,#64099,#64100,#64101,
#64102,#64103,#64104,#64105,#64106,#64107,#64108,#64109,#64110,#64111,#64112,
#64113,#64114,#64115),(#64116,#64117,#64118,#64119,#64120,#64121,#64122,
#64123,#64124,#64125,#64126,#64127,#64128,#64129,#64130,#64131,#64132,#64133,
#64134,#64135,#64136,#64137,#64138,#64139,#64140,#64141,#64142,#64143,#64144,
#64145,#64146,#64147,#64148,#64149,#64150,#64151,#64152,#64153,#64154,#64155,
#64156,#64157,#64158,#64159,#64160,#64161,#64162,#64163,#64164,#64165,#64166,
#64167,#64168,#64169,#64170,#64171,#64172,#64173,#64174,#64175,#64176,#64177,
#64178,#64179,#64180,#64181,#64182,#64183,#64184,#64185,#64186,#64187,#64188,
#64189,#64190,#64191,#64192,#64193,#64194,#64195,#64196,#64197,#64198,#64199,
#64200,#64201,#64202,#64203,#64204,#64205,#64206,#64207,#64208,#64209,#64210,
#64211,#64212,#64213,#64214,#64215,#64216,#64217,#64218,#64219,#64220,#64221,
#64222,#64223,#64224,#64225,#64226,#64227,#64228,#64229,#64230,#64231,#64232,
#64233,#64234,#64235,#64236,#64237,#64238,#64239,#64240,#64241,#64242,#64243,
#64244,#64245,#64246,#64247,#64248,#64249,#64250,#64251,#64252,#64253,#64254,
#64255,#64256,#64257,#64258,#64259,#64260,#64261,#64262,#64263,#64264,#64265,
#64266,#64267,#64268,#64269,#64270,#64271,#64272,#64273,#64274,#64275,#64276,
#64277,#64278,#64279,#64280,#64281,#64282,#64283,#64284,#64285,#64286,#64287,
#64288,#64289,#64290,#64291,#64292,#64293,#64294,#64295,#64296,#64297,#64298,
#64299,#64300,#64301,#64302,#64303,#64304,#64305,#64306,#64307,#64308,#64309,
#64310,#64311,#64312,#64313,#64314,#64315,#64316,#64317,#64318,#64319,#64320,
#64321,#64322,#64323,#64324,#64325,#64326,#64327,#64328,#64329,#64330,#64331,
#64332,#64333,#64334,#64335,#64336,#64337,#64338,#64339,#64340,#64341,#64342,
#64343,#64344,#64345,#64346,#64347,#64348,#64349,#64350,#64351,#64352,#64353,
#64354,#64355,#64356,#64357,#64358,#64359,#64360,#64361,#64362,#64363,#64364,
#64365,#64366,#64367,#64368,#64369,#64370,#64371,#64372,#64373,#64374,#64375,
#64376,#64377,#64378,#64379,#64380,#64381,#64382,#64383,#64384,#64385,#64386,
#64387,#64388,#64389,#64390,#64391,#64392,#64393,#64394,#64395,#64396,#64397,
#64398,#64399,#64400,#64401,#64402,#64403,#64404,#64405,#64406,#64407,#64408,
#64409,#64410,#64411,#64412,#64413,#64414,#64415,#64416,#64417,#64418,#64419,
#64420,#64421,#64422,#64423,#64424,#64425,#64426,#64427,#64428,#64429,#64430,
#64431,#64432,#64433,#64434,#64435,#64436,#64437,#64438,#64439,#64440,#64441,
#64442,#64443,#64444,#64445,#64446,#64447,#64448,#64449,#64450,#64451,#64452,
#64453,#64454,#64455,#64456,#64457,#64458,#64459,#64460,#64461,#64462,#64463,
#64464,#64465,#64466,#64467,#64468,#64469,#64470,#64471,#64472,#64473,#64474,
#64475,#64476,#64477,#64478,#64479,#64480,#64481,#64482,#64483,#64484,#64485,
#64486,#64487,#64488)),.UNSPECIFIED.,.F.,.F.,.F.)
B_SPLINE_SURFACE_WITH_KNOTS((2,2),(3,2,2,2,2,2,2,2,2,2,2,2,2,2,2,2,2,2,
2,2,2,2,2,2,2,2,2,2,2,2,2,2,2,2,2,2,2,2,2,2,2,2,2,2,2,2,2,2,2,2,2,2,2,2,
2,2,2,2,2,2,2,2,2,2,2,2,2,2,2,2,2,2,2,2,2,2,2,2,2,2,2,2,2,2,2,2,2,2,2,2,
2,2,2,2,2,2,2,2,2,2,2,2,2,2,2,2,2,2,2,2,2,2,2,2,2,2,2,2,2,2,2,2,2,2,2,2,
2,2,2,2,2,2,2,2,2,2,2,2,2,2,2,2,2,2,2,2,2,2,2,2,2,2,2,2,2,2,2,2,2,2,2,2,
2,2,2,2,2,2,2,2,2,2,2,2,2,2,2,2,2,2,2,2,2,2,2,2,3),(-2.30253870309941E-5,
1.),(0.,0.00537634408602151,0.010752688172043,0.0161290322580645,0.021505376344086,
0.0268817204301075,0.032258064516129,0.0376344086021505,0.043010752688172,
0.0483870967741935,0.0537634408602151,0.0591397849462366,0.0645161290322581,
0.0698924731182796,0.0752688172043011,0.0806451612903226,0.0860215053763441,
0.0913978494623656,0.0967741935483871,0.102150537634409,0.10752688172043,
0.112903225806452,0.118279569892473,0.123655913978495,0.129032258064516,
0.134408602150538,0.139784946236559,0.145161290322581,0.150537634408602,
0.155913978494624,0.161290322580645,0.166666666666667,0.172043010752688,
0.17741935483871,0.182795698924731,0.188172043010753,0.193548387096774,
0.198924731182796,0.204301075268817,0.209677419354839,0.21505376344086,
0.220430107526882,0.225806451612903,0.231182795698925,0.236559139784946,
0.241935483870968,0.247311827956989,0.252688172043011,0.258064516129032,
0.263440860215054,0.268817204301075,0.274193548387097,0.279569892473118,
0.28494623655914,0.290322580645161,0.295698924731183,0.301075268817204,
0.306451612903226,0.311827956989247,0.317204301075269,0.32258064516129,
0.327956989247312,0.333333333333333,0.338709677419355,0.344086021505376,
0.349462365591398,0.354838709677419,0.360215053763441,0.365591397849462,
0.370967741935484,0.376344086021505,0.381720430107527,0.387096774193548,
0.39247311827957,0.397849462365591,0.403225806451613,0.408602150537634,
0.413978494623656,0.419354838709677,0.424731182795699,0.43010752688172,
0.435483870967742,0.440860215053763,0.446236559139785,0.451612903225806,
0.456989247311828,0.462365591397849,0.467741935483871,0.473118279569892,
0.478494623655914,0.483870967741935,0.489247311827957,0.494623655913978,
0.5,0.505376344086022,0.510752688172043,0.516129032258065,0.521505376344086,
0.526881720430108,0.532258064516129,0.537634408602151,0.543010752688172,
0.548387096774194,0.553763440860215,0.559139784946237,0.564516129032258,
0.56989247311828,0.575268817204301,0.580645161290323,0.586021505376344,
0.591397849462366,0.596774193548387,0.602150537634409,0.60752688172043,
0.612903225806452,0.618279569892473,0.623655913978495,0.629032258064516,
0.634408602150538,0.639784946236559,0.645161290322581,0.650537634408602,
0.655913978494624,0.661290322580645,0.666666666666667,0.672043010752688,
0.67741935483871,0.682795698924731,0.688172043010753,0.693548387096774,
0.698924731182796,0.704301075268817,0.709677419354839,0.71505376344086,
0.720430107526882,0.725806451612903,0.731182795698925,0.736559139784946,
0.741935483870968,0.747311827956989,0.752688172043011,0.758064516129032,
0.763440860215054,0.768817204301075,0.774193548387097,0.779569892473118,
0.78494623655914,0.790322580645161,0.795698924731183,0.801075268817204,
0.806451612903226,0.811827956989247,0.817204301075269,0.82258064516129,
0.827956989247312,0.833333333333333,0.838709677419355,0.844086021505376,
0.849462365591398,0.854838709677419,0.860215053763441,0.865591397849462,
0.870967741935484,0.876344086021505,0.881720430107527,0.887096774193548,
0.89247311827957,0.897849462365591,0.903225806451613,0.908602150537634,
0.913978494623656,0.919354838709677,0.924731182795699,0.93010752688172,
0.935483870967742,0.940860215053763,0.946236559139785,0.951612903225806,
0.956989247311828,0.962365591397849,0.967741935483871,0.973118279569892,
0.978494623655914,0.983870967741935,0.989247311827957,0.994623655913978,
1.),.UNSPECIFIED.)
GEOMETRIC_REPRESENTATION_ITEM()
RATIONAL_B_SPLINE_SURFACE(((1.,0.866025403784439,1.,0.866025403784439,1.,
0.866025403784439,1.,0.866025403784439,1.,0.866025403784439,1.,0.866025403784439,
1.,0.866025403784439,1.,0.866025403784439,1.,0.866025403784439,1.,0.866025403784439,
1.,0.866025403784439,1.,0.866025403784439,1.,0.866025403784439,1.,0.866025403784439,
1.,0.866025403784439,1.,0.866025403784439,1.,0.866025403784439,1.,0.866025403784439,
1.,0.866025403784439,1.,0.866025403784439,1.,0.866025403784439,1.,0.866025403784439,
1.,0.866025403784439,1.,0.866025403784439,1.,0.866025403784439,1.,0.866025403784439,
1.,0.866025403784439,1.,0.866025403784439,1.,0.866025403784439,1.,0.866025403784439,
1.,0.866025403784439,1.,0.866025403784439,1.,0.866025403784439,1.,0.866025403784439,
1.,0.866025403784439,1.,0.866025403784439,1.,0.866025403784439,1.,0.866025403784439,
1.,0.866025403784439,1.,0.866025403784439,1.,0.866025403784439,1.,0.866025403784439,
1.,0.866025403784439,1.,0.866025403784439,1.,0.866025403784439,1.,0.866025403784439,
1.,0.866025403784439,1.,0.866025403784439,1.,0.866025403784439,1.,0.866025403784439,
1.,0.866025403784439,1.,0.866025403784439,1.,0.866025403784439,1.,0.866025403784439,
1.,0.866025403784439,1.,0.866025403784439,1.,0.866025403784439,1.,0.866025403784439,
1.,0.866025403784439,1.,0.866025403784439,1.,0.866025403784439,1.,0.866025403784439,
1.,0.866025403784439,1.,0.866025403784439,1.,0.866025403784439,1.,0.866025403784439,
1.,0.866025403784439,1.,0.866025403784439,1.,0.866025403784439,1.,0.866025403784439,
1.,0.866025403784439,1.,0.866025403784439,1.,0.866025403784439,1.,0.866025403784439,
1.,0.866025403784439,1.,0.866025403784439,1.,0.866025403784439,1.,0.866025403784439,
1.,0.866025403784439,1.,0.866025403784439,1.,0.866025403784439,1.,0.866025403784439,
1.,0.866025403784439,1.,0.866025403784439,1.,0.866025403784439,1.,0.866025403784439,
1.,0.866025403784439,1.,0.866025403784439,1.,0.866025403784439,1.,0.866025403784439,
1.,0.866025403784439,1.,0.866025403784439,1.,0.866025403784439,1.,0.866025403784439,
1.,0.866025403784439,1.,0.866025403784439,1.,0.866025403784439,1.,0.866025403784439,
1.,0.866025403784439,1.,0.866025403784439,1.,0.866025403784439,1.,0.866025403784439,
1.,0.866025403784439,1.,0.866025403784439,1.,0.866025403784439,1.,0.866025403784439,
1.,0.866025403784439,1.,0.866025403784439,1.,0.866025403784439,1.,0.866025403784439,
1.,0.866025403784439,1.,0.866025403784439,1.,0.866025403784439,1.,0.866025403784439,
1.,0.866025403784439,1.,0.866025403784439,1.,0.866025403784439,1.,0.866025403784439,
1.,0.866025403784439,1.,0.866025403784439,1.,0.866025403784439,1.,0.866025403784439,
1.,0.866025403784439,1.,0.866025403784439,1.,0.866025403784439,1.,0.866025403784439,
1.,0.866025403784439,1.,0.866025403784439,1.,0.866025403784439,1.,0.866025403784439,
1.,0.866025403784439,1.,0.866025403784439,1.,0.866025403784439,1.,0.866025403784439,
1.,0.866025403784439,1.,0.866025403784439,1.,0.866025403784439,1.,0.866025403784439,
1.,0.866025403784439,1.,0.866025403784439,1.,0.866025403784439,1.,0.866025403784439,
1.,0.866025403784439,1.,0.866025403784439,1.,0.866025403784439,1.,0.866025403784439,
1.,0.866025403784439,1.,0.866025403784439,1.,0.866025403784439,1.,0.866025403784439,
1.,0.866025403784439,1.,0.866025403784439,1.,0.866025403784439,1.,0.866025403784439,
1.,0.866025403784439,1.,0.866025403784439,1.,0.866025403784439,1.,0.866025403784439,
1.,0.866025403784439,1.,0.866025403784439,1.,0.866025403784439,1.,0.866025403784439,
1.,0.866025403784439,1.,0.866025403784439,1.,0.866025403784439,1.,0.866025403784439,
1.,0.866025403784439,1.,0.866025403784439,1.,0.866025403784439,1.,0.866025403784439,
1.,0.866025403784439,1.,0.866025403784439,1.,0.866025403784439,1.,0.866025403784439,
1.,0.866025403784439,1.,0.866025403784439,1.,0.866025403784439,1.,0.866025403784439,
1.,0.866025403784439,1.,0.866025403784439,1.,0.866025403784439,1.,0.866025403784439,
1.,0.866025403784439,1.,0.866025403784439,1.,0.866025403784439,1.,0.866025403784439,
1.),(1.,0.866025403784439,1.,0.866025403784439,1.,0.866025403784439,1.,
0.866025403784439,1.,0.866025403784439,1.,0.866025403784439,1.,0.866025403784439,
1.,0.866025403784439,1.,0.866025403784439,1.,0.866025403784439,1.,0.866025403784439,
1.,0.866025403784439,1.,0.866025403784439,1.,0.866025403784439,1.,0.866025403784439,
1.,0.866025403784439,1.,0.866025403784439,1.,0.866025403784439,1.,0.866025403784439,
1.,0.866025403784439,1.,0.866025403784439,1.,0.866025403784439,1.,0.866025403784439,
1.,0.866025403784439,1.,0.866025403784439,1.,0.866025403784439,1.,0.866025403784439,
1.,0.866025403784439,1.,0.866025403784439,1.,0.866025403784439,1.,0.866025403784439,
1.,0.866025403784439,1.,0.866025403784439,1.,0.866025403784439,1.,0.866025403784439,
1.,0.866025403784439,1.,0.866025403784439,1.,0.866025403784439,1.,0.866025403784439,
1.,0.866025403784439,1.,0.866025403784439,1.,0.866025403784439,1.,0.866025403784439,
1.,0.866025403784439,1.,0.866025403784439,1.,0.866025403784439,1.,0.866025403784439,
1.,0.866025403784439,1.,0.866025403784439,1.,0.866025403784439,1.,0.866025403784439,
1.,0.866025403784439,1.,0.866025403784439,1.,0.866025403784439,1.,0.866025403784439,
1.,0.866025403784439,1.,0.866025403784439,1.,0.866025403784439,1.,0.866025403784439,
1.,0.866025403784439,1.,0.866025403784439,1.,0.866025403784439,1.,0.866025403784439,
1.,0.866025403784439,1.,0.866025403784439,1.,0.866025403784439,1.,0.866025403784439,
1.,0.866025403784439,1.,0.866025403784439,1.,0.866025403784439,1.,0.866025403784439,
1.,0.866025403784439,1.,0.866025403784439,1.,0.866025403784439,1.,0.866025403784439,
1.,0.866025403784439,1.,0.866025403784439,1.,0.866025403784439,1.,0.866025403784439,
1.,0.866025403784439,1.,0.866025403784439,1.,0.866025403784439,1.,0.866025403784439,
1.,0.866025403784439,1.,0.866025403784439,1.,0.866025403784439,1.,0.866025403784439,
1.,0.866025403784439,1.,0.866025403784439,1.,0.866025403784439,1.,0.866025403784439,
1.,0.866025403784439,1.,0.866025403784439,1.,0.866025403784439,1.,0.866025403784439,
1.,0.866025403784439,1.,0.866025403784439,1.,0.866025403784439,1.,0.866025403784439,
1.,0.866025403784439,1.,0.866025403784439,1.,0.866025403784439,1.,0.866025403784439,
1.,0.866025403784439,1.,0.866025403784439,1.,0.866025403784439,1.,0.866025403784439,
1.,0.866025403784439,1.,0.866025403784439,1.,0.866025403784439,1.,0.866025403784439,
1.,0.866025403784439,1.,0.866025403784439,1.,0.866025403784439,1.,0.866025403784439,
1.,0.866025403784439,1.,0.866025403784439,1.,0.866025403784439,1.,0.866025403784439,
1.,0.866025403784439,1.,0.866025403784439,1.,0.866025403784439,1.,0.866025403784439,
1.,0.866025403784439,1.,0.866025403784439,1.,0.866025403784439,1.,0.866025403784439,
1.,0.866025403784439,1.,0.866025403784439,1.,0.866025403784439,1.,0.866025403784439,
1.,0.866025403784439,1.,0.866025403784439,1.,0.866025403784439,1.,0.866025403784439,
1.,0.866025403784439,1.,0.866025403784439,1.,0.866025403784439,1.,0.866025403784439,
1.,0.866025403784439,1.,0.866025403784439,1.,0.866025403784439,1.,0.866025403784439,
1.,0.866025403784439,1.,0.866025403784439,1.,0.866025403784439,1.,0.866025403784439,
1.,0.866025403784439,1.,0.866025403784439,1.,0.866025403784439,1.,0.866025403784439,
1.,0.866025403784439,1.,0.866025403784439,1.,0.866025403784439,1.,0.866025403784439,
1.,0.866025403784439,1.,0.866025403784439,1.,0.866025403784439,1.,0.866025403784439,
1.,0.866025403784439,1.,0.866025403784439,1.,0.866025403784439,1.,0.866025403784439,
1.,0.866025403784439,1.,0.866025403784439,1.,0.866025403784439,1.,0.866025403784439,
1.,0.866025403784439,1.,0.866025403784439,1.,0.866025403784439,1.,0.866025403784439,
1.,0.866025403784439,1.,0.866025403784439,1.,0.866025403784439,1.,0.866025403784439,
1.,0.866025403784439,1.,0.866025403784439,1.,0.866025403784439,1.,0.866025403784439,
1.,0.866025403784439,1.,0.866025403784439,1.,0.866025403784439,1.,0.866025403784439,
1.,0.866025403784439,1.,0.866025403784439,1.,0.866025403784439,1.)))
REPRESENTATION_ITEM('')
SURFACE()
);
#46=(
BOUNDED_SURFACE()
B_SPLINE_SURFACE(1,2,((#64517,#64518,#64519,#64520,#64521,#64522,#64523,
#64524,#64525,#64526,#64527,#64528,#64529,#64530,#64531,#64532,#64533,#64534,
#64535,#64536,#64537,#64538,#64539,#64540,#64541,#64542,#64543,#64544,#64545,
#64546,#64547,#64548,#64549,#64550,#64551,#64552,#64553,#64554,#64555,#64556,
#64557,#64558,#64559,#64560,#64561,#64562,#64563,#64564,#64565,#64566,#64567,
#64568,#64569,#64570,#64571,#64572,#64573,#64574,#64575,#64576,#64577,#64578,
#64579,#64580,#64581,#64582,#64583,#64584,#64585,#64586,#64587,#64588,#64589,
#64590,#64591,#64592,#64593,#64594,#64595,#64596,#64597,#64598,#64599,#64600,
#64601,#64602,#64603,#64604,#64605,#64606,#64607,#64608,#64609,#64610,#64611,
#64612,#64613,#64614,#64615,#64616,#64617,#64618,#64619,#64620,#64621,#64622,
#64623,#64624,#64625,#64626,#64627,#64628,#64629,#64630,#64631,#64632,#64633,
#64634,#64635,#64636,#64637,#64638,#64639,#64640,#64641,#64642,#64643,#64644,
#64645,#64646,#64647,#64648,#64649,#64650,#64651,#64652,#64653,#64654,#64655,
#64656,#64657,#64658,#64659,#64660,#64661,#64662,#64663,#64664,#64665,#64666,
#64667,#64668,#64669,#64670,#64671,#64672,#64673,#64674,#64675,#64676,#64677,
#64678,#64679,#64680,#64681,#64682,#64683,#64684,#64685,#64686,#64687,#64688,
#64689,#64690,#64691,#64692,#64693,#64694,#64695,#64696,#64697,#64698,#64699,
#64700,#64701,#64702,#64703,#64704,#64705,#64706,#64707,#64708,#64709,#64710,
#64711,#64712,#64713,#64714,#64715,#64716,#64717,#64718,#64719,#64720,#64721,
#64722,#64723,#64724,#64725,#64726,#64727,#64728,#64729,#64730,#64731,#64732,
#64733,#64734,#64735,#64736,#64737,#64738,#64739,#64740,#64741,#64742,#64743,
#64744,#64745,#64746,#64747,#64748,#64749,#64750,#64751,#64752,#64753,#64754,
#64755,#64756,#64757,#64758,#64759,#64760,#64761,#64762,#64763,#64764,#64765,
#64766,#64767,#64768,#64769,#64770,#64771,#64772,#64773,#64774,#64775,#64776,
#64777,#64778,#64779,#64780,#64781,#64782,#64783,#64784,#64785,#64786,#64787,
#64788,#64789,#64790,#64791,#64792,#64793,#64794,#64795,#64796,#64797,#64798,
#64799,#64800,#64801,#64802,#64803,#64804,#64805,#64806,#64807,#64808,#64809,
#64810,#64811,#64812,#64813,#64814,#64815,#64816,#64817,#64818,#64819,#64820,
#64821,#64822,#64823,#64824,#64825,#64826,#64827,#64828,#64829,#64830,#64831,
#64832,#64833,#64834,#64835,#64836,#64837,#64838,#64839,#64840,#64841,#64842,
#64843,#64844,#64845,#64846,#64847,#64848,#64849,#64850,#64851,#64852,#64853,
#64854,#64855,#64856,#64857,#64858,#64859,#64860,#64861,#64862,#64863,#64864,
#64865,#64866,#64867,#64868,#64869,#64870,#64871,#64872,#64873,#64874,#64875,
#64876,#64877,#64878,#64879,#64880,#64881,#64882,#64883,#64884,#64885,#64886,
#64887,#64888,#64889),(#64890,#64891,#64892,#64893,#64894,#64895,#64896,
#64897,#64898,#64899,#64900,#64901,#64902,#64903,#64904,#64905,#64906,#64907,
#64908,#64909,#64910,#64911,#64912,#64913,#64914,#64915,#64916,#64917,#64918,
#64919,#64920,#64921,#64922,#64923,#64924,#64925,#64926,#64927,#64928,#64929,
#64930,#64931,#64932,#64933,#64934,#64935,#64936,#64937,#64938,#64939,#64940,
#64941,#64942,#64943,#64944,#64945,#64946,#64947,#64948,#64949,#64950,#64951,
#64952,#64953,#64954,#64955,#64956,#64957,#64958,#64959,#64960,#64961,#64962,
#64963,#64964,#64965,#64966,#64967,#64968,#64969,#64970,#64971,#64972,#64973,
#64974,#64975,#64976,#64977,#64978,#64979,#64980,#64981,#64982,#64983,#64984,
#64985,#64986,#64987,#64988,#64989,#64990,#64991,#64992,#64993,#64994,#64995,
#64996,#64997,#64998,#64999,#65000,#65001,#65002,#65003,#65004,#65005,#65006,
#65007,#65008,#65009,#65010,#65011,#65012,#65013,#65014,#65015,#65016,#65017,
#65018,#65019,#65020,#65021,#65022,#65023,#65024,#65025,#65026,#65027,#65028,
#65029,#65030,#65031,#65032,#65033,#65034,#65035,#65036,#65037,#65038,#65039,
#65040,#65041,#65042,#65043,#65044,#65045,#65046,#65047,#65048,#65049,#65050,
#65051,#65052,#65053,#65054,#65055,#65056,#65057,#65058,#65059,#65060,#65061,
#65062,#65063,#65064,#65065,#65066,#65067,#65068,#65069,#65070,#65071,#65072,
#65073,#65074,#65075,#65076,#65077,#65078,#65079,#65080,#65081,#65082,#65083,
#65084,#65085,#65086,#65087,#65088,#65089,#65090,#65091,#65092,#65093,#65094,
#65095,#65096,#65097,#65098,#65099,#65100,#65101,#65102,#65103,#65104,#65105,
#65106,#65107,#65108,#65109,#65110,#65111,#65112,#65113,#65114,#65115,#65116,
#65117,#65118,#65119,#65120,#65121,#65122,#65123,#65124,#65125,#65126,#65127,
#65128,#65129,#65130,#65131,#65132,#65133,#65134,#65135,#65136,#65137,#65138,
#65139,#65140,#65141,#65142,#65143,#65144,#65145,#65146,#65147,#65148,#65149,
#65150,#65151,#65152,#65153,#65154,#65155,#65156,#65157,#65158,#65159,#65160,
#65161,#65162,#65163,#65164,#65165,#65166,#65167,#65168,#65169,#65170,#65171,
#65172,#65173,#65174,#65175,#65176,#65177,#65178,#65179,#65180,#65181,#65182,
#65183,#65184,#65185,#65186,#65187,#65188,#65189,#65190,#65191,#65192,#65193,
#65194,#65195,#65196,#65197,#65198,#65199,#65200,#65201,#65202,#65203,#65204,
#65205,#65206,#65207,#65208,#65209,#65210,#65211,#65212,#65213,#65214,#65215,
#65216,#65217,#65218,#65219,#65220,#65221,#65222,#65223,#65224,#65225,#65226,
#65227,#65228,#65229,#65230,#65231,#65232,#65233,#65234,#65235,#65236,#65237,
#65238,#65239,#65240,#65241,#65242,#65243,#65244,#65245,#65246,#65247,#65248,
#65249,#65250,#65251,#65252,#65253,#65254,#65255,#65256,#65257,#65258,#65259,
#65260,#65261,#65262)),.UNSPECIFIED.,.F.,.F.,.F.)
B_SPLINE_SURFACE_WITH_KNOTS((2,2),(3,2,2,2,2,2,2,2,2,2,2,2,2,2,2,2,2,2,
2,2,2,2,2,2,2,2,2,2,2,2,2,2,2,2,2,2,2,2,2,2,2,2,2,2,2,2,2,2,2,2,2,2,2,2,
2,2,2,2,2,2,2,2,2,2,2,2,2,2,2,2,2,2,2,2,2,2,2,2,2,2,2,2,2,2,2,2,2,2,2,2,
2,2,2,2,2,2,2,2,2,2,2,2,2,2,2,2,2,2,2,2,2,2,2,2,2,2,2,2,2,2,2,2,2,2,2,2,
2,2,2,2,2,2,2,2,2,2,2,2,2,2,2,2,2,2,2,2,2,2,2,2,2,2,2,2,2,2,2,2,2,2,2,2,
2,2,2,2,2,2,2,2,2,2,2,2,2,2,2,2,2,2,2,2,2,2,2,2,3),(0.,1.00001535537392),
(0.,0.00537634408602151,0.010752688172043,0.0161290322580645,0.021505376344086,
0.0268817204301075,0.032258064516129,0.0376344086021505,0.043010752688172,
0.0483870967741935,0.0537634408602151,0.0591397849462366,0.0645161290322581,
0.0698924731182796,0.0752688172043011,0.0806451612903226,0.0860215053763441,
0.0913978494623656,0.0967741935483871,0.102150537634409,0.10752688172043,
0.112903225806452,0.118279569892473,0.123655913978495,0.129032258064516,
0.134408602150538,0.139784946236559,0.145161290322581,0.150537634408602,
0.155913978494624,0.161290322580645,0.166666666666667,0.172043010752688,
0.17741935483871,0.182795698924731,0.188172043010753,0.193548387096774,
0.198924731182796,0.204301075268817,0.209677419354839,0.21505376344086,
0.220430107526882,0.225806451612903,0.231182795698925,0.236559139784946,
0.241935483870968,0.247311827956989,0.252688172043011,0.258064516129032,
0.263440860215054,0.268817204301075,0.274193548387097,0.279569892473118,
0.28494623655914,0.290322580645161,0.295698924731183,0.301075268817204,
0.306451612903226,0.311827956989247,0.317204301075269,0.32258064516129,
0.327956989247312,0.333333333333333,0.338709677419355,0.344086021505376,
0.349462365591398,0.354838709677419,0.360215053763441,0.365591397849462,
0.370967741935484,0.376344086021505,0.381720430107527,0.387096774193548,
0.39247311827957,0.397849462365591,0.403225806451613,0.408602150537634,
0.413978494623656,0.419354838709677,0.424731182795699,0.43010752688172,
0.435483870967742,0.440860215053763,0.446236559139785,0.451612903225806,
0.456989247311828,0.462365591397849,0.467741935483871,0.473118279569892,
0.478494623655914,0.483870967741935,0.489247311827957,0.494623655913978,
0.5,0.505376344086022,0.510752688172043,0.516129032258065,0.521505376344086,
0.526881720430108,0.532258064516129,0.537634408602151,0.543010752688172,
0.548387096774194,0.553763440860215,0.559139784946237,0.564516129032258,
0.56989247311828,0.575268817204301,0.580645161290323,0.586021505376344,
0.591397849462366,0.596774193548387,0.602150537634409,0.60752688172043,
0.612903225806452,0.618279569892473,0.623655913978495,0.629032258064516,
0.634408602150538,0.639784946236559,0.645161290322581,0.650537634408602,
0.655913978494624,0.661290322580645,0.666666666666667,0.672043010752688,
0.67741935483871,0.682795698924731,0.688172043010753,0.693548387096774,
0.698924731182796,0.704301075268817,0.709677419354839,0.71505376344086,
0.720430107526882,0.725806451612903,0.731182795698925,0.736559139784946,
0.741935483870968,0.747311827956989,0.752688172043011,0.758064516129032,
0.763440860215054,0.768817204301075,0.774193548387097,0.779569892473118,
0.78494623655914,0.790322580645161,0.795698924731183,0.801075268817204,
0.806451612903226,0.811827956989247,0.817204301075269,0.82258064516129,
0.827956989247312,0.833333333333333,0.838709677419355,0.844086021505376,
0.849462365591398,0.854838709677419,0.860215053763441,0.865591397849462,
0.870967741935484,0.876344086021505,0.881720430107527,0.887096774193548,
0.89247311827957,0.897849462365591,0.903225806451613,0.908602150537634,
0.913978494623656,0.919354838709677,0.924731182795699,0.93010752688172,
0.935483870967742,0.940860215053763,0.946236559139785,0.951612903225806,
0.956989247311828,0.962365591397849,0.967741935483871,0.973118279569892,
0.978494623655914,0.983870967741935,0.989247311827957,0.994623655913978,
1.),.UNSPECIFIED.)
GEOMETRIC_REPRESENTATION_ITEM()
RATIONAL_B_SPLINE_SURFACE(((1.,0.866025403784439,1.,0.866025403784439,1.,
0.866025403784439,1.,0.866025403784439,1.,0.866025403784439,1.,0.866025403784439,
1.,0.866025403784439,1.,0.866025403784439,1.,0.866025403784439,1.,0.866025403784439,
1.,0.866025403784439,1.,0.866025403784439,1.,0.866025403784439,1.,0.866025403784439,
1.,0.866025403784439,1.,0.866025403784439,1.,0.866025403784439,1.,0.866025403784439,
1.,0.866025403784439,1.,0.866025403784439,1.,0.866025403784439,1.,0.866025403784439,
1.,0.866025403784439,1.,0.866025403784439,1.,0.866025403784439,1.,0.866025403784439,
1.,0.866025403784439,1.,0.866025403784439,1.,0.866025403784439,1.,0.866025403784439,
1.,0.866025403784439,1.,0.866025403784439,1.,0.866025403784439,1.,0.866025403784439,
1.,0.866025403784439,1.,0.866025403784439,1.,0.866025403784439,1.,0.866025403784439,
1.,0.866025403784439,1.,0.866025403784439,1.,0.866025403784439,1.,0.866025403784439,
1.,0.866025403784439,1.,0.866025403784439,1.,0.866025403784439,1.,0.866025403784439,
1.,0.866025403784439,1.,0.866025403784439,1.,0.866025403784439,1.,0.866025403784439,
1.,0.866025403784439,1.,0.866025403784439,1.,0.866025403784439,1.,0.866025403784439,
1.,0.866025403784439,1.,0.866025403784439,1.,0.866025403784439,1.,0.866025403784439,
1.,0.866025403784439,1.,0.866025403784439,1.,0.866025403784439,1.,0.866025403784439,
1.,0.866025403784439,1.,0.866025403784439,1.,0.866025403784439,1.,0.866025403784439,
1.,0.866025403784439,1.,0.866025403784439,1.,0.866025403784439,1.,0.866025403784439,
1.,0.866025403784439,1.,0.866025403784439,1.,0.866025403784439,1.,0.866025403784439,
1.,0.866025403784439,1.,0.866025403784439,1.,0.866025403784439,1.,0.866025403784439,
1.,0.866025403784439,1.,0.866025403784439,1.,0.866025403784439,1.,0.866025403784439,
1.,0.866025403784439,1.,0.866025403784439,1.,0.866025403784439,1.,0.866025403784439,
1.,0.866025403784439,1.,0.866025403784439,1.,0.866025403784439,1.,0.866025403784439,
1.,0.866025403784439,1.,0.866025403784439,1.,0.866025403784439,1.,0.866025403784439,
1.,0.866025403784439,1.,0.866025403784439,1.,0.866025403784439,1.,0.866025403784439,
1.,0.866025403784439,1.,0.866025403784439,1.,0.866025403784439,1.,0.866025403784439,
1.,0.866025403784439,1.,0.866025403784439,1.,0.866025403784439,1.,0.866025403784439,
1.,0.866025403784439,1.,0.866025403784439,1.,0.866025403784439,1.,0.866025403784439,
1.,0.866025403784439,1.,0.866025403784439,1.,0.866025403784439,1.,0.866025403784439,
1.,0.866025403784439,1.,0.866025403784439,1.,0.866025403784439,1.,0.866025403784439,
1.,0.866025403784439,1.,0.866025403784439,1.,0.866025403784439,1.,0.866025403784439,
1.,0.866025403784439,1.,0.866025403784439,1.,0.866025403784439,1.,0.866025403784439,
1.,0.866025403784439,1.,0.866025403784439,1.,0.866025403784439,1.,0.866025403784439,
1.,0.866025403784439,1.,0.866025403784439,1.,0.866025403784439,1.,0.866025403784439,
1.,0.866025403784439,1.,0.866025403784439,1.,0.866025403784439,1.,0.866025403784439,
1.,0.866025403784439,1.,0.866025403784439,1.,0.866025403784439,1.,0.866025403784439,
1.,0.866025403784439,1.,0.866025403784439,1.,0.866025403784439,1.,0.866025403784439,
1.,0.866025403784439,1.,0.866025403784439,1.,0.866025403784439,1.,0.866025403784439,
1.,0.866025403784439,1.,0.866025403784439,1.,0.866025403784439,1.,0.866025403784439,
1.,0.866025403784439,1.,0.866025403784439,1.,0.866025403784439,1.,0.866025403784439,
1.,0.866025403784439,1.,0.866025403784439,1.,0.866025403784439,1.,0.866025403784439,
1.,0.866025403784439,1.,0.866025403784439,1.,0.866025403784439,1.,0.866025403784439,
1.,0.866025403784439,1.,0.866025403784439,1.,0.866025403784439,1.,0.866025403784439,
1.,0.866025403784439,1.,0.866025403784439,1.,0.866025403784439,1.,0.866025403784439,
1.,0.866025403784439,1.,0.866025403784439,1.,0.866025403784439,1.,0.866025403784439,
1.,0.866025403784439,1.,0.866025403784439,1.,0.866025403784439,1.,0.866025403784439,
1.,0.866025403784439,1.,0.866025403784439,1.,0.866025403784439,1.,0.866025403784439,
1.),(1.,0.866025403784439,1.,0.866025403784439,1.,0.866025403784439,1.,
0.866025403784439,1.,0.866025403784439,1.,0.866025403784439,1.,0.866025403784439,
1.,0.866025403784439,1.,0.866025403784439,1.,0.866025403784439,1.,0.866025403784439,
1.,0.866025403784439,1.,0.866025403784439,1.,0.866025403784439,1.,0.866025403784439,
1.,0.866025403784439,1.,0.866025403784439,1.,0.866025403784439,1.,0.866025403784439,
1.,0.866025403784439,1.,0.866025403784439,1.,0.866025403784439,1.,0.866025403784439,
1.,0.866025403784439,1.,0.866025403784439,1.,0.866025403784439,1.,0.866025403784439,
1.,0.866025403784439,1.,0.866025403784439,1.,0.866025403784439,1.,0.866025403784439,
1.,0.866025403784439,1.,0.866025403784439,1.,0.866025403784439,1.,0.866025403784439,
1.,0.866025403784439,1.,0.866025403784439,1.,0.866025403784439,1.,0.866025403784439,
1.,0.866025403784439,1.,0.866025403784439,1.,0.866025403784439,1.,0.866025403784439,
1.,0.866025403784439,1.,0.866025403784439,1.,0.866025403784439,1.,0.866025403784439,
1.,0.866025403784439,1.,0.866025403784439,1.,0.866025403784439,1.,0.866025403784439,
1.,0.866025403784439,1.,0.866025403784439,1.,0.866025403784439,1.,0.866025403784439,
1.,0.866025403784439,1.,0.866025403784439,1.,0.866025403784439,1.,0.866025403784439,
1.,0.866025403784439,1.,0.866025403784439,1.,0.866025403784439,1.,0.866025403784439,
1.,0.866025403784439,1.,0.866025403784439,1.,0.866025403784439,1.,0.866025403784439,
1.,0.866025403784439,1.,0.866025403784439,1.,0.866025403784439,1.,0.866025403784439,
1.,0.866025403784439,1.,0.866025403784439,1.,0.866025403784439,1.,0.866025403784439,
1.,0.866025403784439,1.,0.866025403784439,1.,0.866025403784439,1.,0.866025403784439,
1.,0.866025403784439,1.,0.866025403784439,1.,0.866025403784439,1.,0.866025403784439,
1.,0.866025403784439,1.,0.866025403784439,1.,0.866025403784439,1.,0.866025403784439,
1.,0.866025403784439,1.,0.866025403784439,1.,0.866025403784439,1.,0.866025403784439,
1.,0.866025403784439,1.,0.866025403784439,1.,0.866025403784439,1.,0.866025403784439,
1.,0.866025403784439,1.,0.866025403784439,1.,0.866025403784439,1.,0.866025403784439,
1.,0.866025403784439,1.,0.866025403784439,1.,0.866025403784439,1.,0.866025403784439,
1.,0.866025403784439,1.,0.866025403784439,1.,0.866025403784439,1.,0.866025403784439,
1.,0.866025403784439,1.,0.866025403784439,1.,0.866025403784439,1.,0.866025403784439,
1.,0.866025403784439,1.,0.866025403784439,1.,0.866025403784439,1.,0.866025403784439,
1.,0.866025403784439,1.,0.866025403784439,1.,0.866025403784439,1.,0.866025403784439,
1.,0.866025403784439,1.,0.866025403784439,1.,0.866025403784439,1.,0.866025403784439,
1.,0.866025403784439,1.,0.866025403784439,1.,0.866025403784439,1.,0.866025403784439,
1.,0.866025403784439,1.,0.866025403784439,1.,0.866025403784439,1.,0.866025403784439,
1.,0.866025403784439,1.,0.866025403784439,1.,0.866025403784439,1.,0.866025403784439,
1.,0.866025403784439,1.,0.866025403784439,1.,0.866025403784439,1.,0.866025403784439,
1.,0.866025403784439,1.,0.866025403784439,1.,0.866025403784439,1.,0.866025403784439,
1.,0.866025403784439,1.,0.866025403784439,1.,0.866025403784439,1.,0.866025403784439,
1.,0.866025403784439,1.,0.866025403784439,1.,0.866025403784439,1.,0.866025403784439,
1.,0.866025403784439,1.,0.866025403784439,1.,0.866025403784439,1.,0.866025403784439,
1.,0.866025403784439,1.,0.866025403784439,1.,0.866025403784439,1.,0.866025403784439,
1.,0.866025403784439,1.,0.866025403784439,1.,0.866025403784439,1.,0.866025403784439,
1.,0.866025403784439,1.,0.866025403784439,1.,0.866025403784439,1.,0.866025403784439,
1.,0.866025403784439,1.,0.866025403784439,1.,0.866025403784439,1.,0.866025403784439,
1.,0.866025403784439,1.,0.866025403784439,1.,0.866025403784439,1.,0.866025403784439,
1.,0.866025403784439,1.,0.866025403784439,1.,0.866025403784439,1.,0.866025403784439,
1.,0.866025403784439,1.,0.866025403784439,1.,0.866025403784439,1.,0.866025403784439,
1.,0.866025403784439,1.,0.866025403784439,1.,0.866025403784439,1.)))
REPRESENTATION_ITEM('')
SURFACE()
);
#213=TOROIDAL_SURFACE('',#33694,2.58058373926377,0.0468749999999982);
#214=TOROIDAL_SURFACE('',#33990,2.721875,0.0468749999999996);
#215=TOROIDAL_SURFACE('',#33995,2.60625,0.0687500000000002);
#216=TOROIDAL_SURFACE('',#33998,1.65,0.15);
#217=TOROIDAL_SURFACE('',#34001,2.703125,0.0468750000000018);
#218=TOROIDAL_SURFACE('',#34005,2.703125,0.0468750000000018);
#219=TOROIDAL_SURFACE('',#34009,2.703125,0.0468750000000018);
#220=TOROIDAL_SURFACE('',#34013,2.703125,0.0468750000000018);
#221=TOROIDAL_SURFACE('',#34017,2.703125,0.0468750000000018);
#222=TOROIDAL_SURFACE('',#34021,2.703125,0.0468750000000018);
#223=TOROIDAL_SURFACE('',#34025,2.703125,0.0468750000000018);
#224=TOROIDAL_SURFACE('',#34029,2.703125,0.0468750000000018);
#225=TOROIDAL_SURFACE('',#34033,2.703125,0.0468750000000018);
#226=TOROIDAL_SURFACE('',#34037,2.703125,0.0468750000000018);
#227=TOROIDAL_SURFACE('',#34041,2.703125,0.0468750000000018);
#228=TOROIDAL_SURFACE('',#34045,2.703125,0.0468750000000018);
#229=TOROIDAL_SURFACE('',#34049,2.703125,0.0468750000000018);
#230=TOROIDAL_SURFACE('',#34053,2.703125,0.0468750000000018);
#231=TOROIDAL_SURFACE('',#34057,2.703125,0.0468750000000018);
#232=TOROIDAL_SURFACE('',#34061,2.703125,0.0468750000000018);
#233=TOROIDAL_SURFACE('',#34065,2.703125,0.0468750000000018);
#234=TOROIDAL_SURFACE('',#34069,2.703125,0.0468750000000018);
#235=TOROIDAL_SURFACE('',#34073,2.703125,0.0468750000000018);
#236=TOROIDAL_SURFACE('',#34077,2.703125,0.0468750000000018);
#237=TOROIDAL_SURFACE('',#34081,2.703125,0.0468750000000018);
#238=TOROIDAL_SURFACE('',#34085,2.703125,0.0468750000000018);
#239=TOROIDAL_SURFACE('',#34089,2.703125,0.0468750000000018);
#240=TOROIDAL_SURFACE('',#34093,2.703125,0.0468750000000018);
#241=TOROIDAL_SURFACE('',#34097,2.703125,0.0468750000000018);
#242=TOROIDAL_SURFACE('',#34101,2.703125,0.0468750000000018);
#243=TOROIDAL_SURFACE('',#34105,2.703125,0.0468750000000018);
#244=TOROIDAL_SURFACE('',#34109,2.703125,0.0468750000000018);
#245=TOROIDAL_SURFACE('',#34113,2.703125,0.0468750000000018);
#246=TOROIDAL_SURFACE('',#34117,2.703125,0.0468750000000018);
#247=TOROIDAL_SURFACE('',#34121,2.703125,0.0468750000000018);
#248=TOROIDAL_SURFACE('',#34125,2.703125,0.0468750000000018);
#249=TOROIDAL_SURFACE('',#34129,2.703125,0.0468750000000018);
#250=TOROIDAL_SURFACE('',#34133,2.703125,0.0468750000000018);
#251=TOROIDAL_SURFACE('',#34137,2.703125,0.0468750000000018);
#252=TOROIDAL_SURFACE('',#34141,2.703125,0.0468750000000018);
#253=TOROIDAL_SURFACE('',#34145,2.703125,0.0468750000000018);
#254=TOROIDAL_SURFACE('',#34149,2.703125,0.0468750000000018);
#255=TOROIDAL_SURFACE('',#34153,2.703125,0.0468750000000018);
#256=TOROIDAL_SURFACE('',#34157,2.703125,0.0468750000000018);
#257=TOROIDAL_SURFACE('',#34161,2.703125,0.0468750000000018);
#258=TOROIDAL_SURFACE('',#34165,2.703125,0.0468750000000018);
#259=TOROIDAL_SURFACE('',#34169,2.703125,0.0468750000000018);
#260=TOROIDAL_SURFACE('',#34173,2.703125,0.0468750000000018);
#261=TOROIDAL_SURFACE('',#34177,2.703125,0.0468750000000018);
#262=TOROIDAL_SURFACE('',#34181,2.703125,0.0468750000000018);
#263=TOROIDAL_SURFACE('',#34185,2.703125,0.0468750000000018);
#264=TOROIDAL_SURFACE('',#34189,2.703125,0.0468750000000018);
#265=TOROIDAL_SURFACE('',#34193,2.703125,0.0468750000000018);
#266=TOROIDAL_SURFACE('',#34197,2.703125,0.0468750000000018);
#267=TOROIDAL_SURFACE('',#34201,2.703125,0.0468750000000018);
#268=TOROIDAL_SURFACE('',#34205,2.703125,0.0468750000000018);
#269=TOROIDAL_SURFACE('',#34209,2.703125,0.0468750000000018);
#270=TOROIDAL_SURFACE('',#34213,2.703125,0.0468750000000018);
#271=TOROIDAL_SURFACE('',#34217,2.703125,0.0468750000000018);
#272=TOROIDAL_SURFACE('',#34221,2.703125,0.0468750000000018);
#273=TOROIDAL_SURFACE('',#34225,2.703125,0.0468750000000018);
#274=TOROIDAL_SURFACE('',#34229,2.703125,0.0468750000000018);
#275=TOROIDAL_SURFACE('',#34233,2.703125,0.0468750000000018);
#276=TOROIDAL_SURFACE('',#34237,2.703125,0.0468750000000018);
#277=TOROIDAL_SURFACE('',#34241,2.703125,0.0468750000000018);
#278=TOROIDAL_SURFACE('',#34245,2.703125,0.0468750000000018);
#279=TOROIDAL_SURFACE('',#34249,2.703125,0.0468750000000018);
#280=TOROIDAL_SURFACE('',#34253,2.703125,0.0468750000000018);
#281=TOROIDAL_SURFACE('',#34257,2.703125,0.0468750000000018);
#282=TOROIDAL_SURFACE('',#34261,2.703125,0.0468750000000018);
#283=TOROIDAL_SURFACE('',#34265,2.703125,0.0468750000000018);
#284=TOROIDAL_SURFACE('',#34269,2.703125,0.0468750000000018);
#285=TOROIDAL_SURFACE('',#34273,2.703125,0.0468750000000018);
#286=TOROIDAL_SURFACE('',#34277,2.703125,0.0468750000000018);
#287=TOROIDAL_SURFACE('',#34281,2.703125,0.0468750000000018);
#288=TOROIDAL_SURFACE('',#34285,2.703125,0.0468750000000018);
#289=TOROIDAL_SURFACE('',#34289,2.703125,0.0468750000000018);
#290=TOROIDAL_SURFACE('',#34293,2.703125,0.0468750000000018);
#291=TOROIDAL_SURFACE('',#34297,2.703125,0.0468750000000018);
#292=TOROIDAL_SURFACE('',#34301,2.703125,0.0468750000000018);
#293=TOROIDAL_SURFACE('',#34305,2.703125,0.0468750000000018);
#294=TOROIDAL_SURFACE('',#34309,2.703125,0.0468750000000018);
#295=TOROIDAL_SURFACE('',#34313,2.703125,0.0468750000000018);
#296=TOROIDAL_SURFACE('',#34475,2.703125,0.046874999999999);
#297=TOROIDAL_SURFACE('',#34478,2.703125,0.046874999999999);
#298=TOROIDAL_SURFACE('',#34481,2.703125,0.046874999999999);
#299=TOROIDAL_SURFACE('',#34484,2.703125,0.046874999999999);
#300=TOROIDAL_SURFACE('',#34487,2.703125,0.046874999999999);
#301=TOROIDAL_SURFACE('',#34490,2.703125,0.046874999999999);
#302=TOROIDAL_SURFACE('',#34493,2.703125,0.046874999999999);
#303=TOROIDAL_SURFACE('',#34496,2.703125,0.046874999999999);
#304=TOROIDAL_SURFACE('',#34499,2.703125,0.046874999999999);
#305=TOROIDAL_SURFACE('',#34502,2.703125,0.046874999999999);
#306=TOROIDAL_SURFACE('',#34505,2.703125,0.046874999999999);
#307=TOROIDAL_SURFACE('',#34508,2.703125,0.046874999999999);
#308=TOROIDAL_SURFACE('',#34511,2.703125,0.046874999999999);
#309=TOROIDAL_SURFACE('',#34514,2.703125,0.046874999999999);
#310=TOROIDAL_SURFACE('',#34517,2.703125,0.046874999999999);
#311=TOROIDAL_SURFACE('',#34520,2.703125,0.046874999999999);
#312=TOROIDAL_SURFACE('',#34523,2.703125,0.046874999999999);
#313=TOROIDAL_SURFACE('',#34526,2.703125,0.046874999999999);
#314=TOROIDAL_SURFACE('',#34529,2.703125,0.046874999999999);
#315=TOROIDAL_SURFACE('',#34532,2.703125,0.046874999999999);
#316=TOROIDAL_SURFACE('',#34535,2.703125,0.046874999999999);
#317=TOROIDAL_SURFACE('',#34538,2.703125,0.046874999999999);
#318=TOROIDAL_SURFACE('',#34541,2.703125,0.046874999999999);
#319=TOROIDAL_SURFACE('',#34544,2.703125,0.046874999999999);
#320=TOROIDAL_SURFACE('',#34547,2.703125,0.046874999999999);
#321=TOROIDAL_SURFACE('',#34550,2.703125,0.046874999999999);
#322=TOROIDAL_SURFACE('',#34553,2.703125,0.046874999999999);
#323=TOROIDAL_SURFACE('',#34556,2.703125,0.046874999999999);
#324=TOROIDAL_SURFACE('',#34559,2.703125,0.046874999999999);
#325=TOROIDAL_SURFACE('',#34562,2.703125,0.046874999999999);
#326=TOROIDAL_SURFACE('',#34565,2.703125,0.046874999999999);
#327=TOROIDAL_SURFACE('',#34568,2.703125,0.046874999999999);
#328=TOROIDAL_SURFACE('',#34571,2.703125,0.046874999999999);
#329=TOROIDAL_SURFACE('',#34574,2.703125,0.046874999999999);
#330=TOROIDAL_SURFACE('',#34577,2.703125,0.046874999999999);
#331=TOROIDAL_SURFACE('',#34580,2.703125,0.046874999999999);
#332=TOROIDAL_SURFACE('',#34583,2.703125,0.046874999999999);
#333=TOROIDAL_SURFACE('',#34586,2.703125,0.046874999999999);
#334=TOROIDAL_SURFACE('',#34589,2.703125,0.046874999999999);
#335=TOROIDAL_SURFACE('',#34592,2.703125,0.046874999999999);
#336=TOROIDAL_SURFACE('',#34595,2.703125,0.046874999999999);
#337=TOROIDAL_SURFACE('',#34598,2.703125,0.046874999999999);
#338=TOROIDAL_SURFACE('',#34601,2.703125,0.046874999999999);
#339=TOROIDAL_SURFACE('',#34604,2.703125,0.046874999999999);
#340=TOROIDAL_SURFACE('',#34607,2.703125,0.046874999999999);
#341=TOROIDAL_SURFACE('',#34610,2.703125,0.046874999999999);
#342=TOROIDAL_SURFACE('',#34613,2.703125,0.046874999999999);
#343=TOROIDAL_SURFACE('',#34616,2.703125,0.046874999999999);
#344=TOROIDAL_SURFACE('',#34619,2.703125,0.046874999999999);
#345=TOROIDAL_SURFACE('',#34622,2.703125,0.046874999999999);
#346=TOROIDAL_SURFACE('',#34625,2.703125,0.046874999999999);
#347=TOROIDAL_SURFACE('',#34628,2.703125,0.046874999999999);
#348=TOROIDAL_SURFACE('',#34631,2.703125,0.046874999999999);
#349=TOROIDAL_SURFACE('',#34634,2.703125,0.046874999999999);
#350=TOROIDAL_SURFACE('',#34637,2.703125,0.046874999999999);
#351=TOROIDAL_SURFACE('',#34640,2.703125,0.046874999999999);
#352=TOROIDAL_SURFACE('',#34643,2.703125,0.046874999999999);
#353=TOROIDAL_SURFACE('',#34646,2.703125,0.046874999999999);
#354=TOROIDAL_SURFACE('',#34649,2.703125,0.046874999999999);
#355=TOROIDAL_SURFACE('',#34652,2.703125,0.046874999999999);
#356=TOROIDAL_SURFACE('',#34655,2.703125,0.046874999999999);
#357=TOROIDAL_SURFACE('',#34658,2.703125,0.046874999999999);
#358=TOROIDAL_SURFACE('',#34661,2.703125,0.046874999999999);
#359=TOROIDAL_SURFACE('',#34664,2.703125,0.046874999999999);
#360=TOROIDAL_SURFACE('',#34667,2.703125,0.046874999999999);
#361=TOROIDAL_SURFACE('',#34670,2.703125,0.046874999999999);
#362=TOROIDAL_SURFACE('',#34673,2.703125,0.046874999999999);
#363=TOROIDAL_SURFACE('',#34676,2.703125,0.046874999999999);
#364=TOROIDAL_SURFACE('',#34679,2.703125,0.046874999999999);
#365=TOROIDAL_SURFACE('',#34682,2.703125,0.046874999999999);
#366=TOROIDAL_SURFACE('',#34685,2.703125,0.046874999999999);
#367=TOROIDAL_SURFACE('',#34688,2.703125,0.046874999999999);
#368=TOROIDAL_SURFACE('',#34691,2.703125,0.046874999999999);
#369=TOROIDAL_SURFACE('',#34694,2.703125,0.046874999999999);
#370=TOROIDAL_SURFACE('',#34697,2.703125,0.046874999999999);
#371=TOROIDAL_SURFACE('',#34700,2.703125,0.046874999999999);
#372=TOROIDAL_SURFACE('',#34703,2.703125,0.046874999999999);
#373=TOROIDAL_SURFACE('',#34706,2.703125,0.046874999999999);
#374=TOROIDAL_SURFACE('',#34709,2.703125,0.046874999999999);
#375=TOROIDAL_SURFACE('',#34714,2.703125,0.0468750000000018);
#376=TOROIDAL_SURFACE('',#34720,2.703125,0.046874999999999);
#868=(
BOUNDED_CURVE()
B_SPLINE_CURVE(2,(#60594,#60595,#60596),.UNSPECIFIED.,.F.,.F.)
B_SPLINE_CURVE_WITH_KNOTS((3,3),(-0.375752880509706,-0.25773139970398),
 .UNSPECIFIED.)
CURVE()
GEOMETRIC_REPRESENTATION_ITEM()
RATIONAL_B_SPLINE_CURVE((1.41147367097488,1.52065153937885,1.52065153937885))
REPRESENTATION_ITEM('')
);
#869=(
BOUNDED_CURVE()
B_SPLINE_CURVE(2,(#60598,#60599,#60600),.UNSPECIFIED.,.F.,.F.)
B_SPLINE_CURVE_WITH_KNOTS((3,3),(-0.375752880509709,-0.139709918898254),
 .UNSPECIFIED.)
CURVE()
GEOMETRIC_REPRESENTATION_ITEM()
RATIONAL_B_SPLINE_CURVE((1.41147367097488,1.62982940778282,1.41147367097488))
REPRESENTATION_ITEM('')
);
#870=(
BOUNDED_CURVE()
B_SPLINE_CURVE(2,(#60602,#60603,#60604),.UNSPECIFIED.,.F.,.F.)
B_SPLINE_CURVE_WITH_KNOTS((3,3),(-0.375752880509709,-0.139709918898254),
 .UNSPECIFIED.)
CURVE()
GEOMETRIC_REPRESENTATION_ITEM()
RATIONAL_B_SPLINE_CURVE((1.41147367097488,1.62982940778282,1.41147367097488))
REPRESENTATION_ITEM('')
);
#871=(
BOUNDED_CURVE()
B_SPLINE_CURVE(2,(#60606,#60607,#60608),.UNSPECIFIED.,.F.,.F.)
B_SPLINE_CURVE_WITH_KNOTS((3,3),(-0.375752880509708,-0.139709918898254),
 .UNSPECIFIED.)
CURVE()
GEOMETRIC_REPRESENTATION_ITEM()
RATIONAL_B_SPLINE_CURVE((1.41147367097487,1.62982940778281,1.41147367097487))
REPRESENTATION_ITEM('')
);
#872=(
BOUNDED_CURVE()
B_SPLINE_CURVE(2,(#60610,#60611,#60612),.UNSPECIFIED.,.F.,.F.)
B_SPLINE_CURVE_WITH_KNOTS((3,3),(-0.375752880509709,-0.139709918898253),
 .UNSPECIFIED.)
CURVE()
GEOMETRIC_REPRESENTATION_ITEM()
RATIONAL_B_SPLINE_CURVE((1.41147367097488,1.62982940778282,1.41147367097488))
REPRESENTATION_ITEM('')
);
#873=(
BOUNDED_CURVE()
B_SPLINE_CURVE(2,(#60614,#60615,#60616),.UNSPECIFIED.,.F.,.F.)
B_SPLINE_CURVE_WITH_KNOTS((3,3),(-0.375752880509709,-0.139709918898254),
 .UNSPECIFIED.)
CURVE()
GEOMETRIC_REPRESENTATION_ITEM()
RATIONAL_B_SPLINE_CURVE((1.41147367097488,1.62982940778282,1.41147367097488))
REPRESENTATION_ITEM('')
);
#874=(
BOUNDED_CURVE()
B_SPLINE_CURVE(2,(#60617,#60618,#60619),.UNSPECIFIED.,.F.,.F.)
B_SPLINE_CURVE_WITH_KNOTS((3,3),(-0.25773139970398,-0.139709918898256),
 .UNSPECIFIED.)
CURVE()
GEOMETRIC_REPRESENTATION_ITEM()
RATIONAL_B_SPLINE_CURVE((1.52065153937885,1.52065153937885,1.41147367097488))
REPRESENTATION_ITEM('')
);
#875=(
BOUNDED_CURVE()
B_SPLINE_CURVE(2,(#60641,#60642,#60643),.UNSPECIFIED.,.F.,.F.)
B_SPLINE_CURVE_WITH_KNOTS((3,3),(0.367644516946548,0.373830527582523),
 .UNSPECIFIED.)
CURVE()
GEOMETRIC_REPRESENTATION_ITEM()
RATIONAL_B_SPLINE_CURVE((1.13426390111316,1.13389822901309,1.13348223894575))
REPRESENTATION_ITEM('')
);
#876=(
BOUNDED_CURVE()
B_SPLINE_CURVE(2,(#60647,#60648,#60649),.UNSPECIFIED.,.F.,.F.)
B_SPLINE_CURVE_WITH_KNOTS((3,3),(0.271548216895916,0.277734227531904),
 .UNSPECIFIED.)
CURVE()
GEOMETRIC_REPRESENTATION_ITEM()
RATIONAL_B_SPLINE_CURVE((1.13348223894615,1.1338982290135,1.13426390111357))
REPRESENTATION_ITEM('')
);
#877=(
BOUNDED_CURVE()
B_SPLINE_CURVE(2,(#60653,#60654,#60655),.UNSPECIFIED.,.F.,.F.)
B_SPLINE_CURVE_WITH_KNOTS((3,3),(0.36764451694656,0.373830527582529),
 .UNSPECIFIED.)
CURVE()
GEOMETRIC_REPRESENTATION_ITEM()
RATIONAL_B_SPLINE_CURVE((1.13426390111306,1.13389822901299,1.13348223894565))
REPRESENTATION_ITEM('')
);
#878=(
BOUNDED_CURVE()
B_SPLINE_CURVE(2,(#60659,#60660,#60661),.UNSPECIFIED.,.F.,.F.)
B_SPLINE_CURVE_WITH_KNOTS((3,3),(0.271548216895914,0.277734227531901),
 .UNSPECIFIED.)
CURVE()
GEOMETRIC_REPRESENTATION_ITEM()
RATIONAL_B_SPLINE_CURVE((1.13348223894612,1.13389822901347,1.13426390111354))
REPRESENTATION_ITEM('')
);
#879=(
BOUNDED_CURVE()
B_SPLINE_CURVE(2,(#60665,#60666,#60667),.UNSPECIFIED.,.F.,.F.)
B_SPLINE_CURVE_WITH_KNOTS((3,3),(0.367644516946562,0.373830527582532),
 .UNSPECIFIED.)
CURVE()
GEOMETRIC_REPRESENTATION_ITEM()
RATIONAL_B_SPLINE_CURVE((1.13426390111304,1.13389822901297,1.13348223894563))
REPRESENTATION_ITEM('')
);
#880=(
BOUNDED_CURVE()
B_SPLINE_CURVE(2,(#60671,#60672,#60673),.UNSPECIFIED.,.F.,.F.)
B_SPLINE_CURVE_WITH_KNOTS((3,3),(0.27154821689591,0.277734227531895),
 .UNSPECIFIED.)
CURVE()
GEOMETRIC_REPRESENTATION_ITEM()
RATIONAL_B_SPLINE_CURVE((1.13348223894613,1.13389822901348,1.13426390111355))
REPRESENTATION_ITEM('')
);
#881=(
BOUNDED_CURVE()
B_SPLINE_CURVE(2,(#60677,#60678,#60679),.UNSPECIFIED.,.F.,.F.)
B_SPLINE_CURVE_WITH_KNOTS((3,3),(0.367644516946554,0.373830527582529),
 .UNSPECIFIED.)
CURVE()
GEOMETRIC_REPRESENTATION_ITEM()
RATIONAL_B_SPLINE_CURVE((1.13426390111305,1.13389822901299,1.13348223894564))
REPRESENTATION_ITEM('')
);
#882=(
BOUNDED_CURVE()
B_SPLINE_CURVE(2,(#60683,#60684,#60685),.UNSPECIFIED.,.F.,.F.)
B_SPLINE_CURVE_WITH_KNOTS((3,3),(0.271548216895907,0.277734227531893),
 .UNSPECIFIED.)
CURVE()
GEOMETRIC_REPRESENTATION_ITEM()
RATIONAL_B_SPLINE_CURVE((1.13348223894611,1.13389822901346,1.13426390111353))
REPRESENTATION_ITEM('')
);
#883=(
BOUNDED_CURVE()
B_SPLINE_CURVE(2,(#60689,#60690,#60691),.UNSPECIFIED.,.F.,.F.)
B_SPLINE_CURVE_WITH_KNOTS((3,3),(0.367644516946562,0.373830527582532),
 .UNSPECIFIED.)
CURVE()
GEOMETRIC_REPRESENTATION_ITEM()
RATIONAL_B_SPLINE_CURVE((1.13426390111302,1.13389822901296,1.13348223894561))
REPRESENTATION_ITEM('')
);
#884=(
BOUNDED_CURVE()
B_SPLINE_CURVE(2,(#60695,#60696,#60697),.UNSPECIFIED.,.F.,.F.)
B_SPLINE_CURVE_WITH_KNOTS((3,3),(0.271548216895914,0.277734227531899),
 .UNSPECIFIED.)
CURVE()
GEOMETRIC_REPRESENTATION_ITEM()
RATIONAL_B_SPLINE_CURVE((1.13348223894609,1.13389822901344,1.13426390111351))
REPRESENTATION_ITEM('')
);
#885=(
BOUNDED_CURVE()
B_SPLINE_CURVE(2,(#60701,#60702,#60703),.UNSPECIFIED.,.F.,.F.)
B_SPLINE_CURVE_WITH_KNOTS((3,3),(0.36764451694656,0.373830527582535),
 .UNSPECIFIED.)
CURVE()
GEOMETRIC_REPRESENTATION_ITEM()
RATIONAL_B_SPLINE_CURVE((1.13426390111302,1.13389822901295,1.1334822389456))
REPRESENTATION_ITEM('')
);
#886=(
BOUNDED_CURVE()
B_SPLINE_CURVE(2,(#60707,#60708,#60709),.UNSPECIFIED.,.F.,.F.)
B_SPLINE_CURVE_WITH_KNOTS((3,3),(0.271548216895908,0.277734227531894),
 .UNSPECIFIED.)
CURVE()
GEOMETRIC_REPRESENTATION_ITEM()
RATIONAL_B_SPLINE_CURVE((1.1334822389461,1.13389822901345,1.13426390111352))
REPRESENTATION_ITEM('')
);
#887=(
BOUNDED_CURVE()
B_SPLINE_CURVE(2,(#60713,#60714,#60715),.UNSPECIFIED.,.F.,.F.)
B_SPLINE_CURVE_WITH_KNOTS((3,3),(0.367644516946558,0.373830527582536),
 .UNSPECIFIED.)
CURVE()
GEOMETRIC_REPRESENTATION_ITEM()
RATIONAL_B_SPLINE_CURVE((1.13426390111302,1.13389822901295,1.13348223894561))
REPRESENTATION_ITEM('')
);
#888=(
BOUNDED_CURVE()
B_SPLINE_CURVE(2,(#60719,#60720,#60721),.UNSPECIFIED.,.F.,.F.)
B_SPLINE_CURVE_WITH_KNOTS((3,3),(0.271548216895914,0.277734227531899),
 .UNSPECIFIED.)
CURVE()
GEOMETRIC_REPRESENTATION_ITEM()
RATIONAL_B_SPLINE_CURVE((1.13348223894613,1.13389822901348,1.13426390111355))
REPRESENTATION_ITEM('')
);
#889=(
BOUNDED_CURVE()
B_SPLINE_CURVE(2,(#60725,#60726,#60727),.UNSPECIFIED.,.F.,.F.)
B_SPLINE_CURVE_WITH_KNOTS((3,3),(0.367644516946564,0.373830527582534),
 .UNSPECIFIED.)
CURVE()
GEOMETRIC_REPRESENTATION_ITEM()
RATIONAL_B_SPLINE_CURVE((1.13426390111303,1.13389822901296,1.13348223894561))
REPRESENTATION_ITEM('')
);
#890=(
BOUNDED_CURVE()
B_SPLINE_CURVE(2,(#60731,#60732,#60733),.UNSPECIFIED.,.F.,.F.)
B_SPLINE_CURVE_WITH_KNOTS((3,3),(0.271548216895916,0.277734227531901),
 .UNSPECIFIED.)
CURVE()
GEOMETRIC_REPRESENTATION_ITEM()
RATIONAL_B_SPLINE_CURVE((1.13348223894614,1.13389822901349,1.13426390111357))
REPRESENTATION_ITEM('')
);
#891=(
BOUNDED_CURVE()
B_SPLINE_CURVE(2,(#60737,#60738,#60739),.UNSPECIFIED.,.F.,.F.)
B_SPLINE_CURVE_WITH_KNOTS((3,3),(0.367644516946554,0.373830527582527),
 .UNSPECIFIED.)
CURVE()
GEOMETRIC_REPRESENTATION_ITEM()
RATIONAL_B_SPLINE_CURVE((1.13426390111312,1.13389822901305,1.13348223894571))
REPRESENTATION_ITEM('')
);
#892=(
BOUNDED_CURVE()
B_SPLINE_CURVE(2,(#60743,#60744,#60745),.UNSPECIFIED.,.F.,.F.)
B_SPLINE_CURVE_WITH_KNOTS((3,3),(0.271548216895913,0.2777342275319),
 .UNSPECIFIED.)
CURVE()
GEOMETRIC_REPRESENTATION_ITEM()
RATIONAL_B_SPLINE_CURVE((1.13348223894615,1.1338982290135,1.13426390111358))
REPRESENTATION_ITEM('')
);
#893=(
BOUNDED_CURVE()
B_SPLINE_CURVE(2,(#60749,#60750,#60751),.UNSPECIFIED.,.F.,.F.)
B_SPLINE_CURVE_WITH_KNOTS((3,3),(0.367644516946564,0.373830527582538),
 .UNSPECIFIED.)
CURVE()
GEOMETRIC_REPRESENTATION_ITEM()
RATIONAL_B_SPLINE_CURVE((1.134263901113,1.13389822901293,1.13348223894559))
REPRESENTATION_ITEM('')
);
#894=(
BOUNDED_CURVE()
B_SPLINE_CURVE(2,(#60755,#60756,#60757),.UNSPECIFIED.,.F.,.F.)
B_SPLINE_CURVE_WITH_KNOTS((3,3),(0.271548216895908,0.277734227531895),
 .UNSPECIFIED.)
CURVE()
GEOMETRIC_REPRESENTATION_ITEM()
RATIONAL_B_SPLINE_CURVE((1.13348223894615,1.1338982290135,1.13426390111358))
REPRESENTATION_ITEM('')
);
#895=(
BOUNDED_CURVE()
B_SPLINE_CURVE(2,(#60761,#60762,#60763),.UNSPECIFIED.,.F.,.F.)
B_SPLINE_CURVE_WITH_KNOTS((3,3),(0.367644516946561,0.373830527582532),
 .UNSPECIFIED.)
CURVE()
GEOMETRIC_REPRESENTATION_ITEM()
RATIONAL_B_SPLINE_CURVE((1.13426390111309,1.13389822901302,1.13348223894568))
REPRESENTATION_ITEM('')
);
#896=(
BOUNDED_CURVE()
B_SPLINE_CURVE(2,(#60767,#60768,#60769),.UNSPECIFIED.,.F.,.F.)
B_SPLINE_CURVE_WITH_KNOTS((3,3),(0.271548216895921,0.277734227531907),
 .UNSPECIFIED.)
CURVE()
GEOMETRIC_REPRESENTATION_ITEM()
RATIONAL_B_SPLINE_CURVE((1.13348223894616,1.13389822901351,1.13426390111358))
REPRESENTATION_ITEM('')
);
#897=(
BOUNDED_CURVE()
B_SPLINE_CURVE(2,(#60773,#60774,#60775),.UNSPECIFIED.,.F.,.F.)
B_SPLINE_CURVE_WITH_KNOTS((3,3),(0.367644516946558,0.373830527582535),
 .UNSPECIFIED.)
CURVE()
GEOMETRIC_REPRESENTATION_ITEM()
RATIONAL_B_SPLINE_CURVE((1.13426390111305,1.13389822901298,1.13348223894564))
REPRESENTATION_ITEM('')
);
#898=(
BOUNDED_CURVE()
B_SPLINE_CURVE(2,(#60779,#60780,#60781),.UNSPECIFIED.,.F.,.F.)
B_SPLINE_CURVE_WITH_KNOTS((3,3),(0.271548216895908,0.27773422753189),
 .UNSPECIFIED.)
CURVE()
GEOMETRIC_REPRESENTATION_ITEM()
RATIONAL_B_SPLINE_CURVE((1.13348223894616,1.13389822901351,1.13426390111359))
REPRESENTATION_ITEM('')
);
#899=(
BOUNDED_CURVE()
B_SPLINE_CURVE(2,(#60785,#60786,#60787),.UNSPECIFIED.,.F.,.F.)
B_SPLINE_CURVE_WITH_KNOTS((3,3),(0.367644516946548,0.373830527582523),
 .UNSPECIFIED.)
CURVE()
GEOMETRIC_REPRESENTATION_ITEM()
RATIONAL_B_SPLINE_CURVE((1.13426390111314,1.13389822901308,1.13348223894573))
REPRESENTATION_ITEM('')
);
#900=(
BOUNDED_CURVE()
B_SPLINE_CURVE(2,(#60791,#60792,#60793),.UNSPECIFIED.,.F.,.F.)
B_SPLINE_CURVE_WITH_KNOTS((3,3),(0.271548216895905,0.277734227531892),
 .UNSPECIFIED.)
CURVE()
GEOMETRIC_REPRESENTATION_ITEM()
RATIONAL_B_SPLINE_CURVE((1.13348223894608,1.13389822901343,1.1342639011135))
REPRESENTATION_ITEM('')
);
#901=(
BOUNDED_CURVE()
B_SPLINE_CURVE(2,(#60797,#60798,#60799),.UNSPECIFIED.,.F.,.F.)
B_SPLINE_CURVE_WITH_KNOTS((3,3),(0.36764451694655,0.373830527582528),
 .UNSPECIFIED.)
CURVE()
GEOMETRIC_REPRESENTATION_ITEM()
RATIONAL_B_SPLINE_CURVE((1.1342639011131,1.13389822901304,1.13348223894569))
REPRESENTATION_ITEM('')
);
#902=(
BOUNDED_CURVE()
B_SPLINE_CURVE(2,(#60803,#60804,#60805),.UNSPECIFIED.,.F.,.F.)
B_SPLINE_CURVE_WITH_KNOTS((3,3),(0.27154821689591,0.277734227531895),
 .UNSPECIFIED.)
CURVE()
GEOMETRIC_REPRESENTATION_ITEM()
RATIONAL_B_SPLINE_CURVE((1.13348223894612,1.13389822901347,1.13426390111354))
REPRESENTATION_ITEM('')
);
#903=(
BOUNDED_CURVE()
B_SPLINE_CURVE(2,(#60809,#60810,#60811),.UNSPECIFIED.,.F.,.F.)
B_SPLINE_CURVE_WITH_KNOTS((3,3),(0.367644516946551,0.373830527582525),
 .UNSPECIFIED.)
CURVE()
GEOMETRIC_REPRESENTATION_ITEM()
RATIONAL_B_SPLINE_CURVE((1.13426390111313,1.13389822901307,1.13348223894572))
REPRESENTATION_ITEM('')
);
#904=(
BOUNDED_CURVE()
B_SPLINE_CURVE(2,(#60815,#60816,#60817),.UNSPECIFIED.,.F.,.F.)
B_SPLINE_CURVE_WITH_KNOTS((3,3),(0.271548216895914,0.277734227531894),
 .UNSPECIFIED.)
CURVE()
GEOMETRIC_REPRESENTATION_ITEM()
RATIONAL_B_SPLINE_CURVE((1.13348223894619,1.13389822901354,1.13426390111361))
REPRESENTATION_ITEM('')
);
#905=(
BOUNDED_CURVE()
B_SPLINE_CURVE(2,(#60821,#60822,#60823),.UNSPECIFIED.,.F.,.F.)
B_SPLINE_CURVE_WITH_KNOTS((3,3),(0.367644516946565,0.373830527582531),
 .UNSPECIFIED.)
CURVE()
GEOMETRIC_REPRESENTATION_ITEM()
RATIONAL_B_SPLINE_CURVE((1.134263901113,1.13389822901293,1.13348223894559))
REPRESENTATION_ITEM('')
);
#906=(
BOUNDED_CURVE()
B_SPLINE_CURVE(2,(#60827,#60828,#60829),.UNSPECIFIED.,.F.,.F.)
B_SPLINE_CURVE_WITH_KNOTS((3,3),(0.271548216895912,0.277734227531896),
 .UNSPECIFIED.)
CURVE()
GEOMETRIC_REPRESENTATION_ITEM()
RATIONAL_B_SPLINE_CURVE((1.13348223894612,1.13389822901347,1.13426390111354))
REPRESENTATION_ITEM('')
);
#907=(
BOUNDED_CURVE()
B_SPLINE_CURVE(2,(#60833,#60834,#60835),.UNSPECIFIED.,.F.,.F.)
B_SPLINE_CURVE_WITH_KNOTS((3,3),(0.367644516946563,0.373830527582537),
 .UNSPECIFIED.)
CURVE()
GEOMETRIC_REPRESENTATION_ITEM()
RATIONAL_B_SPLINE_CURVE((1.13426390111305,1.13389822901298,1.13348223894564))
REPRESENTATION_ITEM('')
);
#908=(
BOUNDED_CURVE()
B_SPLINE_CURVE(2,(#60839,#60840,#60841),.UNSPECIFIED.,.F.,.F.)
B_SPLINE_CURVE_WITH_KNOTS((3,3),(0.271548216895909,0.277734227531891),
 .UNSPECIFIED.)
CURVE()
GEOMETRIC_REPRESENTATION_ITEM()
RATIONAL_B_SPLINE_CURVE((1.13348223894604,1.13389822901339,1.13426390111346))
REPRESENTATION_ITEM('')
);
#909=(
BOUNDED_CURVE()
B_SPLINE_CURVE(2,(#60845,#60846,#60847),.UNSPECIFIED.,.F.,.F.)
B_SPLINE_CURVE_WITH_KNOTS((3,3),(0.367644516946552,0.373830527582532),
 .UNSPECIFIED.)
CURVE()
GEOMETRIC_REPRESENTATION_ITEM()
RATIONAL_B_SPLINE_CURVE((1.13426390111305,1.13389822901299,1.13348223894564))
REPRESENTATION_ITEM('')
);
#910=(
BOUNDED_CURVE()
B_SPLINE_CURVE(2,(#60851,#60852,#60853),.UNSPECIFIED.,.F.,.F.)
B_SPLINE_CURVE_WITH_KNOTS((3,3),(0.271548216895916,0.277734227531902),
 .UNSPECIFIED.)
CURVE()
GEOMETRIC_REPRESENTATION_ITEM()
RATIONAL_B_SPLINE_CURVE((1.13348223894616,1.13389822901351,1.13426390111359))
REPRESENTATION_ITEM('')
);
#911=(
BOUNDED_CURVE()
B_SPLINE_CURVE(2,(#60857,#60858,#60859),.UNSPECIFIED.,.F.,.F.)
B_SPLINE_CURVE_WITH_KNOTS((3,3),(0.367644516946562,0.373830527582535),
 .UNSPECIFIED.)
CURVE()
GEOMETRIC_REPRESENTATION_ITEM()
RATIONAL_B_SPLINE_CURVE((1.13426390111309,1.13389822901302,1.13348223894568))
REPRESENTATION_ITEM('')
);
#912=(
BOUNDED_CURVE()
B_SPLINE_CURVE(2,(#60863,#60864,#60865),.UNSPECIFIED.,.F.,.F.)
B_SPLINE_CURVE_WITH_KNOTS((3,3),(0.271548216895913,0.277734227531904),
 .UNSPECIFIED.)
CURVE()
GEOMETRIC_REPRESENTATION_ITEM()
RATIONAL_B_SPLINE_CURVE((1.13348223894619,1.13389822901354,1.13426390111362))
REPRESENTATION_ITEM('')
);
#913=(
BOUNDED_CURVE()
B_SPLINE_CURVE(2,(#60869,#60870,#60871),.UNSPECIFIED.,.F.,.F.)
B_SPLINE_CURVE_WITH_KNOTS((3,3),(0.36764451694655,0.373830527582524),
 .UNSPECIFIED.)
CURVE()
GEOMETRIC_REPRESENTATION_ITEM()
RATIONAL_B_SPLINE_CURVE((1.13426390111312,1.13389822901305,1.13348223894571))
REPRESENTATION_ITEM('')
);
#914=(
BOUNDED_CURVE()
B_SPLINE_CURVE(2,(#60875,#60876,#60877),.UNSPECIFIED.,.F.,.F.)
B_SPLINE_CURVE_WITH_KNOTS((3,3),(0.271548216895921,0.277734227531899),
 .UNSPECIFIED.)
CURVE()
GEOMETRIC_REPRESENTATION_ITEM()
RATIONAL_B_SPLINE_CURVE((1.13348223894619,1.13389822901354,1.13426390111361))
REPRESENTATION_ITEM('')
);
#915=(
BOUNDED_CURVE()
B_SPLINE_CURVE(2,(#60881,#60882,#60883),.UNSPECIFIED.,.F.,.F.)
B_SPLINE_CURVE_WITH_KNOTS((3,3),(0.367644516946559,0.373830527582526),
 .UNSPECIFIED.)
CURVE()
GEOMETRIC_REPRESENTATION_ITEM()
RATIONAL_B_SPLINE_CURVE((1.1342639011131,1.13389822901303,1.13348223894569))
REPRESENTATION_ITEM('')
);
#916=(
BOUNDED_CURVE()
B_SPLINE_CURVE(2,(#60887,#60888,#60889),.UNSPECIFIED.,.F.,.F.)
B_SPLINE_CURVE_WITH_KNOTS((3,3),(0.271548216895914,0.2777342275319),
 .UNSPECIFIED.)
CURVE()
GEOMETRIC_REPRESENTATION_ITEM()
RATIONAL_B_SPLINE_CURVE((1.13348223894616,1.13389822901351,1.13426390111358))
REPRESENTATION_ITEM('')
);
#917=(
BOUNDED_CURVE()
B_SPLINE_CURVE(2,(#60893,#60894,#60895),.UNSPECIFIED.,.F.,.F.)
B_SPLINE_CURVE_WITH_KNOTS((3,3),(0.367644516946557,0.373830527582536),
 .UNSPECIFIED.)
CURVE()
GEOMETRIC_REPRESENTATION_ITEM()
RATIONAL_B_SPLINE_CURVE((1.13426390111309,1.13389822901303,1.13348223894568))
REPRESENTATION_ITEM('')
);
#918=(
BOUNDED_CURVE()
B_SPLINE_CURVE(2,(#60899,#60900,#60901),.UNSPECIFIED.,.F.,.F.)
B_SPLINE_CURVE_WITH_KNOTS((3,3),(0.271548216895912,0.277734227531897),
 .UNSPECIFIED.)
CURVE()
GEOMETRIC_REPRESENTATION_ITEM()
RATIONAL_B_SPLINE_CURVE((1.13348223894616,1.13389822901351,1.13426390111358))
REPRESENTATION_ITEM('')
);
#919=(
BOUNDED_CURVE()
B_SPLINE_CURVE(2,(#60905,#60906,#60907),.UNSPECIFIED.,.F.,.F.)
B_SPLINE_CURVE_WITH_KNOTS((3,3),(0.367644516946558,0.373830527582532),
 .UNSPECIFIED.)
CURVE()
GEOMETRIC_REPRESENTATION_ITEM()
RATIONAL_B_SPLINE_CURVE((1.13426390111307,1.13389822901301,1.13348223894566))
REPRESENTATION_ITEM('')
);
#920=(
BOUNDED_CURVE()
B_SPLINE_CURVE(2,(#60911,#60912,#60913),.UNSPECIFIED.,.F.,.F.)
B_SPLINE_CURVE_WITH_KNOTS((3,3),(0.271548216895914,0.277734227531905),
 .UNSPECIFIED.)
CURVE()
GEOMETRIC_REPRESENTATION_ITEM()
RATIONAL_B_SPLINE_CURVE((1.13348223894616,1.13389822901351,1.13426390111358))
REPRESENTATION_ITEM('')
);
#921=(
BOUNDED_CURVE()
B_SPLINE_CURVE(2,(#60917,#60918,#60919),.UNSPECIFIED.,.F.,.F.)
B_SPLINE_CURVE_WITH_KNOTS((3,3),(0.367644516946569,0.373830527582539),
 .UNSPECIFIED.)
CURVE()
GEOMETRIC_REPRESENTATION_ITEM()
RATIONAL_B_SPLINE_CURVE((1.13426390111301,1.13389822901295,1.1334822389456))
REPRESENTATION_ITEM('')
);
#922=(
BOUNDED_CURVE()
B_SPLINE_CURVE(2,(#60923,#60924,#60925),.UNSPECIFIED.,.F.,.F.)
B_SPLINE_CURVE_WITH_KNOTS((3,3),(0.271548216895913,0.2777342275319),
 .UNSPECIFIED.)
CURVE()
GEOMETRIC_REPRESENTATION_ITEM()
RATIONAL_B_SPLINE_CURVE((1.13348223894614,1.13389822901349,1.13426390111356))
REPRESENTATION_ITEM('')
);
#923=(
BOUNDED_CURVE()
B_SPLINE_CURVE(2,(#60929,#60930,#60931),.UNSPECIFIED.,.F.,.F.)
B_SPLINE_CURVE_WITH_KNOTS((3,3),(0.367644516946566,0.373830527582539),
 .UNSPECIFIED.)
CURVE()
GEOMETRIC_REPRESENTATION_ITEM()
RATIONAL_B_SPLINE_CURVE((1.13426390111297,1.1338982290129,1.13348223894556))
REPRESENTATION_ITEM('')
);
#924=(
BOUNDED_CURVE()
B_SPLINE_CURVE(2,(#60935,#60936,#60937),.UNSPECIFIED.,.F.,.F.)
B_SPLINE_CURVE_WITH_KNOTS((3,3),(0.271548216895926,0.277734227531904),
 .UNSPECIFIED.)
CURVE()
GEOMETRIC_REPRESENTATION_ITEM()
RATIONAL_B_SPLINE_CURVE((1.13348223894627,1.13389822901362,1.1342639011137))
REPRESENTATION_ITEM('')
);
#925=(
BOUNDED_CURVE()
B_SPLINE_CURVE(2,(#60941,#60942,#60943),.UNSPECIFIED.,.F.,.F.)
B_SPLINE_CURVE_WITH_KNOTS((3,3),(0.367644516946557,0.373830527582532),
 .UNSPECIFIED.)
CURVE()
GEOMETRIC_REPRESENTATION_ITEM()
RATIONAL_B_SPLINE_CURVE((1.13426390111306,1.13389822901299,1.13348223894565))
REPRESENTATION_ITEM('')
);
#926=(
BOUNDED_CURVE()
B_SPLINE_CURVE(2,(#60947,#60948,#60949),.UNSPECIFIED.,.F.,.F.)
B_SPLINE_CURVE_WITH_KNOTS((3,3),(0.271548216895913,0.277734227531899),
 .UNSPECIFIED.)
CURVE()
GEOMETRIC_REPRESENTATION_ITEM()
RATIONAL_B_SPLINE_CURVE((1.13348223894618,1.13389822901353,1.13426390111361))
REPRESENTATION_ITEM('')
);
#927=(
BOUNDED_CURVE()
B_SPLINE_CURVE(2,(#60953,#60954,#60955),.UNSPECIFIED.,.F.,.F.)
B_SPLINE_CURVE_WITH_KNOTS((3,3),(0.367644516946561,0.373830527582535),
 .UNSPECIFIED.)
CURVE()
GEOMETRIC_REPRESENTATION_ITEM()
RATIONAL_B_SPLINE_CURVE((1.13426390111305,1.13389822901298,1.13348223894564))
REPRESENTATION_ITEM('')
);
#928=(
BOUNDED_CURVE()
B_SPLINE_CURVE(2,(#60959,#60960,#60961),.UNSPECIFIED.,.F.,.F.)
B_SPLINE_CURVE_WITH_KNOTS((3,3),(0.271548216895915,0.277734227531905),
 .UNSPECIFIED.)
CURVE()
GEOMETRIC_REPRESENTATION_ITEM()
RATIONAL_B_SPLINE_CURVE((1.13348223894613,1.13389822901348,1.13426390111356))
REPRESENTATION_ITEM('')
);
#929=(
BOUNDED_CURVE()
B_SPLINE_CURVE(2,(#60965,#60966,#60967),.UNSPECIFIED.,.F.,.F.)
B_SPLINE_CURVE_WITH_KNOTS((3,3),(0.367644516946559,0.373830527582528),
 .UNSPECIFIED.)
CURVE()
GEOMETRIC_REPRESENTATION_ITEM()
RATIONAL_B_SPLINE_CURVE((1.13426390111303,1.13389822901297,1.13348223894562))
REPRESENTATION_ITEM('')
);
#930=(
BOUNDED_CURVE()
B_SPLINE_CURVE(2,(#60971,#60972,#60973),.UNSPECIFIED.,.F.,.F.)
B_SPLINE_CURVE_WITH_KNOTS((3,3),(0.271548216895913,0.277734227531899),
 .UNSPECIFIED.)
CURVE()
GEOMETRIC_REPRESENTATION_ITEM()
RATIONAL_B_SPLINE_CURVE((1.13348223894613,1.13389822901348,1.13426390111356))
REPRESENTATION_ITEM('')
);
#931=(
BOUNDED_CURVE()
B_SPLINE_CURVE(2,(#60977,#60978,#60979),.UNSPECIFIED.,.F.,.F.)
B_SPLINE_CURVE_WITH_KNOTS((3,3),(0.367644516946557,0.373830527582533),
 .UNSPECIFIED.)
CURVE()
GEOMETRIC_REPRESENTATION_ITEM()
RATIONAL_B_SPLINE_CURVE((1.13426390111302,1.13389822901296,1.13348223894561))
REPRESENTATION_ITEM('')
);
#932=(
BOUNDED_CURVE()
B_SPLINE_CURVE(2,(#60983,#60984,#60985),.UNSPECIFIED.,.F.,.F.)
B_SPLINE_CURVE_WITH_KNOTS((3,3),(0.271548216895926,0.277734227531906),
 .UNSPECIFIED.)
CURVE()
GEOMETRIC_REPRESENTATION_ITEM()
RATIONAL_B_SPLINE_CURVE((1.13348223894624,1.13389822901359,1.13426390111366))
REPRESENTATION_ITEM('')
);
#933=(
BOUNDED_CURVE()
B_SPLINE_CURVE(2,(#60989,#60990,#60991),.UNSPECIFIED.,.F.,.F.)
B_SPLINE_CURVE_WITH_KNOTS((3,3),(0.367644516946561,0.373830527582536),
 .UNSPECIFIED.)
CURVE()
GEOMETRIC_REPRESENTATION_ITEM()
RATIONAL_B_SPLINE_CURVE((1.13426390111306,1.13389822901299,1.13348223894564))
REPRESENTATION_ITEM('')
);
#934=(
BOUNDED_CURVE()
B_SPLINE_CURVE(2,(#60995,#60996,#60997),.UNSPECIFIED.,.F.,.F.)
B_SPLINE_CURVE_WITH_KNOTS((3,3),(0.271548216895911,0.277734227531901),
 .UNSPECIFIED.)
CURVE()
GEOMETRIC_REPRESENTATION_ITEM()
RATIONAL_B_SPLINE_CURVE((1.13348223894609,1.13389822901344,1.13426390111352))
REPRESENTATION_ITEM('')
);
#935=(
BOUNDED_CURVE()
B_SPLINE_CURVE(2,(#61001,#61002,#61003),.UNSPECIFIED.,.F.,.F.)
B_SPLINE_CURVE_WITH_KNOTS((3,3),(0.367644516946558,0.373830527582533),
 .UNSPECIFIED.)
CURVE()
GEOMETRIC_REPRESENTATION_ITEM()
RATIONAL_B_SPLINE_CURVE((1.1342639011131,1.13389822901303,1.13348223894569))
REPRESENTATION_ITEM('')
);
#936=(
BOUNDED_CURVE()
B_SPLINE_CURVE(2,(#61007,#61008,#61009),.UNSPECIFIED.,.F.,.F.)
B_SPLINE_CURVE_WITH_KNOTS((3,3),(0.271548216895922,0.277734227531909),
 .UNSPECIFIED.)
CURVE()
GEOMETRIC_REPRESENTATION_ITEM()
RATIONAL_B_SPLINE_CURVE((1.13348223894623,1.13389822901358,1.13426390111366))
REPRESENTATION_ITEM('')
);
#937=(
BOUNDED_CURVE()
B_SPLINE_CURVE(2,(#61013,#61014,#61015),.UNSPECIFIED.,.F.,.F.)
B_SPLINE_CURVE_WITH_KNOTS((3,3),(0.367644516946562,0.373830527582538),
 .UNSPECIFIED.)
CURVE()
GEOMETRIC_REPRESENTATION_ITEM()
RATIONAL_B_SPLINE_CURVE((1.13426390111305,1.13389822901298,1.13348223894563))
REPRESENTATION_ITEM('')
);
#938=(
BOUNDED_CURVE()
B_SPLINE_CURVE(2,(#61019,#61020,#61021),.UNSPECIFIED.,.F.,.F.)
B_SPLINE_CURVE_WITH_KNOTS((3,3),(0.271548216895906,0.277734227531898),
 .UNSPECIFIED.)
CURVE()
GEOMETRIC_REPRESENTATION_ITEM()
RATIONAL_B_SPLINE_CURVE((1.13348223894604,1.13389822901339,1.13426390111346))
REPRESENTATION_ITEM('')
);
#939=(
BOUNDED_CURVE()
B_SPLINE_CURVE(2,(#61025,#61026,#61027),.UNSPECIFIED.,.F.,.F.)
B_SPLINE_CURVE_WITH_KNOTS((3,3),(0.367644516946563,0.373830527582537),
 .UNSPECIFIED.)
CURVE()
GEOMETRIC_REPRESENTATION_ITEM()
RATIONAL_B_SPLINE_CURVE((1.134263901113,1.13389822901294,1.13348223894559))
REPRESENTATION_ITEM('')
);
#940=(
BOUNDED_CURVE()
B_SPLINE_CURVE(2,(#61031,#61032,#61033),.UNSPECIFIED.,.F.,.F.)
B_SPLINE_CURVE_WITH_KNOTS((3,3),(0.271548216895914,0.277734227531897),
 .UNSPECIFIED.)
CURVE()
GEOMETRIC_REPRESENTATION_ITEM()
RATIONAL_B_SPLINE_CURVE((1.13348223894613,1.13389822901348,1.13426390111355))
REPRESENTATION_ITEM('')
);
#941=(
BOUNDED_CURVE()
B_SPLINE_CURVE(2,(#61037,#61038,#61039),.UNSPECIFIED.,.F.,.F.)
B_SPLINE_CURVE_WITH_KNOTS((3,3),(0.367644516946558,0.373830527582532),
 .UNSPECIFIED.)
CURVE()
GEOMETRIC_REPRESENTATION_ITEM()
RATIONAL_B_SPLINE_CURVE((1.13426390111307,1.133898229013,1.13348223894566))
REPRESENTATION_ITEM('')
);
#942=(
BOUNDED_CURVE()
B_SPLINE_CURVE(2,(#61043,#61044,#61045),.UNSPECIFIED.,.F.,.F.)
B_SPLINE_CURVE_WITH_KNOTS((3,3),(0.271548216895917,0.277734227531901),
 .UNSPECIFIED.)
CURVE()
GEOMETRIC_REPRESENTATION_ITEM()
RATIONAL_B_SPLINE_CURVE((1.13348223894616,1.1338982290135,1.13426390111358))
REPRESENTATION_ITEM('')
);
#943=(
BOUNDED_CURVE()
B_SPLINE_CURVE(2,(#61049,#61050,#61051),.UNSPECIFIED.,.F.,.F.)
B_SPLINE_CURVE_WITH_KNOTS((3,3),(0.367644516946556,0.37383052758253),
 .UNSPECIFIED.)
CURVE()
GEOMETRIC_REPRESENTATION_ITEM()
RATIONAL_B_SPLINE_CURVE((1.13426390111304,1.13389822901297,1.13348223894563))
REPRESENTATION_ITEM('')
);
#944=(
BOUNDED_CURVE()
B_SPLINE_CURVE(2,(#61055,#61056,#61057),.UNSPECIFIED.,.F.,.F.)
B_SPLINE_CURVE_WITH_KNOTS((3,3),(0.271548216895911,0.277734227531893),
 .UNSPECIFIED.)
CURVE()
GEOMETRIC_REPRESENTATION_ITEM()
RATIONAL_B_SPLINE_CURVE((1.13348223894607,1.13389822901342,1.13426390111349))
REPRESENTATION_ITEM('')
);
#945=(
BOUNDED_CURVE()
B_SPLINE_CURVE(2,(#61061,#61062,#61063),.UNSPECIFIED.,.F.,.F.)
B_SPLINE_CURVE_WITH_KNOTS((3,3),(0.367644516946565,0.373830527582539),
 .UNSPECIFIED.)
CURVE()
GEOMETRIC_REPRESENTATION_ITEM()
RATIONAL_B_SPLINE_CURVE((1.13426390111301,1.13389822901295,1.1334822389456))
REPRESENTATION_ITEM('')
);
#946=(
BOUNDED_CURVE()
B_SPLINE_CURVE(2,(#61067,#61068,#61069),.UNSPECIFIED.,.F.,.F.)
B_SPLINE_CURVE_WITH_KNOTS((3,3),(0.271548216895916,0.277734227531897),
 .UNSPECIFIED.)
CURVE()
GEOMETRIC_REPRESENTATION_ITEM()
RATIONAL_B_SPLINE_CURVE((1.13348223894613,1.13389822901348,1.13426390111355))
REPRESENTATION_ITEM('')
);
#947=(
BOUNDED_CURVE()
B_SPLINE_CURVE(2,(#61073,#61074,#61075),.UNSPECIFIED.,.F.,.F.)
B_SPLINE_CURVE_WITH_KNOTS((3,3),(0.36764451694656,0.373830527582534),
 .UNSPECIFIED.)
CURVE()
GEOMETRIC_REPRESENTATION_ITEM()
RATIONAL_B_SPLINE_CURVE((1.13426390111306,1.13389822901299,1.13348223894564))
REPRESENTATION_ITEM('')
);
#948=(
BOUNDED_CURVE()
B_SPLINE_CURVE(2,(#61079,#61080,#61081),.UNSPECIFIED.,.F.,.F.)
B_SPLINE_CURVE_WITH_KNOTS((3,3),(0.271548216895918,0.277734227531904),
 .UNSPECIFIED.)
CURVE()
GEOMETRIC_REPRESENTATION_ITEM()
RATIONAL_B_SPLINE_CURVE((1.13348223894613,1.13389822901348,1.13426390111355))
REPRESENTATION_ITEM('')
);
#949=(
BOUNDED_CURVE()
B_SPLINE_CURVE(2,(#61085,#61086,#61087),.UNSPECIFIED.,.F.,.F.)
B_SPLINE_CURVE_WITH_KNOTS((3,3),(0.367644516946555,0.373830527582533),
 .UNSPECIFIED.)
CURVE()
GEOMETRIC_REPRESENTATION_ITEM()
RATIONAL_B_SPLINE_CURVE((1.13426390111305,1.13389822901298,1.13348223894564))
REPRESENTATION_ITEM('')
);
#950=(
BOUNDED_CURVE()
B_SPLINE_CURVE(2,(#61091,#61092,#61093),.UNSPECIFIED.,.F.,.F.)
B_SPLINE_CURVE_WITH_KNOTS((3,3),(0.271548216895928,0.277734227531916),
 .UNSPECIFIED.)
CURVE()
GEOMETRIC_REPRESENTATION_ITEM()
RATIONAL_B_SPLINE_CURVE((1.13348223894621,1.13389822901356,1.13426390111363))
REPRESENTATION_ITEM('')
);
#951=(
BOUNDED_CURVE()
B_SPLINE_CURVE(2,(#61097,#61098,#61099),.UNSPECIFIED.,.F.,.F.)
B_SPLINE_CURVE_WITH_KNOTS((3,3),(0.367644516946548,0.373830527582523),
 .UNSPECIFIED.)
CURVE()
GEOMETRIC_REPRESENTATION_ITEM()
RATIONAL_B_SPLINE_CURVE((1.13426390111312,1.13389822901305,1.13348223894571))
REPRESENTATION_ITEM('')
);
#952=(
BOUNDED_CURVE()
B_SPLINE_CURVE(2,(#61103,#61104,#61105),.UNSPECIFIED.,.F.,.F.)
B_SPLINE_CURVE_WITH_KNOTS((3,3),(0.271548216895918,0.277734227531905),
 .UNSPECIFIED.)
CURVE()
GEOMETRIC_REPRESENTATION_ITEM()
RATIONAL_B_SPLINE_CURVE((1.13348223894611,1.13389822901346,1.13426390111354))
REPRESENTATION_ITEM('')
);
#953=(
BOUNDED_CURVE()
B_SPLINE_CURVE(2,(#61109,#61110,#61111),.UNSPECIFIED.,.F.,.F.)
B_SPLINE_CURVE_WITH_KNOTS((3,3),(0.367644516946559,0.373830527582532),
 .UNSPECIFIED.)
CURVE()
GEOMETRIC_REPRESENTATION_ITEM()
RATIONAL_B_SPLINE_CURVE((1.13426390111305,1.13389822901298,1.13348223894564))
REPRESENTATION_ITEM('')
);
#954=(
BOUNDED_CURVE()
B_SPLINE_CURVE(2,(#61115,#61116,#61117),.UNSPECIFIED.,.F.,.F.)
B_SPLINE_CURVE_WITH_KNOTS((3,3),(0.271548216895915,0.277734227531901),
 .UNSPECIFIED.)
CURVE()
GEOMETRIC_REPRESENTATION_ITEM()
RATIONAL_B_SPLINE_CURVE((1.13348223894615,1.1338982290135,1.13426390111357))
REPRESENTATION_ITEM('')
);
#955=(
BOUNDED_CURVE()
B_SPLINE_CURVE(2,(#61121,#61122,#61123),.UNSPECIFIED.,.F.,.F.)
B_SPLINE_CURVE_WITH_KNOTS((3,3),(0.367644516946548,0.373830527582526),
 .UNSPECIFIED.)
CURVE()
GEOMETRIC_REPRESENTATION_ITEM()
RATIONAL_B_SPLINE_CURVE((1.13426390111308,1.13389822901302,1.13348223894567))
REPRESENTATION_ITEM('')
);
#956=(
BOUNDED_CURVE()
B_SPLINE_CURVE(2,(#61127,#61128,#61129),.UNSPECIFIED.,.F.,.F.)
B_SPLINE_CURVE_WITH_KNOTS((3,3),(0.271548216895917,0.277734227531902),
 .UNSPECIFIED.)
CURVE()
GEOMETRIC_REPRESENTATION_ITEM()
RATIONAL_B_SPLINE_CURVE((1.13348223894615,1.1338982290135,1.13426390111358))
REPRESENTATION_ITEM('')
);
#957=(
BOUNDED_CURVE()
B_SPLINE_CURVE(2,(#61133,#61134,#61135),.UNSPECIFIED.,.F.,.F.)
B_SPLINE_CURVE_WITH_KNOTS((3,3),(0.367644516946561,0.373830527582534),
 .UNSPECIFIED.)
CURVE()
GEOMETRIC_REPRESENTATION_ITEM()
RATIONAL_B_SPLINE_CURVE((1.13426390111303,1.13389822901296,1.13348223894562))
REPRESENTATION_ITEM('')
);
#958=(
BOUNDED_CURVE()
B_SPLINE_CURVE(2,(#61139,#61140,#61141),.UNSPECIFIED.,.F.,.F.)
B_SPLINE_CURVE_WITH_KNOTS((3,3),(0.271548216895922,0.277734227531908),
 .UNSPECIFIED.)
CURVE()
GEOMETRIC_REPRESENTATION_ITEM()
RATIONAL_B_SPLINE_CURVE((1.13348223894617,1.13389822901352,1.1342639011136))
REPRESENTATION_ITEM('')
);
#959=(
BOUNDED_CURVE()
B_SPLINE_CURVE(2,(#61145,#61146,#61147),.UNSPECIFIED.,.F.,.F.)
B_SPLINE_CURVE_WITH_KNOTS((3,3),(0.367644516946555,0.373830527582532),
 .UNSPECIFIED.)
CURVE()
GEOMETRIC_REPRESENTATION_ITEM()
RATIONAL_B_SPLINE_CURVE((1.13426390111307,1.133898229013,1.13348223894566))
REPRESENTATION_ITEM('')
);
#960=(
BOUNDED_CURVE()
B_SPLINE_CURVE(2,(#61151,#61152,#61153),.UNSPECIFIED.,.F.,.F.)
B_SPLINE_CURVE_WITH_KNOTS((3,3),(0.27154821689592,0.277734227531907),
 .UNSPECIFIED.)
CURVE()
GEOMETRIC_REPRESENTATION_ITEM()
RATIONAL_B_SPLINE_CURVE((1.13348223894614,1.13389822901349,1.13426390111356))
REPRESENTATION_ITEM('')
);
#961=(
BOUNDED_CURVE()
B_SPLINE_CURVE(2,(#61157,#61158,#61159),.UNSPECIFIED.,.F.,.F.)
B_SPLINE_CURVE_WITH_KNOTS((3,3),(0.367644516946564,0.373830527582538),
 .UNSPECIFIED.)
CURVE()
GEOMETRIC_REPRESENTATION_ITEM()
RATIONAL_B_SPLINE_CURVE((1.13426390111299,1.13389822901292,1.13348223894557))
REPRESENTATION_ITEM('')
);
#962=(
BOUNDED_CURVE()
B_SPLINE_CURVE(2,(#61163,#61164,#61165),.UNSPECIFIED.,.F.,.F.)
B_SPLINE_CURVE_WITH_KNOTS((3,3),(0.271548216895926,0.277734227531912),
 .UNSPECIFIED.)
CURVE()
GEOMETRIC_REPRESENTATION_ITEM()
RATIONAL_B_SPLINE_CURVE((1.13348223894617,1.13389822901352,1.13426390111359))
REPRESENTATION_ITEM('')
);
#963=(
BOUNDED_CURVE()
B_SPLINE_CURVE(2,(#61169,#61170,#61171),.UNSPECIFIED.,.F.,.F.)
B_SPLINE_CURVE_WITH_KNOTS((3,3),(0.367644516946548,0.373830527582525),
 .UNSPECIFIED.)
CURVE()
GEOMETRIC_REPRESENTATION_ITEM()
RATIONAL_B_SPLINE_CURVE((1.13426390111308,1.13389822901301,1.13348223894567))
REPRESENTATION_ITEM('')
);
#964=(
BOUNDED_CURVE()
B_SPLINE_CURVE(2,(#61175,#61176,#61177),.UNSPECIFIED.,.F.,.F.)
B_SPLINE_CURVE_WITH_KNOTS((3,3),(0.271548216895921,0.277734227531907),
 .UNSPECIFIED.)
CURVE()
GEOMETRIC_REPRESENTATION_ITEM()
RATIONAL_B_SPLINE_CURVE((1.13348223894617,1.13389822901352,1.13426390111359))
REPRESENTATION_ITEM('')
);
#965=(
BOUNDED_CURVE()
B_SPLINE_CURVE(2,(#61181,#61182,#61183),.UNSPECIFIED.,.F.,.F.)
B_SPLINE_CURVE_WITH_KNOTS((3,3),(0.367644516946557,0.373830527582527),
 .UNSPECIFIED.)
CURVE()
GEOMETRIC_REPRESENTATION_ITEM()
RATIONAL_B_SPLINE_CURVE((1.1342639011131,1.13389822901303,1.13348223894569))
REPRESENTATION_ITEM('')
);
#966=(
BOUNDED_CURVE()
B_SPLINE_CURVE(2,(#61186,#61187,#61188),.UNSPECIFIED.,.F.,.F.)
B_SPLINE_CURVE_WITH_KNOTS((3,3),(0.271548216895922,0.277734227531908),
 .UNSPECIFIED.)
CURVE()
GEOMETRIC_REPRESENTATION_ITEM()
RATIONAL_B_SPLINE_CURVE((1.13348223894615,1.1338982290135,1.13426390111358))
REPRESENTATION_ITEM('')
);
#967=(
BOUNDED_CURVE()
B_SPLINE_CURVE(2,(#61190,#61191,#61192),.UNSPECIFIED.,.F.,.F.)
B_SPLINE_CURVE_WITH_KNOTS((3,3),(0.367644516946556,0.373830527582529),
 .UNSPECIFIED.)
CURVE()
GEOMETRIC_REPRESENTATION_ITEM()
RATIONAL_B_SPLINE_CURVE((1.13426390111308,1.13389822901301,1.13348223894567))
REPRESENTATION_ITEM('')
);
#968=(
BOUNDED_CURVE()
B_SPLINE_CURVE(2,(#61195,#61196,#61197),.UNSPECIFIED.,.F.,.F.)
B_SPLINE_CURVE_WITH_KNOTS((3,3),(0.271548216895921,0.277734227531909),
 .UNSPECIFIED.)
CURVE()
GEOMETRIC_REPRESENTATION_ITEM()
RATIONAL_B_SPLINE_CURVE((1.13348223894619,1.13389822901354,1.13426390111361))
REPRESENTATION_ITEM('')
);
#969=(
BOUNDED_CURVE()
B_SPLINE_CURVE(2,(#61199,#61200,#61201),.UNSPECIFIED.,.F.,.F.)
B_SPLINE_CURVE_WITH_KNOTS((3,3),(0.36764451694656,0.37383052758253),
 .UNSPECIFIED.)
CURVE()
GEOMETRIC_REPRESENTATION_ITEM()
RATIONAL_B_SPLINE_CURVE((1.13426390111303,1.13389822901296,1.13348223894562))
REPRESENTATION_ITEM('')
);
#970=(
BOUNDED_CURVE()
B_SPLINE_CURVE(2,(#61204,#61205,#61206),.UNSPECIFIED.,.F.,.F.)
B_SPLINE_CURVE_WITH_KNOTS((3,3),(0.271548216895921,0.277734227531907),
 .UNSPECIFIED.)
CURVE()
GEOMETRIC_REPRESENTATION_ITEM()
RATIONAL_B_SPLINE_CURVE((1.13348223894618,1.13389822901353,1.1342639011136))
REPRESENTATION_ITEM('')
);
#971=(
BOUNDED_CURVE()
B_SPLINE_CURVE(2,(#61208,#61209,#61210),.UNSPECIFIED.,.F.,.F.)
B_SPLINE_CURVE_WITH_KNOTS((3,3),(0.367644516946553,0.373830527582534),
 .UNSPECIFIED.)
CURVE()
GEOMETRIC_REPRESENTATION_ITEM()
RATIONAL_B_SPLINE_CURVE((1.13426390111306,1.13389822901299,1.13348223894565))
REPRESENTATION_ITEM('')
);
#972=(
BOUNDED_CURVE()
B_SPLINE_CURVE(2,(#61213,#61214,#61215),.UNSPECIFIED.,.F.,.F.)
B_SPLINE_CURVE_WITH_KNOTS((3,3),(0.271548216895916,0.277734227531903),
 .UNSPECIFIED.)
CURVE()
GEOMETRIC_REPRESENTATION_ITEM()
RATIONAL_B_SPLINE_CURVE((1.13348223894615,1.1338982290135,1.13426390111357))
REPRESENTATION_ITEM('')
);
#973=(
BOUNDED_CURVE()
B_SPLINE_CURVE(2,(#61217,#61218,#61219),.UNSPECIFIED.,.F.,.F.)
B_SPLINE_CURVE_WITH_KNOTS((3,3),(0.367644516946558,0.373830527582532),
 .UNSPECIFIED.)
CURVE()
GEOMETRIC_REPRESENTATION_ITEM()
RATIONAL_B_SPLINE_CURVE((1.13426390111307,1.13389822901301,1.13348223894566))
REPRESENTATION_ITEM('')
);
#974=(
BOUNDED_CURVE()
B_SPLINE_CURVE(2,(#61222,#61223,#61224),.UNSPECIFIED.,.F.,.F.)
B_SPLINE_CURVE_WITH_KNOTS((3,3),(0.271548216895911,0.277734227531895),
 .UNSPECIFIED.)
CURVE()
GEOMETRIC_REPRESENTATION_ITEM()
RATIONAL_B_SPLINE_CURVE((1.13348223894606,1.13389822901341,1.13426390111348))
REPRESENTATION_ITEM('')
);
#975=(
BOUNDED_CURVE()
B_SPLINE_CURVE(2,(#61226,#61227,#61228),.UNSPECIFIED.,.F.,.F.)
B_SPLINE_CURVE_WITH_KNOTS((3,3),(0.367644516946553,0.373830527582531),
 .UNSPECIFIED.)
CURVE()
GEOMETRIC_REPRESENTATION_ITEM()
RATIONAL_B_SPLINE_CURVE((1.13426390111307,1.133898229013,1.13348223894566))
REPRESENTATION_ITEM('')
);
#976=(
BOUNDED_CURVE()
B_SPLINE_CURVE(2,(#61231,#61232,#61233),.UNSPECIFIED.,.F.,.F.)
B_SPLINE_CURVE_WITH_KNOTS((3,3),(0.271548216895918,0.277734227531903),
 .UNSPECIFIED.)
CURVE()
GEOMETRIC_REPRESENTATION_ITEM()
RATIONAL_B_SPLINE_CURVE((1.13348223894611,1.13389822901346,1.13426390111353))
REPRESENTATION_ITEM('')
);
#977=(
BOUNDED_CURVE()
B_SPLINE_CURVE(2,(#61235,#61236,#61237),.UNSPECIFIED.,.F.,.F.)
B_SPLINE_CURVE_WITH_KNOTS((3,3),(0.367644516946551,0.373830527582526),
 .UNSPECIFIED.)
CURVE()
GEOMETRIC_REPRESENTATION_ITEM()
RATIONAL_B_SPLINE_CURVE((1.1342639011131,1.13389822901304,1.13348223894569))
REPRESENTATION_ITEM('')
);
#978=(
BOUNDED_CURVE()
B_SPLINE_CURVE(2,(#61240,#61241,#61242),.UNSPECIFIED.,.F.,.F.)
B_SPLINE_CURVE_WITH_KNOTS((3,3),(0.271548216895922,0.277734227531909),
 .UNSPECIFIED.)
CURVE()
GEOMETRIC_REPRESENTATION_ITEM()
RATIONAL_B_SPLINE_CURVE((1.13348223894615,1.1338982290135,1.13426390111357))
REPRESENTATION_ITEM('')
);
#979=(
BOUNDED_CURVE()
B_SPLINE_CURVE(2,(#61244,#61245,#61246),.UNSPECIFIED.,.F.,.F.)
B_SPLINE_CURVE_WITH_KNOTS((3,3),(0.36764451694656,0.373830527582534),
 .UNSPECIFIED.)
CURVE()
GEOMETRIC_REPRESENTATION_ITEM()
RATIONAL_B_SPLINE_CURVE((1.13426390111304,1.13389822901297,1.13348223894563))
REPRESENTATION_ITEM('')
);
#980=(
BOUNDED_CURVE()
B_SPLINE_CURVE(2,(#61249,#61250,#61251),.UNSPECIFIED.,.F.,.F.)
B_SPLINE_CURVE_WITH_KNOTS((3,3),(0.271548216895917,0.277734227531904),
 .UNSPECIFIED.)
CURVE()
GEOMETRIC_REPRESENTATION_ITEM()
RATIONAL_B_SPLINE_CURVE((1.13348223894616,1.13389822901351,1.13426390111359))
REPRESENTATION_ITEM('')
);
#981=(
BOUNDED_CURVE()
B_SPLINE_CURVE(2,(#61253,#61254,#61255),.UNSPECIFIED.,.F.,.F.)
B_SPLINE_CURVE_WITH_KNOTS((3,3),(0.367644516946562,0.373830527582537),
 .UNSPECIFIED.)
CURVE()
GEOMETRIC_REPRESENTATION_ITEM()
RATIONAL_B_SPLINE_CURVE((1.13426390111298,1.13389822901291,1.13348223894556))
REPRESENTATION_ITEM('')
);
#982=(
BOUNDED_CURVE()
B_SPLINE_CURVE(2,(#61258,#61259,#61260),.UNSPECIFIED.,.F.,.F.)
B_SPLINE_CURVE_WITH_KNOTS((3,3),(0.271548216895925,0.277734227531911),
 .UNSPECIFIED.)
CURVE()
GEOMETRIC_REPRESENTATION_ITEM()
RATIONAL_B_SPLINE_CURVE((1.13348223894616,1.13389822901351,1.13426390111359))
REPRESENTATION_ITEM('')
);
#983=(
BOUNDED_CURVE()
B_SPLINE_CURVE(2,(#61262,#61263,#61264),.UNSPECIFIED.,.F.,.F.)
B_SPLINE_CURVE_WITH_KNOTS((3,3),(0.367644516946555,0.373830527582529),
 .UNSPECIFIED.)
CURVE()
GEOMETRIC_REPRESENTATION_ITEM()
RATIONAL_B_SPLINE_CURVE((1.13426390111312,1.13389822901305,1.13348223894571))
REPRESENTATION_ITEM('')
);
#984=(
BOUNDED_CURVE()
B_SPLINE_CURVE(2,(#61267,#61268,#61269),.UNSPECIFIED.,.F.,.F.)
B_SPLINE_CURVE_WITH_KNOTS((3,3),(0.271548216895925,0.277734227531912),
 .UNSPECIFIED.)
CURVE()
GEOMETRIC_REPRESENTATION_ITEM()
RATIONAL_B_SPLINE_CURVE((1.13348223894618,1.13389822901353,1.1342639011136))
REPRESENTATION_ITEM('')
);
#985=(
BOUNDED_CURVE()
B_SPLINE_CURVE(2,(#61271,#61272,#61273),.UNSPECIFIED.,.F.,.F.)
B_SPLINE_CURVE_WITH_KNOTS((3,3),(0.367644516946557,0.373830527582532),
 .UNSPECIFIED.)
CURVE()
GEOMETRIC_REPRESENTATION_ITEM()
RATIONAL_B_SPLINE_CURVE((1.13426390111306,1.13389822901299,1.13348223894564))
REPRESENTATION_ITEM('')
);
#986=(
BOUNDED_CURVE()
B_SPLINE_CURVE(2,(#61276,#61277,#61278),.UNSPECIFIED.,.F.,.F.)
B_SPLINE_CURVE_WITH_KNOTS((3,3),(0.271548216895908,0.277734227531892),
 .UNSPECIFIED.)
CURVE()
GEOMETRIC_REPRESENTATION_ITEM()
RATIONAL_B_SPLINE_CURVE((1.13348223894609,1.13389822901344,1.13426390111352))
REPRESENTATION_ITEM('')
);
#987=(
BOUNDED_CURVE()
B_SPLINE_CURVE(2,(#61280,#61281,#61282),.UNSPECIFIED.,.F.,.F.)
B_SPLINE_CURVE_WITH_KNOTS((3,3),(0.367644516946557,0.373830527582522),
 .UNSPECIFIED.)
CURVE()
GEOMETRIC_REPRESENTATION_ITEM()
RATIONAL_B_SPLINE_CURVE((1.13426390111309,1.13389822901302,1.13348223894568))
REPRESENTATION_ITEM('')
);
#988=(
BOUNDED_CURVE()
B_SPLINE_CURVE(2,(#61285,#61286,#61287),.UNSPECIFIED.,.F.,.F.)
B_SPLINE_CURVE_WITH_KNOTS((3,3),(0.271548216895913,0.277734227531902),
 .UNSPECIFIED.)
CURVE()
GEOMETRIC_REPRESENTATION_ITEM()
RATIONAL_B_SPLINE_CURVE((1.1334822389461,1.13389822901345,1.13426390111352))
REPRESENTATION_ITEM('')
);
#989=(
BOUNDED_CURVE()
B_SPLINE_CURVE(2,(#61289,#61290,#61291),.UNSPECIFIED.,.F.,.F.)
B_SPLINE_CURVE_WITH_KNOTS((3,3),(0.367644516946559,0.373830527582539),
 .UNSPECIFIED.)
CURVE()
GEOMETRIC_REPRESENTATION_ITEM()
RATIONAL_B_SPLINE_CURVE((1.13426390111296,1.13389822901289,1.13348223894555))
REPRESENTATION_ITEM('')
);
#990=(
BOUNDED_CURVE()
B_SPLINE_CURVE(2,(#61294,#61295,#61296),.UNSPECIFIED.,.F.,.F.)
B_SPLINE_CURVE_WITH_KNOTS((3,3),(0.271548216895926,0.277734227531913),
 .UNSPECIFIED.)
CURVE()
GEOMETRIC_REPRESENTATION_ITEM()
RATIONAL_B_SPLINE_CURVE((1.13348223894622,1.13389822901357,1.13426390111365))
REPRESENTATION_ITEM('')
);
#991=(
BOUNDED_CURVE()
B_SPLINE_CURVE(2,(#61298,#61299,#61300),.UNSPECIFIED.,.F.,.F.)
B_SPLINE_CURVE_WITH_KNOTS((3,3),(0.36764451694656,0.373830527582534),
 .UNSPECIFIED.)
CURVE()
GEOMETRIC_REPRESENTATION_ITEM()
RATIONAL_B_SPLINE_CURVE((1.13426390111298,1.13389822901291,1.13348223894557))
REPRESENTATION_ITEM('')
);
#992=(
BOUNDED_CURVE()
B_SPLINE_CURVE(2,(#61303,#61304,#61305),.UNSPECIFIED.,.F.,.F.)
B_SPLINE_CURVE_WITH_KNOTS((3,3),(0.271548216895926,0.277734227531909),
 .UNSPECIFIED.)
CURVE()
GEOMETRIC_REPRESENTATION_ITEM()
RATIONAL_B_SPLINE_CURVE((1.13348223894617,1.13389822901352,1.13426390111359))
REPRESENTATION_ITEM('')
);
#993=(
BOUNDED_CURVE()
B_SPLINE_CURVE(2,(#61307,#61308,#61309),.UNSPECIFIED.,.F.,.F.)
B_SPLINE_CURVE_WITH_KNOTS((3,3),(0.367644516946566,0.373830527582539),
 .UNSPECIFIED.)
CURVE()
GEOMETRIC_REPRESENTATION_ITEM()
RATIONAL_B_SPLINE_CURVE((1.13426390111296,1.13389822901289,1.13348223894555))
REPRESENTATION_ITEM('')
);
#994=(
BOUNDED_CURVE()
B_SPLINE_CURVE(2,(#61312,#61313,#61314),.UNSPECIFIED.,.F.,.F.)
B_SPLINE_CURVE_WITH_KNOTS((3,3),(0.271548216895918,0.277734227531904),
 .UNSPECIFIED.)
CURVE()
GEOMETRIC_REPRESENTATION_ITEM()
RATIONAL_B_SPLINE_CURVE((1.13348223894611,1.13389822901346,1.13426390111353))
REPRESENTATION_ITEM('')
);
#995=(
BOUNDED_CURVE()
B_SPLINE_CURVE(2,(#61316,#61317,#61318),.UNSPECIFIED.,.F.,.F.)
B_SPLINE_CURVE_WITH_KNOTS((3,3),(0.367644516946555,0.373830527582529),
 .UNSPECIFIED.)
CURVE()
GEOMETRIC_REPRESENTATION_ITEM()
RATIONAL_B_SPLINE_CURVE((1.13426390111303,1.13389822901296,1.13348223894562))
REPRESENTATION_ITEM('')
);
#996=(
BOUNDED_CURVE()
B_SPLINE_CURVE(2,(#61322,#61323,#61324),.UNSPECIFIED.,.F.,.F.)
B_SPLINE_CURVE_WITH_KNOTS((3,3),(0.271548216895927,0.277734227531913),
 .UNSPECIFIED.)
CURVE()
GEOMETRIC_REPRESENTATION_ITEM()
RATIONAL_B_SPLINE_CURVE((1.13348223894624,1.13389822901359,1.13426390111366))
REPRESENTATION_ITEM('')
);
#997=(
BOUNDED_CURVE()
B_SPLINE_CURVE(2,(#61328,#61329,#61330),.UNSPECIFIED.,.F.,.F.)
B_SPLINE_CURVE_WITH_KNOTS((3,3),(0.367644516946557,0.373830527582527),
 .UNSPECIFIED.)
CURVE()
GEOMETRIC_REPRESENTATION_ITEM()
RATIONAL_B_SPLINE_CURVE((1.1342639011131,1.13389822901303,1.13348223894569))
REPRESENTATION_ITEM('')
);
#998=(
BOUNDED_CURVE()
B_SPLINE_CURVE(2,(#61334,#61335,#61336),.UNSPECIFIED.,.F.,.F.)
B_SPLINE_CURVE_WITH_KNOTS((3,3),(0.27154821689592,0.277734227531904),
 .UNSPECIFIED.)
CURVE()
GEOMETRIC_REPRESENTATION_ITEM()
RATIONAL_B_SPLINE_CURVE((1.13348223894613,1.13389822901348,1.13426390111355))
REPRESENTATION_ITEM('')
);
#999=(
BOUNDED_CURVE()
B_SPLINE_CURVE(2,(#61340,#61341,#61342),.UNSPECIFIED.,.F.,.F.)
B_SPLINE_CURVE_WITH_KNOTS((3,3),(0.367644516946566,0.373830527582538),
 .UNSPECIFIED.)
CURVE()
GEOMETRIC_REPRESENTATION_ITEM()
RATIONAL_B_SPLINE_CURVE((1.13426390111301,1.13389822901294,1.1334822389456))
REPRESENTATION_ITEM('')
);
#1000=(
BOUNDED_CURVE()
B_SPLINE_CURVE(2,(#61346,#61347,#61348),.UNSPECIFIED.,.F.,.F.)
B_SPLINE_CURVE_WITH_KNOTS((3,3),(0.27154821689592,0.277734227531902),
 .UNSPECIFIED.)
CURVE()
GEOMETRIC_REPRESENTATION_ITEM()
RATIONAL_B_SPLINE_CURVE((1.1334822389461,1.13389822901344,1.13426390111352))
REPRESENTATION_ITEM('')
);
#1001=(
BOUNDED_CURVE()
B_SPLINE_CURVE(2,(#61352,#61353,#61354),.UNSPECIFIED.,.F.,.F.)
B_SPLINE_CURVE_WITH_KNOTS((3,3),(0.367644516946558,0.373830527582536),
 .UNSPECIFIED.)
CURVE()
GEOMETRIC_REPRESENTATION_ITEM()
RATIONAL_B_SPLINE_CURVE((1.13426390111303,1.13389822901296,1.13348223894562))
REPRESENTATION_ITEM('')
);
#1002=(
BOUNDED_CURVE()
B_SPLINE_CURVE(2,(#61358,#61359,#61360),.UNSPECIFIED.,.F.,.F.)
B_SPLINE_CURVE_WITH_KNOTS((3,3),(0.271548216895916,0.277734227531903),
 .UNSPECIFIED.)
CURVE()
GEOMETRIC_REPRESENTATION_ITEM()
RATIONAL_B_SPLINE_CURVE((1.13348223894608,1.13389822901343,1.1342639011135))
REPRESENTATION_ITEM('')
);
#1003=(
BOUNDED_CURVE()
B_SPLINE_CURVE(2,(#61364,#61365,#61366),.UNSPECIFIED.,.F.,.F.)
B_SPLINE_CURVE_WITH_KNOTS((3,3),(0.367644516946558,0.373830527582538),
 .UNSPECIFIED.)
CURVE()
GEOMETRIC_REPRESENTATION_ITEM()
RATIONAL_B_SPLINE_CURVE((1.13426390111299,1.13389822901292,1.13348223894558))
REPRESENTATION_ITEM('')
);
#1004=(
BOUNDED_CURVE()
B_SPLINE_CURVE(2,(#61370,#61371,#61372),.UNSPECIFIED.,.F.,.F.)
B_SPLINE_CURVE_WITH_KNOTS((3,3),(0.271548216895918,0.277734227531905),
 .UNSPECIFIED.)
CURVE()
GEOMETRIC_REPRESENTATION_ITEM()
RATIONAL_B_SPLINE_CURVE((1.13348223894618,1.13389822901353,1.1342639011136))
REPRESENTATION_ITEM('')
);
#1005=(
BOUNDED_CURVE()
B_SPLINE_CURVE(2,(#61376,#61377,#61378),.UNSPECIFIED.,.F.,.F.)
B_SPLINE_CURVE_WITH_KNOTS((3,3),(0.367644516946549,0.373830527582523),
 .UNSPECIFIED.)
CURVE()
GEOMETRIC_REPRESENTATION_ITEM()
RATIONAL_B_SPLINE_CURVE((1.13426390111313,1.13389822901306,1.13348223894572))
REPRESENTATION_ITEM('')
);
#1006=(
BOUNDED_CURVE()
B_SPLINE_CURVE(2,(#61382,#61383,#61384),.UNSPECIFIED.,.F.,.F.)
B_SPLINE_CURVE_WITH_KNOTS((3,3),(0.271548216895918,0.277734227531904),
 .UNSPECIFIED.)
CURVE()
GEOMETRIC_REPRESENTATION_ITEM()
RATIONAL_B_SPLINE_CURVE((1.13348223894607,1.13389822901342,1.1342639011135))
REPRESENTATION_ITEM('')
);
#1007=(
BOUNDED_CURVE()
B_SPLINE_CURVE(2,(#61388,#61389,#61390),.UNSPECIFIED.,.F.,.F.)
B_SPLINE_CURVE_WITH_KNOTS((3,3),(0.367644516946553,0.373830527582525),
 .UNSPECIFIED.)
CURVE()
GEOMETRIC_REPRESENTATION_ITEM()
RATIONAL_B_SPLINE_CURVE((1.13426390111306,1.133898229013,1.13348223894565))
REPRESENTATION_ITEM('')
);
#1008=(
BOUNDED_CURVE()
B_SPLINE_CURVE(2,(#61394,#61395,#61396),.UNSPECIFIED.,.F.,.F.)
B_SPLINE_CURVE_WITH_KNOTS((3,3),(0.271548216895918,0.277734227531897),
 .UNSPECIFIED.)
CURVE()
GEOMETRIC_REPRESENTATION_ITEM()
RATIONAL_B_SPLINE_CURVE((1.13348223894613,1.13389822901348,1.13426390111355))
REPRESENTATION_ITEM('')
);
#1009=(
BOUNDED_CURVE()
B_SPLINE_CURVE(2,(#61400,#61401,#61402),.UNSPECIFIED.,.F.,.F.)
B_SPLINE_CURVE_WITH_KNOTS((3,3),(0.367644516946551,0.373830527582524),
 .UNSPECIFIED.)
CURVE()
GEOMETRIC_REPRESENTATION_ITEM()
RATIONAL_B_SPLINE_CURVE((1.13426390111309,1.13389822901302,1.13348223894568))
REPRESENTATION_ITEM('')
);
#1010=(
BOUNDED_CURVE()
B_SPLINE_CURVE(2,(#61406,#61407,#61408),.UNSPECIFIED.,.F.,.F.)
B_SPLINE_CURVE_WITH_KNOTS((3,3),(0.271548216895914,0.2777342275319),
 .UNSPECIFIED.)
CURVE()
GEOMETRIC_REPRESENTATION_ITEM()
RATIONAL_B_SPLINE_CURVE((1.13348223894608,1.13389822901343,1.13426390111351))
REPRESENTATION_ITEM('')
);
#1011=(
BOUNDED_CURVE()
B_SPLINE_CURVE(2,(#61412,#61413,#61414),.UNSPECIFIED.,.F.,.F.)
B_SPLINE_CURVE_WITH_KNOTS((3,3),(0.367644516946559,0.373830527582536),
 .UNSPECIFIED.)
CURVE()
GEOMETRIC_REPRESENTATION_ITEM()
RATIONAL_B_SPLINE_CURVE((1.13426390111305,1.13389822901298,1.13348223894564))
REPRESENTATION_ITEM('')
);
#1012=(
BOUNDED_CURVE()
B_SPLINE_CURVE(2,(#61418,#61419,#61420),.UNSPECIFIED.,.F.,.F.)
B_SPLINE_CURVE_WITH_KNOTS((3,3),(0.27154821689591,0.277734227531898),
 .UNSPECIFIED.)
CURVE()
GEOMETRIC_REPRESENTATION_ITEM()
RATIONAL_B_SPLINE_CURVE((1.13348223894607,1.13389822901342,1.1342639011135))
REPRESENTATION_ITEM('')
);
#1013=(
BOUNDED_CURVE()
B_SPLINE_CURVE(2,(#61424,#61425,#61426),.UNSPECIFIED.,.F.,.F.)
B_SPLINE_CURVE_WITH_KNOTS((3,3),(0.367644516946559,0.373830527582532),
 .UNSPECIFIED.)
CURVE()
GEOMETRIC_REPRESENTATION_ITEM()
RATIONAL_B_SPLINE_CURVE((1.13426390111307,1.133898229013,1.13348223894566))
REPRESENTATION_ITEM('')
);
#1014=(
BOUNDED_CURVE()
B_SPLINE_CURVE(2,(#61430,#61431,#61432),.UNSPECIFIED.,.F.,.F.)
B_SPLINE_CURVE_WITH_KNOTS((3,3),(0.271548216895924,0.277734227531905),
 .UNSPECIFIED.)
CURVE()
GEOMETRIC_REPRESENTATION_ITEM()
RATIONAL_B_SPLINE_CURVE((1.13348223894618,1.13389822901353,1.1342639011136))
REPRESENTATION_ITEM('')
);
#1015=(
BOUNDED_CURVE()
B_SPLINE_CURVE(2,(#61436,#61437,#61438),.UNSPECIFIED.,.F.,.F.)
B_SPLINE_CURVE_WITH_KNOTS((3,3),(0.367644516946555,0.373830527582531),
 .UNSPECIFIED.)
CURVE()
GEOMETRIC_REPRESENTATION_ITEM()
RATIONAL_B_SPLINE_CURVE((1.134263901113,1.13389822901293,1.13348223894559))
REPRESENTATION_ITEM('')
);
#1016=(
BOUNDED_CURVE()
B_SPLINE_CURVE(2,(#61442,#61443,#61444),.UNSPECIFIED.,.F.,.F.)
B_SPLINE_CURVE_WITH_KNOTS((3,3),(0.271548216895916,0.277734227531902),
 .UNSPECIFIED.)
CURVE()
GEOMETRIC_REPRESENTATION_ITEM()
RATIONAL_B_SPLINE_CURVE((1.13348223894612,1.13389822901347,1.13426390111355))
REPRESENTATION_ITEM('')
);
#1017=(
BOUNDED_CURVE()
B_SPLINE_CURVE(2,(#61448,#61449,#61450),.UNSPECIFIED.,.F.,.F.)
B_SPLINE_CURVE_WITH_KNOTS((3,3),(0.36764451694656,0.373830527582534),
 .UNSPECIFIED.)
CURVE()
GEOMETRIC_REPRESENTATION_ITEM()
RATIONAL_B_SPLINE_CURVE((1.13426390111302,1.13389822901296,1.13348223894561))
REPRESENTATION_ITEM('')
);
#1018=(
BOUNDED_CURVE()
B_SPLINE_CURVE(2,(#61454,#61455,#61456),.UNSPECIFIED.,.F.,.F.)
B_SPLINE_CURVE_WITH_KNOTS((3,3),(0.271548216895913,0.277734227531896),
 .UNSPECIFIED.)
CURVE()
GEOMETRIC_REPRESENTATION_ITEM()
RATIONAL_B_SPLINE_CURVE((1.13348223894608,1.13389822901343,1.1342639011135))
REPRESENTATION_ITEM('')
);
#1019=(
BOUNDED_CURVE()
B_SPLINE_CURVE(2,(#61460,#61461,#61462),.UNSPECIFIED.,.F.,.F.)
B_SPLINE_CURVE_WITH_KNOTS((3,3),(0.367644516946558,0.373830527582535),
 .UNSPECIFIED.)
CURVE()
GEOMETRIC_REPRESENTATION_ITEM()
RATIONAL_B_SPLINE_CURVE((1.13426390111305,1.13389822901298,1.13348223894563))
REPRESENTATION_ITEM('')
);
#1020=(
BOUNDED_CURVE()
B_SPLINE_CURVE(2,(#61466,#61467,#61468),.UNSPECIFIED.,.F.,.F.)
B_SPLINE_CURVE_WITH_KNOTS((3,3),(0.271548216895911,0.277734227531902),
 .UNSPECIFIED.)
CURVE()
GEOMETRIC_REPRESENTATION_ITEM()
RATIONAL_B_SPLINE_CURVE((1.13348223894613,1.13389822901348,1.13426390111355))
REPRESENTATION_ITEM('')
);
#1021=(
BOUNDED_CURVE()
B_SPLINE_CURVE(2,(#61472,#61473,#61474),.UNSPECIFIED.,.F.,.F.)
B_SPLINE_CURVE_WITH_KNOTS((3,3),(0.367644516946552,0.373830527582527),
 .UNSPECIFIED.)
CURVE()
GEOMETRIC_REPRESENTATION_ITEM()
RATIONAL_B_SPLINE_CURVE((1.13426390111308,1.13389822901301,1.13348223894567))
REPRESENTATION_ITEM('')
);
#1022=(
BOUNDED_CURVE()
B_SPLINE_CURVE(2,(#61478,#61479,#61480),.UNSPECIFIED.,.F.,.F.)
B_SPLINE_CURVE_WITH_KNOTS((3,3),(0.271548216895913,0.277734227531896),
 .UNSPECIFIED.)
CURVE()
GEOMETRIC_REPRESENTATION_ITEM()
RATIONAL_B_SPLINE_CURVE((1.13348223894609,1.13389822901344,1.13426390111351))
REPRESENTATION_ITEM('')
);
#1023=(
BOUNDED_CURVE()
B_SPLINE_CURVE(2,(#61484,#61485,#61486),.UNSPECIFIED.,.F.,.F.)
B_SPLINE_CURVE_WITH_KNOTS((3,3),(0.367644516946554,0.373830527582527),
 .UNSPECIFIED.)
CURVE()
GEOMETRIC_REPRESENTATION_ITEM()
RATIONAL_B_SPLINE_CURVE((1.13426390111307,1.13389822901301,1.13348223894566))
REPRESENTATION_ITEM('')
);
#1024=(
BOUNDED_CURVE()
B_SPLINE_CURVE(2,(#61490,#61491,#61492),.UNSPECIFIED.,.F.,.F.)
B_SPLINE_CURVE_WITH_KNOTS((3,3),(0.271548216895912,0.277734227531901),
 .UNSPECIFIED.)
CURVE()
GEOMETRIC_REPRESENTATION_ITEM()
RATIONAL_B_SPLINE_CURVE((1.13348223894619,1.13389822901354,1.13426390111361))
REPRESENTATION_ITEM('')
);
#1025=(
BOUNDED_CURVE()
B_SPLINE_CURVE(2,(#61496,#61497,#61498),.UNSPECIFIED.,.F.,.F.)
B_SPLINE_CURVE_WITH_KNOTS((3,3),(0.367644516946552,0.373830527582526),
 .UNSPECIFIED.)
CURVE()
GEOMETRIC_REPRESENTATION_ITEM()
RATIONAL_B_SPLINE_CURVE((1.13426390111306,1.13389822901299,1.13348223894565))
REPRESENTATION_ITEM('')
);
#1026=(
BOUNDED_CURVE()
B_SPLINE_CURVE(2,(#61502,#61503,#61504),.UNSPECIFIED.,.F.,.F.)
B_SPLINE_CURVE_WITH_KNOTS((3,3),(0.271548216895908,0.277734227531896),
 .UNSPECIFIED.)
CURVE()
GEOMETRIC_REPRESENTATION_ITEM()
RATIONAL_B_SPLINE_CURVE((1.13348223894609,1.13389822901344,1.13426390111351))
REPRESENTATION_ITEM('')
);
#1027=(
BOUNDED_CURVE()
B_SPLINE_CURVE(2,(#61508,#61509,#61510),.UNSPECIFIED.,.F.,.F.)
B_SPLINE_CURVE_WITH_KNOTS((3,3),(0.367644516946558,0.373830527582532),
 .UNSPECIFIED.)
CURVE()
GEOMETRIC_REPRESENTATION_ITEM()
RATIONAL_B_SPLINE_CURVE((1.13426390111305,1.13389822901298,1.13348223894564))
REPRESENTATION_ITEM('')
);
#1028=(
BOUNDED_CURVE()
B_SPLINE_CURVE(2,(#61514,#61515,#61516),.UNSPECIFIED.,.F.,.F.)
B_SPLINE_CURVE_WITH_KNOTS((3,3),(0.271548216895918,0.27773422753191),
 .UNSPECIFIED.)
CURVE()
GEOMETRIC_REPRESENTATION_ITEM()
RATIONAL_B_SPLINE_CURVE((1.1334822389462,1.13389822901355,1.13426390111362))
REPRESENTATION_ITEM('')
);
#1029=(
BOUNDED_CURVE()
B_SPLINE_CURVE(2,(#61520,#61521,#61522),.UNSPECIFIED.,.F.,.F.)
B_SPLINE_CURVE_WITH_KNOTS((3,3),(0.367644516946559,0.373830527582532),
 .UNSPECIFIED.)
CURVE()
GEOMETRIC_REPRESENTATION_ITEM()
RATIONAL_B_SPLINE_CURVE((1.13426390111305,1.13389822901299,1.13348223894564))
REPRESENTATION_ITEM('')
);
#1030=(
BOUNDED_CURVE()
B_SPLINE_CURVE(2,(#61526,#61527,#61528),.UNSPECIFIED.,.F.,.F.)
B_SPLINE_CURVE_WITH_KNOTS((3,3),(0.271548216895917,0.277734227531899),
 .UNSPECIFIED.)
CURVE()
GEOMETRIC_REPRESENTATION_ITEM()
RATIONAL_B_SPLINE_CURVE((1.13348223894612,1.13389822901347,1.13426390111355))
REPRESENTATION_ITEM('')
);
#1031=(
BOUNDED_CURVE()
B_SPLINE_CURVE(2,(#61532,#61533,#61534),.UNSPECIFIED.,.F.,.F.)
B_SPLINE_CURVE_WITH_KNOTS((3,3),(0.367644516946562,0.373830527582533),
 .UNSPECIFIED.)
CURVE()
GEOMETRIC_REPRESENTATION_ITEM()
RATIONAL_B_SPLINE_CURVE((1.13426390111306,1.13389822901299,1.13348223894564))
REPRESENTATION_ITEM('')
);
#1032=(
BOUNDED_CURVE()
B_SPLINE_CURVE(2,(#61538,#61539,#61540),.UNSPECIFIED.,.F.,.F.)
B_SPLINE_CURVE_WITH_KNOTS((3,3),(0.271548216895905,0.277734227531891),
 .UNSPECIFIED.)
CURVE()
GEOMETRIC_REPRESENTATION_ITEM()
RATIONAL_B_SPLINE_CURVE((1.13348223894609,1.13389822901344,1.13426390111351))
REPRESENTATION_ITEM('')
);
#1033=(
BOUNDED_CURVE()
B_SPLINE_CURVE(2,(#61544,#61545,#61546),.UNSPECIFIED.,.F.,.F.)
B_SPLINE_CURVE_WITH_KNOTS((3,3),(0.367644516946557,0.373830527582533),
 .UNSPECIFIED.)
CURVE()
GEOMETRIC_REPRESENTATION_ITEM()
RATIONAL_B_SPLINE_CURVE((1.13426390111305,1.13389822901299,1.13348223894564))
REPRESENTATION_ITEM('')
);
#1034=(
BOUNDED_CURVE()
B_SPLINE_CURVE(2,(#61550,#61551,#61552),.UNSPECIFIED.,.F.,.F.)
B_SPLINE_CURVE_WITH_KNOTS((3,3),(0.271548216895918,0.277734227531906),
 .UNSPECIFIED.)
CURVE()
GEOMETRIC_REPRESENTATION_ITEM()
RATIONAL_B_SPLINE_CURVE((1.13348223894616,1.13389822901351,1.13426390111358))
REPRESENTATION_ITEM('')
);
#1035=(
BOUNDED_CURVE()
B_SPLINE_CURVE(2,(#61574,#61575,#61576),.UNSPECIFIED.,.F.,.F.)
B_SPLINE_CURVE_WITH_KNOTS((3,3),(0.376641898803529,0.382940702095941),
 .UNSPECIFIED.)
CURVE()
GEOMETRIC_REPRESENTATION_ITEM()
RATIONAL_B_SPLINE_CURVE((1.12071541658433,1.1202411994692,1.11971735964528))
REPRESENTATION_ITEM('')
);
#1036=(
BOUNDED_CURVE()
B_SPLINE_CURVE(2,(#61580,#61581,#61582),.UNSPECIFIED.,.F.,.F.)
B_SPLINE_CURVE_WITH_KNOTS((3,3),(0.249954652430657,0.25625345571807),
 .UNSPECIFIED.)
CURVE()
GEOMETRIC_REPRESENTATION_ITEM()
RATIONAL_B_SPLINE_CURVE((1.1197173596462,1.12024119946966,1.12071541658442))
REPRESENTATION_ITEM('')
);
#1037=(
BOUNDED_CURVE()
B_SPLINE_CURVE(2,(#61586,#61587,#61588),.UNSPECIFIED.,.F.,.F.)
B_SPLINE_CURVE_WITH_KNOTS((3,3),(0.376641898803524,0.382940702095934),
 .UNSPECIFIED.)
CURVE()
GEOMETRIC_REPRESENTATION_ITEM()
RATIONAL_B_SPLINE_CURVE((1.12071541658448,1.12024119946934,1.11971735964542))
REPRESENTATION_ITEM('')
);
#1038=(
BOUNDED_CURVE()
B_SPLINE_CURVE(2,(#61592,#61593,#61594),.UNSPECIFIED.,.F.,.F.)
B_SPLINE_CURVE_WITH_KNOTS((3,3),(0.249954652430655,0.256253455718069),
 .UNSPECIFIED.)
CURVE()
GEOMETRIC_REPRESENTATION_ITEM()
RATIONAL_B_SPLINE_CURVE((1.11971735964613,1.1202411994696,1.12071541658435))
REPRESENTATION_ITEM('')
);
#1039=(
BOUNDED_CURVE()
B_SPLINE_CURVE(2,(#61598,#61599,#61600),.UNSPECIFIED.,.F.,.F.)
B_SPLINE_CURVE_WITH_KNOTS((3,3),(0.376641898803532,0.382940702095944),
 .UNSPECIFIED.)
CURVE()
GEOMETRIC_REPRESENTATION_ITEM()
RATIONAL_B_SPLINE_CURVE((1.12071541658434,1.12024119946921,1.11971735964529))
REPRESENTATION_ITEM('')
);
#1040=(
BOUNDED_CURVE()
B_SPLINE_CURVE(2,(#61604,#61605,#61606),.UNSPECIFIED.,.F.,.F.)
B_SPLINE_CURVE_WITH_KNOTS((3,3),(0.249954652430645,0.256253455718059),
 .UNSPECIFIED.)
CURVE()
GEOMETRIC_REPRESENTATION_ITEM()
RATIONAL_B_SPLINE_CURVE((1.11971735964598,1.12024119946945,1.1207154165842))
REPRESENTATION_ITEM('')
);
#1041=(
BOUNDED_CURVE()
B_SPLINE_CURVE(2,(#61610,#61611,#61612),.UNSPECIFIED.,.F.,.F.)
B_SPLINE_CURVE_WITH_KNOTS((3,3),(0.376641898803521,0.382940702095933),
 .UNSPECIFIED.)
CURVE()
GEOMETRIC_REPRESENTATION_ITEM()
RATIONAL_B_SPLINE_CURVE((1.1207154165845,1.12024119946936,1.11971735964544))
REPRESENTATION_ITEM('')
);
#1042=(
BOUNDED_CURVE()
B_SPLINE_CURVE(2,(#61616,#61617,#61618),.UNSPECIFIED.,.F.,.F.)
B_SPLINE_CURVE_WITH_KNOTS((3,3),(0.249954652430661,0.256253455718076),
 .UNSPECIFIED.)
CURVE()
GEOMETRIC_REPRESENTATION_ITEM()
RATIONAL_B_SPLINE_CURVE((1.1197173596463,1.12024119946977,1.12071541658453))
REPRESENTATION_ITEM('')
);
#1043=(
BOUNDED_CURVE()
B_SPLINE_CURVE(2,(#61622,#61623,#61624),.UNSPECIFIED.,.F.,.F.)
B_SPLINE_CURVE_WITH_KNOTS((3,3),(0.376641898803535,0.382940702095943),
 .UNSPECIFIED.)
CURVE()
GEOMETRIC_REPRESENTATION_ITEM()
RATIONAL_B_SPLINE_CURVE((1.12071541658437,1.12024119946923,1.11971735964532))
REPRESENTATION_ITEM('')
);
#1044=(
BOUNDED_CURVE()
B_SPLINE_CURVE(2,(#61628,#61629,#61630),.UNSPECIFIED.,.F.,.F.)
B_SPLINE_CURVE_WITH_KNOTS((3,3),(0.249954652430645,0.256253455718058),
 .UNSPECIFIED.)
CURVE()
GEOMETRIC_REPRESENTATION_ITEM()
RATIONAL_B_SPLINE_CURVE((1.11971735964609,1.12024119946955,1.12071541658431))
REPRESENTATION_ITEM('')
);
#1045=(
BOUNDED_CURVE()
B_SPLINE_CURVE(2,(#61634,#61635,#61636),.UNSPECIFIED.,.F.,.F.)
B_SPLINE_CURVE_WITH_KNOTS((3,3),(0.376641898803531,0.382940702095942),
 .UNSPECIFIED.)
CURVE()
GEOMETRIC_REPRESENTATION_ITEM()
RATIONAL_B_SPLINE_CURVE((1.12071541658437,1.12024119946923,1.11971735964532))
REPRESENTATION_ITEM('')
);
#1046=(
BOUNDED_CURVE()
B_SPLINE_CURVE(2,(#61640,#61641,#61642),.UNSPECIFIED.,.F.,.F.)
B_SPLINE_CURVE_WITH_KNOTS((3,3),(0.249954652430646,0.256253455718059),
 .UNSPECIFIED.)
CURVE()
GEOMETRIC_REPRESENTATION_ITEM()
RATIONAL_B_SPLINE_CURVE((1.11971735964605,1.12024119946951,1.12071541658427))
REPRESENTATION_ITEM('')
);
#1047=(
BOUNDED_CURVE()
B_SPLINE_CURVE(2,(#61646,#61647,#61648),.UNSPECIFIED.,.F.,.F.)
B_SPLINE_CURVE_WITH_KNOTS((3,3),(0.376641898803521,0.382940702095931),
 .UNSPECIFIED.)
CURVE()
GEOMETRIC_REPRESENTATION_ITEM()
RATIONAL_B_SPLINE_CURVE((1.12071541658451,1.12024119946938,1.11971735964546))
REPRESENTATION_ITEM('')
);
#1048=(
BOUNDED_CURVE()
B_SPLINE_CURVE(2,(#61652,#61653,#61654),.UNSPECIFIED.,.F.,.F.)
B_SPLINE_CURVE_WITH_KNOTS((3,3),(0.249954652430639,0.256253455718052),
 .UNSPECIFIED.)
CURVE()
GEOMETRIC_REPRESENTATION_ITEM()
RATIONAL_B_SPLINE_CURVE((1.11971735964601,1.12024119946948,1.12071541658424))
REPRESENTATION_ITEM('')
);
#1049=(
BOUNDED_CURVE()
B_SPLINE_CURVE(2,(#61658,#61659,#61660),.UNSPECIFIED.,.F.,.F.)
B_SPLINE_CURVE_WITH_KNOTS((3,3),(0.376641898803533,0.382940702095945),
 .UNSPECIFIED.)
CURVE()
GEOMETRIC_REPRESENTATION_ITEM()
RATIONAL_B_SPLINE_CURVE((1.12071541658434,1.1202411994692,1.11971735964528))
REPRESENTATION_ITEM('')
);
#1050=(
BOUNDED_CURVE()
B_SPLINE_CURVE(2,(#61664,#61665,#61666),.UNSPECIFIED.,.F.,.F.)
B_SPLINE_CURVE_WITH_KNOTS((3,3),(0.249954652430659,0.256253455718072),
 .UNSPECIFIED.)
CURVE()
GEOMETRIC_REPRESENTATION_ITEM()
RATIONAL_B_SPLINE_CURVE((1.11971735964624,1.12024119946971,1.12071541658447))
REPRESENTATION_ITEM('')
);
#1051=(
BOUNDED_CURVE()
B_SPLINE_CURVE(2,(#61670,#61671,#61672),.UNSPECIFIED.,.F.,.F.)
B_SPLINE_CURVE_WITH_KNOTS((3,3),(0.376641898803529,0.382940702095948),
 .UNSPECIFIED.)
CURVE()
GEOMETRIC_REPRESENTATION_ITEM()
RATIONAL_B_SPLINE_CURVE((1.12071541658446,1.12024119946932,1.1197173596454))
REPRESENTATION_ITEM('')
);
#1052=(
BOUNDED_CURVE()
B_SPLINE_CURVE(2,(#61676,#61677,#61678),.UNSPECIFIED.,.F.,.F.)
B_SPLINE_CURVE_WITH_KNOTS((3,3),(0.249954652430643,0.256253455718057),
 .UNSPECIFIED.)
CURVE()
GEOMETRIC_REPRESENTATION_ITEM()
RATIONAL_B_SPLINE_CURVE((1.11971735964609,1.12024119946956,1.12071541658432))
REPRESENTATION_ITEM('')
);
#1053=(
BOUNDED_CURVE()
B_SPLINE_CURVE(2,(#61682,#61683,#61684),.UNSPECIFIED.,.F.,.F.)
B_SPLINE_CURVE_WITH_KNOTS((3,3),(0.376641898803523,0.382940702095941),
 .UNSPECIFIED.)
CURVE()
GEOMETRIC_REPRESENTATION_ITEM()
RATIONAL_B_SPLINE_CURVE((1.12071541658451,1.12024119946937,1.11971735964545))
REPRESENTATION_ITEM('')
);
#1054=(
BOUNDED_CURVE()
B_SPLINE_CURVE(2,(#61688,#61689,#61690),.UNSPECIFIED.,.F.,.F.)
B_SPLINE_CURVE_WITH_KNOTS((3,3),(0.249954652430644,0.256253455718058),
 .UNSPECIFIED.)
CURVE()
GEOMETRIC_REPRESENTATION_ITEM()
RATIONAL_B_SPLINE_CURVE((1.11971735964615,1.12024119946961,1.12071541658437))
REPRESENTATION_ITEM('')
);
#1055=(
BOUNDED_CURVE()
B_SPLINE_CURVE(2,(#61694,#61695,#61696),.UNSPECIFIED.,.F.,.F.)
B_SPLINE_CURVE_WITH_KNOTS((3,3),(0.376641898803536,0.382940702095946),
 .UNSPECIFIED.)
CURVE()
GEOMETRIC_REPRESENTATION_ITEM()
RATIONAL_B_SPLINE_CURVE((1.12071541658451,1.12024119946938,1.11971735964546))
REPRESENTATION_ITEM('')
);
#1056=(
BOUNDED_CURVE()
B_SPLINE_CURVE(2,(#61700,#61701,#61702),.UNSPECIFIED.,.F.,.F.)
B_SPLINE_CURVE_WITH_KNOTS((3,3),(0.24995465243065,0.256253455718062),
 .UNSPECIFIED.)
CURVE()
GEOMETRIC_REPRESENTATION_ITEM()
RATIONAL_B_SPLINE_CURVE((1.11971735964599,1.12024119946946,1.12071541658421))
REPRESENTATION_ITEM('')
);
#1057=(
BOUNDED_CURVE()
B_SPLINE_CURVE(2,(#61706,#61707,#61708),.UNSPECIFIED.,.F.,.F.)
B_SPLINE_CURVE_WITH_KNOTS((3,3),(0.376641898803523,0.38294070209593),
 .UNSPECIFIED.)
CURVE()
GEOMETRIC_REPRESENTATION_ITEM()
RATIONAL_B_SPLINE_CURVE((1.1207154165845,1.12024119946936,1.11971735964544))
REPRESENTATION_ITEM('')
);
#1058=(
BOUNDED_CURVE()
B_SPLINE_CURVE(2,(#61712,#61713,#61714),.UNSPECIFIED.,.F.,.F.)
B_SPLINE_CURVE_WITH_KNOTS((3,3),(0.249954652430653,0.256253455718064),
 .UNSPECIFIED.)
CURVE()
GEOMETRIC_REPRESENTATION_ITEM()
RATIONAL_B_SPLINE_CURVE((1.11971735964611,1.12024119946957,1.12071541658433))
REPRESENTATION_ITEM('')
);
#1059=(
BOUNDED_CURVE()
B_SPLINE_CURVE(2,(#61718,#61719,#61720),.UNSPECIFIED.,.F.,.F.)
B_SPLINE_CURVE_WITH_KNOTS((3,3),(0.376641898803521,0.382940702095931),
 .UNSPECIFIED.)
CURVE()
GEOMETRIC_REPRESENTATION_ITEM()
RATIONAL_B_SPLINE_CURVE((1.12071541658461,1.12024119946947,1.11971735964555))
REPRESENTATION_ITEM('')
);
#1060=(
BOUNDED_CURVE()
B_SPLINE_CURVE(2,(#61724,#61725,#61726),.UNSPECIFIED.,.F.,.F.)
B_SPLINE_CURVE_WITH_KNOTS((3,3),(0.249954652430661,0.256253455718072),
 .UNSPECIFIED.)
CURVE()
GEOMETRIC_REPRESENTATION_ITEM()
RATIONAL_B_SPLINE_CURVE((1.11971735964623,1.1202411994697,1.12071541658446))
REPRESENTATION_ITEM('')
);
#1061=(
BOUNDED_CURVE()
B_SPLINE_CURVE(2,(#61730,#61731,#61732),.UNSPECIFIED.,.F.,.F.)
B_SPLINE_CURVE_WITH_KNOTS((3,3),(0.376641898803537,0.382940702095947),
 .UNSPECIFIED.)
CURVE()
GEOMETRIC_REPRESENTATION_ITEM()
RATIONAL_B_SPLINE_CURVE((1.1207154165845,1.12024119946936,1.11971735964544))
REPRESENTATION_ITEM('')
);
#1062=(
BOUNDED_CURVE()
B_SPLINE_CURVE(2,(#61736,#61737,#61738),.UNSPECIFIED.,.F.,.F.)
B_SPLINE_CURVE_WITH_KNOTS((3,3),(0.249954652430645,0.256253455718056),
 .UNSPECIFIED.)
CURVE()
GEOMETRIC_REPRESENTATION_ITEM()
RATIONAL_B_SPLINE_CURVE((1.11971735964613,1.1202411994696,1.12071541658435))
REPRESENTATION_ITEM('')
);
#1063=(
BOUNDED_CURVE()
B_SPLINE_CURVE(2,(#61742,#61743,#61744),.UNSPECIFIED.,.F.,.F.)
B_SPLINE_CURVE_WITH_KNOTS((3,3),(0.376641898803536,0.382940702095954),
 .UNSPECIFIED.)
CURVE()
GEOMETRIC_REPRESENTATION_ITEM()
RATIONAL_B_SPLINE_CURVE((1.12071541658435,1.12024119946922,1.1197173596453))
REPRESENTATION_ITEM('')
);
#1064=(
BOUNDED_CURVE()
B_SPLINE_CURVE(2,(#61748,#61749,#61750),.UNSPECIFIED.,.F.,.F.)
B_SPLINE_CURVE_WITH_KNOTS((3,3),(0.249954652430663,0.256253455718072),
 .UNSPECIFIED.)
CURVE()
GEOMETRIC_REPRESENTATION_ITEM()
RATIONAL_B_SPLINE_CURVE((1.11971735964633,1.1202411994698,1.12071541658456))
REPRESENTATION_ITEM('')
);
#1065=(
BOUNDED_CURVE()
B_SPLINE_CURVE(2,(#61754,#61755,#61756),.UNSPECIFIED.,.F.,.F.)
B_SPLINE_CURVE_WITH_KNOTS((3,3),(0.376641898803512,0.382940702095922),
 .UNSPECIFIED.)
CURVE()
GEOMETRIC_REPRESENTATION_ITEM()
RATIONAL_B_SPLINE_CURVE((1.12071541658461,1.12024119946947,1.11971735964555))
REPRESENTATION_ITEM('')
);
#1066=(
BOUNDED_CURVE()
B_SPLINE_CURVE(2,(#61760,#61761,#61762),.UNSPECIFIED.,.F.,.F.)
B_SPLINE_CURVE_WITH_KNOTS((3,3),(0.249954652430648,0.256253455718062),
 .UNSPECIFIED.)
CURVE()
GEOMETRIC_REPRESENTATION_ITEM()
RATIONAL_B_SPLINE_CURVE((1.11971735964605,1.12024119946951,1.12071541658427))
REPRESENTATION_ITEM('')
);
#1067=(
BOUNDED_CURVE()
B_SPLINE_CURVE(2,(#61766,#61767,#61768),.UNSPECIFIED.,.F.,.F.)
B_SPLINE_CURVE_WITH_KNOTS((3,3),(0.376641898803527,0.382940702095944),
 .UNSPECIFIED.)
CURVE()
GEOMETRIC_REPRESENTATION_ITEM()
RATIONAL_B_SPLINE_CURVE((1.12071541658444,1.12024119946931,1.11971735964539))
REPRESENTATION_ITEM('')
);
#1068=(
BOUNDED_CURVE()
B_SPLINE_CURVE(2,(#61772,#61773,#61774),.UNSPECIFIED.,.F.,.F.)
B_SPLINE_CURVE_WITH_KNOTS((3,3),(0.24995465243065,0.256253455718066),
 .UNSPECIFIED.)
CURVE()
GEOMETRIC_REPRESENTATION_ITEM()
RATIONAL_B_SPLINE_CURVE((1.11971735964612,1.12024119946958,1.12071541658434))
REPRESENTATION_ITEM('')
);
#1069=(
BOUNDED_CURVE()
B_SPLINE_CURVE(2,(#61778,#61779,#61780),.UNSPECIFIED.,.F.,.F.)
B_SPLINE_CURVE_WITH_KNOTS((3,3),(0.37664189880352,0.382940702095936),
 .UNSPECIFIED.)
CURVE()
GEOMETRIC_REPRESENTATION_ITEM()
RATIONAL_B_SPLINE_CURVE((1.12071541658452,1.12024119946938,1.11971735964546))
REPRESENTATION_ITEM('')
);
#1070=(
BOUNDED_CURVE()
B_SPLINE_CURVE(2,(#61784,#61785,#61786),.UNSPECIFIED.,.F.,.F.)
B_SPLINE_CURVE_WITH_KNOTS((3,3),(0.249954652430664,0.25625345571808),
 .UNSPECIFIED.)
CURVE()
GEOMETRIC_REPRESENTATION_ITEM()
RATIONAL_B_SPLINE_CURVE((1.11971735964628,1.12024119946975,1.12071541658451))
REPRESENTATION_ITEM('')
);
#1071=(
BOUNDED_CURVE()
B_SPLINE_CURVE(2,(#61790,#61791,#61792),.UNSPECIFIED.,.F.,.F.)
B_SPLINE_CURVE_WITH_KNOTS((3,3),(0.376641898803518,0.382940702095937),
 .UNSPECIFIED.)
CURVE()
GEOMETRIC_REPRESENTATION_ITEM()
RATIONAL_B_SPLINE_CURVE((1.12071541658454,1.12024119946941,1.11971735964549))
REPRESENTATION_ITEM('')
);
#1072=(
BOUNDED_CURVE()
B_SPLINE_CURVE(2,(#61796,#61797,#61798),.UNSPECIFIED.,.F.,.F.)
B_SPLINE_CURVE_WITH_KNOTS((3,3),(0.249954652430639,0.256253455718056),
 .UNSPECIFIED.)
CURVE()
GEOMETRIC_REPRESENTATION_ITEM()
RATIONAL_B_SPLINE_CURVE((1.11971735964609,1.12024119946956,1.12071541658432))
REPRESENTATION_ITEM('')
);
#1073=(
BOUNDED_CURVE()
B_SPLINE_CURVE(2,(#61802,#61803,#61804),.UNSPECIFIED.,.F.,.F.)
B_SPLINE_CURVE_WITH_KNOTS((3,3),(0.376641898803522,0.382940702095936),
 .UNSPECIFIED.)
CURVE()
GEOMETRIC_REPRESENTATION_ITEM()
RATIONAL_B_SPLINE_CURVE((1.12071541658447,1.12024119946934,1.11971735964542))
REPRESENTATION_ITEM('')
);
#1074=(
BOUNDED_CURVE()
B_SPLINE_CURVE(2,(#61808,#61809,#61810),.UNSPECIFIED.,.F.,.F.)
B_SPLINE_CURVE_WITH_KNOTS((3,3),(0.249954652430657,0.256253455718066),
 .UNSPECIFIED.)
CURVE()
GEOMETRIC_REPRESENTATION_ITEM()
RATIONAL_B_SPLINE_CURVE((1.11971735964622,1.12024119946968,1.12071541658444))
REPRESENTATION_ITEM('')
);
#1075=(
BOUNDED_CURVE()
B_SPLINE_CURVE(2,(#61814,#61815,#61816),.UNSPECIFIED.,.F.,.F.)
B_SPLINE_CURVE_WITH_KNOTS((3,3),(0.376641898803533,0.38294070209594),
 .UNSPECIFIED.)
CURVE()
GEOMETRIC_REPRESENTATION_ITEM()
RATIONAL_B_SPLINE_CURVE((1.12071541658433,1.1202411994692,1.11971735964528))
REPRESENTATION_ITEM('')
);
#1076=(
BOUNDED_CURVE()
B_SPLINE_CURVE(2,(#61820,#61821,#61822),.UNSPECIFIED.,.F.,.F.)
B_SPLINE_CURVE_WITH_KNOTS((3,3),(0.249954652430642,0.256253455718055),
 .UNSPECIFIED.)
CURVE()
GEOMETRIC_REPRESENTATION_ITEM()
RATIONAL_B_SPLINE_CURVE((1.11971735964602,1.12024119946948,1.12071541658424))
REPRESENTATION_ITEM('')
);
#1077=(
BOUNDED_CURVE()
B_SPLINE_CURVE(2,(#61826,#61827,#61828),.UNSPECIFIED.,.F.,.F.)
B_SPLINE_CURVE_WITH_KNOTS((3,3),(0.376641898803547,0.382940702095962),
 .UNSPECIFIED.)
CURVE()
GEOMETRIC_REPRESENTATION_ITEM()
RATIONAL_B_SPLINE_CURVE((1.12071541658418,1.12024119946904,1.11971735964512))
REPRESENTATION_ITEM('')
);
#1078=(
BOUNDED_CURVE()
B_SPLINE_CURVE(2,(#61832,#61833,#61834),.UNSPECIFIED.,.F.,.F.)
B_SPLINE_CURVE_WITH_KNOTS((3,3),(0.249954652430658,0.256253455718078),
 .UNSPECIFIED.)
CURVE()
GEOMETRIC_REPRESENTATION_ITEM()
RATIONAL_B_SPLINE_CURVE((1.1197173596463,1.12024119946977,1.12071541658453))
REPRESENTATION_ITEM('')
);
#1079=(
BOUNDED_CURVE()
B_SPLINE_CURVE(2,(#61838,#61839,#61840),.UNSPECIFIED.,.F.,.F.)
B_SPLINE_CURVE_WITH_KNOTS((3,3),(0.376641898803522,0.382940702095938),
 .UNSPECIFIED.)
CURVE()
GEOMETRIC_REPRESENTATION_ITEM()
RATIONAL_B_SPLINE_CURVE((1.12071541658451,1.12024119946937,1.11971735964545))
REPRESENTATION_ITEM('')
);
#1080=(
BOUNDED_CURVE()
B_SPLINE_CURVE(2,(#61844,#61845,#61846),.UNSPECIFIED.,.F.,.F.)
B_SPLINE_CURVE_WITH_KNOTS((3,3),(0.249954652430655,0.25625345571807),
 .UNSPECIFIED.)
CURVE()
GEOMETRIC_REPRESENTATION_ITEM()
RATIONAL_B_SPLINE_CURVE((1.11971735964625,1.12024119946971,1.12071541658447))
REPRESENTATION_ITEM('')
);
#1081=(
BOUNDED_CURVE()
B_SPLINE_CURVE(2,(#61850,#61851,#61852),.UNSPECIFIED.,.F.,.F.)
B_SPLINE_CURVE_WITH_KNOTS((3,3),(0.376641898803531,0.382940702095945),
 .UNSPECIFIED.)
CURVE()
GEOMETRIC_REPRESENTATION_ITEM()
RATIONAL_B_SPLINE_CURVE((1.12071541658432,1.12024119946919,1.11971735964527))
REPRESENTATION_ITEM('')
);
#1082=(
BOUNDED_CURVE()
B_SPLINE_CURVE(2,(#61856,#61857,#61858),.UNSPECIFIED.,.F.,.F.)
B_SPLINE_CURVE_WITH_KNOTS((3,3),(0.249954652430637,0.256253455718055),
 .UNSPECIFIED.)
CURVE()
GEOMETRIC_REPRESENTATION_ITEM()
RATIONAL_B_SPLINE_CURVE((1.11971735964599,1.12024119946945,1.12071541658421))
REPRESENTATION_ITEM('')
);
#1083=(
BOUNDED_CURVE()
B_SPLINE_CURVE(2,(#61862,#61863,#61864),.UNSPECIFIED.,.F.,.F.)
B_SPLINE_CURVE_WITH_KNOTS((3,3),(0.376641898803544,0.382940702095957),
 .UNSPECIFIED.)
CURVE()
GEOMETRIC_REPRESENTATION_ITEM()
RATIONAL_B_SPLINE_CURVE((1.12071541658422,1.12024119946908,1.11971735964516))
REPRESENTATION_ITEM('')
);
#1084=(
BOUNDED_CURVE()
B_SPLINE_CURVE(2,(#61868,#61869,#61870),.UNSPECIFIED.,.F.,.F.)
B_SPLINE_CURVE_WITH_KNOTS((3,3),(0.249954652430653,0.256253455718062),
 .UNSPECIFIED.)
CURVE()
GEOMETRIC_REPRESENTATION_ITEM()
RATIONAL_B_SPLINE_CURVE((1.11971735964616,1.12024119946962,1.12071541658438))
REPRESENTATION_ITEM('')
);
#1085=(
BOUNDED_CURVE()
B_SPLINE_CURVE(2,(#61874,#61875,#61876),.UNSPECIFIED.,.F.,.F.)
B_SPLINE_CURVE_WITH_KNOTS((3,3),(0.376641898803539,0.38294070209595),
 .UNSPECIFIED.)
CURVE()
GEOMETRIC_REPRESENTATION_ITEM()
RATIONAL_B_SPLINE_CURVE((1.12071541658449,1.12024119946935,1.11971735964543))
REPRESENTATION_ITEM('')
);
#1086=(
BOUNDED_CURVE()
B_SPLINE_CURVE(2,(#61880,#61881,#61882),.UNSPECIFIED.,.F.,.F.)
B_SPLINE_CURVE_WITH_KNOTS((3,3),(0.249954652430653,0.256253455718071),
 .UNSPECIFIED.)
CURVE()
GEOMETRIC_REPRESENTATION_ITEM()
RATIONAL_B_SPLINE_CURVE((1.11971735964627,1.12024119946973,1.12071541658449))
REPRESENTATION_ITEM('')
);
#1087=(
BOUNDED_CURVE()
B_SPLINE_CURVE(2,(#61886,#61887,#61888),.UNSPECIFIED.,.F.,.F.)
B_SPLINE_CURVE_WITH_KNOTS((3,3),(0.376641898803533,0.382940702095944),
 .UNSPECIFIED.)
CURVE()
GEOMETRIC_REPRESENTATION_ITEM()
RATIONAL_B_SPLINE_CURVE((1.12071541658435,1.12024119946922,1.1197173596453))
REPRESENTATION_ITEM('')
);
#1088=(
BOUNDED_CURVE()
B_SPLINE_CURVE(2,(#61892,#61893,#61894),.UNSPECIFIED.,.F.,.F.)
B_SPLINE_CURVE_WITH_KNOTS((3,3),(0.249954652430647,0.256253455718059),
 .UNSPECIFIED.)
CURVE()
GEOMETRIC_REPRESENTATION_ITEM()
RATIONAL_B_SPLINE_CURVE((1.11971735964614,1.12024119946961,1.12071541658437))
REPRESENTATION_ITEM('')
);
#1089=(
BOUNDED_CURVE()
B_SPLINE_CURVE(2,(#61898,#61899,#61900),.UNSPECIFIED.,.F.,.F.)
B_SPLINE_CURVE_WITH_KNOTS((3,3),(0.376641898803539,0.382940702095955),
 .UNSPECIFIED.)
CURVE()
GEOMETRIC_REPRESENTATION_ITEM()
RATIONAL_B_SPLINE_CURVE((1.12071541658434,1.1202411994692,1.11971735964528))
REPRESENTATION_ITEM('')
);
#1090=(
BOUNDED_CURVE()
B_SPLINE_CURVE(2,(#61904,#61905,#61906),.UNSPECIFIED.,.F.,.F.)
B_SPLINE_CURVE_WITH_KNOTS((3,3),(0.249954652430656,0.256253455718067),
 .UNSPECIFIED.)
CURVE()
GEOMETRIC_REPRESENTATION_ITEM()
RATIONAL_B_SPLINE_CURVE((1.11971735964622,1.12024119946969,1.12071541658444))
REPRESENTATION_ITEM('')
);
#1091=(
BOUNDED_CURVE()
B_SPLINE_CURVE(2,(#61910,#61911,#61912),.UNSPECIFIED.,.F.,.F.)
B_SPLINE_CURVE_WITH_KNOTS((3,3),(0.376641898803524,0.382940702095936),
 .UNSPECIFIED.)
CURVE()
GEOMETRIC_REPRESENTATION_ITEM()
RATIONAL_B_SPLINE_CURVE((1.12071541658457,1.12024119946943,1.11971735964551))
REPRESENTATION_ITEM('')
);
#1092=(
BOUNDED_CURVE()
B_SPLINE_CURVE(2,(#61916,#61917,#61918),.UNSPECIFIED.,.F.,.F.)
B_SPLINE_CURVE_WITH_KNOTS((3,3),(0.249954652430651,0.256253455718065),
 .UNSPECIFIED.)
CURVE()
GEOMETRIC_REPRESENTATION_ITEM()
RATIONAL_B_SPLINE_CURVE((1.11971735964615,1.12024119946961,1.12071541658437))
REPRESENTATION_ITEM('')
);
#1093=(
BOUNDED_CURVE()
B_SPLINE_CURVE(2,(#61922,#61923,#61924),.UNSPECIFIED.,.F.,.F.)
B_SPLINE_CURVE_WITH_KNOTS((3,3),(0.376641898803518,0.382940702095931),
 .UNSPECIFIED.)
CURVE()
GEOMETRIC_REPRESENTATION_ITEM()
RATIONAL_B_SPLINE_CURVE((1.12071541658449,1.12024119946936,1.11971735964544))
REPRESENTATION_ITEM('')
);
#1094=(
BOUNDED_CURVE()
B_SPLINE_CURVE(2,(#61928,#61929,#61930),.UNSPECIFIED.,.F.,.F.)
B_SPLINE_CURVE_WITH_KNOTS((3,3),(0.249954652430648,0.256253455718058),
 .UNSPECIFIED.)
CURVE()
GEOMETRIC_REPRESENTATION_ITEM()
RATIONAL_B_SPLINE_CURVE((1.11971735964614,1.1202411994696,1.12071541658436))
REPRESENTATION_ITEM('')
);
#1095=(
BOUNDED_CURVE()
B_SPLINE_CURVE(2,(#61934,#61935,#61936),.UNSPECIFIED.,.F.,.F.)
B_SPLINE_CURVE_WITH_KNOTS((3,3),(0.376641898803531,0.382940702095945),
 .UNSPECIFIED.)
CURVE()
GEOMETRIC_REPRESENTATION_ITEM()
RATIONAL_B_SPLINE_CURVE((1.12071541658451,1.12024119946937,1.11971735964545))
REPRESENTATION_ITEM('')
);
#1096=(
BOUNDED_CURVE()
B_SPLINE_CURVE(2,(#61940,#61941,#61942),.UNSPECIFIED.,.F.,.F.)
B_SPLINE_CURVE_WITH_KNOTS((3,3),(0.249954652430648,0.256253455718067),
 .UNSPECIFIED.)
CURVE()
GEOMETRIC_REPRESENTATION_ITEM()
RATIONAL_B_SPLINE_CURVE((1.11971735964618,1.12024119946964,1.1207154165844))
REPRESENTATION_ITEM('')
);
#1097=(
BOUNDED_CURVE()
B_SPLINE_CURVE(2,(#61946,#61947,#61948),.UNSPECIFIED.,.F.,.F.)
B_SPLINE_CURVE_WITH_KNOTS((3,3),(0.376641898803536,0.382940702095949),
 .UNSPECIFIED.)
CURVE()
GEOMETRIC_REPRESENTATION_ITEM()
RATIONAL_B_SPLINE_CURVE((1.12071541658431,1.12024119946918,1.11971735964526))
REPRESENTATION_ITEM('')
);
#1098=(
BOUNDED_CURVE()
B_SPLINE_CURVE(2,(#61952,#61953,#61954),.UNSPECIFIED.,.F.,.F.)
B_SPLINE_CURVE_WITH_KNOTS((3,3),(0.249954652430665,0.256253455718077),
 .UNSPECIFIED.)
CURVE()
GEOMETRIC_REPRESENTATION_ITEM()
RATIONAL_B_SPLINE_CURVE((1.11971735964631,1.12024119946977,1.12071541658453))
REPRESENTATION_ITEM('')
);
#1099=(
BOUNDED_CURVE()
B_SPLINE_CURVE(2,(#61958,#61959,#61960),.UNSPECIFIED.,.F.,.F.)
B_SPLINE_CURVE_WITH_KNOTS((3,3),(0.376641898803534,0.382940702095945),
 .UNSPECIFIED.)
CURVE()
GEOMETRIC_REPRESENTATION_ITEM()
RATIONAL_B_SPLINE_CURVE((1.12071541658427,1.12024119946914,1.11971735964522))
REPRESENTATION_ITEM('')
);
#1100=(
BOUNDED_CURVE()
B_SPLINE_CURVE(2,(#61964,#61965,#61966),.UNSPECIFIED.,.F.,.F.)
B_SPLINE_CURVE_WITH_KNOTS((3,3),(0.249954652430654,0.256253455718069),
 .UNSPECIFIED.)
CURVE()
GEOMETRIC_REPRESENTATION_ITEM()
RATIONAL_B_SPLINE_CURVE((1.11971735964621,1.12024119946968,1.12071541658444))
REPRESENTATION_ITEM('')
);
#1101=(
BOUNDED_CURVE()
B_SPLINE_CURVE(2,(#61970,#61971,#61972),.UNSPECIFIED.,.F.,.F.)
B_SPLINE_CURVE_WITH_KNOTS((3,3),(0.376641898803532,0.382940702095944),
 .UNSPECIFIED.)
CURVE()
GEOMETRIC_REPRESENTATION_ITEM()
RATIONAL_B_SPLINE_CURVE((1.12071541658432,1.12024119946919,1.11971735964527))
REPRESENTATION_ITEM('')
);
#1102=(
BOUNDED_CURVE()
B_SPLINE_CURVE(2,(#61976,#61977,#61978),.UNSPECIFIED.,.F.,.F.)
B_SPLINE_CURVE_WITH_KNOTS((3,3),(0.249954652430654,0.256253455718072),
 .UNSPECIFIED.)
CURVE()
GEOMETRIC_REPRESENTATION_ITEM()
RATIONAL_B_SPLINE_CURVE((1.11971735964625,1.12024119946971,1.12071541658447))
REPRESENTATION_ITEM('')
);
#1103=(
BOUNDED_CURVE()
B_SPLINE_CURVE(2,(#61982,#61983,#61984),.UNSPECIFIED.,.F.,.F.)
B_SPLINE_CURVE_WITH_KNOTS((3,3),(0.376641898803539,0.382940702095952),
 .UNSPECIFIED.)
CURVE()
GEOMETRIC_REPRESENTATION_ITEM()
RATIONAL_B_SPLINE_CURVE((1.1207154165844,1.12024119946926,1.11971735964534))
REPRESENTATION_ITEM('')
);
#1104=(
BOUNDED_CURVE()
B_SPLINE_CURVE(2,(#61988,#61989,#61990),.UNSPECIFIED.,.F.,.F.)
B_SPLINE_CURVE_WITH_KNOTS((3,3),(0.249954652430648,0.256253455718062),
 .UNSPECIFIED.)
CURVE()
GEOMETRIC_REPRESENTATION_ITEM()
RATIONAL_B_SPLINE_CURVE((1.11971735964618,1.12024119946965,1.12071541658441))
REPRESENTATION_ITEM('')
);
#1105=(
BOUNDED_CURVE()
B_SPLINE_CURVE(2,(#61994,#61995,#61996),.UNSPECIFIED.,.F.,.F.)
B_SPLINE_CURVE_WITH_KNOTS((3,3),(0.376641898803519,0.382940702095932),
 .UNSPECIFIED.)
CURVE()
GEOMETRIC_REPRESENTATION_ITEM()
RATIONAL_B_SPLINE_CURVE((1.12071541658452,1.12024119946938,1.11971735964546))
REPRESENTATION_ITEM('')
);
#1106=(
BOUNDED_CURVE()
B_SPLINE_CURVE(2,(#62000,#62001,#62002),.UNSPECIFIED.,.F.,.F.)
B_SPLINE_CURVE_WITH_KNOTS((3,3),(0.249954652430659,0.256253455718071),
 .UNSPECIFIED.)
CURVE()
GEOMETRIC_REPRESENTATION_ITEM()
RATIONAL_B_SPLINE_CURVE((1.11971735964627,1.12024119946974,1.1207154165845))
REPRESENTATION_ITEM('')
);
#1107=(
BOUNDED_CURVE()
B_SPLINE_CURVE(2,(#62006,#62007,#62008),.UNSPECIFIED.,.F.,.F.)
B_SPLINE_CURVE_WITH_KNOTS((3,3),(0.376641898803527,0.382940702095942),
 .UNSPECIFIED.)
CURVE()
GEOMETRIC_REPRESENTATION_ITEM()
RATIONAL_B_SPLINE_CURVE((1.12071541658453,1.1202411994694,1.11971735964547))
REPRESENTATION_ITEM('')
);
#1108=(
BOUNDED_CURVE()
B_SPLINE_CURVE(2,(#62012,#62013,#62014),.UNSPECIFIED.,.F.,.F.)
B_SPLINE_CURVE_WITH_KNOTS((3,3),(0.249954652430662,0.256253455718075),
 .UNSPECIFIED.)
CURVE()
GEOMETRIC_REPRESENTATION_ITEM()
RATIONAL_B_SPLINE_CURVE((1.11971735964629,1.12024119946976,1.12071541658452))
REPRESENTATION_ITEM('')
);
#1109=(
BOUNDED_CURVE()
B_SPLINE_CURVE(2,(#62018,#62019,#62020),.UNSPECIFIED.,.F.,.F.)
B_SPLINE_CURVE_WITH_KNOTS((3,3),(0.376641898803543,0.382940702095954),
 .UNSPECIFIED.)
CURVE()
GEOMETRIC_REPRESENTATION_ITEM()
RATIONAL_B_SPLINE_CURVE((1.12071541658423,1.1202411994691,1.11971735964518))
REPRESENTATION_ITEM('')
);
#1110=(
BOUNDED_CURVE()
B_SPLINE_CURVE(2,(#62024,#62025,#62026),.UNSPECIFIED.,.F.,.F.)
B_SPLINE_CURVE_WITH_KNOTS((3,3),(0.249954652430648,0.256253455718061),
 .UNSPECIFIED.)
CURVE()
GEOMETRIC_REPRESENTATION_ITEM()
RATIONAL_B_SPLINE_CURVE((1.11971735964609,1.12024119946956,1.12071541658431))
REPRESENTATION_ITEM('')
);
#1111=(
BOUNDED_CURVE()
B_SPLINE_CURVE(2,(#62030,#62031,#62032),.UNSPECIFIED.,.F.,.F.)
B_SPLINE_CURVE_WITH_KNOTS((3,3),(0.376641898803529,0.382940702095943),
 .UNSPECIFIED.)
CURVE()
GEOMETRIC_REPRESENTATION_ITEM()
RATIONAL_B_SPLINE_CURVE((1.12071541658438,1.12024119946925,1.11971735964533))
REPRESENTATION_ITEM('')
);
#1112=(
BOUNDED_CURVE()
B_SPLINE_CURVE(2,(#62036,#62037,#62038),.UNSPECIFIED.,.F.,.F.)
B_SPLINE_CURVE_WITH_KNOTS((3,3),(0.249954652430657,0.256253455718069),
 .UNSPECIFIED.)
CURVE()
GEOMETRIC_REPRESENTATION_ITEM()
RATIONAL_B_SPLINE_CURVE((1.11971735964625,1.12024119946971,1.12071541658447))
REPRESENTATION_ITEM('')
);
#1113=(
BOUNDED_CURVE()
B_SPLINE_CURVE(2,(#62042,#62043,#62044),.UNSPECIFIED.,.F.,.F.)
B_SPLINE_CURVE_WITH_KNOTS((3,3),(0.376641898803529,0.382940702095941),
 .UNSPECIFIED.)
CURVE()
GEOMETRIC_REPRESENTATION_ITEM()
RATIONAL_B_SPLINE_CURVE((1.12071541658439,1.12024119946925,1.11971735964533))
REPRESENTATION_ITEM('')
);
#1114=(
BOUNDED_CURVE()
B_SPLINE_CURVE(2,(#62048,#62049,#62050),.UNSPECIFIED.,.F.,.F.)
B_SPLINE_CURVE_WITH_KNOTS((3,3),(0.24995465243065,0.256253455718062),
 .UNSPECIFIED.)
CURVE()
GEOMETRIC_REPRESENTATION_ITEM()
RATIONAL_B_SPLINE_CURVE((1.11971735964607,1.12024119946954,1.12071541658429))
REPRESENTATION_ITEM('')
);
#1115=(
BOUNDED_CURVE()
B_SPLINE_CURVE(2,(#62054,#62055,#62056),.UNSPECIFIED.,.F.,.F.)
B_SPLINE_CURVE_WITH_KNOTS((3,3),(0.376641898803544,0.382940702095955),
 .UNSPECIFIED.)
CURVE()
GEOMETRIC_REPRESENTATION_ITEM()
RATIONAL_B_SPLINE_CURVE((1.12071541658421,1.12024119946907,1.11971735964515))
REPRESENTATION_ITEM('')
);
#1116=(
BOUNDED_CURVE()
B_SPLINE_CURVE(2,(#62060,#62061,#62062),.UNSPECIFIED.,.F.,.F.)
B_SPLINE_CURVE_WITH_KNOTS((3,3),(0.249954652430658,0.256253455718075),
 .UNSPECIFIED.)
CURVE()
GEOMETRIC_REPRESENTATION_ITEM()
RATIONAL_B_SPLINE_CURVE((1.11971735964629,1.12024119946976,1.12071541658452))
REPRESENTATION_ITEM('')
);
#1117=(
BOUNDED_CURVE()
B_SPLINE_CURVE(2,(#62066,#62067,#62068),.UNSPECIFIED.,.F.,.F.)
B_SPLINE_CURVE_WITH_KNOTS((3,3),(0.376641898803543,0.382940702095958),
 .UNSPECIFIED.)
CURVE()
GEOMETRIC_REPRESENTATION_ITEM()
RATIONAL_B_SPLINE_CURVE((1.12071541658432,1.12024119946919,1.11971735964527))
REPRESENTATION_ITEM('')
);
#1118=(
BOUNDED_CURVE()
B_SPLINE_CURVE(2,(#62072,#62073,#62074),.UNSPECIFIED.,.F.,.F.)
B_SPLINE_CURVE_WITH_KNOTS((3,3),(0.249954652430663,0.256253455718076),
 .UNSPECIFIED.)
CURVE()
GEOMETRIC_REPRESENTATION_ITEM()
RATIONAL_B_SPLINE_CURVE((1.11971735964633,1.12024119946979,1.12071541658455))
REPRESENTATION_ITEM('')
);
#1119=(
BOUNDED_CURVE()
B_SPLINE_CURVE(2,(#62078,#62079,#62080),.UNSPECIFIED.,.F.,.F.)
B_SPLINE_CURVE_WITH_KNOTS((3,3),(0.37664189880352,0.382940702095933),
 .UNSPECIFIED.)
CURVE()
GEOMETRIC_REPRESENTATION_ITEM()
RATIONAL_B_SPLINE_CURVE((1.1207154165845,1.12024119946936,1.11971735964544))
REPRESENTATION_ITEM('')
);
#1120=(
BOUNDED_CURVE()
B_SPLINE_CURVE(2,(#62084,#62085,#62086),.UNSPECIFIED.,.F.,.F.)
B_SPLINE_CURVE_WITH_KNOTS((3,3),(0.249954652430661,0.256253455718074),
 .UNSPECIFIED.)
CURVE()
GEOMETRIC_REPRESENTATION_ITEM()
RATIONAL_B_SPLINE_CURVE((1.11971735964627,1.12024119946973,1.12071541658449))
REPRESENTATION_ITEM('')
);
#1121=(
BOUNDED_CURVE()
B_SPLINE_CURVE(2,(#62090,#62091,#62092),.UNSPECIFIED.,.F.,.F.)
B_SPLINE_CURVE_WITH_KNOTS((3,3),(0.376641898803524,0.382940702095942),
 .UNSPECIFIED.)
CURVE()
GEOMETRIC_REPRESENTATION_ITEM()
RATIONAL_B_SPLINE_CURVE((1.12071541658449,1.12024119946935,1.11971735964543))
REPRESENTATION_ITEM('')
);
#1122=(
BOUNDED_CURVE()
B_SPLINE_CURVE(2,(#62096,#62097,#62098),.UNSPECIFIED.,.F.,.F.)
B_SPLINE_CURVE_WITH_KNOTS((3,3),(0.249954652430645,0.256253455718058),
 .UNSPECIFIED.)
CURVE()
GEOMETRIC_REPRESENTATION_ITEM()
RATIONAL_B_SPLINE_CURVE((1.11971735964602,1.12024119946949,1.12071541658425))
REPRESENTATION_ITEM('')
);
#1123=(
BOUNDED_CURVE()
B_SPLINE_CURVE(2,(#62102,#62103,#62104),.UNSPECIFIED.,.F.,.F.)
B_SPLINE_CURVE_WITH_KNOTS((3,3),(0.376641898803526,0.382940702095943),
 .UNSPECIFIED.)
CURVE()
GEOMETRIC_REPRESENTATION_ITEM()
RATIONAL_B_SPLINE_CURVE((1.12071541658447,1.12024119946934,1.11971735964542))
REPRESENTATION_ITEM('')
);
#1124=(
BOUNDED_CURVE()
B_SPLINE_CURVE(2,(#62108,#62109,#62110),.UNSPECIFIED.,.F.,.F.)
B_SPLINE_CURVE_WITH_KNOTS((3,3),(0.249954652430656,0.25625345571807),
 .UNSPECIFIED.)
CURVE()
GEOMETRIC_REPRESENTATION_ITEM()
RATIONAL_B_SPLINE_CURVE((1.11971735964623,1.12024119946969,1.12071541658445))
REPRESENTATION_ITEM('')
);
#1125=(
BOUNDED_CURVE()
B_SPLINE_CURVE(2,(#62114,#62115,#62116),.UNSPECIFIED.,.F.,.F.)
B_SPLINE_CURVE_WITH_KNOTS((3,3),(0.376641898803539,0.382940702095953),
 .UNSPECIFIED.)
CURVE()
GEOMETRIC_REPRESENTATION_ITEM()
RATIONAL_B_SPLINE_CURVE((1.12071541658437,1.12024119946923,1.11971735964531))
REPRESENTATION_ITEM('')
);
#1126=(
BOUNDED_CURVE()
B_SPLINE_CURVE(2,(#62120,#62121,#62122),.UNSPECIFIED.,.F.,.F.)
B_SPLINE_CURVE_WITH_KNOTS((3,3),(0.249954652430661,0.256253455718075),
 .UNSPECIFIED.)
CURVE()
GEOMETRIC_REPRESENTATION_ITEM()
RATIONAL_B_SPLINE_CURVE((1.11971735964628,1.12024119946974,1.1207154165845))
REPRESENTATION_ITEM('')
);
#1127=(
BOUNDED_CURVE()
B_SPLINE_CURVE(2,(#62126,#62127,#62128),.UNSPECIFIED.,.F.,.F.)
B_SPLINE_CURVE_WITH_KNOTS((3,3),(0.376641898803538,0.382940702095948),
 .UNSPECIFIED.)
CURVE()
GEOMETRIC_REPRESENTATION_ITEM()
RATIONAL_B_SPLINE_CURVE((1.12071541658433,1.1202411994692,1.11971735964528))
REPRESENTATION_ITEM('')
);
#1128=(
BOUNDED_CURVE()
B_SPLINE_CURVE(2,(#62132,#62133,#62134),.UNSPECIFIED.,.F.,.F.)
B_SPLINE_CURVE_WITH_KNOTS((3,3),(0.249954652430662,0.256253455718076),
 .UNSPECIFIED.)
CURVE()
GEOMETRIC_REPRESENTATION_ITEM()
RATIONAL_B_SPLINE_CURVE((1.11971735964622,1.12024119946968,1.12071541658444))
REPRESENTATION_ITEM('')
);
#1129=(
BOUNDED_CURVE()
B_SPLINE_CURVE(2,(#62138,#62139,#62140),.UNSPECIFIED.,.F.,.F.)
B_SPLINE_CURVE_WITH_KNOTS((3,3),(0.37664189880352,0.382940702095935),
 .UNSPECIFIED.)
CURVE()
GEOMETRIC_REPRESENTATION_ITEM()
RATIONAL_B_SPLINE_CURVE((1.12071541658454,1.12024119946941,1.11971735964549))
REPRESENTATION_ITEM('')
);
#1130=(
BOUNDED_CURVE()
B_SPLINE_CURVE(2,(#62144,#62145,#62146),.UNSPECIFIED.,.F.,.F.)
B_SPLINE_CURVE_WITH_KNOTS((3,3),(0.24995465243066,0.256253455718075),
 .UNSPECIFIED.)
CURVE()
GEOMETRIC_REPRESENTATION_ITEM()
RATIONAL_B_SPLINE_CURVE((1.1197173596463,1.12024119946976,1.12071541658452))
REPRESENTATION_ITEM('')
);
#1131=(
BOUNDED_CURVE()
B_SPLINE_CURVE(2,(#62150,#62151,#62152),.UNSPECIFIED.,.F.,.F.)
B_SPLINE_CURVE_WITH_KNOTS((3,3),(0.376641898803523,0.382940702095934),
 .UNSPECIFIED.)
CURVE()
GEOMETRIC_REPRESENTATION_ITEM()
RATIONAL_B_SPLINE_CURVE((1.12071541658448,1.12024119946934,1.11971735964542))
REPRESENTATION_ITEM('')
);
#1132=(
BOUNDED_CURVE()
B_SPLINE_CURVE(2,(#62156,#62157,#62158),.UNSPECIFIED.,.F.,.F.)
B_SPLINE_CURVE_WITH_KNOTS((3,3),(0.249954652430663,0.256253455718077),
 .UNSPECIFIED.)
CURVE()
GEOMETRIC_REPRESENTATION_ITEM()
RATIONAL_B_SPLINE_CURVE((1.11971735964627,1.12024119946973,1.12071541658449))
REPRESENTATION_ITEM('')
);
#1133=(
BOUNDED_CURVE()
B_SPLINE_CURVE(2,(#62162,#62163,#62164),.UNSPECIFIED.,.F.,.F.)
B_SPLINE_CURVE_WITH_KNOTS((3,3),(0.376641898803548,0.382940702095957),
 .UNSPECIFIED.)
CURVE()
GEOMETRIC_REPRESENTATION_ITEM()
RATIONAL_B_SPLINE_CURVE((1.12071541658418,1.12024119946905,1.11971735964513))
REPRESENTATION_ITEM('')
);
#1134=(
BOUNDED_CURVE()
B_SPLINE_CURVE(2,(#62168,#62169,#62170),.UNSPECIFIED.,.F.,.F.)
B_SPLINE_CURVE_WITH_KNOTS((3,3),(0.249954652430651,0.256253455718065),
 .UNSPECIFIED.)
CURVE()
GEOMETRIC_REPRESENTATION_ITEM()
RATIONAL_B_SPLINE_CURVE((1.1197173596461,1.12024119946956,1.12071541658432))
REPRESENTATION_ITEM('')
);
#1135=(
BOUNDED_CURVE()
B_SPLINE_CURVE(2,(#62174,#62175,#62176),.UNSPECIFIED.,.F.,.F.)
B_SPLINE_CURVE_WITH_KNOTS((3,3),(0.376641898803522,0.382940702095932),
 .UNSPECIFIED.)
CURVE()
GEOMETRIC_REPRESENTATION_ITEM()
RATIONAL_B_SPLINE_CURVE((1.12071541658448,1.12024119946934,1.11971735964542))
REPRESENTATION_ITEM('')
);
#1136=(
BOUNDED_CURVE()
B_SPLINE_CURVE(2,(#62180,#62181,#62182),.UNSPECIFIED.,.F.,.F.)
B_SPLINE_CURVE_WITH_KNOTS((3,3),(0.249954652430654,0.256253455718068),
 .UNSPECIFIED.)
CURVE()
GEOMETRIC_REPRESENTATION_ITEM()
RATIONAL_B_SPLINE_CURVE((1.11971735964629,1.12024119946976,1.12071541658452))
REPRESENTATION_ITEM('')
);
#1137=(
BOUNDED_CURVE()
B_SPLINE_CURVE(2,(#62186,#62187,#62188),.UNSPECIFIED.,.F.,.F.)
B_SPLINE_CURVE_WITH_KNOTS((3,3),(0.376641898803521,0.382940702095935),
 .UNSPECIFIED.)
CURVE()
GEOMETRIC_REPRESENTATION_ITEM()
RATIONAL_B_SPLINE_CURVE((1.12071541658442,1.12024119946928,1.11971735964536))
REPRESENTATION_ITEM('')
);
#1138=(
BOUNDED_CURVE()
B_SPLINE_CURVE(2,(#62192,#62193,#62194),.UNSPECIFIED.,.F.,.F.)
B_SPLINE_CURVE_WITH_KNOTS((3,3),(0.24995465243066,0.256253455718076),
 .UNSPECIFIED.)
CURVE()
GEOMETRIC_REPRESENTATION_ITEM()
RATIONAL_B_SPLINE_CURVE((1.11971735964628,1.12024119946975,1.12071541658451))
REPRESENTATION_ITEM('')
);
#1139=(
BOUNDED_CURVE()
B_SPLINE_CURVE(2,(#62198,#62199,#62200),.UNSPECIFIED.,.F.,.F.)
B_SPLINE_CURVE_WITH_KNOTS((3,3),(0.37664189880352,0.382940702095931),
 .UNSPECIFIED.)
CURVE()
GEOMETRIC_REPRESENTATION_ITEM()
RATIONAL_B_SPLINE_CURVE((1.12071541658452,1.12024119946938,1.11971735964546))
REPRESENTATION_ITEM('')
);
#1140=(
BOUNDED_CURVE()
B_SPLINE_CURVE(2,(#62204,#62205,#62206),.UNSPECIFIED.,.F.,.F.)
B_SPLINE_CURVE_WITH_KNOTS((3,3),(0.249954652430663,0.25625345571808),
 .UNSPECIFIED.)
CURVE()
GEOMETRIC_REPRESENTATION_ITEM()
RATIONAL_B_SPLINE_CURVE((1.11971735964629,1.12024119946975,1.12071541658451))
REPRESENTATION_ITEM('')
);
#1141=(
BOUNDED_CURVE()
B_SPLINE_CURVE(2,(#62210,#62211,#62212),.UNSPECIFIED.,.F.,.F.)
B_SPLINE_CURVE_WITH_KNOTS((3,3),(0.376641898803514,0.382940702095925),
 .UNSPECIFIED.)
CURVE()
GEOMETRIC_REPRESENTATION_ITEM()
RATIONAL_B_SPLINE_CURVE((1.12071541658449,1.12024119946936,1.11971735964544))
REPRESENTATION_ITEM('')
);
#1142=(
BOUNDED_CURVE()
B_SPLINE_CURVE(2,(#62216,#62217,#62218),.UNSPECIFIED.,.F.,.F.)
B_SPLINE_CURVE_WITH_KNOTS((3,3),(0.249954652430668,0.25625345571808),
 .UNSPECIFIED.)
CURVE()
GEOMETRIC_REPRESENTATION_ITEM()
RATIONAL_B_SPLINE_CURVE((1.11971735964628,1.12024119946974,1.1207154165845))
REPRESENTATION_ITEM('')
);
#1143=(
BOUNDED_CURVE()
B_SPLINE_CURVE(2,(#62222,#62223,#62224),.UNSPECIFIED.,.F.,.F.)
B_SPLINE_CURVE_WITH_KNOTS((3,3),(0.376641898803516,0.382940702095925),
 .UNSPECIFIED.)
CURVE()
GEOMETRIC_REPRESENTATION_ITEM()
RATIONAL_B_SPLINE_CURVE((1.1207154165845,1.12024119946936,1.11971735964544))
REPRESENTATION_ITEM('')
);
#1144=(
BOUNDED_CURVE()
B_SPLINE_CURVE(2,(#62228,#62229,#62230),.UNSPECIFIED.,.F.,.F.)
B_SPLINE_CURVE_WITH_KNOTS((3,3),(0.24995465243065,0.256253455718064),
 .UNSPECIFIED.)
CURVE()
GEOMETRIC_REPRESENTATION_ITEM()
RATIONAL_B_SPLINE_CURVE((1.11971735964608,1.12024119946955,1.1207154165843))
REPRESENTATION_ITEM('')
);
#1145=(
BOUNDED_CURVE()
B_SPLINE_CURVE(2,(#62234,#62235,#62236),.UNSPECIFIED.,.F.,.F.)
B_SPLINE_CURVE_WITH_KNOTS((3,3),(0.376641898803537,0.382940702095953),
 .UNSPECIFIED.)
CURVE()
GEOMETRIC_REPRESENTATION_ITEM()
RATIONAL_B_SPLINE_CURVE((1.12071541658421,1.12024119946908,1.11971735964516))
REPRESENTATION_ITEM('')
);
#1146=(
BOUNDED_CURVE()
B_SPLINE_CURVE(2,(#62240,#62241,#62242),.UNSPECIFIED.,.F.,.F.)
B_SPLINE_CURVE_WITH_KNOTS((3,3),(0.249954652430652,0.256253455718068),
 .UNSPECIFIED.)
CURVE()
GEOMETRIC_REPRESENTATION_ITEM()
RATIONAL_B_SPLINE_CURVE((1.11971735964626,1.12024119946972,1.12071541658448))
REPRESENTATION_ITEM('')
);
#1147=(
BOUNDED_CURVE()
B_SPLINE_CURVE(2,(#62246,#62247,#62248),.UNSPECIFIED.,.F.,.F.)
B_SPLINE_CURVE_WITH_KNOTS((3,3),(0.376641898803534,0.382940702095941),
 .UNSPECIFIED.)
CURVE()
GEOMETRIC_REPRESENTATION_ITEM()
RATIONAL_B_SPLINE_CURVE((1.12071541658423,1.1202411994691,1.11971735964518))
REPRESENTATION_ITEM('')
);
#1148=(
BOUNDED_CURVE()
B_SPLINE_CURVE(2,(#62252,#62253,#62254),.UNSPECIFIED.,.F.,.F.)
B_SPLINE_CURVE_WITH_KNOTS((3,3),(0.249954652430639,0.256253455718054),
 .UNSPECIFIED.)
CURVE()
GEOMETRIC_REPRESENTATION_ITEM()
RATIONAL_B_SPLINE_CURVE((1.11971735964598,1.12024119946944,1.1207154165842))
REPRESENTATION_ITEM('')
);
#1149=(
BOUNDED_CURVE()
B_SPLINE_CURVE(2,(#62258,#62259,#62260),.UNSPECIFIED.,.F.,.F.)
B_SPLINE_CURVE_WITH_KNOTS((3,3),(0.376641898803521,0.382940702095926),
 .UNSPECIFIED.)
CURVE()
GEOMETRIC_REPRESENTATION_ITEM()
RATIONAL_B_SPLINE_CURVE((1.12071541658441,1.12024119946928,1.11971735964536))
REPRESENTATION_ITEM('')
);
#1150=(
BOUNDED_CURVE()
B_SPLINE_CURVE(2,(#62264,#62265,#62266),.UNSPECIFIED.,.F.,.F.)
B_SPLINE_CURVE_WITH_KNOTS((3,3),(0.249954652430644,0.256253455718059),
 .UNSPECIFIED.)
CURVE()
GEOMETRIC_REPRESENTATION_ITEM()
RATIONAL_B_SPLINE_CURVE((1.11971735964605,1.12024119946951,1.12071541658427))
REPRESENTATION_ITEM('')
);
#1151=(
BOUNDED_CURVE()
B_SPLINE_CURVE(2,(#62270,#62271,#62272),.UNSPECIFIED.,.F.,.F.)
B_SPLINE_CURVE_WITH_KNOTS((3,3),(0.376641898803522,0.382940702095933),
 .UNSPECIFIED.)
CURVE()
GEOMETRIC_REPRESENTATION_ITEM()
RATIONAL_B_SPLINE_CURVE((1.12071541658452,1.12024119946939,1.11971735964547))
REPRESENTATION_ITEM('')
);
#1152=(
BOUNDED_CURVE()
B_SPLINE_CURVE(2,(#62276,#62277,#62278),.UNSPECIFIED.,.F.,.F.)
B_SPLINE_CURVE_WITH_KNOTS((3,3),(0.249954652430652,0.256253455718069),
 .UNSPECIFIED.)
CURVE()
GEOMETRIC_REPRESENTATION_ITEM()
RATIONAL_B_SPLINE_CURVE((1.11971735964616,1.12024119946962,1.12071541658438))
REPRESENTATION_ITEM('')
);
#1153=(
BOUNDED_CURVE()
B_SPLINE_CURVE(2,(#62282,#62283,#62284),.UNSPECIFIED.,.F.,.F.)
B_SPLINE_CURVE_WITH_KNOTS((3,3),(0.376641898803538,0.38294070209595),
 .UNSPECIFIED.)
CURVE()
GEOMETRIC_REPRESENTATION_ITEM()
RATIONAL_B_SPLINE_CURVE((1.12071541658426,1.12024119946913,1.11971735964521))
REPRESENTATION_ITEM('')
);
#1154=(
BOUNDED_CURVE()
B_SPLINE_CURVE(2,(#62287,#62288,#62289),.UNSPECIFIED.,.F.,.F.)
B_SPLINE_CURVE_WITH_KNOTS((3,3),(0.249954652430655,0.256253455718073),
 .UNSPECIFIED.)
CURVE()
GEOMETRIC_REPRESENTATION_ITEM()
RATIONAL_B_SPLINE_CURVE((1.11971735964623,1.1202411994697,1.12071541658446))
REPRESENTATION_ITEM('')
);
#1155=(
BOUNDED_CURVE()
B_SPLINE_CURVE(2,(#62291,#62292,#62293),.UNSPECIFIED.,.F.,.F.)
B_SPLINE_CURVE_WITH_KNOTS((3,3),(0.376641898803523,0.38294070209594),
 .UNSPECIFIED.)
CURVE()
GEOMETRIC_REPRESENTATION_ITEM()
RATIONAL_B_SPLINE_CURVE((1.12071541658441,1.12024119946928,1.11971735964536))
REPRESENTATION_ITEM('')
);
#1156=(
BOUNDED_CURVE()
B_SPLINE_CURVE(2,(#62296,#62297,#62298),.UNSPECIFIED.,.F.,.F.)
B_SPLINE_CURVE_WITH_KNOTS((3,3),(0.249954652430659,0.256253455718073),
 .UNSPECIFIED.)
CURVE()
GEOMETRIC_REPRESENTATION_ITEM()
RATIONAL_B_SPLINE_CURVE((1.11971735964623,1.12024119946969,1.12071541658445))
REPRESENTATION_ITEM('')
);
#1157=(
BOUNDED_CURVE()
B_SPLINE_CURVE(2,(#62300,#62301,#62302),.UNSPECIFIED.,.F.,.F.)
B_SPLINE_CURVE_WITH_KNOTS((3,3),(0.376641898803521,0.382940702095929),
 .UNSPECIFIED.)
CURVE()
GEOMETRIC_REPRESENTATION_ITEM()
RATIONAL_B_SPLINE_CURVE((1.12071541658454,1.1202411994694,1.11971735964548))
REPRESENTATION_ITEM('')
);
#1158=(
BOUNDED_CURVE()
B_SPLINE_CURVE(2,(#62305,#62306,#62307),.UNSPECIFIED.,.F.,.F.)
B_SPLINE_CURVE_WITH_KNOTS((3,3),(0.249954652430646,0.256253455718056),
 .UNSPECIFIED.)
CURVE()
GEOMETRIC_REPRESENTATION_ITEM()
RATIONAL_B_SPLINE_CURVE((1.11971735964596,1.12024119946942,1.12071541658418))
REPRESENTATION_ITEM('')
);
#1159=(
BOUNDED_CURVE()
B_SPLINE_CURVE(2,(#62309,#62310,#62311),.UNSPECIFIED.,.F.,.F.)
B_SPLINE_CURVE_WITH_KNOTS((3,3),(0.376641898803528,0.382940702095943),
 .UNSPECIFIED.)
CURVE()
GEOMETRIC_REPRESENTATION_ITEM()
RATIONAL_B_SPLINE_CURVE((1.12071541658433,1.1202411994692,1.11971735964528))
REPRESENTATION_ITEM('')
);
#1160=(
BOUNDED_CURVE()
B_SPLINE_CURVE(2,(#62314,#62315,#62316),.UNSPECIFIED.,.F.,.F.)
B_SPLINE_CURVE_WITH_KNOTS((3,3),(0.24995465243066,0.256253455718077),
 .UNSPECIFIED.)
CURVE()
GEOMETRIC_REPRESENTATION_ITEM()
RATIONAL_B_SPLINE_CURVE((1.11971735964636,1.12024119946983,1.12071541658459))
REPRESENTATION_ITEM('')
);
#1161=(
BOUNDED_CURVE()
B_SPLINE_CURVE(2,(#62318,#62319,#62320),.UNSPECIFIED.,.F.,.F.)
B_SPLINE_CURVE_WITH_KNOTS((3,3),(0.376641898803527,0.382940702095942),
 .UNSPECIFIED.)
CURVE()
GEOMETRIC_REPRESENTATION_ITEM()
RATIONAL_B_SPLINE_CURVE((1.12071541658443,1.12024119946929,1.11971735964537))
REPRESENTATION_ITEM('')
);
#1162=(
BOUNDED_CURVE()
B_SPLINE_CURVE(2,(#62323,#62324,#62325),.UNSPECIFIED.,.F.,.F.)
B_SPLINE_CURVE_WITH_KNOTS((3,3),(0.249954652430663,0.256253455718073),
 .UNSPECIFIED.)
CURVE()
GEOMETRIC_REPRESENTATION_ITEM()
RATIONAL_B_SPLINE_CURVE((1.11971735964622,1.12024119946969,1.12071541658445))
REPRESENTATION_ITEM('')
);
#1163=(
BOUNDED_CURVE()
B_SPLINE_CURVE(2,(#62327,#62328,#62329),.UNSPECIFIED.,.F.,.F.)
B_SPLINE_CURVE_WITH_KNOTS((3,3),(0.376641898803534,0.382940702095947),
 .UNSPECIFIED.)
CURVE()
GEOMETRIC_REPRESENTATION_ITEM()
RATIONAL_B_SPLINE_CURVE((1.12071541658425,1.12024119946912,1.1197173596452))
REPRESENTATION_ITEM('')
);
#1164=(
BOUNDED_CURVE()
B_SPLINE_CURVE(2,(#62332,#62333,#62334),.UNSPECIFIED.,.F.,.F.)
B_SPLINE_CURVE_WITH_KNOTS((3,3),(0.249954652430658,0.256253455718067),
 .UNSPECIFIED.)
CURVE()
GEOMETRIC_REPRESENTATION_ITEM()
RATIONAL_B_SPLINE_CURVE((1.1197173596462,1.12024119946966,1.12071541658442))
REPRESENTATION_ITEM('')
);
#1165=(
BOUNDED_CURVE()
B_SPLINE_CURVE(2,(#62336,#62337,#62338),.UNSPECIFIED.,.F.,.F.)
B_SPLINE_CURVE_WITH_KNOTS((3,3),(0.376641898803512,0.382940702095926),
 .UNSPECIFIED.)
CURVE()
GEOMETRIC_REPRESENTATION_ITEM()
RATIONAL_B_SPLINE_CURVE((1.12071541658454,1.12024119946941,1.11971735964549))
REPRESENTATION_ITEM('')
);
#1166=(
BOUNDED_CURVE()
B_SPLINE_CURVE(2,(#62341,#62342,#62343),.UNSPECIFIED.,.F.,.F.)
B_SPLINE_CURVE_WITH_KNOTS((3,3),(0.249954652430648,0.256253455718064),
 .UNSPECIFIED.)
CURVE()
GEOMETRIC_REPRESENTATION_ITEM()
RATIONAL_B_SPLINE_CURVE((1.11971735964605,1.12024119946951,1.12071541658427))
REPRESENTATION_ITEM('')
);
#1167=(
BOUNDED_CURVE()
B_SPLINE_CURVE(2,(#62345,#62346,#62347),.UNSPECIFIED.,.F.,.F.)
B_SPLINE_CURVE_WITH_KNOTS((3,3),(0.37664189880353,0.382940702095945),
 .UNSPECIFIED.)
CURVE()
GEOMETRIC_REPRESENTATION_ITEM()
RATIONAL_B_SPLINE_CURVE((1.12071541658432,1.12024119946919,1.11971735964527))
REPRESENTATION_ITEM('')
);
#1168=(
BOUNDED_CURVE()
B_SPLINE_CURVE(2,(#62350,#62351,#62352),.UNSPECIFIED.,.F.,.F.)
B_SPLINE_CURVE_WITH_KNOTS((3,3),(0.24995465243065,0.256253455718062),
 .UNSPECIFIED.)
CURVE()
GEOMETRIC_REPRESENTATION_ITEM()
RATIONAL_B_SPLINE_CURVE((1.1197173596462,1.12024119946966,1.12071541658442))
REPRESENTATION_ITEM('')
);
#1169=(
BOUNDED_CURVE()
B_SPLINE_CURVE(2,(#62354,#62355,#62356),.UNSPECIFIED.,.F.,.F.)
B_SPLINE_CURVE_WITH_KNOTS((3,3),(0.376641898803514,0.382940702095926),
 .UNSPECIFIED.)
CURVE()
GEOMETRIC_REPRESENTATION_ITEM()
RATIONAL_B_SPLINE_CURVE((1.12071541658458,1.12024119946944,1.11971735964552))
REPRESENTATION_ITEM('')
);
#1170=(
BOUNDED_CURVE()
B_SPLINE_CURVE(2,(#62359,#62360,#62361),.UNSPECIFIED.,.F.,.F.)
B_SPLINE_CURVE_WITH_KNOTS((3,3),(0.249954652430654,0.256253455718075),
 .UNSPECIFIED.)
CURVE()
GEOMETRIC_REPRESENTATION_ITEM()
RATIONAL_B_SPLINE_CURVE((1.11971735964632,1.12024119946978,1.12071541658454))
REPRESENTATION_ITEM('')
);
#1171=(
BOUNDED_CURVE()
B_SPLINE_CURVE(2,(#62363,#62364,#62365),.UNSPECIFIED.,.F.,.F.)
B_SPLINE_CURVE_WITH_KNOTS((3,3),(0.376641898803524,0.382940702095939),
 .UNSPECIFIED.)
CURVE()
GEOMETRIC_REPRESENTATION_ITEM()
RATIONAL_B_SPLINE_CURVE((1.12071541658443,1.1202411994693,1.11971735964538))
REPRESENTATION_ITEM('')
);
#1172=(
BOUNDED_CURVE()
B_SPLINE_CURVE(2,(#62368,#62369,#62370),.UNSPECIFIED.,.F.,.F.)
B_SPLINE_CURVE_WITH_KNOTS((3,3),(0.249954652430651,0.256253455718065),
 .UNSPECIFIED.)
CURVE()
GEOMETRIC_REPRESENTATION_ITEM()
RATIONAL_B_SPLINE_CURVE((1.11971735964614,1.12024119946961,1.12071541658437))
REPRESENTATION_ITEM('')
);
#1173=(
BOUNDED_CURVE()
B_SPLINE_CURVE(2,(#62372,#62373,#62374),.UNSPECIFIED.,.F.,.F.)
B_SPLINE_CURVE_WITH_KNOTS((3,3),(0.376641898803524,0.382940702095937),
 .UNSPECIFIED.)
CURVE()
GEOMETRIC_REPRESENTATION_ITEM()
RATIONAL_B_SPLINE_CURVE((1.12071541658443,1.1202411994693,1.11971735964538))
REPRESENTATION_ITEM('')
);
#1174=(
BOUNDED_CURVE()
B_SPLINE_CURVE(2,(#62377,#62378,#62379),.UNSPECIFIED.,.F.,.F.)
B_SPLINE_CURVE_WITH_KNOTS((3,3),(0.24995465243066,0.256253455718078),
 .UNSPECIFIED.)
CURVE()
GEOMETRIC_REPRESENTATION_ITEM()
RATIONAL_B_SPLINE_CURVE((1.11971735964625,1.12024119946971,1.12071541658447))
REPRESENTATION_ITEM('')
);
#1175=(
BOUNDED_CURVE()
B_SPLINE_CURVE(2,(#62381,#62382,#62383),.UNSPECIFIED.,.F.,.F.)
B_SPLINE_CURVE_WITH_KNOTS((3,3),(0.376641898803522,0.382940702095931),
 .UNSPECIFIED.)
CURVE()
GEOMETRIC_REPRESENTATION_ITEM()
RATIONAL_B_SPLINE_CURVE((1.1207154165845,1.12024119946936,1.11971735964544))
REPRESENTATION_ITEM('')
);
#1176=(
BOUNDED_CURVE()
B_SPLINE_CURVE(2,(#62386,#62387,#62388),.UNSPECIFIED.,.F.,.F.)
B_SPLINE_CURVE_WITH_KNOTS((3,3),(0.249954652430652,0.256253455718071),
 .UNSPECIFIED.)
CURVE()
GEOMETRIC_REPRESENTATION_ITEM()
RATIONAL_B_SPLINE_CURVE((1.11971735964614,1.12024119946961,1.12071541658437))
REPRESENTATION_ITEM('')
);
#1177=(
BOUNDED_CURVE()
B_SPLINE_CURVE(2,(#62390,#62391,#62392),.UNSPECIFIED.,.F.,.F.)
B_SPLINE_CURVE_WITH_KNOTS((3,3),(0.376641898803528,0.382940702095942),
 .UNSPECIFIED.)
CURVE()
GEOMETRIC_REPRESENTATION_ITEM()
RATIONAL_B_SPLINE_CURVE((1.12071541658436,1.12024119946922,1.1197173596453))
REPRESENTATION_ITEM('')
);
#1178=(
BOUNDED_CURVE()
B_SPLINE_CURVE(2,(#62395,#62396,#62397),.UNSPECIFIED.,.F.,.F.)
B_SPLINE_CURVE_WITH_KNOTS((3,3),(0.249954652430651,0.256253455718071),
 .UNSPECIFIED.)
CURVE()
GEOMETRIC_REPRESENTATION_ITEM()
RATIONAL_B_SPLINE_CURVE((1.11971735964609,1.12024119946955,1.12071541658431))
REPRESENTATION_ITEM('')
);
#1179=(
BOUNDED_CURVE()
B_SPLINE_CURVE(2,(#62399,#62400,#62401),.UNSPECIFIED.,.F.,.F.)
B_SPLINE_CURVE_WITH_KNOTS((3,3),(0.376641898803537,0.382940702095949),
 .UNSPECIFIED.)
CURVE()
GEOMETRIC_REPRESENTATION_ITEM()
RATIONAL_B_SPLINE_CURVE((1.12071541658424,1.1202411994691,1.11971735964519))
REPRESENTATION_ITEM('')
);
#1180=(
BOUNDED_CURVE()
B_SPLINE_CURVE(2,(#62404,#62405,#62406),.UNSPECIFIED.,.F.,.F.)
B_SPLINE_CURVE_WITH_KNOTS((3,3),(0.249954652430663,0.256253455718077),
 .UNSPECIFIED.)
CURVE()
GEOMETRIC_REPRESENTATION_ITEM()
RATIONAL_B_SPLINE_CURVE((1.11971735964627,1.12024119946974,1.1207154165845))
REPRESENTATION_ITEM('')
);
#1181=(
BOUNDED_CURVE()
B_SPLINE_CURVE(2,(#62408,#62409,#62410),.UNSPECIFIED.,.F.,.F.)
B_SPLINE_CURVE_WITH_KNOTS((3,3),(0.376641898803535,0.382940702095948),
 .UNSPECIFIED.)
CURVE()
GEOMETRIC_REPRESENTATION_ITEM()
RATIONAL_B_SPLINE_CURVE((1.12071541658433,1.1202411994692,1.11971735964528))
REPRESENTATION_ITEM('')
);
#1182=(
BOUNDED_CURVE()
B_SPLINE_CURVE(2,(#62413,#62414,#62415),.UNSPECIFIED.,.F.,.F.)
B_SPLINE_CURVE_WITH_KNOTS((3,3),(0.249954652430657,0.256253455718068),
 .UNSPECIFIED.)
CURVE()
GEOMETRIC_REPRESENTATION_ITEM()
RATIONAL_B_SPLINE_CURVE((1.11971735964623,1.1202411994697,1.12071541658445))
REPRESENTATION_ITEM('')
);
#1183=(
BOUNDED_CURVE()
B_SPLINE_CURVE(2,(#62417,#62418,#62419),.UNSPECIFIED.,.F.,.F.)
B_SPLINE_CURVE_WITH_KNOTS((3,3),(0.376641898803534,0.382940702095946),
 .UNSPECIFIED.)
CURVE()
GEOMETRIC_REPRESENTATION_ITEM()
RATIONAL_B_SPLINE_CURVE((1.12071541658428,1.12024119946915,1.11971735964523))
REPRESENTATION_ITEM('')
);
#1184=(
BOUNDED_CURVE()
B_SPLINE_CURVE(2,(#62423,#62424,#62425),.UNSPECIFIED.,.F.,.F.)
B_SPLINE_CURVE_WITH_KNOTS((3,3),(0.249954652430652,0.256253455718065),
 .UNSPECIFIED.)
CURVE()
GEOMETRIC_REPRESENTATION_ITEM()
RATIONAL_B_SPLINE_CURVE((1.11971735964615,1.12024119946961,1.12071541658437))
REPRESENTATION_ITEM('')
);
#1185=(
BOUNDED_CURVE()
B_SPLINE_CURVE(2,(#62429,#62430,#62431),.UNSPECIFIED.,.F.,.F.)
B_SPLINE_CURVE_WITH_KNOTS((3,3),(0.376641898803528,0.38294070209594),
 .UNSPECIFIED.)
CURVE()
GEOMETRIC_REPRESENTATION_ITEM()
RATIONAL_B_SPLINE_CURVE((1.12071541658438,1.12024119946925,1.11971735964533))
REPRESENTATION_ITEM('')
);
#1186=(
BOUNDED_CURVE()
B_SPLINE_CURVE(2,(#62435,#62436,#62437),.UNSPECIFIED.,.F.,.F.)
B_SPLINE_CURVE_WITH_KNOTS((3,3),(0.249954652430646,0.256253455718057),
 .UNSPECIFIED.)
CURVE()
GEOMETRIC_REPRESENTATION_ITEM()
RATIONAL_B_SPLINE_CURVE((1.11971735964604,1.12024119946951,1.12071541658426))
REPRESENTATION_ITEM('')
);
#1187=(
BOUNDED_CURVE()
B_SPLINE_CURVE(2,(#62441,#62442,#62443),.UNSPECIFIED.,.F.,.F.)
B_SPLINE_CURVE_WITH_KNOTS((3,3),(0.376641898803525,0.382940702095939),
 .UNSPECIFIED.)
CURVE()
GEOMETRIC_REPRESENTATION_ITEM()
RATIONAL_B_SPLINE_CURVE((1.12071541658443,1.1202411994693,1.11971735964538))
REPRESENTATION_ITEM('')
);
#1188=(
BOUNDED_CURVE()
B_SPLINE_CURVE(2,(#62447,#62448,#62449),.UNSPECIFIED.,.F.,.F.)
B_SPLINE_CURVE_WITH_KNOTS((3,3),(0.249954652430639,0.256253455718051),
 .UNSPECIFIED.)
CURVE()
GEOMETRIC_REPRESENTATION_ITEM()
RATIONAL_B_SPLINE_CURVE((1.11971735964598,1.12024119946945,1.1207154165842))
REPRESENTATION_ITEM('')
);
#1189=(
BOUNDED_CURVE()
B_SPLINE_CURVE(2,(#62453,#62454,#62455),.UNSPECIFIED.,.F.,.F.)
B_SPLINE_CURVE_WITH_KNOTS((3,3),(0.376641898803521,0.382940702095934),
 .UNSPECIFIED.)
CURVE()
GEOMETRIC_REPRESENTATION_ITEM()
RATIONAL_B_SPLINE_CURVE((1.12071541658441,1.12024119946928,1.11971735964536))
REPRESENTATION_ITEM('')
);
#1190=(
BOUNDED_CURVE()
B_SPLINE_CURVE(2,(#62459,#62460,#62461),.UNSPECIFIED.,.F.,.F.)
B_SPLINE_CURVE_WITH_KNOTS((3,3),(0.249954652430652,0.256253455718065),
 .UNSPECIFIED.)
CURVE()
GEOMETRIC_REPRESENTATION_ITEM()
RATIONAL_B_SPLINE_CURVE((1.11971735964616,1.12024119946962,1.12071541658438))
REPRESENTATION_ITEM('')
);
#1191=(
BOUNDED_CURVE()
B_SPLINE_CURVE(2,(#62465,#62466,#62467),.UNSPECIFIED.,.F.,.F.)
B_SPLINE_CURVE_WITH_KNOTS((3,3),(0.376641898803544,0.382940702095957),
 .UNSPECIFIED.)
CURVE()
GEOMETRIC_REPRESENTATION_ITEM()
RATIONAL_B_SPLINE_CURVE((1.12071541658424,1.1202411994691,1.11971735964518))
REPRESENTATION_ITEM('')
);
#1192=(
BOUNDED_CURVE()
B_SPLINE_CURVE(2,(#62471,#62472,#62473),.UNSPECIFIED.,.F.,.F.)
B_SPLINE_CURVE_WITH_KNOTS((3,3),(0.249954652430643,0.256253455718053),
 .UNSPECIFIED.)
CURVE()
GEOMETRIC_REPRESENTATION_ITEM()
RATIONAL_B_SPLINE_CURVE((1.11971735964601,1.12024119946947,1.12071541658423))
REPRESENTATION_ITEM('')
);
#1193=(
BOUNDED_CURVE()
B_SPLINE_CURVE(2,(#62477,#62478,#62479),.UNSPECIFIED.,.F.,.F.)
B_SPLINE_CURVE_WITH_KNOTS((3,3),(0.376641898803543,0.382940702095953),
 .UNSPECIFIED.)
CURVE()
GEOMETRIC_REPRESENTATION_ITEM()
RATIONAL_B_SPLINE_CURVE((1.12071541658425,1.12024119946911,1.1197173596452))
REPRESENTATION_ITEM('')
);
#1194=(
BOUNDED_CURVE()
B_SPLINE_CURVE(2,(#62483,#62484,#62485),.UNSPECIFIED.,.F.,.F.)
B_SPLINE_CURVE_WITH_KNOTS((3,3),(0.249954652430649,0.256253455718062),
 .UNSPECIFIED.)
CURVE()
GEOMETRIC_REPRESENTATION_ITEM()
RATIONAL_B_SPLINE_CURVE((1.11971735964607,1.12024119946954,1.12071541658429))
REPRESENTATION_ITEM('')
);
#2000=ELLIPSE('',#33648,0.0195162536838815,0.0137573643715162);
#2001=ELLIPSE('',#33649,0.0195162536830269,0.0137573643713391);
#2002=ELLIPSE('',#33651,0.0195162536835621,0.0137573643714695);
#2003=ELLIPSE('',#33652,0.019516253683001,0.0137573643713521);
#2004=ELLIPSE('',#33654,0.0195162536836977,0.0137573643714721);
#2005=ELLIPSE('',#33655,0.0195162536830636,0.0137573643713535);
#2006=ELLIPSE('',#33657,0.0195162536837443,0.0137573643714943);
#2007=ELLIPSE('',#33658,0.0195162536831223,0.0137573643713688);
#2008=ELLIPSE('',#33660,0.019516253683803,0.013757364371504);
#2009=ELLIPSE('',#33661,0.0195162536829111,0.0137573643713217);
#2010=ELLIPSE('',#33663,0.0195162536837688,0.0137573643714986);
#2011=ELLIPSE('',#33664,0.0195162536830749,0.0137573643713556);
#2012=ELLIPSE('',#33666,0.0195162536837257,0.0137573643714922);
#2013=ELLIPSE('',#33667,0.0195162536830703,0.0137573643713494);
#2014=ELLIPSE('',#33669,0.0195162536838104,0.013757364371505);
#2015=ELLIPSE('',#33670,0.0195162536830614,0.0137573643713493);
#2016=ELLIPSE('',#33672,0.0195162536837473,0.0137573643714877);
#2017=ELLIPSE('',#33673,0.0195162536830537,0.0137573643713548);
#2018=ELLIPSE('',#33675,0.0195162536838422,0.0137573643715182);
#2019=ELLIPSE('',#33676,0.0195162536831755,0.0137573643713807);
#2020=ELLIPSE('',#33678,0.0195162536837639,0.0137573643714952);
#2021=ELLIPSE('',#33679,0.0195162536830792,0.0137573643713542);
#2022=ELLIPSE('',#33681,0.0195162536835653,0.0137573643714501);
#2023=ELLIPSE('',#33682,0.0195162536831025,0.0137573643713567);
#2024=ELLIPSE('',#33684,0.0195162536835776,0.0137573643714587);
#2025=ELLIPSE('',#33685,0.0195162536828947,0.01375736437132);
#2026=ELLIPSE('',#33687,0.0195162536837483,0.0137573643714995);
#2027=ELLIPSE('',#33688,0.0195162536831204,0.0137573643713664);
#2028=ELLIPSE('',#33690,0.0195162536835793,0.0137573643714601);
#2029=ELLIPSE('',#33691,0.0195162536830448,0.0137573643713492);
#2030=ELLIPSE('',#33700,0.0195034997306777,0.013754915723726);
#2031=ELLIPSE('',#33702,0.0195030685020683,0.0137548403891227);
#2032=ELLIPSE('',#33704,0.0195027524929284,0.0137547851848027);
#2033=ELLIPSE('',#33706,0.0195025132809572,0.0137547433941177);
#2034=ELLIPSE('',#33708,0.0195023280193677,0.0137547110253133);
#2035=ELLIPSE('',#33710,0.0195021823053853,0.0137546855626127);
#2036=ELLIPSE('',#33712,0.0195020666474465,0.0137546653482711);
#2037=ELLIPSE('',#33714,0.0195019745733047,0.0137546492518586);
#2038=ELLIPSE('',#33716,0.0195019015620118,0.0137546364836367);
#2039=ELLIPSE('',#33718,0.0195018443987318,0.0137546264818649);
#2040=ELLIPSE('',#33720,0.0195018007910573,0.0137546188457545);
#2041=ELLIPSE('',#33722,0.0195017691158091,0.0137546132912077);
#2042=ELLIPSE('',#33724,0.0195017482624769,0.0137546096234092);
#2043=ELLIPSE('',#33726,0.0195017375337946,0.0137546077193674);
#2044=ELLIPSE('',#33728,0.0195017365885567,0.0137546075177427);
#2045=ELLIPSE('',#33730,0.0195017454175912,0.0137546090143427);
#2046=ELLIPSE('',#33732,0.0195017643506138,0.0137546122627749);
#2047=ELLIPSE('',#33734,0.0195017941005044,0.0137546173811011);
#2048=ELLIPSE('',#33736,0.0195018358641676,0.0137546245672221);
#2049=ELLIPSE('',#33738,0.0195018727625836,0.013754631431718);
#2050=ELLIPSE('',#33740,0.0195034997306828,0.0137549157237274);
#2051=ELLIPSE('',#33742,0.0195030685021256,0.0137548403891337);
#2052=ELLIPSE('',#33744,0.0195027524929019,0.0137547851847966);
#2053=ELLIPSE('',#33746,0.0195025132809425,0.0137547433941156);
#2054=ELLIPSE('',#33748,0.0195023280193708,0.0137547110253143);
#2055=ELLIPSE('',#33750,0.0195021823053841,0.0137546855626124);
#2056=ELLIPSE('',#33752,0.0195020666474398,0.0137546653482691);
#2057=ELLIPSE('',#33754,0.0195019745733335,0.0137546492518631);
#2058=ELLIPSE('',#33756,0.0195019015619959,0.0137546364836322);
#2059=ELLIPSE('',#33758,0.0195018443987879,0.0137546264818748);
#2060=ELLIPSE('',#33760,0.0195018007910457,0.0137546188457536);
#2061=ELLIPSE('',#33762,0.0195017691158159,0.0137546132912084);
#2062=ELLIPSE('',#33764,0.0195017482624727,0.013754609623408);
#2063=ELLIPSE('',#33766,0.0195017375337736,0.0137546077193644);
#2064=ELLIPSE('',#33768,0.0195017365885347,0.0137546075177382);
#2065=ELLIPSE('',#33770,0.019501745417596,0.0137546090143437);
#2066=ELLIPSE('',#33772,0.0195017643505816,0.0137546122627688);
#2067=ELLIPSE('',#33774,0.0195017941005605,0.0137546173811125);
#2068=ELLIPSE('',#33776,0.019501835864167,0.0137546245672222);
#2069=ELLIPSE('',#33778,0.0195162536830855,0.0137573643713537);
#2070=ELLIPSE('',#33780,0.0195034997307414,0.013754915723739);
#2071=ELLIPSE('',#33782,0.0195030685021161,0.0137548403891323);
#2072=ELLIPSE('',#33784,0.0195027524929008,0.0137547851847961);
#2073=ELLIPSE('',#33786,0.0195025132809546,0.0137547433941189);
#2074=ELLIPSE('',#33788,0.0195023280193482,0.0137547110253084);
#2075=ELLIPSE('',#33805,0.0195034997306463,0.0137549157237206);
#2076=ELLIPSE('',#33807,0.0195030685021557,0.0137548403891397);
#2077=ELLIPSE('',#33809,0.0195027524928776,0.0137547851847918);
#2078=ELLIPSE('',#33811,0.0195025132809776,0.0137547433941213);
#2079=ELLIPSE('',#33813,0.019502328019347,0.0137547110253081);
#2080=ELLIPSE('',#33815,0.0195021823053738,0.0137546855626116);
#2081=ELLIPSE('',#33817,0.0195020666474525,0.0137546653482711);
#2082=ELLIPSE('',#33819,0.0195019745733739,0.013754649251872);
#2083=ELLIPSE('',#33821,0.0195019015619764,0.0137546364836293);
#2084=ELLIPSE('',#33823,0.0195018443987816,0.0137546264818739);
#2085=ELLIPSE('',#33825,0.0195018007910337,0.0137546188457504);
#2086=ELLIPSE('',#33827,0.0195017691158341,0.0137546132912121);
#2087=ELLIPSE('',#33829,0.0195017482624509,0.0137546096234037);
#2088=ELLIPSE('',#33831,0.0195017375337853,0.0137546077193653);
#2089=ELLIPSE('',#33833,0.0195017365886309,0.0137546075177561);
#2090=ELLIPSE('',#33835,0.0195017454176055,0.0137546090143461);
#2091=ELLIPSE('',#33837,0.0195017643505986,0.0137546122627731);
#2092=ELLIPSE('',#33839,0.0195017941005311,0.0137546173811059);
#2093=ELLIPSE('',#33841,0.0195018358641241,0.0137546245672129);
#2094=ELLIPSE('',#33845,0.0195034997306858,0.0137549157237271);
#2095=ELLIPSE('',#33847,0.0195030685021635,0.0137548403891432);
#2096=ELLIPSE('',#33849,0.019502752492881,0.0137547851847926);
#2097=ELLIPSE('',#33851,0.0195025132809236,0.0137547433941134);
#2098=ELLIPSE('',#33853,0.0195023280193679,0.0137547110253125);
#2099=ELLIPSE('',#33855,0.0195021823054267,0.0137546855626225);
#2100=ELLIPSE('',#33857,0.0195020666474927,0.0137546653482813);
#2101=ELLIPSE('',#33859,0.019501974573308,0.0137546492518591);
#2102=ELLIPSE('',#33861,0.0195019015619601,0.0137546364836262);
#2103=ELLIPSE('',#33863,0.0195018443987825,0.0137546264818736);
#2104=ELLIPSE('',#33865,0.0195018007910841,0.0137546188457617);
#2105=ELLIPSE('',#33867,0.0195017691158046,0.0137546132912069);
#2106=ELLIPSE('',#33869,0.0195017482624746,0.0137546096234107);
#2107=ELLIPSE('',#33871,0.0195017375337627,0.0137546077193623);
#2108=ELLIPSE('',#33873,0.0195017365885639,0.0137546075177438);
#2109=ELLIPSE('',#33875,0.0195017454175912,0.0137546090143448);
#2110=ELLIPSE('',#33877,0.0195017643506125,0.0137546122627745);
#2111=ELLIPSE('',#33879,0.0195017941005712,0.0137546173811145);
#2112=ELLIPSE('',#33881,0.0195018358641553,0.013754624567221);
#2113=ELLIPSE('',#33883,0.0195018727626295,0.0137546314317287);
#2114=ELLIPSE('',#33885,0.0195034997307231,0.0137549157237351);
#2115=ELLIPSE('',#33887,0.0195030685021692,0.0137548403891432);
#2116=ELLIPSE('',#33889,0.0195027524928953,0.013754785184795);
#2117=ELLIPSE('',#33891,0.0195025132809505,0.0137547433941165);
#2118=ELLIPSE('',#33893,0.0195023280194302,0.0137547110253254);
#2119=ELLIPSE('',#33895,0.019502182305463,0.0137546855626286);
#2120=ELLIPSE('',#33897,0.0195020666474861,0.0137546653482797);
#2121=ELLIPSE('',#33899,0.0195019745732981,0.0137546492518571);
#2122=ELLIPSE('',#33901,0.019501901562003,0.0137546364836345);
#2123=ELLIPSE('',#33903,0.0195018443988218,0.0137546264818824);
#2124=ELLIPSE('',#33905,0.0195018007911448,0.0137546188457728);
#2125=ELLIPSE('',#33907,0.0195017691157916,0.0137546132912057);
#2126=ELLIPSE('',#33909,0.0195017482624564,0.013754609623407);
#2127=ELLIPSE('',#33911,0.0195017375338029,0.0137546077193704);
#2128=ELLIPSE('',#33913,0.0195017365886144,0.0137546075177533);
#2129=ELLIPSE('',#33915,0.0195017454176306,0.0137546090143512);
#2130=ELLIPSE('',#33917,0.0195017643505891,0.0137546122627708);
#2131=ELLIPSE('',#33919,0.0195017941005193,0.013754617381105);
#2132=ELLIPSE('',#33921,0.0195018358642213,0.0137546245672329);
#2133=ELLIPSE('',#33923,0.0195162536837232,0.0137573643714884);
#2134=ELLIPSE('',#33925,0.0195034997306679,0.0137549157237246);
#2135=ELLIPSE('',#33927,0.0195030685021047,0.0137548403891311);
#2136=ELLIPSE('',#33929,0.0195027524929266,0.0137547851848028);
#2137=ELLIPSE('',#33931,0.0195025132809874,0.0137547433941253);
#2138=ELLIPSE('',#33933,0.0195023280194086,0.013754711025321);
#2139=ELLIPSE('',#33935,0.0195021823054203,0.0137546855626212);
#2140=ELLIPSE('',#33937,0.0195020666475111,0.0137546653482846);
#2141=ELLIPSE('',#33939,0.0195019745733549,0.0137546492518684);
#2142=ELLIPSE('',#33941,0.0195019015619592,0.0137546364836273);
#2143=ELLIPSE('',#33943,0.0195018443988324,0.0137546264818843);
#2144=ELLIPSE('',#33945,0.0195018007910703,0.0137546188457585);
#2145=ELLIPSE('',#33947,0.0195017691158645,0.0137546132912193);
#2146=ELLIPSE('',#33949,0.0195017482624579,0.0137546096234066);
#2147=ELLIPSE('',#33951,0.0195017375338027,0.0137546077193706);
#2148=ELLIPSE('',#33953,0.0195017365886083,0.0137546075177516);
#2149=ELLIPSE('',#33955,0.019501745417535,0.0137546090143326);
#2150=ELLIPSE('',#33957,0.0195017643506093,0.0137546122627733);
#2151=ELLIPSE('',#33959,0.0195017941005168,0.013754617381103);
#2152=ELLIPSE('',#33961,0.0195018358640787,0.0137546245672056);
#2153=ELLIPSE('',#33978,0.0195017365886013,0.0137546075177502);
#2154=ELLIPSE('',#33980,0.0195017454175941,0.0137546090143434);
#2155=ELLIPSE('',#33982,0.0195017643505789,0.0137546122627681);
#2156=ELLIPSE('',#33984,0.0195017941005255,0.0137546173811058);
#2157=ELLIPSE('',#33986,0.0195018358641318,0.0137546245672154);
#2158=ELLIPSE('',#34002,0.051274964768551,0.0469971417993774);
#2159=ELLIPSE('',#34004,0.0512707788579671,0.0469842741354326);
#2160=ELLIPSE('',#34006,0.0512707788562332,0.0469842741344865);
#2161=ELLIPSE('',#34007,0.0512749647685533,0.0469971417993787);
#2162=ELLIPSE('',#34010,0.0512707788571307,0.0469842741349983);
#2163=ELLIPSE('',#34011,0.0512749647672664,0.0469971417987026);
#2164=ELLIPSE('',#34014,0.0512707788571389,0.0469842741349856);
#2165=ELLIPSE('',#34015,0.0512749647681367,0.0469971417991575);
#2166=ELLIPSE('',#34018,0.0512707788569124,0.0469842741348335);
#2167=ELLIPSE('',#34019,0.051274964768467,0.0469971417993732);
#2168=ELLIPSE('',#34022,0.051270778857559,0.0469842741351648);
#2169=ELLIPSE('',#34023,0.0512749647697504,0.0469971418000396);
#2170=ELLIPSE('',#34026,0.051270778857562,0.0469842741352078);
#2171=ELLIPSE('',#34027,0.0512749647676798,0.0469971417989218);
#2172=ELLIPSE('',#34030,0.0512707788610954,0.0469842741371193);
#2173=ELLIPSE('',#34031,0.0512749647674827,0.0469971417988075);
#2174=ELLIPSE('',#34034,0.0512707788555596,0.0469842741341208);
#2175=ELLIPSE('',#34035,0.0512749647677061,0.0469971417989105);
#2176=ELLIPSE('',#34038,0.0512707788650729,0.0469842741392919);
#2177=ELLIPSE('',#34039,0.0512749647702881,0.0469971418003199);
#2178=ELLIPSE('',#34042,0.0512707788560203,0.0469842741343728);
#2179=ELLIPSE('',#34043,0.0512749647689969,0.0469971417996401);
#2180=ELLIPSE('',#34046,0.0512707788567884,0.046984274134799);
#2181=ELLIPSE('',#34047,0.0512749647681247,0.0469971417991492);
#2182=ELLIPSE('',#34050,0.0512707788573083,0.0469842741350659);
#2183=ELLIPSE('',#34051,0.0512749647690658,0.0469971417996437);
#2184=ELLIPSE('',#34054,0.0512707788615306,0.046984274137359);
#2185=ELLIPSE('',#34055,0.051274964767619,0.0469971417988856);
#2186=ELLIPSE('',#34058,0.0512707788928482,0.0469842741544496);
#2187=ELLIPSE('',#34059,0.0512749647695684,0.0469971417999069);
#2188=ELLIPSE('',#34062,0.051270778857717,0.0469842741353091);
#2189=ELLIPSE('',#34063,0.0512749647683041,0.0469971417992544);
#2190=ELLIPSE('',#34066,0.051270778855901,0.046984274134278);
#2191=ELLIPSE('',#34067,0.0512749647692079,0.0469971417997307);
#2192=ELLIPSE('',#34070,0.0512707788585063,0.0469842741357279);
#2193=ELLIPSE('',#34071,0.0512749647681597,0.0469971417991513);
#2194=ELLIPSE('',#34074,0.0512707788568602,0.0469842741348085);
#2195=ELLIPSE('',#34075,0.0512749647674443,0.0469971417987893);
#2196=ELLIPSE('',#34078,0.0512707788568387,0.0469842741347804);
#2197=ELLIPSE('',#34079,0.0512749647678151,0.0469971417990189);
#2198=ELLIPSE('',#34082,0.0512707788582789,0.0469842741356006);
#2199=ELLIPSE('',#34083,0.05127496476906,0.0469971417996405);
#2200=ELLIPSE('',#34086,0.051270778856965,0.0469842741348763);
#2201=ELLIPSE('',#34087,0.0512749647686908,0.046997141799481);
#2202=ELLIPSE('',#34090,0.0512707788563555,0.0469842741344815);
#2203=ELLIPSE('',#34091,0.0512749647673275,0.0469971417987118);
#2204=ELLIPSE('',#34094,0.0512707788571547,0.0469842741350112);
#2205=ELLIPSE('',#34095,0.0512749647685426,0.046997141799397);
#2206=ELLIPSE('',#34098,0.0512707788556612,0.0469842741341707);
#2207=ELLIPSE('',#34099,0.0512749647699517,0.0469971418001559);
#2208=ELLIPSE('',#34102,0.0512707788576472,0.0469842741352346);
#2209=ELLIPSE('',#34103,0.0512749647672529,0.0469971417986806);
#2210=ELLIPSE('',#34106,0.0512707788618793,0.0469842741375491);
#2211=ELLIPSE('',#34107,0.0512749647679756,0.0469971417990623);
#2212=ELLIPSE('',#34110,0.0512707788555002,0.0469842741340957);
#2213=ELLIPSE('',#34111,0.0512749647688844,0.046997141799544);
#2214=ELLIPSE('',#34114,0.0512707788566344,0.0469842741346946);
#2215=ELLIPSE('',#34115,0.051274964769648,0.046997141799953);
#2216=ELLIPSE('',#34118,0.0512707788584597,0.0469842741356599);
#2217=ELLIPSE('',#34119,0.0512749647679757,0.0469971417990702);
#2218=ELLIPSE('',#34122,0.0512707788568172,0.0469842741347837);
#2219=ELLIPSE('',#34123,0.051274964767697,0.0469971417989173);
#2220=ELLIPSE('',#34126,0.0512707788670663,0.0469842741404324);
#2221=ELLIPSE('',#34127,0.0512749647689531,0.0469971417995761);
#2222=ELLIPSE('',#34130,0.0512707788557115,0.0469842741341769);
#2223=ELLIPSE('',#34131,0.0512749647694815,0.0469971417999415);
#2224=ELLIPSE('',#34134,0.0512707788568934,0.0469842741348491);
#2225=ELLIPSE('',#34135,0.0512749647661315,0.0469971417980767);
#2226=ELLIPSE('',#34138,0.0512707788572177,0.0469842741350563);
#2227=ELLIPSE('',#34139,0.0512749647680353,0.0469971417991282);
#2228=ELLIPSE('',#34142,0.0512707788587383,0.046984274135853);
#2229=ELLIPSE('',#34143,0.0512749647684727,0.0469971417993084);
#2230=ELLIPSE('',#34146,0.0512707788631157,0.0469842741382362);
#2231=ELLIPSE('',#34147,0.0512749647685272,0.0469971417993756);
#2232=ELLIPSE('',#34150,0.0512707788564907,0.0469842741346169);
#2233=ELLIPSE('',#34151,0.0512749647685682,0.0469971417994032);
#2234=ELLIPSE('',#34154,0.0512707788585969,0.0469842741357701);
#2235=ELLIPSE('',#34155,0.0512749647676235,0.0469971417988947);
#2236=ELLIPSE('',#34158,0.0512707788751318,0.0469842741447984);
#2237=ELLIPSE('',#34159,0.0512749647678178,0.0469971417990053);
#2238=ELLIPSE('',#34162,0.0512707788575899,0.0469842741352132);
#2239=ELLIPSE('',#34163,0.0512749647677413,0.0469971417989442);
#2240=ELLIPSE('',#34166,0.0512707788579549,0.0469842741354182);
#2241=ELLIPSE('',#34167,0.0512749647704146,0.0469971418003949);
#2242=ELLIPSE('',#34170,0.0512707788581164,0.0469842741355277);
#2243=ELLIPSE('',#34171,0.0512749647678976,0.0469971417990442);
#2244=ELLIPSE('',#34174,0.0512707788570414,0.0469842741348829);
#2245=ELLIPSE('',#34175,0.0512749647696248,0.0469971417999634);
#2246=ELLIPSE('',#34178,0.0512707789395351,0.0469842741799766);
#2247=ELLIPSE('',#34179,0.0512749647687745,0.0469971417995203);
#2248=ELLIPSE('',#34182,0.0512707788562593,0.0469842741344864);
#2249=ELLIPSE('',#34183,0.0512749647684955,0.046997141799316);
#2250=ELLIPSE('',#34186,0.0512707788603725,0.0469842741367327);
#2251=ELLIPSE('',#34187,0.0512749647690289,0.0469971417996681);
#2252=ELLIPSE('',#34190,0.0512707788577797,0.0469842741353011);
#2253=ELLIPSE('',#34191,0.0512749647683414,0.0469971417992803);
#2254=ELLIPSE('',#34194,0.051270778856875,0.0469842741348193);
#2255=ELLIPSE('',#34195,0.0512749647684586,0.0469971417993373);
#2256=ELLIPSE('',#34198,0.051270778920832,0.0469842741697548);
#2257=ELLIPSE('',#34199,0.0512749647689089,0.0469971417995588);
#2258=ELLIPSE('',#34202,0.0512707788568015,0.0469842741347871);
#2259=ELLIPSE('',#34203,0.0512749647679381,0.0469971417990666);
#2260=ELLIPSE('',#34206,0.0512707788566487,0.046984274134668);
#2261=ELLIPSE('',#34207,0.0512749647684683,0.0469971417993365);
#2262=ELLIPSE('',#34210,0.051270778856618,0.0469842741346731);
#2263=ELLIPSE('',#34211,0.0512749647693393,0.0469971417998184);
#2264=ELLIPSE('',#34214,0.0512707788568358,0.0469842741348282);
#2265=ELLIPSE('',#34215,0.0512749647674564,0.0469971417987839);
#2266=ELLIPSE('',#34218,0.0512707788557633,0.0469842741342339);
#2267=ELLIPSE('',#34219,0.0512749647690638,0.0469971417996539);
#2268=ELLIPSE('',#34222,0.0512707788566786,0.0469842741346996);
#2269=ELLIPSE('',#34223,0.0512749647672967,0.0469971417987006);
#2270=ELLIPSE('',#34226,0.0512707788621377,0.0469842741376985);
#2271=ELLIPSE('',#34227,0.0512749647686591,0.046997141799446);
#2272=ELLIPSE('',#34230,0.0512707788564809,0.0469842741346051);
#2273=ELLIPSE('',#34231,0.0512749647682497,0.0469971417992212);
#2274=ELLIPSE('',#34234,0.0512707788573564,0.0469842741350646);
#2275=ELLIPSE('',#34235,0.0512749647687658,0.0469971417994997);
#2276=ELLIPSE('',#34238,0.051270778874813,0.0469842741446368);
#2277=ELLIPSE('',#34239,0.0512749647675386,0.046997141798832);
#2278=ELLIPSE('',#34242,0.0512707788565269,0.0469842741346491);
#2279=ELLIPSE('',#34243,0.0512749647691996,0.0469971417997275);
#2280=ELLIPSE('',#34246,0.0512707788580797,0.0469842741354721);
#2281=ELLIPSE('',#34247,0.0512749647681002,0.0469971417991393);
#2282=ELLIPSE('',#34250,0.0512707788579047,0.0469842741354009);
#2283=ELLIPSE('',#34251,0.0512749647678865,0.0469971417990283);
#2284=ELLIPSE('',#34254,0.0512707788574115,0.046984274135125);
#2285=ELLIPSE('',#34255,0.0512749647671369,0.0469971417986091);
#2286=ELLIPSE('',#34258,0.0512749647690318,0.0469971417996552);
#2287=ELLIPSE('',#34260,0.0512707788566348,0.0469842741346708);
#2288=ELLIPSE('',#34262,0.0512749647679538,0.0469971417990534);
#2289=ELLIPSE('',#34264,0.0512707788562212,0.0469842741344524);
#2290=ELLIPSE('',#34266,0.051274964768521,0.0469971417993772);
#2291=ELLIPSE('',#34268,0.051270778856042,0.0469842741343731);
#2292=ELLIPSE('',#34270,0.0512749647675581,0.0469971417988677);
#2293=ELLIPSE('',#34272,0.0512707788559885,0.0469842741343514);
#2294=ELLIPSE('',#34274,0.0512749647693218,0.0469971417997968);
#2295=ELLIPSE('',#34276,0.0512707788571387,0.0469842741349643);
#2296=ELLIPSE('',#34278,0.0512749647679417,0.0469971417990759);
#2297=ELLIPSE('',#34280,0.0512707788922353,0.0469842741541131);
#2298=ELLIPSE('',#34282,0.051274964769059,0.046997141799664);
#2299=ELLIPSE('',#34284,0.0512707788612464,0.0469842741372165);
#2300=ELLIPSE('',#34286,0.0512749647686166,0.0469971417994078);
#2301=ELLIPSE('',#34288,0.0512707788558472,0.0469842741342397);
#2302=ELLIPSE('',#34290,0.0512749647686363,0.0469971417994427);
#2303=ELLIPSE('',#34292,0.0512707788567449,0.0469842741347651);
#2304=ELLIPSE('',#34294,0.0512749647684367,0.0469971417993216);
#2305=ELLIPSE('',#34296,0.0512707788561666,0.0469842741344253);
#2306=ELLIPSE('',#34298,0.0512749647683517,0.046997141799283);
#2307=ELLIPSE('',#34300,0.0512707788648064,0.0469842741391505);
#2308=ELLIPSE('',#34302,0.0512749647688174,0.0469971417995523);
#2309=ELLIPSE('',#34304,0.051270778857567,0.0469842741352074);
#2310=ELLIPSE('',#34306,0.0512749647694904,0.0469971417998601);
#2311=ELLIPSE('',#34308,0.0512707788575527,0.0469842741351904);
#2312=ELLIPSE('',#34310,0.0512749647677225,0.0469971417989513);
#2313=ELLIPSE('',#34312,0.0512707788585909,0.0469842741357571);
#2314=ELLIPSE('',#34314,0.051270778940575,0.0469842741805314);
#2315=ELLIPSE('',#34315,0.0512749647683344,0.0469971417992899);
#2316=ELLIPSE('',#34476,0.0512707788678624,0.04698427414088);
#2317=ELLIPSE('',#34477,0.0512749647679163,0.0469971417991227);
#2318=ELLIPSE('',#34479,0.0512749647654335,0.0469971417977818);
#2319=ELLIPSE('',#34480,0.0512707788568347,0.0469842741348514);
#2320=ELLIPSE('',#34482,0.0512749647672852,0.0469971417988039);
#2321=ELLIPSE('',#34483,0.0512707788564686,0.0469842741346539);
#2322=ELLIPSE('',#34485,0.0512749647659393,0.0469971417980464);
#2323=ELLIPSE('',#34486,0.0512707788556944,0.0469842741342504);
#2324=ELLIPSE('',#34488,0.0512749647686629,0.0469971417995544);
#2325=ELLIPSE('',#34489,0.0512707788564297,0.0469842741346479);
#2326=ELLIPSE('',#34491,0.0512749647671486,0.0469971417987065);
#2327=ELLIPSE('',#34492,0.0512707788597197,0.0469842741364453);
#2328=ELLIPSE('',#34494,0.0512749647666077,0.0469971417984174);
#2329=ELLIPSE('',#34495,0.0512707788555701,0.0469842741341628);
#2330=ELLIPSE('',#34497,0.0512749647679515,0.0469971417991682);
#2331=ELLIPSE('',#34498,0.0512707788587403,0.0469842741359266);
#2332=ELLIPSE('',#34500,0.0512749647675462,0.0469971417988912);
#2333=ELLIPSE('',#34501,0.0512707788561996,0.0469842741345216);
#2334=ELLIPSE('',#34503,0.0512749647665171,0.0469971417983294);
#2335=ELLIPSE('',#34504,0.0512707788563593,0.0469842741346364);
#2336=ELLIPSE('',#34506,0.0512749647671419,0.0469971417986936);
#2337=ELLIPSE('',#34507,0.0512707788554834,0.0469842741341348);
#2338=ELLIPSE('',#34509,0.0512749647679126,0.0469971417991247);
#2339=ELLIPSE('',#34510,0.0512707788566136,0.0469842741347507);
#2340=ELLIPSE('',#34512,0.051274964765861,0.0469971417980122);
#2341=ELLIPSE('',#34513,0.0512707788569887,0.0469842741349521);
#2342=ELLIPSE('',#34515,0.0512749647673257,0.046997141798794);
#2343=ELLIPSE('',#34516,0.0512707788578384,0.0469842741354011);
#2344=ELLIPSE('',#34518,0.0512749647685051,0.046997141799409);
#2345=ELLIPSE('',#34519,0.0512707788566497,0.0469842741347448);
#2346=ELLIPSE('',#34521,0.0512749647664023,0.0469971417983194);
#2347=ELLIPSE('',#34522,0.0512707788557973,0.0469842741343033);
#2348=ELLIPSE('',#34524,0.0512749647657081,0.0469971417979273);
#2349=ELLIPSE('',#34525,0.0512707788560454,0.0469842741344356);
#2350=ELLIPSE('',#34527,0.0512749647672847,0.0469971417988018);
#2351=ELLIPSE('',#34528,0.0512707788908472,0.0469842741534398);
#2352=ELLIPSE('',#34530,0.0512749647656979,0.0469971417979225);
#2353=ELLIPSE('',#34531,0.0512707788619598,0.0469842741376821);
#2354=ELLIPSE('',#34533,0.0512749647673844,0.0469971417987892);
#2355=ELLIPSE('',#34534,0.0512707788554361,0.0469842741341347);
#2356=ELLIPSE('',#34536,0.0512749647665351,0.0469971417983737);
#2357=ELLIPSE('',#34537,0.051270778857401,0.0469842741351899);
#2358=ELLIPSE('',#34539,0.0512749647648224,0.0469971417974593);
#2359=ELLIPSE('',#34540,0.051270778857135,0.0469842741350546);
#2360=ELLIPSE('',#34542,0.051274964767923,0.046997141799147);
#2361=ELLIPSE('',#34543,0.0512707788632245,0.0469842741383353);
#2362=ELLIPSE('',#34545,0.0512749647670837,0.0469971417986601);
#2363=ELLIPSE('',#34546,0.0512707788575274,0.0469842741352789);
#2364=ELLIPSE('',#34548,0.0512749647661063,0.046997141798163);
#2365=ELLIPSE('',#34549,0.0512707788614728,0.0469842741374068);
#2366=ELLIPSE('',#34551,0.0512749647661745,0.0469971417981727);
#2367=ELLIPSE('',#34552,0.0512707788561374,0.0469842741344828);
#2368=ELLIPSE('',#34554,0.0512749647684627,0.0469971417993818);
#2369=ELLIPSE('',#34555,0.0512707788547222,0.0469842741337518);
#2370=ELLIPSE('',#34557,0.0512749647675423,0.0469971417989238);
#2371=ELLIPSE('',#34558,0.0512707788556497,0.0469842741342235);
#2372=ELLIPSE('',#34560,0.0512749647674664,0.0469971417988657);
#2373=ELLIPSE('',#34561,0.0512707788563694,0.0469842741346094);
#2374=ELLIPSE('',#34563,0.0512749647689012,0.0469971417996608);
#2375=ELLIPSE('',#34564,0.0512707788554915,0.0469842741341037);
#2376=ELLIPSE('',#34566,0.0512749647674053,0.0469971417988339);
#2377=ELLIPSE('',#34567,0.0512707788551391,0.0469842741339346);
#2378=ELLIPSE('',#34569,0.051274964767584,0.046997141798928);
#2379=ELLIPSE('',#34570,0.0512707788578603,0.0469842741354062);
#2380=ELLIPSE('',#34572,0.0512749647667973,0.046997141798492);
#2381=ELLIPSE('',#34573,0.0512707788554342,0.0469842741340614);
#2382=ELLIPSE('',#34575,0.0512749647663277,0.0469971417982546);
#2383=ELLIPSE('',#34576,0.051270778856014,0.0469842741344105);
#2384=ELLIPSE('',#34578,0.0512749647644558,0.0469971417972658);
#2385=ELLIPSE('',#34579,0.051270778856549,0.046984274134693);
#2386=ELLIPSE('',#34581,0.0512749647655728,0.0469971417978321);
#2387=ELLIPSE('',#34582,0.0512707788565064,0.0469842741346634);
#2388=ELLIPSE('',#34584,0.0512749647677657,0.0469971417990299);
#2389=ELLIPSE('',#34585,0.0512707788566898,0.0469842741347819);
#2390=ELLIPSE('',#34587,0.0512749647676116,0.0469971417989766);
#2391=ELLIPSE('',#34588,0.0512707788912617,0.0469842741536714);
#2392=ELLIPSE('',#34590,0.0512749647664018,0.0469971417982991);
#2393=ELLIPSE('',#34591,0.0512707788616718,0.0469842741375278);
#2394=ELLIPSE('',#34593,0.0512749647667201,0.046997141798501);
#2395=ELLIPSE('',#34594,0.0512707788559321,0.046984274134359);
#2396=ELLIPSE('',#34596,0.0512749647688712,0.0469971417996063);
#2397=ELLIPSE('',#34597,0.0512707788570311,0.0469842741349509);
#2398=ELLIPSE('',#34599,0.0512749647675863,0.0469971417989162);
#2399=ELLIPSE('',#34600,0.0512707788563448,0.0469842741345939);
#2400=ELLIPSE('',#34602,0.0512749647671262,0.0469971417987068);
#2401=ELLIPSE('',#34603,0.0512707788650867,0.0469842741393638);
#2402=ELLIPSE('',#34605,0.0512749647686962,0.0469971417995509);
#2403=ELLIPSE('',#34606,0.0512707788567886,0.0469842741348241);
#2404=ELLIPSE('',#34608,0.0512749647672976,0.0469971417987731);
#2405=ELLIPSE('',#34609,0.0512707788570162,0.0469842741349496);
#2406=ELLIPSE('',#34611,0.0512749647667697,0.0469971417984931);
#2407=ELLIPSE('',#34612,0.0512707788584097,0.0469842741357168);
#2408=ELLIPSE('',#34614,0.0512749647672832,0.0469971417987584);
#2409=ELLIPSE('',#34615,0.0512707788570115,0.0469842741349691);
#2410=ELLIPSE('',#34617,0.0512749647672073,0.0469971417987249);
#2411=ELLIPSE('',#34618,0.0512707789405328,0.0469842741805533);
#2412=ELLIPSE('',#34620,0.0512749647662809,0.0469971417982346);
#2413=ELLIPSE('',#34621,0.0512707788564733,0.0469842741346687);
#2414=ELLIPSE('',#34623,0.0512749647659994,0.0469971417980507);
#2415=ELLIPSE('',#34624,0.0512707788571204,0.0469842741349872);
#2416=ELLIPSE('',#34626,0.0512749647671319,0.0469971417987083);
#2417=ELLIPSE('',#34627,0.0512707788566097,0.0469842741347329);
#2418=ELLIPSE('',#34629,0.0512749647668497,0.0469971417985515);
#2419=ELLIPSE('',#34630,0.0512707788560048,0.0469842741344256);
#2420=ELLIPSE('',#34632,0.051274964765999,0.0469971417980718);
#2421=ELLIPSE('',#34633,0.0512707788746663,0.0469842741446355);
#2422=ELLIPSE('',#34635,0.0512749647672519,0.0469971417987563);
#2423=ELLIPSE('',#34636,0.051270778855846,0.0469842741343271);
#2424=ELLIPSE('',#34638,0.0512749647662359,0.0469971417982146);
#2425=ELLIPSE('',#34639,0.0512707788574978,0.0469842741352291);
#2426=ELLIPSE('',#34641,0.0512749647668179,0.0469971417985263);
#2427=ELLIPSE('',#34642,0.0512707788607044,0.0469842741369976);
#2428=ELLIPSE('',#34644,0.0512749647674441,0.0469971417988379);
#2429=ELLIPSE('',#34645,0.0512707788568965,0.0469842741348871);
#2430=ELLIPSE('',#34647,0.0512749647672645,0.0469971417987703);
#2431=ELLIPSE('',#34648,0.0512707788559945,0.0469842741344026);
#2432=ELLIPSE('',#34650,0.0512749647680151,0.0469971417991764);
#2433=ELLIPSE('',#34651,0.0512707788560419,0.04698427413443);
#2434=ELLIPSE('',#34653,0.0512749647667931,0.0469971417984966);
#2435=ELLIPSE('',#34654,0.0512707788563537,0.0469842741346079);
#2436=ELLIPSE('',#34656,0.0512749647674696,0.0469971417988977);
#2437=ELLIPSE('',#34657,0.0512707788571896,0.0469842741350665);
#2438=ELLIPSE('',#34659,0.0512749647673948,0.046997141798837);
#2439=ELLIPSE('',#34660,0.0512707788555549,0.0469842741341569);
#2440=ELLIPSE('',#34662,0.0512749647668783,0.0469971417985539);
#2441=ELLIPSE('',#34663,0.0512707789210852,0.0469842741699459);
#2442=ELLIPSE('',#34665,0.0512749647677305,0.0469971417990099);
#2443=ELLIPSE('',#34666,0.0512707788552415,0.0469842741340032);
#2444=ELLIPSE('',#34668,0.0512707788564181,0.0469842741346374);
#2445=ELLIPSE('',#34669,0.0512749647669761,0.0469971417985938);
#2446=ELLIPSE('',#34671,0.051270778856969,0.0469842741349151);
#2447=ELLIPSE('',#34672,0.0512749647670935,0.046997141798684);
#2448=ELLIPSE('',#34674,0.0512707788562384,0.0469842741345515);
#2449=ELLIPSE('',#34675,0.0512749647675247,0.0469971417988957);
#2450=ELLIPSE('',#34677,0.0512707788573216,0.0469842741351317);
#2451=ELLIPSE('',#34678,0.0512749647668487,0.046997141798569);
#2452=ELLIPSE('',#34680,0.0512707788622439,0.0469842741378278);
#2453=ELLIPSE('',#34681,0.0512749647677751,0.0469971417990674);
#2454=ELLIPSE('',#34683,0.0512707788576837,0.046984274135325);
#2455=ELLIPSE('',#34684,0.0512749647668911,0.0469971417985504);
#2456=ELLIPSE('',#34686,0.0512707788569353,0.0469842741349273);
#2457=ELLIPSE('',#34687,0.0512749647675315,0.0469971417989158);
#2458=ELLIPSE('',#34689,0.0512707788759282,0.0469842741452617);
#2459=ELLIPSE('',#34690,0.0512749647661136,0.0469971417981488);
#2460=ELLIPSE('',#34692,0.0512707788557471,0.0469842741342912);
#2461=ELLIPSE('',#34693,0.051274964767063,0.0469971417986624);
#2462=ELLIPSE('',#34695,0.0512707788562218,0.0469842741345251);
#2463=ELLIPSE('',#34696,0.0512749647674796,0.0469971417988927);
#2464=ELLIPSE('',#34698,0.0512707788562634,0.0469842741345331);
#2465=ELLIPSE('',#34699,0.0512749647672643,0.0469971417987429);
#2466=ELLIPSE('',#34701,0.0512707788550995,0.0469842741339394);
#2467=ELLIPSE('',#34702,0.0512749647667936,0.0469971417984887);
#2468=ELLIPSE('',#34704,0.0512707789393949,0.0469842741799506);
#2469=ELLIPSE('',#34705,0.0512749647666032,0.0469971417983921);
#2470=ELLIPSE('',#34707,0.0512707788579345,0.0469842741354427);
#2471=ELLIPSE('',#34708,0.0512749647659267,0.0469971417980537);
#2472=ELLIPSE('',#34710,0.0512749647694732,0.0469971417999488);
#2473=ELLIPSE('',#34711,0.0512707788565522,0.0469842741347113);
#2474=ELLIPSE('',#34715,0.0512707788554107,0.0469842741340208);
#2475=ELLIPSE('',#34716,0.0512749647674929,0.0469971417988238);
#2476=ELLIPSE('',#34721,0.0512749647664458,0.0469971417983288);
#2477=ELLIPSE('',#34722,0.0512707788586759,0.0469842741358754);
#2962=CONICAL_SURFACE('',#33608,1.17524047358084,0.785398163397443);
#2963=CONICAL_SURFACE('',#33643,1.17524047358084,0.785398163397443);
#2964=CONICAL_SURFACE('',#33692,1.55162884844711,0.78539816339745);
#2965=CONICAL_SURFACE('',#33698,2.73627063036812,0.785398163397448);
#2966=CONICAL_SURFACE('',#33843,2.68872936963188,0.785398163397435);
#2967=CONICAL_SURFACE('',#34731,1732.05080756885,1.04719755119659);
#3100=B_SPLINE_CURVE_WITH_KNOTS('',3,(#55937,#55938,#55939,#55940,#55941,
#55942,#55943,#55944,#55945,#55946,#55947,#55948,#55949,#55950,#55951,#55952,
#55953,#55954,#55955,#55956,#55957,#55958,#55959,#55960,#55961,#55962,#55963,
#55964,#55965,#55966,#55967,#55968,#55969,#55970,#55971,#55972),
 .UNSPECIFIED.,.F.,.F.,(4,2,2,2,2,2,2,2,2,2,2,2,2,2,2,2,2,4),(-0.945073641183675,
-0.895238035194944,-0.83625541046657,-0.779319325111488,-0.719695813140934,
-0.661359932358853,-0.603989382535731,-0.544046656752618,-0.486380595229568,
-0.427463950957105,-0.368285170516134,-0.311258814957492,-0.251615042406746,
-0.193080680180277,-0.135881569867343,-0.0757214675349668,-0.0372079607299379,
-9.99999995143774E-7),.UNSPECIFIED.);
#3101=B_SPLINE_CURVE_WITH_KNOTS('',3,(#55978,#55979,#55980,#55981,#55982,
#55983,#55984,#55985,#55986,#55987,#55988,#55989,#55990,#55991,#55992,#55993,
#55994,#55995,#55996,#55997,#55998,#55999,#56000,#56001,#56002,#56003,#56004,
#56005,#56006,#56007,#56008,#56009,#56010,#56011),.UNSPECIFIED.,.F.,.F.,
(4,2,2,2,2,2,2,2,2,2,2,2,2,2,2,2,4),(-27.258759550315,-27.2281298462553,
-27.1982051538512,-27.1403355656588,-27.0801605899845,-27.0231066733285,
-26.9645639497272,-26.9050010855415,-26.8479917157334,-26.7888070303952,
-26.7302213719406,-26.6725610910419,-26.6126177738291,-26.5554428144319,
-26.4971129260297,-26.4375855046171,-26.4315188069733),.UNSPECIFIED.);
#3102=B_SPLINE_CURVE_WITH_KNOTS('',3,(#56016,#56017,#56018,#56019,#56020,
#56021,#56022,#56023,#56024,#56025,#56026,#56027,#56028,#56029,#56030,#56031,
#56032,#56033,#56034,#56035,#56036,#56037,#56038,#56039,#56040,#56041,#56042,
#56043,#56044,#56045,#56046,#56047,#56048,#56049,#56050,#56051),
 .UNSPECIFIED.,.F.,.F.,(4,2,2,2,2,2,2,2,2,2,2,2,2,2,2,2,2,4),(-1.89025095676006,
-1.83161362612537,-1.77291723413503,-1.71588088128378,-1.65621305093223,
-1.59816806724067,-1.54019307596245,-1.48057902624682,-1.42320721251111,
-1.36315245228605,-1.30433237640506,-1.24738924893859,-1.18775702178512,
-1.12958586526634,-1.07195013380193,-1.0121910944455,-0.954689933605391,
-0.945073641183675),.UNSPECIFIED.);
#3103=B_SPLINE_CURVE_WITH_KNOTS('',3,(#56052,#56053,#56054,#56055,#56056,
#56057,#56058,#56059,#56060,#56061,#56062,#56063,#56064,#56065,#56066,#56067,
#56068,#56069,#56070,#56071,#56072,#56073,#56074,#56075,#56076,#56077,#56078,
#56079,#56080,#56081,#56082,#56083,#56084,#56085,#56086,#56087),
 .UNSPECIFIED.,.F.,.F.,(4,2,2,2,2,2,2,2,2,2,2,2,2,2,2,2,2,4),(-26.4315188069733,
-26.3807149169946,-26.3217404209326,-26.2626652889544,-26.2051855221022,
-26.1454428390691,-26.08804784233,-26.0298996832198,-25.970377539516,-25.9135472636022,
-25.8547523829465,-25.7951046336945,-25.7377721236726,-25.6781939173096,
-25.6204935481626,-25.5624909627037,-25.5029463840743,-25.4881909358829),
 .UNSPECIFIED.);
#3104=B_SPLINE_CURVE_WITH_KNOTS('',3,(#56092,#56093,#56094,#56095,#56096,
#56097,#56098,#56099,#56100,#56101,#56102,#56103,#56104,#56105,#56106,#56107,
#56108,#56109,#56110,#56111,#56112,#56113,#56114,#56115,#56116,#56117,#56118,
#56119,#56120,#56121,#56122,#56123,#56124,#56125,#56126,#56127,#56128,#56129),
 .UNSPECIFIED.,.F.,.F.,(4,2,2,2,2,2,2,2,2,2,2,2,2,2,2,2,2,2,4),(-2.83625896355377,
-2.82853093222041,-2.76886611006394,-2.71046756100465,-2.65308502383756,
-2.59307616772703,-2.5353480705631,-2.47645222776391,-2.41720668492958,
-2.36012338869581,-2.30043449435393,-2.24183347940531,-2.1846099393252,
-2.12437972037366,-2.06645193254166,-2.00798057621261,-1.94850769470731,
-1.89126109663031,-1.89025095676006),.UNSPECIFIED.);
#3105=B_SPLINE_CURVE_WITH_KNOTS('',3,(#56130,#56131,#56132,#56133,#56134,
#56135,#56136,#56137,#56138,#56139,#56140,#56141,#56142,#56143,#56144,#56145,
#56146,#56147,#56148,#56149,#56150,#56151,#56152,#56153,#56154,#56155,#56156,
#56157,#56158,#56159,#56160,#56161,#56162,#56163,#56164,#56165),
 .UNSPECIFIED.,.F.,.F.,(4,2,2,2,2,2,2,2,2,2,2,2,2,2,2,2,2,4),(-25.4881909358829,
-25.4460636732589,-25.3874120918811,-25.3278816537184,-25.2706841301686,
-25.2112575632321,-25.1531186176646,-25.0952452143788,-25.0350644348795,
-24.9780430196917,-24.9194961959997,-24.8599520194551,-24.8029424006809,
-24.7437542679059,-24.6852489172368,-24.6275880933991,-24.5676424609794,
-24.544394043377),.UNSPECIFIED.);
#3106=B_SPLINE_CURVE_WITH_KNOTS('',3,(#56170,#56171,#56172,#56173,#56174,
#56175,#56176,#56177,#56178,#56179,#56180,#56181,#56182,#56183,#56184,#56185,
#56186,#56187,#56188,#56189,#56190,#56191,#56192,#56193,#56194,#56195,#56196,
#56197,#56198,#56199,#56200,#56201,#56202,#56203,#56204,#56205),
 .UNSPECIFIED.,.F.,.F.,(4,2,2,2,2,2,2,2,2,2,2,2,2,2,2,2,2,4),(-3.78192035948685,
-3.76562796298537,-3.70592564973338,-3.6478278361799,-3.5898592957152,-3.53018901929876,
-3.47276427223133,-3.41274694188657,-3.3538687217505,-3.29689298752725,
-3.2372230084892,-3.17899386626536,-3.12135698149028,-3.06153650613278,
-3.00397762776562,-2.94455692608413,-2.88551146939021,-2.83625896355377),
 .UNSPECIFIED.);
#3107=B_SPLINE_CURVE_WITH_KNOTS('',3,(#56206,#56207,#56208,#56209,#56210,
#56211,#56212,#56213,#56214,#56215,#56216,#56217,#56218,#56219,#56220,#56221,
#56222,#56223,#56224,#56225,#56226,#56227,#56228,#56229,#56230,#56231,#56232,
#56233,#56234,#56235,#56236,#56237,#56238,#56239,#56240,#56241),
 .UNSPECIFIED.,.F.,.F.,(4,2,2,2,2,2,2,2,2,2,2,2,2,2,2,2,2,4),(-24.544394043377,
-24.5105131978097,-24.4521827141638,-24.3926780124691,-24.3358195936076,
-24.2768451471733,-24.2178632708879,-24.1603868788961,-24.1006461200198,
-24.0433090290329,-23.9851645307063,-23.9256688814307,-23.8688632830925,
-23.8100726156683,-23.7505272749807,-23.6932025949219,-23.6336311604901,
-23.6014349735858),.UNSPECIFIED.);
#3108=B_SPLINE_CURVE_WITH_KNOTS('',3,(#56246,#56247,#56248,#56249,#56250,
#56251,#56252,#56253,#56254,#56255,#56256,#56257,#56258,#56259,#56260,#56261,
#56262,#56263,#56264,#56265,#56266,#56267,#56268,#56269,#56270,#56271,#56272,
#56273,#56274,#56275,#56276,#56277,#56278,#56279,#56280,#56281),
 .UNSPECIFIED.,.F.,.F.,(4,2,2,2,2,2,2,2,2,2,2,2,2,2,2,2,2,4),(-4.72839430207058,
-4.70337431740566,-4.64331595464347,-4.58554178921411,-4.52667966073054,
-4.4673838894256,-4.41025831032806,-4.35054027250619,-4.29188896156004,
-4.23465469260147,-4.17437122548907,-4.11639389057874,-4.05794278357937,
-3.99841660337735,-3.94111979450562,-3.88143640467257,-3.82268708479341,
-3.78192035948685),.UNSPECIFIED.);
#3109=B_SPLINE_CURVE_WITH_KNOTS('',3,(#56282,#56283,#56284,#56285,#56286,
#56287,#56288,#56289,#56290,#56291,#56292,#56293,#56294,#56295,#56296,#56297,
#56298,#56299,#56300,#56301,#56302,#56303,#56304,#56305,#56306,#56307,#56308,
#56309,#56310,#56311,#56312,#56313,#56314,#56315,#56316,#56317),
 .UNSPECIFIED.,.F.,.F.,(4,2,2,2,2,2,2,2,2,2,2,2,2,2,2,2,2,4),(-23.6014349735858,
-23.5759985868542,-23.5180045036599,-23.458489879113,-23.4016430359386,
-23.3430005479742,-23.2834982736845,-23.226310920464,-23.166893628097,-23.1088378874003,
-23.0509758826866,-22.9908049952875,-22.9338319947597,-22.8752964277514,
-22.8157879004539,-22.7587920199088,-22.6996160282244,-22.6581171675807),
 .UNSPECIFIED.);
#3110=B_SPLINE_CURVE_WITH_KNOTS('',3,(#56322,#56323,#56324,#56325,#56326,
#56327,#56328,#56329,#56330,#56331,#56332,#56333,#56334,#56335,#56336,#56337,
#56338,#56339,#56340,#56341,#56342,#56343,#56344,#56345,#56346,#56347,#56348,
#56349,#56350,#56351,#56352,#56353,#56354,#56355,#56356,#56357),
 .UNSPECIFIED.,.F.,.F.,(4,2,2,2,2,2,2,2,2,2,2,2,2,2,2,2,2,4),(-5.67439159596968,
-5.64047766140835,-5.58076721688331,-5.52330498546526,-5.4633387313466,
-5.40441833910885,-5.34742402529794,-5.28773207490788,-5.22946075409439,
-5.17183622553644,-5.11197061930769,-5.05436969869878,-4.99499338073396,
-4.9359013779351,-4.878890651626,-4.8192004273671,-4.76075532631967,-4.72839430207058),
 .UNSPECIFIED.);
#3111=B_SPLINE_CURVE_WITH_KNOTS('',3,(#56358,#56359,#56360,#56361,#56362,
#56363,#56364,#56365,#56366,#56367,#56368,#56369,#56370,#56371,#56372,#56373,
#56374,#56375,#56376,#56377,#56378,#56379,#56380,#56381,#56382,#56383,#56384,
#56385,#56386,#56387,#56388,#56389,#56390,#56391,#56392,#56393),
 .UNSPECIFIED.,.F.,.F.,(4,2,2,2,2,2,2,2,2,2,2,2,2,2,2,2,2,4),(-22.6581171675807,
-22.6412102410835,-22.5835641689142,-22.5236319902899,-22.4665652482388,
-22.4082496043878,-22.3487848861067,-22.2919531828174,-22.2329943725634,
-22.1741263229248,-22.1166686457465,-22.0569456248039,-21.9996842855768,
-21.9415589369491,-21.8821072544915,-21.8253417468782,-21.7665709936596,
-21.7157628302399),.UNSPECIFIED.);
#3112=B_SPLINE_CURVE_WITH_KNOTS('',3,(#56398,#56399,#56400,#56401,#56402,
#56403,#56404,#56405,#56406,#56407,#56408,#56409,#56410,#56411,#56412,#56413,
#56414,#56415,#56416,#56417,#56418,#56419,#56420,#56421,#56422,#56423,#56424,
#56425,#56426,#56427,#56428,#56429,#56430,#56431,#56432,#56433),
 .UNSPECIFIED.,.F.,.F.,(4,2,2,2,2,2,2,2,2,2,2,2,2,2,2,2,2,4),(-6.62109380521341,
-6.57761768259959,-6.51828740763027,-6.46113362202641,-6.40140207096381,
-6.34271600715298,-6.28548482095171,-6.22516410228413,-6.16715260360109,
-6.10873547077658,-6.04917186097877,-5.99184011673613,-5.93213648107799,
-5.8733499659965,-5.81628212661826,-5.75656105013342,-5.69842598086126,
-5.67439159596968),.UNSPECIFIED.);
#3113=B_SPLINE_CURVE_WITH_KNOTS('',3,(#56434,#56435,#56436,#56437,#56438,
#56439,#56440,#56441,#56442,#56443,#56444,#56445,#56446,#56447,#56448,#56449,
#56450,#56451,#56452,#56453,#56454,#56455,#56456,#56457,#56458,#56459,#56460,
#56461,#56462,#56463,#56464,#56465,#56466,#56467,#56468,#56469),
 .UNSPECIFIED.,.F.,.F.,(4,2,2,2,2,2,2,2,2,2,2,2,2,2,2,2,2,4),(-21.7157628302399,
-21.7071499734112,-21.6498486291818,-21.5902999589255,-21.5327541629797,
-21.4747842600729,-21.4153173211779,-21.3585227590009,-21.2999052492263,
-21.2398720875173,-21.1826905454483,-21.1232764692568,-21.065378520901,
-21.0075245508875,-20.9480158554619,-20.8911101904613,-20.8326059984683,
-20.7731793950157),.UNSPECIFIED.);
#3114=B_SPLINE_CURVE_WITH_KNOTS('',3,(#56474,#56475,#56476,#56477,#56478,
#56479,#56480,#56481,#56482,#56483,#56484,#56485,#56486,#56487,#56488,#56489,
#56490,#56491,#56492,#56493,#56494,#56495,#56496,#56497,#56498,#56499,#56500,
#56501,#56502,#56503,#56504,#56505,#56506,#56507,#56508,#56509),
 .UNSPECIFIED.,.F.,.F.,(4,2,2,2,2,2,2,2,2,2,2,2,2,2,2,2,2,4),(-7.56721318319246,
-7.51440195941646,-7.4554548070908,-7.39845589958658,-7.33875763160917,
-7.28045937419718,-7.22286133868259,-7.16296628560166,-7.10533842940707,
-7.04602095897405,-6.9868979771895,-6.92987099130527,-6.87017100691209,
-6.81169474396116,-6.75432913502786,-6.69423710481114,-6.63643211656935,
-6.62109380521341),.UNSPECIFIED.);
#3115=B_SPLINE_CURVE_WITH_KNOTS('',3,(#56510,#56511,#56512,#56513,#56514,
#56515,#56516,#56517,#56518,#56519,#56520,#56521,#56522,#56523,#56524,#56525,
#56526,#56527,#56528,#56529,#56530,#56531,#56532,#56533,#56534,#56535,#56536,
#56537,#56538,#56539,#56540,#56541,#56542,#56543,#56544,#56545,#56546,#56547),
 .UNSPECIFIED.,.F.,.F.,(4,2,2,2,2,2,2,2,2,2,2,2,2,2,2,2,2,2,4),(-20.7731793950157,
-20.7731201315055,-20.7160582025871,-20.6567792566783,-20.5983599289237,
-20.5406164839802,-20.4805811221967,-20.4234656784966,-20.3650514109911,
-20.305511597516,-20.2485949896086,-20.1895371334662,-20.1306696919239,
-20.0731189832228,-20.0132974755221,-19.9560008596223,-19.8977815738613,
-19.8382589546996,-19.8295444030046),.UNSPECIFIED.);
#3116=B_SPLINE_CURVE_WITH_KNOTS('',3,(#56552,#56553,#56554,#56555,#56556,
#56557,#56558,#56559,#56560,#56561,#56562,#56563,#56564,#56565,#56566,#56567,
#56568,#56569,#56570,#56571,#56572,#56573,#56574,#56575,#56576,#56577,#56578,
#56579,#56580,#56581,#56582,#56583,#56584,#56585,#56586,#56587,#56588,#56589),
 .UNSPECIFIED.,.F.,.F.,(4,2,2,2,2,2,2,2,2,2,2,2,2,2,2,2,2,2,4),(-8.51391269073544,
-8.51222365838152,-8.45249428513948,-8.39378861667143,-8.33657472393003,
-8.27623231073072,-8.21820164401039,-8.1598332741766,-8.10024765479814,
-8.04289584139225,-7.98318755401621,-7.92437912604881,-7.86731677437594,
-7.80759259896721,-7.74943539170332,-7.6915218402897,-7.631786775557,-7.57430204194946,
-7.56721318319246),.UNSPECIFIED.);
#3117=B_SPLINE_CURVE_WITH_KNOTS('',3,(#56590,#56591,#56592,#56593,#56594,
#56595,#56596,#56597,#56598,#56599,#56600,#56601,#56602,#56603,#56604,#56605,
#56606,#56607,#56608,#56609,#56610,#56611,#56612,#56613,#56614,#56615,#56616,
#56617,#56618,#56619,#56620,#56621,#56622,#56623,#56624,#56625),
 .UNSPECIFIED.,.F.,.F.,(4,2,2,2,2,2,2,2,2,2,2,2,2,2,2,2,2,4),(-19.8295444030046,
-19.781422440649,-19.7225572817117,-19.6631471763022,-19.6057577545878,
-19.5461159927651,-19.4885461013889,-19.4304876297435,-19.3709535721035,
-19.3141007093386,-19.2553941827952,-19.1953773792029,-19.1381132548424,
-19.0786120692882,-19.0206974716804,-18.9627608300149,-18.9031885891784,
-18.8860416189937),.UNSPECIFIED.);
#3118=B_SPLINE_CURVE_WITH_KNOTS('',3,(#56630,#56631,#56632,#56633,#56634,
#56635,#56636,#56637,#56638,#56639,#56640,#56641,#56642,#56643,#56644,#56645,
#56646,#56647,#56648,#56649,#56650,#56651,#56652,#56653,#56654,#56655,#56656,
#56657,#56658,#56659,#56660,#56661,#56662,#56663,#56664,#56665),
 .UNSPECIFIED.,.F.,.F.,(4,2,2,2,2,2,2,2,2,2,2,2,2,2,2,2,2,4),(-9.4600020867739,
-9.44946097484441,-9.38977226427863,-9.3314620836995,-9.27390543364871,
-9.21399634460654,-9.15635642704838,-9.09711384600216,-9.03797514352587,
-8.98094579786149,-8.92125183936447,-8.86275948675276,-8.8054237975235,
-8.7453135764027,-8.68749269541132,-8.62874128051507,-8.56939184171518,
-8.51391269073544),.UNSPECIFIED.);
#3119=B_SPLINE_CURVE_WITH_KNOTS('',3,(#56666,#56667,#56668,#56669,#56670,
#56671,#56672,#56673,#56674,#56675,#56676,#56677,#56678,#56679,#56680,#56681,
#56682,#56683,#56684,#56685,#56686,#56687,#56688,#56689,#56690,#56691,#56692,
#56693,#56694,#56695,#56696,#56697,#56698,#56699,#56700,#56701),
 .UNSPECIFIED.,.F.,.F.,(4,2,2,2,2,2,2,2,2,2,2,2,2,2,2,2,2,4),(-18.8860416189937,
-18.8462348900712,-18.7876476548069,-18.7280968440835,-18.6709555484027,
-18.6115929558287,-18.5531716016611,-18.495349324202,-18.4352301709226,
-18.3780798368063,-18.319585679885,-18.2599881331103,-18.2030028878512,
-18.1438648978918,-18.0850090800984,-18.0273834680497,-17.9674824112817,
-17.941522876477),.UNSPECIFIED.);
#3120=B_SPLINE_CURVE_WITH_KNOTS('',3,(#56706,#56707,#56708,#56709,#56710,
#56711,#56712,#56713,#56714,#56715,#56716,#56717,#56718,#56719,#56720,#56721,
#56722,#56723,#56724,#56725,#56726,#56727,#56728,#56729,#56730,#56731,#56732,
#56733,#56734,#56735,#56736,#56737,#56738,#56739,#56740,#56741),
 .UNSPECIFIED.,.F.,.F.,(4,2,2,2,2,2,2,2,2,2,2,2,2,2,2,2,2,4),(-10.4063262286273,
-10.387392591544,-10.3270439303512,-10.2690090232558,-10.210705562305,-10.1511132343272,
-10.09375612853,-10.034059046947,-9.97524386932148,-9.91820163035005,-9.8584903134111,
-9.80032595747233,-9.74246277833438,-9.68271846928724,-9.62522607647149,
-9.56540900336133,-9.50645028314585,-9.4600020867739),.UNSPECIFIED.);
#3121=B_SPLINE_CURVE_WITH_KNOTS('',3,(#56742,#56743,#56744,#56745,#56746,
#56747,#56748,#56749,#56750,#56751,#56752,#56753,#56754,#56755,#56756,#56757,
#56758,#56759,#56760,#56761,#56762,#56763,#56764,#56765,#56766,#56767,#56768,
#56769,#56770,#56771,#56772,#56773,#56774,#56775,#56776,#56777),
 .UNSPECIFIED.,.F.,.F.,(4,2,2,2,2,2,2,2,2,2,2,2,2,2,2,2,2,4),(-17.941522876477,
-17.9101636562757,-17.8518687182981,-17.7922922877475,-17.7354001068821,
-17.6764590004862,-17.6170707989498,-17.5596109797981,-17.4998945731994,
-17.4423134048219,-17.3841841685699,-17.3245998970605,-17.2677034424408,
-17.2089258668494,-17.1489368038417,-17.0916073172332,-17.0320369692312,
-16.997272415308),.UNSPECIFIED.);
#3122=B_SPLINE_CURVE_WITH_KNOTS('',3,(#56782,#56783,#56784,#56785,#56786,
#56787,#56788,#56789,#56790,#56791,#56792,#56793,#56794,#56795,#56796,#56797,
#56798,#56799,#56800,#56801,#56802,#56803,#56804,#56805,#56806,#56807,#56808,
#56809,#56810,#56811,#56812,#56813,#56814,#56815,#56816,#56817),
 .UNSPECIFIED.,.F.,.F.,(4,2,2,2,2,2,2,2,2,2,2,2,2,2,2,2,2,4),(-11.3522871924595,
-11.324430394275,-11.264522730746,-11.2068857092522,-11.1477360236872,-11.08859687367,
-11.0315792760543,-10.9719076335357,-10.9134142640608,-10.8561239489264,
-10.796010976838,-10.7381891351563,-10.6795177406942,-10.620164420077,-10.5629956093436,
-10.5032845165816,-10.4445743180876,-10.4063262286273),.UNSPECIFIED.);
#3123=B_SPLINE_CURVE_WITH_KNOTS('',3,(#56818,#56819,#56820,#56821,#56822,
#56823,#56824,#56825,#56826,#56827,#56828,#56829,#56830,#56831,#56832,#56833,
#56834,#56835,#56836,#56837,#56838,#56839,#56840,#56841,#56842,#56843,#56844,
#56845,#56846,#56847,#56848,#56849,#56850,#56851,#56852,#56853),
 .UNSPECIFIED.,.F.,.F.,(4,2,2,2,2,2,2,2,2,2,2,2,2,2,2,2,2,4),(-16.997272415308,
-16.974118579872,-16.9161165902415,-16.8564975009602,-16.7995101512218,
-16.7408573501075,-16.6812582779792,-16.6240545216982,-16.5646258893359,
-16.5062147666311,-16.448330624569,-16.388145391231,-16.3309738020301,-16.2724169024022,
-16.2127779950283,-16.155739296564,-16.0965384948368,-16.052121842989),
 .UNSPECIFIED.);
#3124=B_SPLINE_CURVE_WITH_KNOTS('',3,(#56858,#56859,#56860,#56861,#56862,
#56863,#56864,#56865,#56866,#56867,#56868,#56869,#56870,#56871,#56872,#56873,
#56874,#56875,#56876,#56877,#56878,#56879,#56880,#56881,#56882,#56883,#56884,
#56885,#56886,#56887,#56888,#56889,#56890,#56891,#56892,#56893),
 .UNSPECIFIED.,.F.,.F.,(4,2,2,2,2,2,2,2,2,2,2,2,2,2,2,2,2,4),(-12.2980151684053,
-12.2608049534251,-12.2012214180354,-12.1438740189948,-12.0842046319712,
-12.0253980696236,-11.9683912868138,-11.9087094544592,-11.8505531273409,
-11.7927573534416,-11.7330193273245,-11.6755342944868,-11.6158192576419,
-11.5568642629696,-11.4998992163216,-11.4402365277277,-11.3819295252021,
-11.3522871924595),.UNSPECIFIED.);
#3125=B_SPLINE_CURVE_WITH_KNOTS('',3,(#56894,#56895,#56896,#56897,#56898,
#56899,#56900,#56901,#56902,#56903,#56904,#56905,#56906,#56907,#56908,#56909,
#56910,#56911,#56912,#56913,#56914,#56915,#56916,#56917,#56918,#56919,#56920,
#56921,#56922,#56923,#56924,#56925,#56926,#56927,#56928,#56929),
 .UNSPECIFIED.,.F.,.F.,(4,2,2,2,2,2,2,2,2,2,2,2,2,2,2,2,2,4),(-16.052121842989,
-16.0377063442003,-15.9800225041649,-15.9200592855784,-15.8627316418797,
-15.8043778785959,-15.7447638720137,-15.6878306019307,-15.6288305455336,
-15.5694764347843,-15.5119625793001,-15.452188569769,-15.3946092699113,
-15.3364257590099,-15.2768073817686,-15.2198815508401,-15.1610495793805,
-15.1073443691545),.UNSPECIFIED.);
#3126=B_SPLINE_CURVE_WITH_KNOTS('',3,(#56934,#56935,#56936,#56937,#56938,
#56939,#56940,#56941,#56942,#56943,#56944,#56945,#56946,#56947,#56948,#56949,
#56950,#56951,#56952,#56953,#56954,#56955,#56956,#56957,#56958,#56959,#56960,
#56961,#56962,#56963,#56964,#56965,#56966,#56967,#56968,#56969),
 .UNSPECIFIED.,.F.,.F.,(4,2,2,2,2,2,2,2,2,2,2,2,2,2,2,2,2,4),(-13.2436220538442,
-13.1973293402993,-13.1382053560805,-13.0812140676331,-13.0215819437106,
-12.9631029490451,-12.905874761448,-12.8457747640532,-12.787967213325,-12.7293949980337,
-12.670053341907,-12.6128978517491,-12.5532219431716,-12.494522530246,-12.4373888207658,
-12.3770495663262,-12.3190255916381,-12.2980151684053),.UNSPECIFIED.);
#3127=B_SPLINE_CURVE_WITH_KNOTS('',3,(#56970,#56971,#56972,#56973,#56974,
#56975,#56976,#56977,#56978,#56979,#56980,#56981,#56982,#56983,#56984,#56985,
#56986,#56987,#56988,#56989,#56990,#56991,#56992,#56993,#56994,#56995,#56996,
#56997,#56998,#56999,#57000,#57001,#57002,#57003,#57004,#57005,#57006,#57007),
 .UNSPECIFIED.,.F.,.F.,(4,2,2,2,2,2,2,2,2,2,2,2,2,2,2,2,2,2,4),(-15.1073443691545,
-15.1011008892937,-15.0437220848592,-14.9840992717133,-14.926190394778,
-14.8681392181562,-14.8084892686686,-14.7514823595925,-14.6927803091387,
-14.6331489331619,-14.5758985339276,-14.5164203125443,-14.4580324516964,
-14.4001023522461,-14.339867608388,-14.2826884114687,-14.2240848432797,
-14.1644203791933,-14.161791521072),.UNSPECIFIED.);
#3128=B_SPLINE_CURVE_WITH_KNOTS('',3,(#57012,#57013,#57014,#57015,#57016,
#57017,#57018,#57019,#57020,#57021,#57022,#57023,#57024,#57025,#57026,#57027,
#57028,#57029,#57030,#57031,#57032,#57033,#57034,#57035,#57036,#57037,#57038,
#57039,#57040,#57041,#57042,#57043,#57044,#57045,#57046,#57047),
 .UNSPECIFIED.,.F.,.F.,(4,2,2,2,2,2,2,2,2,2,2,2,2,2,2,2,2,4),(-14.1885859699234,
-14.1330844909293,-14.0738030834317,-14.0151322001193,-13.9573780431577,
-13.8973369154889,-13.8400747014035,-13.781649842778,-13.7220284098382,
-13.6650669338426,-13.6061313895152,-13.5492060305576,-13.4895868440872,
-13.4312985326842,-13.3738747554208,-13.3139843572995,-13.2563655957482,
-13.2436220538442),.UNSPECIFIED.);
#3129=B_SPLINE_CURVE_WITH_KNOTS('',3,(#57048,#57049,#57050,#57051,#57052,
#57053,#57054,#57055,#57056,#57057,#57058,#57059,#57060,#57061,#57062,#57063,
#57064,#57065,#57066,#57067,#57068,#57069,#57070,#57071,#57072,#57073,#57074,
#57075,#57076,#57077,#57078,#57079,#57080,#57081,#57082,#57083),
 .UNSPECIFIED.,.F.,.F.,(4,2,2,2,2,2,2,2,2,2,2,2,2,2,2,2,2,4),(-14.161791521072,
-14.1073426685626,-14.0480953063394,-13.9892999039839,-13.9315735440484,
-13.8715645099561,-13.8142414960538,-13.7558447627025,-13.6962089327002,
-13.6392486779599,-13.5802573437773,-13.5233108369954,-13.4636758610349,
-13.4053314288153,-13.3479464458854,-13.2879951425265,-13.2303206406094,
-13.2166062380566),.UNSPECIFIED.);
#3130=B_SPLINE_CURVE_WITH_KNOTS('',3,(#57088,#57089,#57090,#57091,#57092,
#57093,#57094,#57095,#57096,#57097,#57098,#57099,#57100,#57101,#57102,#57103,
#57104,#57105,#57106,#57107,#57108,#57109,#57110,#57111,#57112,#57113,#57114,
#57115,#57116,#57117,#57118,#57119,#57120,#57121,#57122,#57123,#57124,#57125),
 .UNSPECIFIED.,.F.,.F.,(4,2,2,2,2,2,2,2,2,2,2,2,2,2,2,2,2,2,4),(-15.1341561055544,
-15.1269994338561,-15.0695799723091,-15.0099125340775,-14.9520739190766,
-14.8939828445778,-14.8343297519005,-14.7773366004228,-14.7185951213641,
-14.6589576423824,-14.6016713251844,-14.5421535644632,-14.4838629359255,
-14.4258987192761,-14.3656251166082,-14.3084824988271,-14.2498440170218,
-14.1901865832963,-14.1885859699234),.UNSPECIFIED.);
#3131=B_SPLINE_CURVE_WITH_KNOTS('',3,(#57126,#57127,#57128,#57129,#57130,
#57131,#57132,#57133,#57134,#57135,#57136,#57137,#57138,#57139,#57140,#57141,
#57142,#57143,#57144,#57145,#57146,#57147,#57148,#57149,#57150,#57151,#57152,
#57153,#57154,#57155,#57156,#57157,#57158,#57159,#57160,#57161),
 .UNSPECIFIED.,.F.,.F.,(4,2,2,2,2,2,2,2,2,2,2,2,2,2,2,2,2,4),(-13.2166062380566,
-13.1713851979337,-13.1121981319385,-13.0551628296182,-12.9955080421381,
-12.9369655576865,-12.8797535453401,-12.819585289645,-12.761715189623,-12.7032194250943,
-12.6438086463492,-12.586620577358,-12.5270150261763,-12.4683803900242,
-12.4113696886299,-12.35174219741,-12.2937588655423,-12.2712695292436),
 .UNSPECIFIED.);
#3132=B_SPLINE_CURVE_WITH_KNOTS('',3,(#57166,#57167,#57168,#57169,#57170,
#57171,#57172,#57173,#57174,#57175,#57176,#57177,#57178,#57179,#57180,#57181,
#57182,#57183,#57184,#57185,#57186,#57187,#57188,#57189,#57190,#57191,#57192,
#57193,#57194,#57195,#57196,#57197,#57198,#57199,#57200,#57201),
 .UNSPECIFIED.,.F.,.F.,(4,2,2,2,2,2,2,2,2,2,2,2,2,2,2,2,2,4),(-16.0791645683298,
-16.0637629880179,-16.0060223350212,-15.9459969234656,-15.8887024341941,
-15.8302912537239,-15.7706612508563,-15.7136999051047,-15.654642811055,
-15.5954057874932,-15.5378426704977,-15.4780146687669,-15.4204898319656,
-15.3622571133794,-15.3026293793744,-15.2456979578477,-15.1868171504776,
-15.1341561055544),.UNSPECIFIED.);
#3133=B_SPLINE_CURVE_WITH_KNOTS('',3,(#57202,#57203,#57204,#57205,#57206,
#57207,#57208,#57209,#57210,#57211,#57212,#57213,#57214,#57215,#57216,#57217,
#57218,#57219,#57220,#57221,#57222,#57223,#57224,#57225,#57226,#57227,#57228,
#57229,#57230,#57231,#57232,#57233,#57234,#57235,#57236,#57237),
 .UNSPECIFIED.,.F.,.F.,(4,2,2,2,2,2,2,2,2,2,2,2,2,2,2,2,2,4),(-12.2712695292436,
-12.2357754508004,-12.1762270533728,-12.1189170680661,-12.0588176303639,
-12.0000655464483,-11.943159299172,-11.8835712422689,-11.8254678956475,
-11.7678321870858,-11.708145031833,-11.6507114242844,-11.5912213696332,
-11.5323122460786,-11.4754266605439,-11.4158513420701,-11.3575887654668,
-11.3269908932583),.UNSPECIFIED.);
#3134=B_SPLINE_CURVE_WITH_KNOTS('',3,(#57242,#57243,#57244,#57245,#57246,
#57247,#57248,#57249,#57250,#57251,#57252,#57253,#57254,#57255,#57256,#57257,
#57258,#57259,#57260,#57261,#57262,#57263,#57264,#57265,#57266,#57267,#57268,
#57269,#57270,#57271,#57272,#57273,#57274,#57275,#57276,#57277),
 .UNSPECIFIED.,.F.,.F.,(4,2,2,2,2,2,2,2,2,2,2,2,2,2,2,2,2,4),(-17.0247741151702,
-17.0006922494049,-16.942620899042,-16.8829683888398,-16.8259674619989,
-16.7672454552544,-16.7076101234707,-16.6503415003102,-16.590843286514,
-16.5325014804607,-16.4745540351945,-16.4142996421448,-16.357137434069,
-16.2985161360182,-16.2388539992256,-16.1817640975146,-16.1224994016558,
-16.0791645683298),.UNSPECIFIED.);
#3135=B_SPLINE_CURVE_WITH_KNOTS('',3,(#57278,#57279,#57280,#57281,#57282,
#57283,#57284,#57285,#57286,#57287,#57288,#57289,#57290,#57291,#57292,#57293,
#57294,#57295,#57296,#57297,#57298,#57299,#57300,#57301,#57302,#57303,#57304,
#57305,#57306,#57307,#57308,#57309,#57310,#57311,#57312,#57313),
 .UNSPECIFIED.,.F.,.F.,(4,2,2,2,2,2,2,2,2,2,2,2,2,2,2,2,2,4),(-11.3269908932583,
-11.3002304831747,-11.2403651502537,-11.1827717007332,-11.1238285355636,
-11.064728011521,-11.0077668972893,-10.9481757635054,-10.8897195155163,
-10.8325471683827,-10.7724692707686,-10.7146842840278,-10.6561946025542,
-10.5968740051404,-10.5397395269343,-10.4801014814801,-10.4214223488875,
-10.3822526002173),.UNSPECIFIED.);
#3136=B_SPLINE_CURVE_WITH_KNOTS('',3,(#57318,#57319,#57320,#57321,#57322,
#57323,#57324,#57325,#57326,#57327,#57328,#57329,#57330,#57331,#57332,#57333,
#57334,#57335,#57336,#57337,#57338,#57339,#57340,#57341,#57342,#57343,#57344,
#57345,#57346,#57347,#57348,#57349,#57350,#57351,#57352,#57353),
 .UNSPECIFIED.,.F.,.F.,(4,2,2,2,2,2,2,2,2,2,2,2,2,2,2,2,2,4),(-17.9696970255303,
-17.937289370862,-17.8789069021961,-17.8192841522869,-17.7623368372575,
-17.7033082433986,-17.6440100001385,-17.5864714106887,-17.526670356869,
-17.4691167328281,-17.4109085209012,-17.3512845924667,-17.2943555190345,
-17.2354990142404,-17.1756126480208,-17.1182132969445,-17.0585679978772,
-17.0247741151702),.UNSPECIFIED.);
#3137=B_SPLINE_CURVE_WITH_KNOTS('',3,(#57354,#57355,#57356,#57357,#57358,
#57359,#57360,#57361,#57362,#57363,#57364,#57365,#57366,#57367,#57368,#57369,
#57370,#57371,#57372,#57373,#57374,#57375,#57376,#57377,#57378,#57379,#57380,
#57381,#57382,#57383,#57384,#57385,#57386,#57387,#57388,#57389),
 .UNSPECIFIED.,.F.,.F.,(4,2,2,2,2,2,2,2,2,2,2,2,2,2,2,2,2,4),(-10.3822526002173,
-10.3643343540307,-10.3046400968479,-10.246613334744,-10.1885181147052,
-10.128927402479,-10.0715754084394,-10.011325400927,-9.9525347708931,-9.89556195447909,
-9.83591091083034,-9.77776999750488,-9.72003077893023,-9.66030722303232,
-9.60283704872725,-9.54320316116386,-9.48426076178981,-9.43689892858011),
 .UNSPECIFIED.);
#3138=B_SPLINE_CURVE_WITH_KNOTS('',3,(#57394,#57395,#57396,#57397,#57398,
#57399,#57400,#57401,#57402,#57403,#57404,#57405,#57406,#57407,#57408,#57409,
#57410,#57411,#57412,#57413,#57414,#57415,#57416,#57417,#57418,#57419,#57420,
#57421,#57422,#57423,#57424,#57425,#57426,#57427,#57428,#57429),
 .UNSPECIFIED.,.F.,.F.,(4,2,2,2,2,2,2,2,2,2,2,2,2,2,2,2,2,4),(-18.9151145034862,
-18.8743164654268,-18.8156291548377,-18.7560115648048,-18.6987754493173,
-18.6393121439161,-18.5809341256596,-18.5230183981635,-18.4627987144582,
-18.4056311968295,-18.3470421802252,-18.2873910545073,-18.2303271150055,
-18.171094421965,-18.1123080260466,-18.0545957689432,-17.9946015046478,
-17.9696970255303),.UNSPECIFIED.);
#3139=B_SPLINE_CURVE_WITH_KNOTS('',3,(#57430,#57431,#57432,#57433,#57434,
#57435,#57436,#57437,#57438,#57439,#57440,#57441,#57442,#57443,#57444,#57445,
#57446,#57447,#57448,#57449,#57450,#57451,#57452,#57453,#57454,#57455,#57456,
#57457,#57458,#57459,#57460,#57461,#57462,#57463,#57464,#57465),
 .UNSPECIFIED.,.F.,.F.,(4,2,2,2,2,2,2,2,2,2,2,2,2,2,2,2,2,4),(-9.43689892858011,
-9.42732171849391,-9.36768738295302,-9.30939248028644,-9.25194272911408,
-9.19204622378449,-9.13442101602013,-9.07534568068709,-9.01621630273034,
-8.95921594082851,-8.89957004368503,-8.84108593111714,-8.78383634874988,
-8.72373170856049,-8.6659190669351,-8.60731272480359,-8.54796686813959,
-8.49156038630827),.UNSPECIFIED.);
#3140=B_SPLINE_CURVE_WITH_KNOTS('',3,(#57470,#57471,#57472,#57473,#57474,
#57475,#57476,#57477,#57478,#57479,#57480,#57481,#57482,#57483,#57484,#57485,
#57486,#57487,#57488,#57489,#57490,#57491,#57492,#57493,#57494,#57495,#57496,
#57497,#57498,#57499,#57500,#57501,#57502,#57503,#57504,#57505),
 .UNSPECIFIED.,.F.,.F.,(4,2,2,2,2,2,2,2,2,2,2,2,2,2,2,2,2,4),(-19.8597382210236,
-19.810451373043,-19.7514667566491,-19.6921219719675,-19.6346229403372,
-19.5748644342208,-19.5172962645061,-19.4591277252691,-19.3995232496075,
-19.3426105099162,-19.2837936446735,-19.2238539608265,-19.1664896413472,
-19.1068819617647,-19.0489837573588,-18.9909471893313,-18.9313109305834,
-18.9151145034862),.UNSPECIFIED.);
#3141=B_SPLINE_CURVE_WITH_KNOTS('',3,(#57506,#57507,#57508,#57509,#57510,
#57511,#57512,#57513,#57514,#57515,#57516,#57517,#57518,#57519,#57520,#57521,
#57522,#57523,#57524,#57525,#57526,#57527,#57528,#57529,#57530,#57531,#57532,
#57533,#57534,#57535,#57536,#57537,#57538,#57539,#57540,#57541,#57542,#57543),
 .UNSPECIFIED.,.F.,.F.,(4,2,2,2,2,2,2,2,2,2,2,2,2,2,2,2,2,2,4),(-8.49156038630827,
-8.49080675575303,-8.43111857134256,-8.37241526446117,-8.31526501763932,
-8.25492233706489,-8.19689441801019,-8.13864530142174,-8.07905854481672,
-8.02170761683104,-7.96202852596394,-7.9032187975688,-7.84619976450985,
-7.78650760972943,-7.72834831916545,-7.67052935317836,-7.61078895216033,
-7.55330118212272,-7.54539583975842),.UNSPECIFIED.);
#3142=B_SPLINE_CURVE_WITH_KNOTS('',3,(#57548,#57549,#57550,#57551,#57552,
#57553,#57554,#57555,#57556,#57557,#57558,#57559,#57560,#57561,#57562,#57563,
#57564,#57565,#57566,#57567,#57568,#57569,#57570,#57571,#57572,#57573,#57574,
#57575,#57576,#57577,#57578,#57579,#57580,#57581,#57582,#57583,#57584,#57585),
 .UNSPECIFIED.,.F.,.F.,(4,2,2,2,2,2,2,2,2,2,2,2,2,2,2,2,2,2,4),(-20.8047268284554,
-20.8036363389145,-20.7464479008663,-20.6870352594353,-20.6286348915891,
-20.5707661629285,-20.510597073108,-20.4534380889162,-20.3948967931479,
-20.3352722771837,-20.2782483009287,-20.219063232801,-20.1602410153004,
-20.1025723093681,-20.0426249323872,-19.9853090960203,-19.9269706384341,
-19.867370764855,-19.8597382210236),.UNSPECIFIED.);
#3143=B_SPLINE_CURVE_WITH_KNOTS('',3,(#57586,#57587,#57588,#57589,#57590,
#57591,#57592,#57593,#57594,#57595,#57596,#57597,#57598,#57599,#57600,#57601,
#57602,#57603,#57604,#57605,#57606,#57607,#57608,#57609,#57610,#57611,#57612,
#57613,#57614,#57615,#57616,#57617,#57618,#57619,#57620,#57621),
 .UNSPECIFIED.,.F.,.F.,(4,2,2,2,2,2,2,2,2,2,2,2,2,2,2,2,2,4),(-7.54539583975842,
-7.49355110204946,-7.43459460077228,-7.37762115395009,-7.31794932817515,
-7.25964100917192,-7.20212210603924,-7.14221371611197,-7.08457547245393,
-7.02539392871746,-6.96625468515904,-6.90923296876007,-6.84955345859718,
-6.79106019408235,-6.73375428080265,-6.6736419972573,-6.61582024058893,
-6.59962043014718),.UNSPECIFIED.);
#3144=B_SPLINE_CURVE_WITH_KNOTS('',3,(#57626,#57627,#57628,#57629,#57630,
#57631,#57632,#57633,#57634,#57635,#57636,#57637,#57638,#57639,#57640,#57641,
#57642,#57643,#57644,#57645,#57646,#57647,#57648,#57649,#57650,#57651,#57652,
#57653,#57654,#57655,#57656,#57657,#57658,#57659,#57660,#57661),
 .UNSPECIFIED.,.F.,.F.,(4,2,2,2,2,2,2,2,2,2,2,2,2,2,2,2,2,4),(-21.7489046572791,
-21.7392153866495,-21.6817714549229,-21.6220716583751,-21.5645025223573,
-21.5063893301253,-21.4468200256293,-21.3899376073178,-21.3311762213552,
-21.2711970668162,-21.2138831121422,-21.1543289862749,-21.0964221879644,
-21.0384358621701,-20.9788315240901,-20.9218575630073,-20.8632205676017,
-20.8047268284554),.UNSPECIFIED.);
#3145=B_SPLINE_CURVE_WITH_KNOTS('',3,(#57662,#57663,#57664,#57665,#57666,
#57667,#57668,#57669,#57670,#57671,#57672,#57673,#57674,#57675,#57676,#57677,
#57678,#57679,#57680,#57681,#57682,#57683,#57684,#57685,#57686,#57687,#57688,
#57689,#57690,#57691,#57692,#57693,#57694,#57695,#57696,#57697),
 .UNSPECIFIED.,.F.,.F.,(4,2,2,2,2,2,2,2,2,2,2,2,2,2,2,2,2,4),(-6.59962043014718,
-6.55712143056447,-6.49776917806976,-6.44060046014423,-6.3808828825634,
-6.32217397813377,-6.26498116754636,-6.20463437850135,-6.14660066752985,
-6.0882749718812,-6.02868466855325,-5.9713291133043,-5.91162795849117,-5.85281481524407,
-5.79576557777481,-5.73604961995392,-5.67788743624381,-5.65305968192749),
 .UNSPECIFIED.);
#3146=B_SPLINE_CURVE_WITH_KNOTS('',3,(#57702,#57703,#57704,#57705,#57706,
#57707,#57708,#57709,#57710,#57711,#57712,#57713,#57714,#57715,#57716,#57717,
#57718,#57719,#57720,#57721,#57722,#57723,#57724,#57725,#57726,#57727,#57728,
#57729,#57730,#57731,#57732,#57733,#57734,#57735,#57736,#57737),
 .UNSPECIFIED.,.F.,.F.,(4,2,2,2,2,2,2,2,2,2,2,2,2,2,2,2,2,4),(-22.6930944862137,
-22.6750742815793,-22.6172685137948,-22.5571666469156,-22.5000298336195,
-22.4415523883347,-22.3819703093803,-22.3250007752965,-22.2658796385637,
-22.2070346049225,-22.1494252073759,-22.0895411174023,-22.0322350703383,
-21.9739565284333,-21.9143953015877,-21.8575179583935,-21.7985933937003,
-21.7489046572791),.UNSPECIFIED.);
#3147=B_SPLINE_CURVE_WITH_KNOTS('',3,(#57738,#57739,#57740,#57741,#57742,
#57743,#57744,#57745,#57746,#57747,#57748,#57749,#57750,#57751,#57752,#57753,
#57754,#57755,#57756,#57757,#57758,#57759,#57760,#57761,#57762,#57763,#57764,
#57765,#57766,#57767,#57768,#57769,#57770,#57771,#57772,#57773),
 .UNSPECIFIED.,.F.,.F.,(4,2,2,2,2,2,2,2,2,2,2,2,2,2,2,2,2,4),(-5.65305968192749,
-5.62000697109407,-5.56026553634326,-5.50277548740805,-5.4429300395589,
-5.38397497750277,-5.32698226097639,-5.2672900308627,-5.20898363219345,
-5.15141280935565,-5.09150820934248,-5.03387211917237,-4.97460397585247,
-4.91547032791341,-4.8584416373336,-4.79874535977046,-4.74025819094778,
-4.7070192889843),.UNSPECIFIED.);
#3148=B_SPLINE_CURVE_WITH_KNOTS('',3,(#57778,#57779,#57780,#57781,#57782,
#57783,#57784,#57785,#57786,#57787,#57788,#57789,#57790,#57791,#57792,#57793,
#57794,#57795,#57796,#57797,#57798,#57799,#57800,#57801,#57802,#57803,#57804,
#57805,#57806,#57807,#57808,#57809,#57810,#57811,#57812,#57813),
 .UNSPECIFIED.,.F.,.F.,(4,2,2,2,2,2,2,2,2,2,2,2,2,2,2,2,2,4),(-23.6367224740298,
-23.6102009889967,-23.5521597036553,-23.4926417159663,-23.435803856614,
-23.3771146729451,-23.3171085926091,-23.2598611088234,-23.2003772998387,
-23.1424751745089,-23.0845553127723,-23.0249989156642,-22.9680595588619,
-22.9094892557851,-22.8499543793008,-22.7928294928815,-22.7334840265615,
-22.6930944862137),.UNSPECIFIED.);
#3149=B_SPLINE_CURVE_WITH_KNOTS('',3,(#57814,#57815,#57816,#57817,#57818,
#57819,#57820,#57821,#57822,#57823,#57824,#57825,#57826,#57827,#57828,#57829,
#57830,#57831,#57832,#57833,#57834,#57835,#57836,#57837,#57838,#57839,#57840,
#57841,#57842,#57843,#57844,#57845,#57846,#57847,#57848,#57849),
 .UNSPECIFIED.,.F.,.F.,(4,2,2,2,2,2,2,2,2,2,2,2,2,2,2,2,2,4),(-4.7070192889843,
-4.68291221701188,-4.62280788263384,-4.56499211835275,-4.50621920975702,
-4.44687598188547,-4.3897125228076,-4.32998213906469,-4.27128283566224,
-4.21406294394457,-4.15372759490239,-4.09570314650131,-4.03731813708901,
-3.97773968458231,-3.92039439080922,-3.86068740451247,-3.80188610698126,
-3.76030733114506),.UNSPECIFIED.);
#3150=B_SPLINE_CURVE_WITH_KNOTS('',3,(#57854,#57855,#57856,#57857,#57858,
#57859,#57860,#57861,#57862,#57863,#57864,#57865,#57866,#57867,#57868,#57869,
#57870,#57871,#57872,#57873,#57874,#57875,#57876,#57877,#57878,#57879,#57880,
#57881,#57882,#57883,#57884,#57885,#57886,#57887,#57888,#57889),
 .UNSPECIFIED.,.F.,.F.,(4,2,2,2,2,2,2,2,2,2,2,2,2,2,2,2,2,4),(-24.5799045977848,
-24.544864402261,-24.4864680402579,-24.4269448204466,-24.3700449713328,
-24.3110051741305,-24.2521492970098,-24.1946159613695,-24.1348126294181,
-24.0775296073419,-24.0193278864891,-23.9598215850082,-23.9030009070175,
-23.8441534701742,-23.7847543450619,-23.7273819445697,-23.667757974583,
-23.6367224740298),.UNSPECIFIED.);
#3151=B_SPLINE_CURVE_WITH_KNOTS('',3,(#57890,#57891,#57892,#57893,#57894,
#57895,#57896,#57897,#57898,#57899,#57900,#57901,#57902,#57903,#57904,#57905,
#57906,#57907,#57908,#57909,#57910,#57911,#57912,#57913,#57914,#57915,#57916,
#57917,#57918,#57919,#57920,#57921,#57922,#57923,#57924,#57925),
 .UNSPECIFIED.,.F.,.F.,(4,2,2,2,2,2,2,2,2,2,2,2,2,2,2,2,2,4),(-3.76030733114506,
-3.74482173076156,-3.6850983260828,-3.62694832744347,-3.56902286769636,
-3.50929583899485,-3.45181843527126,-3.39189585023894,-3.33295745069471,
-3.27595993809932,-3.21626352613547,-3.15797408399984,-3.1003669659872,
-3.04048156422391,-2.98286252158158,-2.92352507208656,-2.86441225193454,
-2.81422223630842),.UNSPECIFIED.);
#3152=B_SPLINE_CURVE_WITH_KNOTS('',3,(#57930,#57931,#57932,#57933,#57934,
#57935,#57936,#57937,#57938,#57939,#57940,#57941,#57942,#57943,#57944,#57945,
#57946,#57947,#57948,#57949,#57950,#57951,#57952,#57953,#57954,#57955,#57956,
#57957,#57958,#57959,#57960,#57961,#57962,#57963,#57964,#57965),
 .UNSPECIFIED.,.F.,.F.,(4,2,2,2,2,2,2,2,2,2,2,2,2,2,2,2,2,4),(-25.5227587485597,
-25.47965708315,-25.421058174348,-25.361036462416,-25.3038727637219,-25.2444773184052,
-25.1865926949701,-25.128756714116,-25.0692650147963,-25.0123746718861,
-24.9538886316087,-24.8944198504469,-24.8373755091807,-24.7781149174187,
-24.7197080007783,-24.6619822469935,-24.6019654058989,-24.5799045977848),
 .UNSPECIFIED.);
#3153=B_SPLINE_CURVE_WITH_KNOTS('',3,(#57966,#57967,#57968,#57969,#57970,
#57971,#57972,#57973,#57974,#57975,#57976,#57977,#57978,#57979,#57980,#57981,
#57982,#57983,#57984,#57985,#57986,#57987,#57988,#57989,#57990,#57991,#57992,
#57993,#57994,#57995,#57996,#57997,#57998,#57999,#58000,#58001,#58002,#58003),
 .UNSPECIFIED.,.F.,.F.,(4,2,2,2,2,2,2,2,2,2,2,2,2,2,2,2,2,2,4),(-2.81422223630842,
-2.80739059809379,-2.74769363128926,-2.68922759545975,-2.63185666495599,
-2.57177569602702,-2.51398082031509,-2.45515020591261,-2.39583126811454,
-2.3386868262193,-2.27895955966271,-2.22028492138649,-2.16305256653281,
-2.1027441052407,-2.04474383487291,-1.98631516239258,-1.92676386570169,
-1.86944360522889,-1.86759610747369),.UNSPECIFIED.);
#3154=B_SPLINE_CURVE_WITH_KNOTS('',3,(#58008,#58009,#58010,#58011,#58012,
#58013,#58014,#58015,#58016,#58017,#58018,#58019,#58020,#58021,#58022,#58023,
#58024,#58025,#58026,#58027,#58028,#58029,#58030,#58031,#58032,#58033,#58034,
#58035,#58036,#58037,#58038,#58039,#58040,#58041,#58042,#58043),
 .UNSPECIFIED.,.F.,.F.,(4,2,2,2,2,2,2,2,2,2,2,2,2,2,2,2,2,4),(-26.4647006629411,
-26.4128164821547,-26.3538770628634,-26.295021282913,-26.2375822529352,
-26.1778787398139,-26.1206318744523,-26.0625253754812,-26.0030911980923,
-25.9463425849355,-25.8875908503495,-25.8281815100278,-25.7708984260118,
-25.7113688412011,-25.6538368035759,-25.595885334023,-25.5364356344578,
-25.5227587485597),.UNSPECIFIED.);
#3155=B_SPLINE_CURVE_WITH_KNOTS('',3,(#58044,#58045,#58046,#58047,#58048,
#58049,#58050,#58051,#58052,#58053,#58054,#58055,#58056,#58057,#58058,#58059,
#58060,#58061,#58062,#58063,#58064,#58065,#58066,#58067,#58068,#58069,#58070,
#58071,#58072,#58073,#58074,#58075,#58076,#58077,#58078,#58079),
 .UNSPECIFIED.,.F.,.F.,(4,2,2,2,2,2,2,2,2,2,2,2,2,2,2,2,2,4),(-1.86759610747369,
-1.8097465170722,-1.7509722323765,-1.69390716991027,-1.63419213717573,-1.57606932036452,
-1.51811407870063,-1.45841685307261,-1.40096694869804,-1.34098343757821,
-1.28207692999559,-1.22508871615811,-1.16540388332849,-1.10714645181714,
-1.0495176707267,-0.989666932708261,-0.932079853846146,-0.921606618540025),
 .UNSPECIFIED.);
#3156=B_SPLINE_CURVE_WITH_KNOTS('',3,(#58085,#58086,#58087,#58088,#58089,
#58090,#58091,#58092,#58093,#58094,#58095,#58096,#58097,#58098,#58099,#58100,
#58101,#58102,#58103,#58104),.UNSPECIFIED.,.F.,.F.,(4,2,2,2,2,2,2,2,2,4),
(9.99987117032003E-7,0.0282047267175922,0.0500972781633209,0.077222937740314,
0.107624298477487,0.137340418712146,0.157932276880896,0.175135732483776,
0.191462844907497,0.203440126186273),.UNSPECIFIED.);
#3157=B_SPLINE_CURVE_WITH_KNOTS('',3,(#58110,#58111,#58112,#58113,#58114,
#58115,#58116,#58117),.UNSPECIFIED.,.F.,.F.,(4,2,2,4),(21.4315064013737,
21.4634357935859,21.4930318613417,21.5226265917604),.UNSPECIFIED.);
#3158=B_SPLINE_CURVE_WITH_KNOTS('',3,(#58123,#58124,#58125,#58126,#58127,
#58128,#58129,#58130,#58131,#58132,#58133,#58134,#58135,#58136,#58137,#58138,
#58139,#58140,#58141,#58142,#58143,#58144,#58145,#58146,#58147,#58148,#58149,
#58150,#58151,#58152,#58153,#58154,#58155,#58156,#58157,#58158),
 .UNSPECIFIED.,.F.,.F.,(4,2,2,2,2,2,2,2,2,2,2,2,2,2,2,2,2,4),(20.6936878716818,
20.7322285263897,20.7783057175789,20.8227795047066,20.8693557730982,20.9149428892879,
20.9597524851927,21.0065846852777,21.0516438851204,21.0976519395239,21.1438788790039,
21.188432473727,21.2350392941589,21.2807854576605,21.3254925240272,21.3724982892632,
21.417717724476,21.4315064013737),.UNSPECIFIED.);
#3159=B_SPLINE_CURVE_WITH_KNOTS('',3,(#58159,#58160,#58161,#58162,#58163,
#58164,#58165,#58166,#58167,#58168,#58169,#58170,#58171,#58172,#58173,#58174,
#58175,#58176,#58177,#58178,#58179,#58180,#58181,#58182,#58183,#58184,#58185,
#58186,#58187,#58188,#58189,#58190,#58191,#58192,#58193,#58194),
 .UNSPECIFIED.,.F.,.F.,(4,2,2,2,2,2,2,2,2,2,2,2,2,2,2,2,2,4),(9.99999999753597E-7,
0.0364903991492045,0.0742057367939146,0.120984278340417,0.165716260437277,
0.212135354668823,0.258243398942271,0.303486376579508,0.350510827449709,
0.395451299070227,0.441223703670797,0.487964967533294,0.532602258835938,
0.578864855147042,0.625329100321987,0.670440021753448,0.717320863549735,
0.740262878339932),.UNSPECIFIED.);
#3160=B_SPLINE_CURVE_WITH_KNOTS('',3,(#58199,#58200,#58201,#58202,#58203,
#58204,#58205,#58206,#58207,#58208,#58209,#58210,#58211,#58212,#58213,#58214,
#58215,#58216,#58217,#58218,#58219,#58220,#58221,#58222,#58223,#58224,#58225,
#58226,#58227,#58228,#58229,#58230,#58231,#58232,#58233,#58234),
 .UNSPECIFIED.,.F.,.F.,(4,2,2,2,2,2,2,2,2,2,2,2,2,2,2,2,2,4),(19.9559680414516,
20.0008504784901,20.0467368410681,20.0912761832143,20.1378918451635,20.1832739295335,
20.2285046006904,20.275104513086,20.3199511087905,20.366754624975,20.4127173643503,
20.4571887454312,20.5037686894442,20.5492336658488,20.5942218762843,20.6409180608554,
20.6858523218674,20.6936878716818),.UNSPECIFIED.);
#3161=B_SPLINE_CURVE_WITH_KNOTS('',3,(#58235,#58236,#58237,#58238,#58239,
#58240,#58241,#58242,#58243,#58244,#58245,#58246,#58247,#58248,#58249,#58250,
#58251,#58252,#58253,#58254,#58255,#58256,#58257,#58258,#58259,#58260,#58261,
#58262,#58263,#58264,#58265,#58266,#58267,#58268,#58269,#58270),
 .UNSPECIFIED.,.F.,.F.,(4,2,2,2,2,2,2,2,2,2,2,2,2,2,2,2,2,4),(0.740262878339932,
0.762427102215096,0.808069985401053,0.854808846272841,0.899429812570394,
0.945570872042072,0.992454683227221,1.03747065146669,1.08424743869661,1.12958660656193,
1.175138889682,1.22190780149668,1.26658471043468,1.31264188421903,1.35939848501362,
1.4043392205548,1.45103260193205,1.48067239646651),.UNSPECIFIED.);
#3162=B_SPLINE_CURVE_WITH_KNOTS('',3,(#58275,#58276,#58277,#58278,#58279,
#58280,#58281,#58282,#58283,#58284,#58285,#58286,#58287,#58288,#58289,#58290,
#58291,#58292,#58293,#58294,#58295,#58296,#58297,#58298,#58299,#58300,#58301,
#58302,#58303,#58304,#58305,#58306,#58307,#58308,#58309,#58310,#58311,#58312),
 .UNSPECIFIED.,.F.,.F.,(4,2,2,2,2,2,2,2,2,2,2,2,2,2,2,2,2,2,4),(19.2175408288878,
19.2219373965907,19.2685210725085,19.3141891378125,19.3589248216993,19.4058460198647,
19.4509870738391,19.4968133764095,19.5431350504829,19.5877640910998,19.6343990565288,
19.6802461513431,19.72492597093,19.7720411959568,19.8173618084826,19.8629496498953,
19.9094715861334,19.954248068259,19.9559680414516),.UNSPECIFIED.);
#3163=B_SPLINE_CURVE_WITH_KNOTS('',3,(#58313,#58314,#58315,#58316,#58317,
#58318,#58319,#58320,#58321,#58322,#58323,#58324,#58325,#58326,#58327,#58328,
#58329,#58330,#58331,#58332,#58333,#58334,#58335,#58336,#58337,#58338,#58339,
#58340,#58341,#58342,#58343,#58344,#58345,#58346,#58347,#58348),
 .UNSPECIFIED.,.F.,.F.,(4,2,2,2,2,2,2,2,2,2,2,2,2,2,2,2,2,4),(1.48067239646651,
1.49671326012625,1.54219831558785,1.5894859449329,1.63428944893413,1.68030245144421,
1.72708174969527,1.77186789842175,1.81835464146615,1.86425678940839,1.90955548631379,
1.95664189809396,2.00148568453804,2.0473126858144,2.0940334671172,2.13867975719358,
2.18499121801513,2.22108960850334),.UNSPECIFIED.);
#3164=B_SPLINE_CURVE_WITH_KNOTS('',3,(#58353,#58354,#58355,#58356,#58357,
#58358,#58359,#58360,#58361,#58362,#58363,#58364,#58365,#58366,#58367,#58368,
#58369,#58370,#58371,#58372,#58373,#58374,#58375,#58376,#58377,#58378,#58379,
#58380,#58381,#58382,#58383,#58384,#58385,#58386,#58387,#58388),
 .UNSPECIFIED.,.F.,.F.,(4,2,2,2,2,2,2,2,2,2,2,2,2,2,2,2,2,4),(18.4801374015765,
18.4907658335562,18.5373515680576,18.5827705444335,18.6278503823358,18.6744946234866,
18.7193811539994,18.7659288026933,18.8119468369207,18.8564049550709,18.9029730508313,
18.9484975984601,18.9933693854802,19.0401328543241,19.0851285772229,19.1312801323088,
19.1774331204032,19.2175408288878),.UNSPECIFIED.);
#3165=B_SPLINE_CURVE_WITH_KNOTS('',3,(#58389,#58390,#58391,#58392,#58393,
#58394,#58395,#58396,#58397,#58398,#58399,#58400,#58401,#58402,#58403,#58404,
#58405,#58406,#58407,#58408,#58409,#58410,#58411,#58412,#58413,#58414,#58415,
#58416,#58417,#58418,#58419,#58420,#58421,#58422,#58423,#58424),
 .UNSPECIFIED.,.F.,.F.,(4,2,2,2,2,2,2,2,2,2,2,2,2,2,2,2,2,4),(2.22108960850334,
2.23120408655543,2.27635041769103,2.32327161206725,2.368237212408,2.41391337637609,
2.46061197050217,2.50519713949817,2.5513666691862,2.59796482416004,2.64299465171328,
2.68978881476098,2.73495033654449,2.78051325760178,2.82722340804027,2.87182391079689,
2.91788757586549,2.96056667106229),.UNSPECIFIED.);
#3166=B_SPLINE_CURVE_WITH_KNOTS('',3,(#58429,#58430,#58431,#58432,#58433,
#58434,#58435,#58436,#58437,#58438,#58439,#58440,#58441,#58442,#58443,#58444,
#58445,#58446,#58447,#58448,#58449,#58450,#58451,#58452,#58453,#58454,#58455,
#58456,#58457,#58458,#58459,#58460,#58461,#58462,#58463,#58464),
 .UNSPECIFIED.,.F.,.F.,(4,2,2,2,2,2,2,2,2,2,2,2,2,2,2,2,2,4),(17.7416164546727,
17.7581937026132,17.8052897667917,17.8505949548622,17.8963342504639,17.9428341472151,
17.9875910340227,18.0342105180494,18.0800707723051,18.124652551507,18.1712871824617,
18.2166406572815,18.2619848045744,18.3085503929415,18.3533657882032,18.4003592098579,
18.446278791736,18.4801374015765),.UNSPECIFIED.);
#3167=B_SPLINE_CURVE_WITH_KNOTS('',3,(#58465,#58466,#58467,#58468,#58469,
#58470,#58471,#58472,#58473,#58474,#58475,#58476,#58477,#58478,#58479,#58480,
#58481,#58482,#58483,#58484,#58485,#58486,#58487,#58488,#58489,#58490,#58491,
#58492,#58493,#58494,#58495,#58496,#58497,#58498,#58499,#58500,#58501,#58502),
 .UNSPECIFIED.,.F.,.F.,(4,2,2,2,2,2,2,2,2,2,2,2,2,2,2,2,2,2,4),(2.96056667106229,
2.96492507840458,3.00987622748865,3.05658369115965,3.10200096713613,3.14749048109044,
3.19424386894225,3.23892780465305,3.28492439308362,3.33166335864177,3.3765506531,
3.42318675517329,3.46898366970959,3.51441887461108,3.56165143931351,3.60649480370264,
3.65245839321213,3.69924258617203,3.70124435567),.UNSPECIFIED.);
#3168=B_SPLINE_CURVE_WITH_KNOTS('',3,(#58507,#58508,#58509,#58510,#58511,
#58512,#58513,#58514,#58515,#58516,#58517,#58518,#58519,#58520,#58521,#58522,
#58523,#58524,#58525,#58526,#58527,#58528,#58529,#58530,#58531,#58532,#58533,
#58534,#58535,#58536,#58537,#58538,#58539,#58540,#58541,#58542),
 .UNSPECIFIED.,.F.,.F.,(4,2,2,2,2,2,2,2,2,2,2,2,2,2,2,2,2,4),(17.002935008964,
17.0259159067871,17.0726902796453,17.117698909592,17.1640720079207,17.2102290646699,
17.2547667636235,17.301404789293,17.3470724875982,17.391917818806,17.4388344123328,
17.4839738011972,17.5299894371059,17.5763017108472,17.6209316820209,17.6676058954979,
17.7134384045876,17.7416164546727),.UNSPECIFIED.);
#3169=B_SPLINE_CURVE_WITH_KNOTS('',3,(#58543,#58544,#58545,#58546,#58547,
#58548,#58549,#58550,#58551,#58552,#58553,#58554,#58555,#58556,#58557,#58558,
#58559,#58560,#58561,#58562,#58563,#58564,#58565,#58566,#58567,#58568,#58569,
#58570,#58571,#58572,#58573,#58574,#58575,#58576,#58577,#58578),
 .UNSPECIFIED.,.F.,.F.,(4,2,2,2,2,2,2,2,2,2,2,2,2,2,2,2,2,4),(3.70124435567,
3.74399270352421,3.79043516379055,3.83649298289209,3.88175593971899,3.92880219425985,
3.97372113000247,4.01951325018307,4.0662546751028,4.11089815702418,4.15717909203302,
4.20358177465394,4.24870726106109,4.29560414076508,4.34067748019848,4.38633433906348,
4.43306819834531,4.44139309323576),.UNSPECIFIED.);
#3170=B_SPLINE_CURVE_WITH_KNOTS('',3,(#58583,#58584,#58585,#58586,#58587,
#58588,#58589,#58590,#58591,#58592,#58593,#58594,#58595,#58596,#58597,#58598,
#58599,#58600,#58601,#58602,#58603,#58604,#58605,#58606,#58607,#58608,#58609,
#58610,#58611,#58612,#58613,#58614,#58615,#58616,#58617,#58618),
 .UNSPECIFIED.,.F.,.F.,(4,2,2,2,2,2,2,2,2,2,2,2,2,2,2,2,2,4),(16.2641372477882,
16.2938030439013,16.3403922128616,16.3852327649267,16.4318876926505,16.4778418228271,
16.5224230010358,16.5690903677485,16.6145405429621,16.6597873151308,16.7064589317587,
16.7513738187352,16.7981669545333,16.8442036947422,16.8887271733991,16.9353636748532,
16.9809031318305,17.002935008964),.UNSPECIFIED.);
#3171=B_SPLINE_CURVE_WITH_KNOTS('',3,(#58619,#58620,#58621,#58622,#58623,
#58624,#58625,#58626,#58627,#58628,#58629,#58630,#58631,#58632,#58633,#58634,
#58635,#58636,#58637,#58638,#58639,#58640,#58641,#58642,#58643,#58644,#58645,
#58646,#58647,#58648,#58649,#58650,#58651,#58652,#58653,#58654),
 .UNSPECIFIED.,.F.,.F.,(4,2,2,2,2,2,2,2,2,2,2,2,2,2,2,2,2,4),(4.44139309323576,
4.47768369479005,4.52383758291686,4.57065155177945,4.61567630686354,4.66246297203597,
4.70776020748785,4.7533204420323,4.80007956137218,4.8447406734777,4.8908048094463,
4.93755248955131,4.98249808878681,5.02919719884178,5.0748218415068,5.12031038865077,
5.16760288129374,5.1818539671131),.UNSPECIFIED.);
#3172=B_SPLINE_CURVE_WITH_KNOTS('',3,(#58659,#58660,#58661,#58662,#58663,
#58664,#58665,#58666,#58667,#58668,#58669,#58670,#58671,#58672,#58673,#58674,
#58675,#58676,#58677,#58678,#58679,#58680,#58681,#58682,#58683,#58684,#58685,
#58686,#58687,#58688,#58689,#58690,#58691,#58692,#58693,#58694),
 .UNSPECIFIED.,.F.,.F.,(4,2,2,2,2,2,2,2,2,2,2,2,2,2,2,2,2,4),(15.5253008226521,
15.5614208712953,15.6076307463169,15.6521806514462,15.6988024510405,15.7445285973342,
15.7892808885852,15.8362633798431,15.8814623032694,15.9272761463232,15.9736600003967,
16.0183472154503,16.0650263145743,16.1109370835491,16.1556467547297,16.2028290254408,
16.2482129532865,16.2641372477882),.UNSPECIFIED.);
#3173=B_SPLINE_CURVE_WITH_KNOTS('',3,(#58695,#58696,#58697,#58698,#58699,
#58700,#58701,#58702,#58703,#58704,#58705,#58706,#58707,#58708,#58709,#58710,
#58711,#58712,#58713,#58714,#58715,#58716,#58717,#58718,#58719,#58720,#58721,
#58722,#58723,#58724,#58725,#58726,#58727,#58728,#58729,#58730),
 .UNSPECIFIED.,.F.,.F.,(4,2,2,2,2,2,2,2,2,2,2,2,2,2,2,2,2,4),(5.1818539671131,
5.21237880454505,5.258394968262,5.30515700825967,5.34994371692685,5.39643143835995,
5.44226233196025,5.48755936077848,5.53464520113254,5.57944804045745,5.62527291369698,
5.67197040786348,5.71660500923211,5.76291244064308,5.80904038797896,5.85417959966551,
5.90109443452282,5.92163532828753),.UNSPECIFIED.);
#3174=B_SPLINE_CURVE_WITH_KNOTS('',3,(#58735,#58736,#58737,#58738,#58739,
#58740,#58741,#58742,#58743,#58744,#58745,#58746,#58747,#58748,#58749,#58750,
#58751,#58752,#58753,#58754,#58755,#58756,#58757,#58758,#58759,#58760,#58761,
#58762,#58763,#58764,#58765,#58766,#58767,#58768,#58769,#58770),
 .UNSPECIFIED.,.F.,.F.,(4,2,2,2,2,2,2,2,2,2,2,2,2,2,2,2,2,4),(14.7873695620709,
14.8300506862385,14.8760153817406,14.9205240016754,14.9671371535707,15.0126019576596,
15.0576755801971,15.1043686547149,15.149301357282,15.1958140370104,15.2418832855322,
15.286374482974,15.3329751561295,15.3785518380475,15.4234279626835,15.4702466599603,
15.5152945505239,15.5253008226521),.UNSPECIFIED.);
#3175=B_SPLINE_CURVE_WITH_KNOTS('',3,(#58771,#58772,#58773,#58774,#58775,
#58776,#58777,#58778,#58779,#58780,#58781,#58782,#58783,#58784,#58785,#58786,
#58787,#58788,#58789,#58790,#58791,#58792,#58793,#58794,#58795,#58796,#58797,
#58798,#58799,#58800,#58801,#58802,#58803,#58804,#58805,#58806),
 .UNSPECIFIED.,.F.,.F.,(4,2,2,2,2,2,2,2,2,2,2,2,2,2,2,2,2,4),(5.92163532828753,
5.94600637034905,5.99167472503286,6.03834442621258,6.08290534138804,6.12906543193699,
6.17556776582538,6.22058468374404,6.26736631647045,6.31246290290152,6.358011917132,
6.40468792773244,6.44925237282631,6.4953007135921,6.54223498706927,6.58716711269207,
6.63385553062737,6.66068791027176),.UNSPECIFIED.);
#3176=B_SPLINE_CURVE_WITH_KNOTS('',3,(#58811,#58812,#58813,#58814,#58815,
#58816,#58817,#58818,#58819,#58820,#58821,#58822,#58823,#58824,#58825,#58826,
#58827,#58828,#58829,#58830,#58831,#58832,#58833,#58834,#58835,#58836,#58837,
#58838,#58839,#58840,#58841,#58842,#58843,#58844,#58845,#58846,#58847,#58848),
 .UNSPECIFIED.,.F.,.F.,(4,2,2,2,2,2,2,2,2,2,2,2,2,2,2,2,2,2,4),(14.0482100339955,
14.0502949245492,14.096984232057,14.142851009537,14.1876060347159,14.2347388331608,
14.2800782706825,14.3257899974572,14.3723273782223,14.41711976203,14.463762437258,
14.5096613573186,14.55425504223,14.6009122351073,14.6463049690835,14.6916352778898,
14.7382430334376,14.7830983471007,14.7873695620709),.UNSPECIFIED.);
#3177=B_SPLINE_CURVE_WITH_KNOTS('',3,(#58849,#58850,#58851,#58852,#58853,
#58854,#58855,#58856,#58857,#58858,#58859,#58860,#58861,#58862,#58863,#58864,
#58865,#58866,#58867,#58868,#58869,#58870,#58871,#58872,#58873,#58874,#58875,
#58876,#58877,#58878,#58879,#58880,#58881,#58882,#58883,#58884),
 .UNSPECIFIED.,.F.,.F.,(4,2,2,2,2,2,2,2,2,2,2,2,2,2,2,2,2,4),(6.66068791027176,
6.67919937428358,6.72466854077273,6.77138281680808,6.8160205136328,6.86199546468963,
6.90869606620136,6.95356006101863,7.00017259357045,7.04588152905359,7.09129151458587,
7.13849904618301,7.1832836822818,7.22922137847032,7.27595882272717,7.32067836819823,
7.3670926336791,7.40074313214862),.UNSPECIFIED.);
#3178=B_SPLINE_CURVE_WITH_KNOTS('',3,(#58889,#58890,#58891,#58892,#58893,
#58894,#58895,#58896,#58897,#58898,#58899,#58900,#58901,#58902,#58903,#58904,
#58905,#58906,#58907,#58908,#58909,#58910,#58911,#58912,#58913,#58914,#58915,
#58916,#58917,#58918,#58919,#58920,#58921,#58922,#58923,#58924),
 .UNSPECIFIED.,.F.,.F.,(4,2,2,2,2,2,2,2,2,2,2,2,2,2,2,2,2,4),(13.3095464675158,
13.3179418806692,13.3645829204745,13.4101456027589,13.4551345123131,13.5019343594699,
13.5469666402861,13.5932875705783,13.6394722908042,13.6840250076321,13.7306726518614,
13.7763692796775,13.8212020202917,13.8681498816812,13.9133183606713,13.9592929931832,
14.0056379903772,14.0482100339955),.UNSPECIFIED.);
#3179=B_SPLINE_CURVE_WITH_KNOTS('',3,(#58925,#58926,#58927,#58928,#58929,
#58930,#58931,#58932,#58933,#58934,#58935,#58936,#58937,#58938,#58939,#58940,
#58941,#58942,#58943,#58944,#58945,#58946,#58947,#58948,#58949,#58950,#58951,
#58952,#58953,#58954,#58955,#58956,#58957,#58958,#58959,#58960),
 .UNSPECIFIED.,.F.,.F.,(4,2,2,2,2,2,2,2,2,2,2,2,2,2,2,2,2,4),(7.40074313214862,
7.41304791193527,7.45828058796883,7.50529645981043,7.55014367964178,7.59590467610001,
7.64259365979734,7.68719438829927,7.73344217485688,7.77972977945611,7.82481959518803,
7.87168035903332,7.91667006179515,7.96229014337893,8.00896624300127,8.05352690669973,
8.09964223179755,8.13994719566162),.UNSPECIFIED.);
#3180=B_SPLINE_CURVE_WITH_KNOTS('',3,(#58965,#58966,#58967,#58968,#58969,
#58970,#58971,#58972,#58973,#58974,#58975,#58976,#58977,#58978,#58979,#58980,
#58981,#58982,#58983,#58984,#58985,#58986,#58987,#58988,#58989,#58990,#58991,
#58992,#58993,#58994,#58995,#58996,#58997,#58998,#58999,#59000),
 .UNSPECIFIED.,.F.,.F.,(4,2,2,2,2,2,2,2,2,2,2,2,2,2,2,2,2,4),(12.5705412100685,
12.5848546363202,12.6320513419363,12.6774479779185,12.7229914291377,12.7695957874756,
12.8144503148156,12.8611058709474,12.9070763074098,12.951650697705,12.9983178350321,
13.0437851961517,13.0889992823918,13.1356902587469,13.1806230630583,13.2273560115123,
13.2734149408359,13.3095464675158),.UNSPECIFIED.);
#3181=B_SPLINE_CURVE_WITH_KNOTS('',3,(#59001,#59002,#59003,#59004,#59005,
#59006,#59007,#59008,#59009,#59010,#59011,#59012,#59013,#59014,#59015,#59016,
#59017,#59018,#59019,#59020,#59021,#59022,#59023,#59024,#59025,#59026,#59027,
#59028,#59029,#59030,#59031,#59032,#59033,#59034,#59035,#59036,#59037,#59038),
 .UNSPECIFIED.,.F.,.F.,(4,2,2,2,2,2,2,2,2,2,2,2,2,2,2,2,2,2,4),(8.13994719566162,
8.1463316268328,8.19131496388372,8.2380593874591,8.28326280667136,8.33020598996195,
8.37537161294956,8.42146167930536,8.46779890512908,8.51245656585315,8.55916791039741,
8.60502388501555,8.64982522039719,8.69694438308839,8.7422725099988,8.78807715134522,
8.83459899420235,8.87937738670119,8.87958134265245),.UNSPECIFIED.);
#3182=B_SPLINE_CURVE_WITH_KNOTS('',3,(#59043,#59044,#59045,#59046,#59047,
#59048,#59049,#59050,#59051,#59052,#59053,#59054,#59055,#59056,#59057,#59058,
#59059,#59060,#59061,#59062,#59063,#59064,#59065,#59066,#59067,#59068,#59069,
#59070,#59071,#59072,#59073,#59074,#59075,#59076,#59077,#59078),
 .UNSPECIFIED.,.F.,.F.,(4,2,2,2,2,2,2,2,2,2,2,2,2,2,2,2,2,4),(11.8321815561307,
11.8527802750529,11.8996021687833,11.9446521456017,11.9907033317147,12.0369186139489,
12.0814657613186,12.1280739153687,12.1738072480122,12.2185277557899,12.2655192350349,
12.3107256977114,12.3564778448273,12.4028721237148,12.4475687949672,12.4942402335744,
12.5401634891127,12.5705412100685),.UNSPECIFIED.);
#3183=B_SPLINE_CURVE_WITH_KNOTS('',3,(#59079,#59080,#59081,#59082,#59083,
#59084,#59085,#59086,#59087,#59088,#59089,#59090,#59091,#59092,#59093,#59094,
#59095,#59096,#59097,#59098,#59099,#59100,#59101,#59102,#59103,#59104,#59105,
#59106,#59107,#59108,#59109,#59110,#59111,#59112,#59113,#59114),
 .UNSPECIFIED.,.F.,.F.,(4,2,2,2,2,2,2,2,2,2,2,2,2,2,2,2,2,4),(8.87958134265245,
8.92602852613987,8.97190922554665,9.01652860508801,9.06319528540556,9.10856829663463,
9.15396816684055,9.20055253946269,9.24538645185148,9.29245567553163,9.33839133852289,
9.38290947461184,9.42952391977244,9.47495799934766,9.52008834525836,9.56674688093536,
9.6116477128901,9.61793661341104),.UNSPECIFIED.);
#3184=B_SPLINE_CURVE_WITH_KNOTS('',3,(#59119,#59120,#59121,#59122,#59123,
#59124,#59125,#59126,#59127,#59128,#59129,#59130,#59131,#59132,#59133,#59134,
#59135,#59136,#59137,#59138,#59139,#59140,#59141,#59142,#59143,#59144,#59145,
#59146,#59147,#59148,#59149,#59150,#59151,#59152,#59153,#59154),
 .UNSPECIFIED.,.F.,.F.,(4,2,2,2,2,2,2,2,2,2,2,2,2,2,2,2,2,4),(11.0945157929649,
11.1213867420797,11.1679850354348,11.212830558321,11.2596899586864,11.3056487691199,
11.3501304725593,11.3967192229775,11.4421794409724,11.4871976310158,11.5338877382452,
11.5788167443302,11.6252436424475,11.6713128846608,11.7157888443594,11.7623703136435,
11.8079484981885,11.8321815561307),.UNSPECIFIED.);
#3185=B_SPLINE_CURVE_WITH_KNOTS('',3,(#59155,#59156,#59157,#59158,#59159,
#59160,#59161,#59162,#59163,#59164,#59165,#59166,#59167,#59168,#59169,#59170,
#59171,#59172,#59173,#59174,#59175,#59176,#59177,#59178,#59179,#59180,#59181,
#59182,#59183,#59184,#59185,#59186,#59187,#59188,#59189,#59190),
 .UNSPECIFIED.,.F.,.F.,(4,2,2,2,2,2,2,2,2,2,2,2,2,2,2,2,2,4),(9.61793661341104,
9.65826687912693,9.70429689093938,9.74877836477337,9.79537166131895,9.84090708321871,
9.88582218876157,9.93259567749554,9.97760169196064,10.0238180381891,10.0699792278232,
10.1144983947581,10.1611035398683,10.2067785301348,10.2515491657397,10.2984763720027,
10.3436239452287,10.3558181882677),.UNSPECIFIED.);
#3186=B_SPLINE_CURVE_WITH_KNOTS('',3,(#59195,#59196,#59197,#59198,#59199,
#59200,#59201,#59202,#59203,#59204,#59205,#59206,#59207,#59208,#59209,#59210,
#59211,#59212,#59213,#59214,#59215,#59216,#59217,#59218,#59219,#59220,#59221,
#59222,#59223,#59224,#59225,#59226,#59227,#59228,#59229,#59230),
 .UNSPECIFIED.,.F.,.F.,(4,2,2,2,2,2,2,2,2,2,2,2,2,2,2,2,2,4),(10.3558181865992,
10.3895062288278,10.4358326314552,10.4804680791543,10.5271205064737,10.5729708577389,
10.6176765737363,10.6647940480184,10.710117621532,10.7557512885806,10.8022746889798,
10.8470530120057,10.8936670905081,10.9395538338801,10.9841105681321,11.0307384394129,
11.0761201700909,11.0945157929649),.UNSPECIFIED.);
#3187=B_SPLINE_CURVE_WITH_KNOTS('',3,(#59231,#59232,#59233,#59234,#59235,
#59236,#59237,#59238,#59239,#59240,#59241,#59242,#59243,#59244,#59245,#59246,
#59247,#59248,#59249,#59250,#59251,#59252,#59253,#59254,#59255,#59256,#59257,
#59258,#59259,#59260,#59261,#59262,#59263,#59264,#59265,#59266),
 .UNSPECIFIED.,.F.,.F.,(4,2,2,2,2,2,2,2,2,2,2,2,2,2,2,2,2,4),(10.3558181882677,
10.3895062304569,10.4358326331012,10.4804680808162,10.5271205081509,10.572970859433,
10.6176765754436,10.6647940497431,10.7101176232735,10.7557512903329,10.8022746907493,
10.8470530137919,10.8936670923103,10.9395538356998,10.9841105699663,11.0307384412633,
11.0761201719588,11.0945157948807),.UNSPECIFIED.);
#3188=B_SPLINE_CURVE_WITH_KNOTS('',3,(#59271,#59272,#59273,#59274,#59275,
#59276,#59277,#59278,#59279,#59280,#59281,#59282,#59283,#59284,#59285,#59286,
#59287,#59288,#59289,#59290,#59291,#59292,#59293,#59294,#59295,#59296,#59297,
#59298,#59299,#59300,#59301,#59302,#59303,#59304,#59305,#59306),
 .UNSPECIFIED.,.F.,.F.,(4,2,2,2,2,2,2,2,2,2,2,2,2,2,2,2,2,4),(9.61793661197057,
9.65826687772365,9.7042968895204,9.74877836334091,9.79537165987244,9.84090708175655,
9.88582218728856,9.93259567600637,9.977601690456,10.0238180366761,10.069979226294,
10.1144983932143,10.16110353831,10.2067785285603,10.2515491641532,10.2984763703993,
10.3436239436092,10.3558181865992),.UNSPECIFIED.);
#3189=B_SPLINE_CURVE_WITH_KNOTS('',3,(#59307,#59308,#59309,#59310,#59311,
#59312,#59313,#59314,#59315,#59316,#59317,#59318,#59319,#59320,#59321,#59322,
#59323,#59324,#59325,#59326,#59327,#59328,#59329,#59330,#59331,#59332,#59333,
#59334,#59335,#59336,#59337,#59338,#59339,#59340,#59341,#59342),
 .UNSPECIFIED.,.F.,.F.,(4,2,2,2,2,2,2,2,2,2,2,2,2,2,2,2,2,4),(11.0945157948807,
11.1213867439599,11.1679850373331,11.2128305602366,11.2596899606121,11.3056487710637,
11.3501304745185,11.3967192249533,11.4421794429662,11.4871976330225,11.5338877402705,
11.5788167463733,11.625243644501,11.6713128867326,11.7157888464474,11.762370315748,
11.8079485003112,11.8321815583089),.UNSPECIFIED.);
#3190=B_SPLINE_CURVE_WITH_KNOTS('',3,(#59347,#59348,#59349,#59350,#59351,
#59352,#59353,#59354,#59355,#59356,#59357,#59358,#59359,#59360,#59361,#59362,
#59363,#59364,#59365,#59366,#59367,#59368,#59369,#59370,#59371,#59372,#59373,
#59374,#59375,#59376,#59377,#59378,#59379,#59380,#59381,#59382),
 .UNSPECIFIED.,.F.,.F.,(4,2,2,2,2,2,2,2,2,2,2,2,2,2,2,2,2,4),(8.87958134142251,
8.92602852493827,8.97190922433066,9.01652860386053,9.06319528416507,9.10856829537987,
9.15396816557657,9.20055253818396,9.24538645055861,9.29245567423173,9.33839133720815,
9.38290947328484,9.42952391843202,9.47495799799238,9.5200883438932,9.56674687955462,
9.61164771149445,9.61793661197057),.UNSPECIFIED.);
#3191=B_SPLINE_CURVE_WITH_KNOTS('',3,(#59383,#59384,#59385,#59386,#59387,
#59388,#59389,#59390,#59391,#59392,#59393,#59394,#59395,#59396,#59397,#59398,
#59399,#59400,#59401,#59402,#59403,#59404,#59405,#59406,#59407,#59408,#59409,
#59410,#59411,#59412,#59413,#59414,#59415,#59416,#59417,#59418),
 .UNSPECIFIED.,.F.,.F.,(4,2,2,2,2,2,2,2,2,2,2,2,2,2,2,2,2,4),(11.8321815583089,
11.8527802771891,11.8996021709384,11.9446521477749,11.9907033338989,12.0369186161519,
12.0814657635389,12.128073917606,12.1738072502682,12.2185277580605,12.2655192373249,
12.31072570002,12.3564778471481,12.402872126055,12.4475687973262,12.4942402359512,
12.5401634915089,12.5705412125212),.UNSPECIFIED.);
#3192=B_SPLINE_CURVE_WITH_KNOTS('',3,(#59423,#59424,#59425,#59426,#59427,
#59428,#59429,#59430,#59431,#59432,#59433,#59434,#59435,#59436,#59437,#59438,
#59439,#59440,#59441,#59442,#59443,#59444,#59445,#59446,#59447,#59448,#59449,
#59450,#59451,#59452,#59453,#59454,#59455,#59456,#59457,#59458,#59459,#59460),
 .UNSPECIFIED.,.F.,.F.,(4,2,2,2,2,2,2,2,2,2,2,2,2,2,2,2,2,2,4),(8.13994719462425,
8.14633162583834,8.19131496287961,8.23805938644507,8.28326280564246,8.33020598891935,
8.37537161189387,8.42146167824292,8.46779890405304,8.51245656476452,8.55916790929672,
8.60502388390122,8.64982521927269,8.69694438194964,8.74227250884644,8.78807715018487,
8.83459899302762,8.87937738551268,8.87958134142251),.UNSPECIFIED.);
#3193=B_SPLINE_CURVE_WITH_KNOTS('',3,(#59461,#59462,#59463,#59464,#59465,
#59466,#59467,#59468,#59469,#59470,#59471,#59472,#59473,#59474,#59475,#59476,
#59477,#59478,#59479,#59480,#59481,#59482,#59483,#59484,#59485,#59486,#59487,
#59488,#59489,#59490,#59491,#59492,#59493,#59494,#59495,#59496),
 .UNSPECIFIED.,.F.,.F.,(4,2,2,2,2,2,2,2,2,2,2,2,2,2,2,2,2,4),(12.5705412125212,
12.5848546387325,12.6320513443688,12.6774479803703,12.7229914316032,12.7695957899609,
12.81445031732,12.8611058734703,12.9070763099523,12.9516507002645,12.99831783761,
13.0437851987491,13.0889992850039,13.1356902613794,13.1806230657103,13.2273560141773,
13.2734149435215,13.3095464702606),.UNSPECIFIED.);
#3194=B_SPLINE_CURVE_WITH_KNOTS('',3,(#59501,#59502,#59503,#59504,#59505,
#59506,#59507,#59508,#59509,#59510,#59511,#59512,#59513,#59514,#59515,#59516,
#59517,#59518,#59519,#59520,#59521,#59522,#59523,#59524,#59525,#59526,#59527,
#59528,#59529,#59530,#59531,#59532,#59533,#59534,#59535,#59536),
 .UNSPECIFIED.,.F.,.F.,(4,2,2,2,2,2,2,2,2,2,2,2,2,2,2,2,2,4),(7.4007431312885,
7.41304791111891,7.45828058714382,7.50529645897655,7.55014367879521,7.59590467524459,
7.64259365893083,7.68719438742294,7.73344217397141,7.7797297785534,7.82481959427612,
7.87168035811193,7.91667006085986,7.96229014243438,8.00896624204524,8.05352690573283,
8.09964223082121,8.13994719462425),.UNSPECIFIED.);
#3195=B_SPLINE_CURVE_WITH_KNOTS('',3,(#59537,#59538,#59539,#59540,#59541,
#59542,#59543,#59544,#59545,#59546,#59547,#59548,#59549,#59550,#59551,#59552,
#59553,#59554,#59555,#59556,#59557,#59558,#59559,#59560,#59561,#59562,#59563,
#59564,#59565,#59566,#59567,#59568,#59569,#59570,#59571,#59572),
 .UNSPECIFIED.,.F.,.F.,(4,2,2,2,2,2,2,2,2,2,2,2,2,2,2,2,2,4),(13.3095464702606,
13.317941883373,13.3645829231975,13.4101456055024,13.4551345150724,13.5019343622502,
13.5469666430868,13.5932875733925,13.6394722936394,13.6840250104865,13.7306726547352,
13.7763692825722,13.8212020232032,13.8681498846145,13.9133183636254,13.9592929961519,
14.0056379933677,14.0482100370503),.UNSPECIFIED.);
#3196=B_SPLINE_CURVE_WITH_KNOTS('',3,(#59577,#59578,#59579,#59580,#59581,
#59582,#59583,#59584,#59585,#59586,#59587,#59588,#59589,#59590,#59591,#59592,
#59593,#59594,#59595,#59596,#59597,#59598,#59599,#59600,#59601,#59602,#59603,
#59604,#59605,#59606,#59607,#59608,#59609,#59610,#59611,#59612),
 .UNSPECIFIED.,.F.,.F.,(4,2,2,2,2,2,2,2,2,2,2,2,2,2,2,2,2,4),(6.66068790957161,
6.67919937362265,6.72466854010414,6.77138281612983,6.81602051294445,6.86199546399339,
6.90869606549543,6.95356006030469,7.00017259284827,7.04588152831696,7.09129151384102,
7.13849904542972,7.18328368151711,7.22922137769738,7.27595882194379,7.32067836740631,
7.36709263287862,7.4007431312885),.UNSPECIFIED.);
#3197=B_SPLINE_CURVE_WITH_KNOTS('',3,(#59613,#59614,#59615,#59616,#59617,
#59618,#59619,#59620,#59621,#59622,#59623,#59624,#59625,#59626,#59627,#59628,
#59629,#59630,#59631,#59632,#59633,#59634,#59635,#59636,#59637,#59638,#59639,
#59640,#59641,#59642,#59643,#59644,#59645,#59646,#59647,#59648,#59649,#59650),
 .UNSPECIFIED.,.F.,.F.,(4,2,2,2,2,2,2,2,2,2,2,2,2,2,2,2,2,2,4),(14.0482100370503,
14.0502949275604,14.0969842350884,14.1428510125903,14.1876060377872,14.2347388362546,
14.2800782737978,14.3257900005883,14.3723273813755,14.4171197652046,14.4637624404534,
14.5096613605359,14.5542550454664,14.6009122383646,14.6463049723626,14.6916352811859,
14.7382430367566,14.7830983504416,14.7873695654535),.UNSPECIFIED.);
#3198=B_SPLINE_CURVE_WITH_KNOTS('',3,(#59655,#59656,#59657,#59658,#59659,
#59660,#59661,#59662,#59663,#59664,#59665,#59666,#59667,#59668,#59669,#59670,
#59671,#59672,#59673,#59674,#59675,#59676,#59677,#59678,#59679,#59680,#59681,
#59682,#59683,#59684,#59685,#59686,#59687,#59688,#59689,#59690),
 .UNSPECIFIED.,.F.,.F.,(4,2,2,2,2,2,2,2,2,2,2,2,2,2,2,2,2,4),(5.92163532773223,
5.94600636983764,5.99167472451486,6.03834442568581,6.08290534085326,6.12906543139539,
6.17556776526837,6.22058468317993,6.26736631589905,6.31246290231792,6.35801191654115,
6.40468792713218,6.44925237221679,6.49530071297518,6.5422349864363,6.58716711205166,
6.6338555299793,6.66068790957161),.UNSPECIFIED.);
#3199=B_SPLINE_CURVE_WITH_KNOTS('',3,(#59691,#59692,#59693,#59694,#59695,
#59696,#59697,#59698,#59699,#59700,#59701,#59702,#59703,#59704,#59705,#59706,
#59707,#59708,#59709,#59710,#59711,#59712,#59713,#59714,#59715,#59716,#59717,
#59718,#59719,#59720,#59721,#59722,#59723,#59724,#59725,#59726),
 .UNSPECIFIED.,.F.,.F.,(4,2,2,2,2,2,2,2,2,2,2,2,2,2,2,2,2,4),(14.7873695654535,
14.8300506895943,14.8760153851188,14.9205240050731,14.9671371569893,15.0126019611003,
15.057675583655,15.1043686581955,15.1493013607845,15.1958140405279,15.2418832890724,
15.2863744865348,15.3329751597116,15.3785518416522,15.4234279663063,15.4702466636066,
15.5152945541928,15.52530082637),.UNSPECIFIED.);
#3200=B_SPLINE_CURVE_WITH_KNOTS('',3,(#59731,#59732,#59733,#59734,#59735,
#59736,#59737,#59738,#59739,#59740,#59741,#59742,#59743,#59744,#59745,#59746,
#59747,#59748,#59749,#59750,#59751,#59752,#59753,#59754,#59755,#59756,#59757,
#59758,#59759,#59760,#59761,#59762,#59763,#59764,#59765,#59766),
 .UNSPECIFIED.,.F.,.F.,(4,2,2,2,2,2,2,2,2,2,2,2,2,2,2,2,2,4),(5.18185396668694,
5.21237880416024,5.25839496787151,5.30515700786141,5.34994371652288,5.39643143795004,
5.44226233153737,5.48755936034949,5.53464520069729,5.57944804001234,5.62527291324563,
5.6719704074037,5.71660500876536,5.76291244016987,5.80904038749152,5.85417959917163,
5.90109443402236,5.92163532773223),.UNSPECIFIED.);
#3201=B_SPLINE_CURVE_WITH_KNOTS('',3,(#59767,#59768,#59769,#59770,#59771,
#59772,#59773,#59774,#59775,#59776,#59777,#59778,#59779,#59780,#59781,#59782,
#59783,#59784,#59785,#59786,#59787,#59788,#59789,#59790,#59791,#59792,#59793,
#59794,#59795,#59796,#59797,#59798,#59799,#59800,#59801,#59802),
 .UNSPECIFIED.,.F.,.F.,(4,2,2,2,2,2,2,2,2,2,2,2,2,2,2,2,2,4),(15.52530082637,
15.5614208749801,15.6076307500252,15.6521806551763,15.6988024547926,15.7445286011097,
15.7892808923799,15.8362633836619,15.8814623071114,15.927276150182,15.9736600042795,
16.0183472193562,16.0650263185026,16.1109370875013,16.1556467587023,16.2028290294383,
16.2482129573077,16.2641372518591),.UNSPECIFIED.);
#3202=B_SPLINE_CURVE_WITH_KNOTS('',3,(#59807,#59808,#59809,#59810,#59811,
#59812,#59813,#59814,#59815,#59816,#59817,#59818,#59819,#59820,#59821,#59822,
#59823,#59824,#59825,#59826,#59827,#59828,#59829,#59830,#59831,#59832,#59833,
#59834,#59835,#59836,#59837,#59838,#59839,#59840,#59841,#59842),
 .UNSPECIFIED.,.F.,.F.,(4,2,2,2,2,2,2,2,2,2,2,2,2,2,2,2,2,4),(4.44139309291887,
4.4776836945143,4.52383758263681,4.5706515514869,4.61567630656631,4.66246297173395,
4.70776020717613,4.75332044171567,4.80007956104877,4.84474067314722,4.89080480911077,
4.93755248920882,4.9824980884388,5.02919719848812,5.0748218411417,5.12031038828011,
5.16760288091741,5.18185396668694),.UNSPECIFIED.);
#3203=B_SPLINE_CURVE_WITH_KNOTS('',3,(#59843,#59844,#59845,#59846,#59847,
#59848,#59849,#59850,#59851,#59852,#59853,#59854,#59855,#59856,#59857,#59858,
#59859,#59860,#59861,#59862,#59863,#59864,#59865,#59866,#59867,#59868,#59869,
#59870,#59871,#59872,#59873,#59874,#59875,#59876,#59877,#59878),
 .UNSPECIFIED.,.F.,.F.,(4,2,2,2,2,2,2,2,2,2,2,2,2,2,2,2,2,4),(16.2641372518591,
16.2938030479407,16.3403922169256,16.3852327690144,16.4318876967614,16.4778418269624,
16.5224230051924,16.5690903719281,16.6145405471659,16.6597873193538,16.7064589360066,
16.7513738230071,16.7981669588227,16.8442036990566,16.8887271777361,16.9353636792139,
16.9809031362162,17.002935013404),.UNSPECIFIED.);
#3204=B_SPLINE_CURVE_WITH_KNOTS('',3,(#59883,#59884,#59885,#59886,#59887,
#59888,#59889,#59890,#59891,#59892,#59893,#59894,#59895,#59896,#59897,#59898,
#59899,#59900,#59901,#59902,#59903,#59904,#59905,#59906,#59907,#59908,#59909,
#59910,#59911,#59912,#59913,#59914,#59915,#59916,#59917,#59918),
 .UNSPECIFIED.,.F.,.F.,(4,2,2,2,2,2,2,2,2,2,2,2,2,2,2,2,2,4),(3.70124435544509,
3.74399270334172,3.79043516360456,3.83649298269546,3.88175593951858,3.92880219405563,
3.97372112979052,4.0195132499672,4.06625467488101,4.11089815679736,4.15717909180209,
4.20358177441128,4.24870726081431,4.29560414051408,4.34067747993884,4.38633433879972,
4.43306819807542,4.44139309291887),.UNSPECIFIED.);
#3205=B_SPLINE_CURVE_WITH_KNOTS('',3,(#59919,#59920,#59921,#59922,#59923,
#59924,#59925,#59926,#59927,#59928,#59929,#59930,#59931,#59932,#59933,#59934,
#59935,#59936,#59937,#59938,#59939,#59940,#59941,#59942,#59943,#59944,#59945,
#59946,#59947,#59948,#59949,#59950,#59951,#59952,#59953,#59954),
 .UNSPECIFIED.,.F.,.F.,(4,2,2,2,2,2,2,2,2,2,2,2,2,2,2,2,2,4),(17.002935013404,
17.025915911193,17.072690284077,17.1176989140485,17.1640720123954,17.2102290691703,
17.2547667681474,17.3014047938411,17.3470724921718,17.3919178234011,17.4388344169549,
17.4839738058451,17.5299894417733,17.576301715541,17.6209316867396,17.6676059002416,
17.7134384093576,17.7416164595014),.UNSPECIFIED.);
#3206=B_SPLINE_CURVE_WITH_KNOTS('',3,(#59959,#59960,#59961,#59962,#59963,
#59964,#59965,#59966,#59967,#59968,#59969,#59970,#59971,#59972,#59973,#59974,
#59975,#59976,#59977,#59978,#59979,#59980,#59981,#59982,#59983,#59984,#59985,
#59986,#59987,#59988,#59989,#59990,#59991,#59992,#59993,#59994,#59995,#59996),
 .UNSPECIFIED.,.F.,.F.,(4,2,2,2,2,2,2,2,2,2,2,2,2,2,2,2,2,2,4),(2.96056667091537,
2.96492507829847,3.00987622737974,3.05658369104791,3.10200096701632,3.14749048096761,
3.19424386881459,3.23892780451988,3.28492439294727,3.33166335850067,3.37655065295563,
3.42318675502558,3.46898366955253,3.51441887445073,3.56165143914983,3.60649480353247,
3.65245839303867,3.69924258599329,3.70124435544509),.UNSPECIFIED.);
#3207=B_SPLINE_CURVE_WITH_KNOTS('',3,(#59997,#59998,#59999,#60000,#60001,
#60002,#60003,#60004,#60005,#60006,#60007,#60008,#60009,#60010,#60011,#60012,
#60013,#60014,#60015,#60016,#60017,#60018,#60019,#60020,#60021,#60022,#60023,
#60024,#60025,#60026,#60027,#60028,#60029,#60030,#60031,#60032),
 .UNSPECIFIED.,.F.,.F.,(4,2,2,2,2,2,2,2,2,2,2,2,2,2,2,2,2,4),(17.7416164595014,
17.7581937074056,17.8052897716113,17.8505949597077,17.8963342553297,17.9428341521077,
17.9875910389412,18.0342105229933,18.0800707772756,18.1246525565008,18.1712871874809,
18.216640662327,18.2619848096412,18.3085503980356,18.3533657933236,18.400359214998,
18.4462787969036,18.4801374068086),.UNSPECIFIED.);
#3208=B_SPLINE_CURVE_WITH_KNOTS('',3,(#60037,#60038,#60039,#60040,#60041,
#60042,#60043,#60044,#60045,#60046,#60047,#60048,#60049,#60050,#60051,#60052,
#60053,#60054,#60055,#60056,#60057,#60058,#60059,#60060,#60061,#60062,#60063,
#60064,#60065,#60066,#60067,#60068,#60069,#60070,#60071,#60072),
 .UNSPECIFIED.,.F.,.F.,(4,2,2,2,2,2,2,2,2,2,2,2,2,2,2,2,2,4),(2.22108960842022,
2.23120408651738,2.27635041765121,2.32327161202571,2.36823721236016,2.41391337632635,
2.46061197044848,2.50519713944098,2.5513666691269,2.59796482409036,2.64299465164124,
2.68978881468655,2.73495033646277,2.78051325751773,2.82722340795193,2.87182391070409,
2.91788757577027,2.96056667091537),.UNSPECIFIED.);
#3209=B_SPLINE_CURVE_WITH_KNOTS('',3,(#60073,#60074,#60075,#60076,#60077,
#60078,#60079,#60080,#60081,#60082,#60083,#60084,#60085,#60086,#60087,#60088,
#60089,#60090,#60091,#60092,#60093,#60094,#60095,#60096,#60097,#60098,#60099,
#60100,#60101,#60102,#60103,#60104,#60105,#60106,#60107,#60108),
 .UNSPECIFIED.,.F.,.F.,(4,2,2,2,2,2,2,2,2,2,2,2,2,2,2,2,2,4),(18.4801374068086,
18.4907658387484,18.5373515732759,18.5827705496792,18.6278503876037,18.6744946287827,
18.7193811593225,18.7659288080364,18.8119468422919,18.8564049604675,18.9029730562544,
18.9484976039111,18.9933693909541,19.040132859827,19.0851285827534,19.1312801378602,
19.1774331259836,19.2175408345414),.UNSPECIFIED.);
#3210=B_SPLINE_CURVE_WITH_KNOTS('',3,(#60113,#60114,#60115,#60116,#60117,
#60118,#60119,#60120,#60121,#60122,#60123,#60124,#60125,#60126,#60127,#60128,
#60129,#60130,#60131,#60132,#60133,#60134,#60135,#60136,#60137,#60138,#60139,
#60140,#60141,#60142,#60143,#60144,#60145,#60146,#60147,#60148),
 .UNSPECIFIED.,.F.,.F.,(4,2,2,2,2,2,2,2,2,2,2,2,2,2,2,2,2,4),(1.48067239643092,
1.4967132601331,1.54219831559389,1.58948594493822,1.63428944893559,1.68030245144475,
1.72708174969294,1.77186789841824,1.81835464146151,1.86425678939566,1.90955548629973,
1.95664189807863,2.00148568451759,2.04731268579268,2.09403346709215,2.13867975716629,
2.18499121798638,2.22108960842022),.UNSPECIFIED.);
#3211=B_SPLINE_CURVE_WITH_KNOTS('',3,(#60149,#60150,#60151,#60152,#60153,
#60154,#60155,#60156,#60157,#60158,#60159,#60160,#60161,#60162,#60163,#60164,
#60165,#60166,#60167,#60168,#60169,#60170,#60171,#60172,#60173,#60174,#60175,
#60176,#60177,#60178,#60179,#60180,#60181,#60182,#60183,#60184,#60185,#60186),
 .UNSPECIFIED.,.F.,.F.,(4,2,2,2,2,2,2,2,2,2,2,2,2,2,2,2,2,2,4),(19.2175408345414,
19.221937402198,19.2685210781433,19.3141891434761,19.3589248273872,19.4058460255822,
19.4509870795851,19.4968133821774,19.5431350562803,19.5877640969252,19.634399062382,
19.6802461572256,19.724925976838,19.7720412018952,19.81736181445,19.862949655886,
19.9094715921544,19.954248074309,19.955968047547),.UNSPECIFIED.);
#3212=B_SPLINE_CURVE_WITH_KNOTS('',3,(#60191,#60192,#60193,#60194,#60195,
#60196,#60197,#60198,#60199,#60200,#60201,#60202,#60203,#60204,#60205,#60206,
#60207,#60208,#60209,#60210,#60211,#60212,#60213,#60214,#60215,#60216,#60217,
#60218,#60219,#60220,#60221,#60222,#60223,#60224,#60225,#60226),
 .UNSPECIFIED.,.F.,.F.,(4,2,2,2,2,2,2,2,2,2,2,2,2,2,2,2,2,4),(0.740262878330326,
0.76242710224918,0.808069985435835,0.854808846306471,0.899429812602798,
0.94557087207502,0.992454683252572,1.03747065149212,1.08424743872217,1.12958660658263,
1.17513888970271,1.22190780151563,1.26658471045133,1.31264188423565,1.35939848502835,
1.40433922056887,1.45103260194552,1.48067239643092),.UNSPECIFIED.);
#3213=B_SPLINE_CURVE_WITH_KNOTS('',3,(#60227,#60228,#60229,#60230,#60231,
#60232,#60233,#60234,#60235,#60236,#60237,#60238,#60239,#60240,#60241,#60242,
#60243,#60244,#60245,#60246,#60247,#60248,#60249,#60250,#60251,#60252,#60253,
#60254,#60255,#60256,#60257,#60258,#60259,#60260,#60261,#60262),
 .UNSPECIFIED.,.F.,.F.,(4,2,2,2,2,2,2,2,2,2,2,2,2,2,2,2,2,4),(19.955968047547,
20.000850484569,20.0467368471769,20.0912761893499,20.1378918513278,20.1832739357276,
20.2285046069091,20.2751045193351,20.3199511150685,20.3667546312751,20.4127173706803,
20.4571887517883,20.5037686958299,20.5492336722642,20.5942218827244,20.6409180673264,
20.685852328368,20.6936878782319),.UNSPECIFIED.);
#3214=B_SPLINE_CURVE_WITH_KNOTS('',3,(#60267,#60268,#60269,#60270,#60271,
#60272,#60273,#60274,#60275,#60276,#60277,#60278,#60279,#60280,#60281,#60282,
#60283,#60284,#60285,#60286,#60287,#60288,#60289,#60290,#60291,#60292,#60293,
#60294,#60295,#60296,#60297,#60298,#60299,#60300,#60301,#60302),
 .UNSPECIFIED.,.F.,.F.,(4,2,2,2,2,2,2,2,2,2,2,2,2,2,2,2,2,4),(1.00000014275486E-6,
0.0364903991724837,0.0742057368406976,0.120984278386942,0.16571626048475,
0.212135354717781,0.258243398985401,0.303486376623694,0.350510827495094,
0.395451299112592,0.441223703714196,0.487964967575798,0.532602258878132,
0.578864855190162,0.62532910035835,0.67044002179057,0.717320863587734,0.740262878330326),
 .UNSPECIFIED.);
#3215=B_SPLINE_CURVE_WITH_KNOTS('',3,(#60303,#60304,#60305,#60306,#60307,
#60308,#60309,#60310,#60311,#60312,#60313,#60314,#60315,#60316,#60317,#60318,
#60319,#60320,#60321,#60322,#60323,#60324,#60325,#60326,#60327,#60328,#60329,
#60330,#60331,#60332,#60333,#60334,#60335,#60336,#60337,#60338),
 .UNSPECIFIED.,.F.,.F.,(4,2,2,2,2,2,2,2,2,2,2,2,2,2,2,2,2,4),(20.6936878782319,
20.732228532913,20.778305724133,20.8227795112891,20.8693557797099,20.9149428959302,
20.9597524918607,21.0065846919771,21.0516438918501,21.0976519462771,21.1438788857884,
21.188432480541,21.2350393010027,21.2807854645354,21.325492530929,21.3724982961973,
21.417717731441,21.4315064083924),.UNSPECIFIED.);
#3216=B_SPLINE_CURVE_WITH_KNOTS('',3,(#60341,#60342,#60343,#60344,#60345,
#60346,#60347,#60348),.UNSPECIFIED.,.F.,.F.,(4,2,2,4),(21.4315064083924,
21.4634358005757,21.493031868375,21.522626598838),.UNSPECIFIED.);
#3217=B_SPLINE_CURVE_WITH_KNOTS('',3,(#60353,#60354,#60355,#60356,#60357,
#60358,#60359,#60360,#60361,#60362,#60363,#60364),.UNSPECIFIED.,.F.,.F.,
(4,2,2,2,2,4),(-0.220493779628296,-0.188155373461082,-0.153829429857051,
-0.103952453260852,-0.0536656706932583,-1.00000014990886E-6),
 .UNSPECIFIED.);
#3218=B_SPLINE_CURVE_WITH_KNOTS('',3,(#60367,#60368,#60369,#60370,#60371,
#60372,#60373,#60374,#60375,#60376,#60377,#60378,#60379,#60380,#60381,#60382,
#60383,#60384,#60385,#60386,#60387,#60388),.UNSPECIFIED.,.F.,.F.,(4,2,2,
2,2,2,2,2,2,2,4),(0.203440126186273,0.213167596868103,0.241856386112924,
0.272211919544501,0.305118112000406,0.341399456620154,0.378879659132554,
0.40534149334872,0.429291364608543,0.44378295238274,0.459192789470913),
 .UNSPECIFIED.);
#3219=B_SPLINE_CURVE_WITH_KNOTS('',3,(#60390,#60391,#60392,#60393,#60394,
#60395,#60396,#60397,#60398,#60399,#60400,#60401,#60402,#60403,#60404,#60405,
#60406,#60407,#60408,#60409,#60410,#60411,#60412,#60413,#60414,#60415,#60416,
#60417,#60418,#60419,#60420,#60421,#60422,#60423),.UNSPECIFIED.,.F.,.F.,
(4,2,2,2,2,2,2,2,2,2,2,2,2,2,2,2,4),(-0.921606618540025,-0.872688627355351,
-0.813612023857313,-0.756611351546357,-0.69692945872276,-0.638499761548747,
-0.581118209737007,-0.521076231967445,-0.463317306881228,-0.4044438926574,
-0.345164740388026,-0.288053249414949,-0.228344796882901,-0.169710130792356,
-0.112479424024743,-0.0563089256119929,-9.99999990258793E-7),
 .UNSPECIFIED.);
#3220=B_SPLINE_CURVE_WITH_KNOTS('',3,(#60424,#60425,#60426,#60427,#60428,
#60429,#60430,#60431,#60432,#60433,#60434,#60435,#60436,#60437,#60438,#60439,
#60440,#60441,#60442,#60443,#60444,#60445,#60446,#60447,#60448,#60449,#60450,
#60451,#60452,#60453,#60454,#60455),.UNSPECIFIED.,.F.,.F.,(4,2,2,2,2,2,
2,2,2,2,2,2,2,2,2,4),(-27.2675995337344,-27.2205810783644,-27.1716030839864,
-27.1114524980469,-27.0544959346273,-26.9959799991961,-26.9364896777515,
-26.8795127522937,-26.8203565510693,-26.7619639947482,-26.7043369916545,
-26.6444247756288,-26.5873734790364,-26.5290771329393,-26.4696302887724,
-26.4647006629411),.UNSPECIFIED.);
#3221=B_SPLINE_CURVE_WITH_KNOTS('',3,(#60632,#60633,#60634,#60635,#60636,
#60637,#60638,#60639),.UNSPECIFIED.,.F.,.F.,(4,2,2,4),(-0.00426615559741139,
-0.00353262795509977,-0.00302253710286643,-0.00251244625063308),
 .UNSPECIFIED.);
#3222=B_SPLINE_CURVE_WITH_KNOTS('',3,(#61553,#61554,#61555,#61556,#61557,
#61558,#61559,#61560),.UNSPECIFIED.,.F.,.F.,(4,2,2,4),(-0.00251244625063308,
-0.00200235539839974,-0.0014922645461664,-0.000758736903856822),
 .UNSPECIFIED.);
#3223=B_SPLINE_CURVE_WITH_KNOTS('',3,(#61565,#61566,#61567,#61568,#61569,
#61570,#61571,#61572),.UNSPECIFIED.,.F.,.F.,(4,2,2,4),(-0.00932716297425779,
-0.00859363533194745,-0.0080835444797141,-0.00757345362748076),
 .UNSPECIFIED.);
#3224=B_SPLINE_CURVE_WITH_KNOTS('',3,(#62486,#62487,#62488,#62489,#62490,
#62491,#62492,#62493),.UNSPECIFIED.,.F.,.F.,(4,2,2,4),(-0.00757345362748076,
-0.00706336277524741,-0.00655327192301407,-0.00581974428070595),
 .UNSPECIFIED.);
#3225=B_SPLINE_CURVE_WITH_KNOTS('',3,(#64489,#64490,#64491,#64492,#64493,
#64494,#64495,#64496,#64497,#64498,#64499,#64500,#64501,#64502,#64503,#64504,
#64505,#64506,#64507,#64508,#64509,#64510,#64511,#64512,#64513,#64514,#64515,
#64516),.UNSPECIFIED.,.F.,.F.,(4,2,2,2,2,2,2,2,2,2,2,2,2,4),(1.00000052656661E-6,
0.0405527857266322,0.0799421814660319,0.1262631587317,0.186952165234641,
0.270820823781497,0.348937293245129,0.459507052180891,0.623823282878412,
0.790896670749941,0.927459468885873,1.05843758188768,1.16179395572833,1.24835467272154),
 .UNSPECIFIED.);
#3361=SHAPE_REPRESENTATION_RELATIONSHIP('SRR','None',#75374,#3369);
#3369=ADVANCED_BREP_SHAPE_REPRESENTATION('',(#3385),#75334);
#3377=STYLED_ITEM('',(#75419),#3385);
#3385=MANIFOLD_SOLID_BREP('Body1',#32027);
#3396=FACE_BOUND('',#7795,.T.);
#3397=FACE_BOUND('',#7800,.T.);
#3775=CIRCLE('',#33579,1.5);
#3776=CIRCLE('',#33580,1.5);
#3777=CIRCLE('',#33609,1.17524047358084);
#3778=CIRCLE('',#33611,1.17524047358084);
#3779=CIRCLE('',#33642,1.1752404735812);
#3780=CIRCLE('',#33644,1.17524047358084);
#3781=CIRCLE('',#33645,1.5);
#3782=CIRCLE('',#33693,1.55162884844711);
#3783=CIRCLE('',#33695,2.61372936963188);
#3784=CIRCLE('',#33696,0.0468749999999982);
#3785=CIRCLE('',#33697,2.58058373926377);
#3786=CIRCLE('',#33699,2.73627063036812);
#3787=CIRCLE('',#33701,2.73627063036812);
#3788=CIRCLE('',#33703,2.73627063036812);
#3789=CIRCLE('',#33705,2.73627063036812);
#3790=CIRCLE('',#33707,2.73627063036812);
#3791=CIRCLE('',#33709,2.73627063036812);
#3792=CIRCLE('',#33711,2.73627063036812);
#3793=CIRCLE('',#33713,2.73627063036812);
#3794=CIRCLE('',#33715,2.73627063036812);
#3795=CIRCLE('',#33717,2.73627063036812);
#3796=CIRCLE('',#33719,2.73627063036812);
#3797=CIRCLE('',#33721,2.73627063036812);
#3798=CIRCLE('',#33723,2.73627063036812);
#3799=CIRCLE('',#33725,2.73627063036812);
#3800=CIRCLE('',#33727,2.73627063036812);
#3801=CIRCLE('',#33729,2.73627063036812);
#3802=CIRCLE('',#33731,2.73627063036812);
#3803=CIRCLE('',#33733,2.73627063036812);
#3804=CIRCLE('',#33735,2.73627063036812);
#3805=CIRCLE('',#33737,2.73627063036812);
#3806=CIRCLE('',#33739,2.73627063036812);
#3807=CIRCLE('',#33741,2.73627063036812);
#3808=CIRCLE('',#33743,2.73627063036812);
#3809=CIRCLE('',#33745,2.73627063036812);
#3810=CIRCLE('',#33747,2.73627063036812);
#3811=CIRCLE('',#33749,2.73627063036812);
#3812=CIRCLE('',#33751,2.73627063036812);
#3813=CIRCLE('',#33753,2.73627063036812);
#3814=CIRCLE('',#33755,2.73627063036812);
#3815=CIRCLE('',#33757,2.73627063036812);
#3816=CIRCLE('',#33759,2.73627063036812);
#3817=CIRCLE('',#33761,2.73627063036812);
#3818=CIRCLE('',#33763,2.73627063036812);
#3819=CIRCLE('',#33765,2.73627063036812);
#3820=CIRCLE('',#33767,2.73627063036812);
#3821=CIRCLE('',#33769,2.73627063036812);
#3822=CIRCLE('',#33771,2.73627063036812);
#3823=CIRCLE('',#33773,2.73627063036812);
#3824=CIRCLE('',#33775,2.73627063036812);
#3825=CIRCLE('',#33777,2.73627063036812);
#3826=CIRCLE('',#33779,2.73627063036812);
#3827=CIRCLE('',#33781,2.73627063036812);
#3828=CIRCLE('',#33783,2.73627063036812);
#3829=CIRCLE('',#33785,2.73627063036812);
#3830=CIRCLE('',#33787,2.73627063036812);
#3831=CIRCLE('',#33789,2.73627063036812);
#3832=CIRCLE('',#33790,2.73627063036812);
#3833=CIRCLE('',#33791,2.73627063036812);
#3834=CIRCLE('',#33792,2.73627063036812);
#3835=CIRCLE('',#33793,2.73627063036812);
#3836=CIRCLE('',#33794,2.73627063036812);
#3837=CIRCLE('',#33795,2.73627063036812);
#3838=CIRCLE('',#33796,2.73627063036812);
#3839=CIRCLE('',#33797,2.73627063036812);
#3840=CIRCLE('',#33798,2.73627063036812);
#3841=CIRCLE('',#33799,2.73627063036812);
#3842=CIRCLE('',#33800,2.73627063036812);
#3843=CIRCLE('',#33801,2.73627063036812);
#3844=CIRCLE('',#33802,2.73627063036812);
#3845=CIRCLE('',#33803,2.73627063036812);
#3846=CIRCLE('',#33804,2.73627063036812);
#3847=CIRCLE('',#33806,2.73627063036812);
#3848=CIRCLE('',#33808,2.73627063036812);
#3849=CIRCLE('',#33810,2.73627063036812);
#3850=CIRCLE('',#33812,2.73627063036812);
#3851=CIRCLE('',#33814,2.73627063036812);
#3852=CIRCLE('',#33816,2.73627063036812);
#3853=CIRCLE('',#33818,2.73627063036812);
#3854=CIRCLE('',#33820,2.73627063036812);
#3855=CIRCLE('',#33822,2.73627063036812);
#3856=CIRCLE('',#33824,2.73627063036812);
#3857=CIRCLE('',#33826,2.73627063036812);
#3858=CIRCLE('',#33828,2.73627063036812);
#3859=CIRCLE('',#33830,2.73627063036812);
#3860=CIRCLE('',#33832,2.73627063036812);
#3861=CIRCLE('',#33834,2.73627063036812);
#3862=CIRCLE('',#33836,2.73627063036812);
#3863=CIRCLE('',#33838,2.73627063036812);
#3864=CIRCLE('',#33840,2.73627063036812);
#3865=CIRCLE('',#33842,2.73627063036812);
#3866=CIRCLE('',#33844,2.73627063036812);
#3867=CIRCLE('',#33846,2.73627063036812);
#3868=CIRCLE('',#33848,2.73627063036812);
#3869=CIRCLE('',#33850,2.73627063036812);
#3870=CIRCLE('',#33852,2.73627063036812);
#3871=CIRCLE('',#33854,2.73627063036812);
#3872=CIRCLE('',#33856,2.73627063036812);
#3873=CIRCLE('',#33858,2.73627063036812);
#3874=CIRCLE('',#33860,2.73627063036812);
#3875=CIRCLE('',#33862,2.73627063036812);
#3876=CIRCLE('',#33864,2.73627063036812);
#3877=CIRCLE('',#33866,2.73627063036812);
#3878=CIRCLE('',#33868,2.73627063036812);
#3879=CIRCLE('',#33870,2.73627063036812);
#3880=CIRCLE('',#33872,2.73627063036812);
#3881=CIRCLE('',#33874,2.73627063036812);
#3882=CIRCLE('',#33876,2.73627063036812);
#3883=CIRCLE('',#33878,2.73627063036812);
#3884=CIRCLE('',#33880,2.73627063036812);
#3885=CIRCLE('',#33882,2.73627063036812);
#3886=CIRCLE('',#33884,2.73627063036812);
#3887=CIRCLE('',#33886,2.73627063036812);
#3888=CIRCLE('',#33888,2.73627063036812);
#3889=CIRCLE('',#33890,2.73627063036812);
#3890=CIRCLE('',#33892,2.73627063036812);
#3891=CIRCLE('',#33894,2.73627063036812);
#3892=CIRCLE('',#33896,2.73627063036812);
#3893=CIRCLE('',#33898,2.73627063036812);
#3894=CIRCLE('',#33900,2.73627063036812);
#3895=CIRCLE('',#33902,2.73627063036812);
#3896=CIRCLE('',#33904,2.73627063036812);
#3897=CIRCLE('',#33906,2.73627063036812);
#3898=CIRCLE('',#33908,2.73627063036812);
#3899=CIRCLE('',#33910,2.73627063036812);
#3900=CIRCLE('',#33912,2.73627063036812);
#3901=CIRCLE('',#33914,2.73627063036812);
#3902=CIRCLE('',#33916,2.73627063036812);
#3903=CIRCLE('',#33918,2.73627063036812);
#3904=CIRCLE('',#33920,2.73627063036812);
#3905=CIRCLE('',#33922,2.73627063036812);
#3906=CIRCLE('',#33924,2.73627063036812);
#3907=CIRCLE('',#33926,2.73627063036812);
#3908=CIRCLE('',#33928,2.73627063036812);
#3909=CIRCLE('',#33930,2.73627063036812);
#3910=CIRCLE('',#33932,2.73627063036812);
#3911=CIRCLE('',#33934,2.73627063036812);
#3912=CIRCLE('',#33936,2.73627063036812);
#3913=CIRCLE('',#33938,2.73627063036812);
#3914=CIRCLE('',#33940,2.73627063036812);
#3915=CIRCLE('',#33942,2.73627063036812);
#3916=CIRCLE('',#33944,2.73627063036812);
#3917=CIRCLE('',#33946,2.73627063036812);
#3918=CIRCLE('',#33948,2.73627063036812);
#3919=CIRCLE('',#33950,2.73627063036812);
#3920=CIRCLE('',#33952,2.73627063036812);
#3921=CIRCLE('',#33954,2.73627063036812);
#3922=CIRCLE('',#33956,2.73627063036812);
#3923=CIRCLE('',#33958,2.73627063036812);
#3924=CIRCLE('',#33960,2.73627063036812);
#3925=CIRCLE('',#33962,2.73627063036812);
#3926=CIRCLE('',#33963,2.73627063036812);
#3927=CIRCLE('',#33964,2.73627063036812);
#3928=CIRCLE('',#33965,2.73627063036812);
#3929=CIRCLE('',#33966,2.73627063036812);
#3930=CIRCLE('',#33967,2.73627063036812);
#3931=CIRCLE('',#33968,2.73627063036812);
#3932=CIRCLE('',#33969,2.73627063036812);
#3933=CIRCLE('',#33970,2.73627063036812);
#3934=CIRCLE('',#33971,2.73627063036812);
#3935=CIRCLE('',#33972,2.73627063036812);
#3936=CIRCLE('',#33973,2.73627063036812);
#3937=CIRCLE('',#33974,2.73627063036812);
#3938=CIRCLE('',#33975,2.73627063036812);
#3939=CIRCLE('',#33976,2.73627063036812);
#3940=CIRCLE('',#33977,2.73627063036812);
#3941=CIRCLE('',#33979,2.73627063036812);
#3942=CIRCLE('',#33981,2.73627063036812);
#3943=CIRCLE('',#33983,2.73627063036812);
#3944=CIRCLE('',#33985,2.73627063036812);
#3945=CIRCLE('',#33987,2.73627063036812);
#3946=CIRCLE('',#33988,2.68872936963188);
#3947=CIRCLE('',#33989,2.68872936963188);
#3948=CIRCLE('',#33991,2.675);
#3949=CIRCLE('',#33992,0.0468749999999996);
#3950=CIRCLE('',#33994,2.675);
#3951=CIRCLE('',#33996,2.60625);
#3952=CIRCLE('',#33997,0.0687500000000002);
#3953=CIRCLE('',#33999,0.15);
#3954=CIRCLE('',#34000,1.65);
#3955=CIRCLE('',#34003,2.75);
#3956=CIRCLE('',#34008,2.75);
#3957=CIRCLE('',#34012,2.75);
#3958=CIRCLE('',#34016,2.75);
#3959=CIRCLE('',#34020,2.75);
#3960=CIRCLE('',#34024,2.75);
#3961=CIRCLE('',#34028,2.75);
#3962=CIRCLE('',#34032,2.75);
#3963=CIRCLE('',#34036,2.75);
#3964=CIRCLE('',#34040,2.75);
#3965=CIRCLE('',#34044,2.75);
#3966=CIRCLE('',#34048,2.75);
#3967=CIRCLE('',#34052,2.75);
#3968=CIRCLE('',#34056,2.75);
#3969=CIRCLE('',#34060,2.75);
#3970=CIRCLE('',#34064,2.75);
#3971=CIRCLE('',#34068,2.75);
#3972=CIRCLE('',#34072,2.75);
#3973=CIRCLE('',#34076,2.75);
#3974=CIRCLE('',#34080,2.75);
#3975=CIRCLE('',#34084,2.75);
#3976=CIRCLE('',#34088,2.75);
#3977=CIRCLE('',#34092,2.75);
#3978=CIRCLE('',#34096,2.75);
#3979=CIRCLE('',#34100,2.75);
#3980=CIRCLE('',#34104,2.75);
#3981=CIRCLE('',#34108,2.75);
#3982=CIRCLE('',#34112,2.75);
#3983=CIRCLE('',#34116,2.75);
#3984=CIRCLE('',#34120,2.75);
#3985=CIRCLE('',#34124,2.75);
#3986=CIRCLE('',#34128,2.75);
#3987=CIRCLE('',#34132,2.75);
#3988=CIRCLE('',#34136,2.75);
#3989=CIRCLE('',#34140,2.75);
#3990=CIRCLE('',#34144,2.75);
#3991=CIRCLE('',#34148,2.75);
#3992=CIRCLE('',#34152,2.75);
#3993=CIRCLE('',#34156,2.75);
#3994=CIRCLE('',#34160,2.75);
#3995=CIRCLE('',#34164,2.75);
#3996=CIRCLE('',#34168,2.75);
#3997=CIRCLE('',#34172,2.75);
#3998=CIRCLE('',#34176,2.75);
#3999=CIRCLE('',#34180,2.75);
#4000=CIRCLE('',#34184,2.75);
#4001=CIRCLE('',#34188,2.75);
#4002=CIRCLE('',#34192,2.75);
#4003=CIRCLE('',#34196,2.75);
#4004=CIRCLE('',#34200,2.75);
#4005=CIRCLE('',#34204,2.75);
#4006=CIRCLE('',#34208,2.75);
#4007=CIRCLE('',#34212,2.75);
#4008=CIRCLE('',#34216,2.75);
#4009=CIRCLE('',#34220,2.75);
#4010=CIRCLE('',#34224,2.75);
#4011=CIRCLE('',#34228,2.75);
#4012=CIRCLE('',#34232,2.75);
#4013=CIRCLE('',#34236,2.75);
#4014=CIRCLE('',#34240,2.75);
#4015=CIRCLE('',#34244,2.75);
#4016=CIRCLE('',#34248,2.75);
#4017=CIRCLE('',#34252,2.75);
#4018=CIRCLE('',#34256,2.75);
#4019=CIRCLE('',#34259,2.75);
#4020=CIRCLE('',#34263,2.75);
#4021=CIRCLE('',#34267,2.75);
#4022=CIRCLE('',#34271,2.75);
#4023=CIRCLE('',#34275,2.75);
#4024=CIRCLE('',#34279,2.75);
#4025=CIRCLE('',#34283,2.75);
#4026=CIRCLE('',#34287,2.75);
#4027=CIRCLE('',#34291,2.75);
#4028=CIRCLE('',#34295,2.75);
#4029=CIRCLE('',#34299,2.75);
#4030=CIRCLE('',#34303,2.75);
#4031=CIRCLE('',#34307,2.75);
#4032=CIRCLE('',#34311,2.75);
#4033=CIRCLE('',#34316,2.75);
#4034=CIRCLE('',#34318,2.75);
#4035=CIRCLE('',#34320,2.75);
#4036=CIRCLE('',#34322,2.75);
#4037=CIRCLE('',#34324,2.75);
#4038=CIRCLE('',#34326,2.75);
#4039=CIRCLE('',#34328,2.75);
#4040=CIRCLE('',#34330,2.75);
#4041=CIRCLE('',#34332,2.75);
#4042=CIRCLE('',#34334,2.75);
#4043=CIRCLE('',#34336,2.75);
#4044=CIRCLE('',#34338,2.75);
#4045=CIRCLE('',#34340,2.75);
#4046=CIRCLE('',#34342,2.75);
#4047=CIRCLE('',#34344,2.75);
#4048=CIRCLE('',#34346,2.75);
#4049=CIRCLE('',#34348,2.75);
#4050=CIRCLE('',#34350,2.75);
#4051=CIRCLE('',#34352,2.75);
#4052=CIRCLE('',#34354,2.75);
#4053=CIRCLE('',#34356,2.75);
#4054=CIRCLE('',#34358,2.75);
#4055=CIRCLE('',#34360,2.75);
#4056=CIRCLE('',#34362,2.75);
#4057=CIRCLE('',#34364,2.75);
#4058=CIRCLE('',#34366,2.75);
#4059=CIRCLE('',#34368,2.75);
#4060=CIRCLE('',#34370,2.75);
#4061=CIRCLE('',#34372,2.75);
#4062=CIRCLE('',#34374,2.75);
#4063=CIRCLE('',#34376,2.75);
#4064=CIRCLE('',#34378,2.75);
#4065=CIRCLE('',#34380,2.75);
#4066=CIRCLE('',#34382,2.75);
#4067=CIRCLE('',#34384,2.75);
#4068=CIRCLE('',#34386,2.75);
#4069=CIRCLE('',#34388,2.75);
#4070=CIRCLE('',#34390,2.75);
#4071=CIRCLE('',#34392,2.75);
#4072=CIRCLE('',#34394,2.75);
#4073=CIRCLE('',#34396,2.75);
#4074=CIRCLE('',#34398,2.75);
#4075=CIRCLE('',#34400,2.75);
#4076=CIRCLE('',#34402,2.75);
#4077=CIRCLE('',#34404,2.75);
#4078=CIRCLE('',#34406,2.75);
#4079=CIRCLE('',#34408,2.75);
#4080=CIRCLE('',#34410,2.75);
#4081=CIRCLE('',#34412,2.75);
#4082=CIRCLE('',#34414,2.75);
#4083=CIRCLE('',#34416,2.75);
#4084=CIRCLE('',#34418,2.75);
#4085=CIRCLE('',#34420,2.75);
#4086=CIRCLE('',#34422,2.75);
#4087=CIRCLE('',#34424,2.75);
#4088=CIRCLE('',#34426,2.75);
#4089=CIRCLE('',#34428,2.75);
#4090=CIRCLE('',#34430,2.75);
#4091=CIRCLE('',#34432,2.75);
#4092=CIRCLE('',#34434,2.75);
#4093=CIRCLE('',#34436,2.75);
#4094=CIRCLE('',#34438,2.75);
#4095=CIRCLE('',#34440,2.75);
#4096=CIRCLE('',#34442,2.75);
#4097=CIRCLE('',#34444,2.75);
#4098=CIRCLE('',#34446,2.75);
#4099=CIRCLE('',#34448,2.75);
#4100=CIRCLE('',#34450,2.75);
#4101=CIRCLE('',#34452,2.75);
#4102=CIRCLE('',#34454,2.75);
#4103=CIRCLE('',#34456,2.75);
#4104=CIRCLE('',#34458,2.75);
#4105=CIRCLE('',#34460,2.75);
#4106=CIRCLE('',#34462,2.75);
#4107=CIRCLE('',#34464,2.75);
#4108=CIRCLE('',#34466,2.75);
#4109=CIRCLE('',#34468,2.75);
#4110=CIRCLE('',#34470,2.75);
#4111=CIRCLE('',#34472,2.75);
#4112=CIRCLE('',#34474,2.75);
#4113=CIRCLE('',#34717,2.75);
#4114=CIRCLE('',#34719,2.75);
#4692=CYLINDRICAL_SURFACE('',#33578,1.5);
#4693=CYLINDRICAL_SURFACE('',#33581,1.5);
#4694=CYLINDRICAL_SURFACE('',#33582,1.5);
#4695=CYLINDRICAL_SURFACE('',#33583,1.5);
#4696=CYLINDRICAL_SURFACE('',#33584,1.5);
#4697=CYLINDRICAL_SURFACE('',#33585,1.5);
#4698=CYLINDRICAL_SURFACE('',#33586,1.5);
#4699=CYLINDRICAL_SURFACE('',#33587,1.5);
#4700=CYLINDRICAL_SURFACE('',#33588,1.5);
#4701=CYLINDRICAL_SURFACE('',#33589,1.5);
#4702=CYLINDRICAL_SURFACE('',#33590,1.5);
#4703=CYLINDRICAL_SURFACE('',#33591,1.5);
#4704=CYLINDRICAL_SURFACE('',#33592,1.5);
#4705=CYLINDRICAL_SURFACE('',#33593,1.5);
#4706=CYLINDRICAL_SURFACE('',#33594,1.5);
#4707=CYLINDRICAL_SURFACE('',#33595,1.5);
#4708=CYLINDRICAL_SURFACE('',#33596,1.5);
#4709=CYLINDRICAL_SURFACE('',#33597,1.5);
#4710=CYLINDRICAL_SURFACE('',#33598,1.5);
#4711=CYLINDRICAL_SURFACE('',#33599,1.5);
#4712=CYLINDRICAL_SURFACE('',#33600,1.5);
#4713=CYLINDRICAL_SURFACE('',#33601,1.5);
#4714=CYLINDRICAL_SURFACE('',#33602,1.5);
#4715=CYLINDRICAL_SURFACE('',#33603,1.5);
#4716=CYLINDRICAL_SURFACE('',#33604,1.5);
#4717=CYLINDRICAL_SURFACE('',#33605,1.5);
#4718=CYLINDRICAL_SURFACE('',#33606,1.5);
#4719=CYLINDRICAL_SURFACE('',#33607,1.5);
#4720=CYLINDRICAL_SURFACE('',#33610,1.17524047358084);
#4721=CYLINDRICAL_SURFACE('',#33612,1.17524047358084);
#4722=CYLINDRICAL_SURFACE('',#33613,1.17524047358084);
#4723=CYLINDRICAL_SURFACE('',#33614,1.17524047358084);
#4724=CYLINDRICAL_SURFACE('',#33615,1.17524047358084);
#4725=CYLINDRICAL_SURFACE('',#33616,1.17524047358084);
#4726=CYLINDRICAL_SURFACE('',#33617,1.17524047358084);
#4727=CYLINDRICAL_SURFACE('',#33618,1.17524047358084);
#4728=CYLINDRICAL_SURFACE('',#33619,1.17524047358084);
#4729=CYLINDRICAL_SURFACE('',#33620,1.17524047358084);
#4730=CYLINDRICAL_SURFACE('',#33621,1.17524047358084);
#4731=CYLINDRICAL_SURFACE('',#33622,1.17524047358084);
#4732=CYLINDRICAL_SURFACE('',#33623,1.17524047358084);
#4733=CYLINDRICAL_SURFACE('',#33624,1.17524047358084);
#4734=CYLINDRICAL_SURFACE('',#33625,1.17524047358084);
#4735=CYLINDRICAL_SURFACE('',#33626,1.17524047358084);
#4736=CYLINDRICAL_SURFACE('',#33627,1.17524047358084);
#4737=CYLINDRICAL_SURFACE('',#33628,1.17524047358084);
#4738=CYLINDRICAL_SURFACE('',#33629,1.17524047358084);
#4739=CYLINDRICAL_SURFACE('',#33630,1.17524047358084);
#4740=CYLINDRICAL_SURFACE('',#33631,1.17524047358084);
#4741=CYLINDRICAL_SURFACE('',#33632,1.17524047358084);
#4742=CYLINDRICAL_SURFACE('',#33633,1.17524047358084);
#4743=CYLINDRICAL_SURFACE('',#33634,1.17524047358084);
#4744=CYLINDRICAL_SURFACE('',#33635,1.17524047358084);
#4745=CYLINDRICAL_SURFACE('',#33636,1.17524047358084);
#4746=CYLINDRICAL_SURFACE('',#33637,1.17524047358084);
#4747=CYLINDRICAL_SURFACE('',#33638,1.17524047358084);
#4748=CYLINDRICAL_SURFACE('',#33639,1.17524047358084);
#4749=CYLINDRICAL_SURFACE('',#33640,1.17524047358084);
#4750=CYLINDRICAL_SURFACE('',#33641,1.17524047358084);
#4751=CYLINDRICAL_SURFACE('',#33646,1.5);
#4752=CYLINDRICAL_SURFACE('',#33647,0.0137499999999999);
#4753=CYLINDRICAL_SURFACE('',#33650,0.0137499999999999);
#4754=CYLINDRICAL_SURFACE('',#33653,0.0137499999999999);
#4755=CYLINDRICAL_SURFACE('',#33656,0.0137499999999999);
#4756=CYLINDRICAL_SURFACE('',#33659,0.0137499999999999);
#4757=CYLINDRICAL_SURFACE('',#33662,0.0137499999999999);
#4758=CYLINDRICAL_SURFACE('',#33665,0.0137499999999999);
#4759=CYLINDRICAL_SURFACE('',#33668,0.0137499999999999);
#4760=CYLINDRICAL_SURFACE('',#33671,0.0137499999999999);
#4761=CYLINDRICAL_SURFACE('',#33674,0.0137499999999999);
#4762=CYLINDRICAL_SURFACE('',#33677,0.0137499999999997);
#4763=CYLINDRICAL_SURFACE('',#33680,0.0137499999999997);
#4764=CYLINDRICAL_SURFACE('',#33683,0.0137499999999997);
#4765=CYLINDRICAL_SURFACE('',#33686,0.0137499999999997);
#4766=CYLINDRICAL_SURFACE('',#33689,0.0137499999999997);
#4767=CYLINDRICAL_SURFACE('',#33993,2.675);
#4768=CYLINDRICAL_SURFACE('',#34317,2.75);
#4769=CYLINDRICAL_SURFACE('',#34319,2.75);
#4770=CYLINDRICAL_SURFACE('',#34321,2.75);
#4771=CYLINDRICAL_SURFACE('',#34323,2.75);
#4772=CYLINDRICAL_SURFACE('',#34325,2.75);
#4773=CYLINDRICAL_SURFACE('',#34327,2.75);
#4774=CYLINDRICAL_SURFACE('',#34329,2.75);
#4775=CYLINDRICAL_SURFACE('',#34331,2.75);
#4776=CYLINDRICAL_SURFACE('',#34333,2.75);
#4777=CYLINDRICAL_SURFACE('',#34335,2.75);
#4778=CYLINDRICAL_SURFACE('',#34337,2.75);
#4779=CYLINDRICAL_SURFACE('',#34339,2.75);
#4780=CYLINDRICAL_SURFACE('',#34341,2.75);
#4781=CYLINDRICAL_SURFACE('',#34343,2.75);
#4782=CYLINDRICAL_SURFACE('',#34345,2.75);
#4783=CYLINDRICAL_SURFACE('',#34347,2.75);
#4784=CYLINDRICAL_SURFACE('',#34349,2.75);
#4785=CYLINDRICAL_SURFACE('',#34351,2.75);
#4786=CYLINDRICAL_SURFACE('',#34353,2.75);
#4787=CYLINDRICAL_SURFACE('',#34355,2.75);
#4788=CYLINDRICAL_SURFACE('',#34357,2.75);
#4789=CYLINDRICAL_SURFACE('',#34359,2.75);
#4790=CYLINDRICAL_SURFACE('',#34361,2.75);
#4791=CYLINDRICAL_SURFACE('',#34363,2.75);
#4792=CYLINDRICAL_SURFACE('',#34365,2.75);
#4793=CYLINDRICAL_SURFACE('',#34367,2.75);
#4794=CYLINDRICAL_SURFACE('',#34369,2.75);
#4795=CYLINDRICAL_SURFACE('',#34371,2.75);
#4796=CYLINDRICAL_SURFACE('',#34373,2.75);
#4797=CYLINDRICAL_SURFACE('',#34375,2.75);
#4798=CYLINDRICAL_SURFACE('',#34377,2.75);
#4799=CYLINDRICAL_SURFACE('',#34379,2.75);
#4800=CYLINDRICAL_SURFACE('',#34381,2.75);
#4801=CYLINDRICAL_SURFACE('',#34383,2.75);
#4802=CYLINDRICAL_SURFACE('',#34385,2.75);
#4803=CYLINDRICAL_SURFACE('',#34387,2.75);
#4804=CYLINDRICAL_SURFACE('',#34389,2.75);
#4805=CYLINDRICAL_SURFACE('',#34391,2.75);
#4806=CYLINDRICAL_SURFACE('',#34393,2.75);
#4807=CYLINDRICAL_SURFACE('',#34395,2.75);
#4808=CYLINDRICAL_SURFACE('',#34397,2.75);
#4809=CYLINDRICAL_SURFACE('',#34399,2.75);
#4810=CYLINDRICAL_SURFACE('',#34401,2.75);
#4811=CYLINDRICAL_SURFACE('',#34403,2.75);
#4812=CYLINDRICAL_SURFACE('',#34405,2.75);
#4813=CYLINDRICAL_SURFACE('',#34407,2.75);
#4814=CYLINDRICAL_SURFACE('',#34409,2.75);
#4815=CYLINDRICAL_SURFACE('',#34411,2.75);
#4816=CYLINDRICAL_SURFACE('',#34413,2.75);
#4817=CYLINDRICAL_SURFACE('',#34415,2.75);
#4818=CYLINDRICAL_SURFACE('',#34417,2.75);
#4819=CYLINDRICAL_SURFACE('',#34419,2.75);
#4820=CYLINDRICAL_SURFACE('',#34421,2.75);
#4821=CYLINDRICAL_SURFACE('',#34423,2.75);
#4822=CYLINDRICAL_SURFACE('',#34425,2.75);
#4823=CYLINDRICAL_SURFACE('',#34427,2.75);
#4824=CYLINDRICAL_SURFACE('',#34429,2.75);
#4825=CYLINDRICAL_SURFACE('',#34431,2.75);
#4826=CYLINDRICAL_SURFACE('',#34433,2.75);
#4827=CYLINDRICAL_SURFACE('',#34435,2.75);
#4828=CYLINDRICAL_SURFACE('',#34437,2.75);
#4829=CYLINDRICAL_SURFACE('',#34439,2.75);
#4830=CYLINDRICAL_SURFACE('',#34441,2.75);
#4831=CYLINDRICAL_SURFACE('',#34443,2.75);
#4832=CYLINDRICAL_SURFACE('',#34445,2.75);
#4833=CYLINDRICAL_SURFACE('',#34447,2.75);
#4834=CYLINDRICAL_SURFACE('',#34449,2.75);
#4835=CYLINDRICAL_SURFACE('',#34451,2.75);
#4836=CYLINDRICAL_SURFACE('',#34453,2.75);
#4837=CYLINDRICAL_SURFACE('',#34455,2.75);
#4838=CYLINDRICAL_SURFACE('',#34457,2.75);
#4839=CYLINDRICAL_SURFACE('',#34459,2.75);
#4840=CYLINDRICAL_SURFACE('',#34461,2.75);
#4841=CYLINDRICAL_SURFACE('',#34463,2.75);
#4842=CYLINDRICAL_SURFACE('',#34465,2.75);
#4843=CYLINDRICAL_SURFACE('',#34467,2.75);
#4844=CYLINDRICAL_SURFACE('',#34469,2.75);
#4845=CYLINDRICAL_SURFACE('',#34471,2.75);
#4846=CYLINDRICAL_SURFACE('',#34473,2.75);
#4847=CYLINDRICAL_SURFACE('',#34718,2.75);
#4848=CYLINDRICAL_SURFACE('',#34733,0.0137499999999997);
#4849=CYLINDRICAL_SURFACE('',#34736,0.0137499999999997);
#4850=CYLINDRICAL_SURFACE('',#34739,0.0137499999999997);
#4851=CYLINDRICAL_SURFACE('',#34742,0.0137499999999997);
#4852=CYLINDRICAL_SURFACE('',#34745,0.0137499999999998);
#4853=CYLINDRICAL_SURFACE('',#34748,0.0137499999999998);
#4854=CYLINDRICAL_SURFACE('',#34751,0.0137499999999997);
#4855=CYLINDRICAL_SURFACE('',#34772,0.0137499999999997);
#4856=CYLINDRICAL_SURFACE('',#34775,0.0137499999999998);
#4857=CYLINDRICAL_SURFACE('',#34778,0.0137499999999998);
#4858=CYLINDRICAL_SURFACE('',#34781,0.0137499999999997);
#4859=CYLINDRICAL_SURFACE('',#34784,0.0137499999999997);
#4860=CYLINDRICAL_SURFACE('',#34787,0.0137499999999997);
#4861=CYLINDRICAL_SURFACE('',#34790,0.0137499999999997);
#4862=CYLINDRICAL_SURFACE('',#34793,0.0137499999999997);
#4863=CYLINDRICAL_SURFACE('',#34796,0.0137499999999997);
#4864=CYLINDRICAL_SURFACE('',#34799,0.0137499999999999);
#4865=CYLINDRICAL_SURFACE('',#34802,0.0137499999999999);
#4866=CYLINDRICAL_SURFACE('',#34805,0.0137499999999999);
#4867=CYLINDRICAL_SURFACE('',#34808,0.0137499999999999);
#4868=CYLINDRICAL_SURFACE('',#34811,0.0137499999999999);
#4869=CYLINDRICAL_SURFACE('',#34814,0.0137499999999999);
#4870=CYLINDRICAL_SURFACE('',#34817,0.0137499999999999);
#4871=CYLINDRICAL_SURFACE('',#34820,0.0137499999999999);
#4872=CYLINDRICAL_SURFACE('',#34823,0.0137499999999999);
#4873=CYLINDRICAL_SURFACE('',#34826,0.0137499999999997);
#4874=CYLINDRICAL_SURFACE('',#34829,0.0137499999999997);
#4875=CYLINDRICAL_SURFACE('',#34832,0.0137499999999997);
#4876=CYLINDRICAL_SURFACE('',#34835,0.0137499999999998);
#4877=CYLINDRICAL_SURFACE('',#34838,0.0137499999999998);
#4878=CYLINDRICAL_SURFACE('',#34841,0.0137499999999997);
#4879=CYLINDRICAL_SURFACE('',#34844,0.0137499999999997);
#4880=CYLINDRICAL_SURFACE('',#34847,0.0137499999999997);
#4881=CYLINDRICAL_SURFACE('',#34850,0.0137499999999997);
#4882=CYLINDRICAL_SURFACE('',#34853,0.0137499999999997);
#4883=CYLINDRICAL_SURFACE('',#34856,0.0137499999999997);
#4884=CYLINDRICAL_SURFACE('',#34859,0.0137499999999999);
#4885=CYLINDRICAL_SURFACE('',#34862,0.0137499999999999);
#4886=CYLINDRICAL_SURFACE('',#34865,0.0137499999999999);
#4887=CYLINDRICAL_SURFACE('',#34868,0.0137499999999999);
#4888=CYLINDRICAL_SURFACE('',#34871,0.0137499999999999);
#4889=CYLINDRICAL_SURFACE('',#34874,0.0137499999999999);
#4890=CYLINDRICAL_SURFACE('',#34877,0.0137499999999999);
#4891=CYLINDRICAL_SURFACE('',#34880,0.0137499999999999);
#4892=CYLINDRICAL_SURFACE('',#34883,0.0137499999999999);
#4893=CYLINDRICAL_SURFACE('',#34886,0.0137499999999999);
#4894=CYLINDRICAL_SURFACE('',#34889,0.0137499999999999);
#4895=CYLINDRICAL_SURFACE('',#34892,0.0137499999999999);
#4896=CYLINDRICAL_SURFACE('',#34895,0.0137499999999999);
#4897=CYLINDRICAL_SURFACE('',#34898,0.0137499999999999);
#4898=CYLINDRICAL_SURFACE('',#34901,0.0137499999999999);
#4899=CYLINDRICAL_SURFACE('',#34904,0.0137499999999999);
#4900=CYLINDRICAL_SURFACE('',#34907,0.0137499999999999);
#4901=CYLINDRICAL_SURFACE('',#34910,0.0137499999999999);
#4902=CYLINDRICAL_SURFACE('',#34913,0.0137499999999999);
#4903=CYLINDRICAL_SURFACE('',#34916,0.0137499999999997);
#4904=CYLINDRICAL_SURFACE('',#34919,0.0137499999999997);
#4905=CYLINDRICAL_SURFACE('',#34922,0.0137499999999997);
#4906=CYLINDRICAL_SURFACE('',#34925,0.0137499999999997);
#4907=CYLINDRICAL_SURFACE('',#34928,0.0137499999999997);
#4908=CYLINDRICAL_SURFACE('',#34931,0.0137499999999997);
#4909=CYLINDRICAL_SURFACE('',#34934,0.0137499999999998);
#4910=CYLINDRICAL_SURFACE('',#34937,0.0137499999999998);
#4911=CYLINDRICAL_SURFACE('',#34940,0.0137499999999997);
#4912=CYLINDRICAL_SURFACE('',#34943,0.0137499999999997);
#5735=FACE_OUTER_BOUND('',#7471,.T.);
#5736=FACE_OUTER_BOUND('',#7472,.T.);
#5737=FACE_OUTER_BOUND('',#7473,.T.);
#5738=FACE_OUTER_BOUND('',#7474,.T.);
#5739=FACE_OUTER_BOUND('',#7475,.T.);
#5740=FACE_OUTER_BOUND('',#7476,.T.);
#5741=FACE_OUTER_BOUND('',#7477,.T.);
#5742=FACE_OUTER_BOUND('',#7478,.T.);
#5743=FACE_OUTER_BOUND('',#7479,.T.);
#5744=FACE_OUTER_BOUND('',#7480,.T.);
#5745=FACE_OUTER_BOUND('',#7481,.T.);
#5746=FACE_OUTER_BOUND('',#7482,.T.);
#5747=FACE_OUTER_BOUND('',#7483,.T.);
#5748=FACE_OUTER_BOUND('',#7484,.T.);
#5749=FACE_OUTER_BOUND('',#7485,.T.);
#5750=FACE_OUTER_BOUND('',#7486,.T.);
#5751=FACE_OUTER_BOUND('',#7487,.T.);
#5752=FACE_OUTER_BOUND('',#7488,.T.);
#5753=FACE_OUTER_BOUND('',#7489,.T.);
#5754=FACE_OUTER_BOUND('',#7490,.T.);
#5755=FACE_OUTER_BOUND('',#7491,.T.);
#5756=FACE_OUTER_BOUND('',#7492,.T.);
#5757=FACE_OUTER_BOUND('',#7493,.T.);
#5758=FACE_OUTER_BOUND('',#7494,.T.);
#5759=FACE_OUTER_BOUND('',#7495,.T.);
#5760=FACE_OUTER_BOUND('',#7496,.T.);
#5761=FACE_OUTER_BOUND('',#7497,.T.);
#5762=FACE_OUTER_BOUND('',#7498,.T.);
#5763=FACE_OUTER_BOUND('',#7499,.T.);
#5764=FACE_OUTER_BOUND('',#7500,.T.);
#5765=FACE_OUTER_BOUND('',#7501,.T.);
#5766=FACE_OUTER_BOUND('',#7502,.T.);
#5767=FACE_OUTER_BOUND('',#7503,.T.);
#5768=FACE_OUTER_BOUND('',#7504,.T.);
#5769=FACE_OUTER_BOUND('',#7505,.T.);
#5770=FACE_OUTER_BOUND('',#7506,.T.);
#5771=FACE_OUTER_BOUND('',#7507,.T.);
#5772=FACE_OUTER_BOUND('',#7508,.T.);
#5773=FACE_OUTER_BOUND('',#7509,.T.);
#5774=FACE_OUTER_BOUND('',#7510,.T.);
#5775=FACE_OUTER_BOUND('',#7511,.T.);
#5776=FACE_OUTER_BOUND('',#7512,.T.);
#5777=FACE_OUTER_BOUND('',#7513,.T.);
#5778=FACE_OUTER_BOUND('',#7514,.T.);
#5779=FACE_OUTER_BOUND('',#7515,.T.);
#5780=FACE_OUTER_BOUND('',#7516,.T.);
#5781=FACE_OUTER_BOUND('',#7517,.T.);
#5782=FACE_OUTER_BOUND('',#7518,.T.);
#5783=FACE_OUTER_BOUND('',#7519,.T.);
#5784=FACE_OUTER_BOUND('',#7520,.T.);
#5785=FACE_OUTER_BOUND('',#7521,.T.);
#5786=FACE_OUTER_BOUND('',#7522,.T.);
#5787=FACE_OUTER_BOUND('',#7523,.T.);
#5788=FACE_OUTER_BOUND('',#7524,.T.);
#5789=FACE_OUTER_BOUND('',#7525,.T.);
#5790=FACE_OUTER_BOUND('',#7526,.T.);
#5791=FACE_OUTER_BOUND('',#7527,.T.);
#5792=FACE_OUTER_BOUND('',#7528,.T.);
#5793=FACE_OUTER_BOUND('',#7529,.T.);
#5794=FACE_OUTER_BOUND('',#7530,.T.);
#5795=FACE_OUTER_BOUND('',#7531,.T.);
#5796=FACE_OUTER_BOUND('',#7532,.T.);
#5797=FACE_OUTER_BOUND('',#7533,.T.);
#5798=FACE_OUTER_BOUND('',#7534,.T.);
#5799=FACE_OUTER_BOUND('',#7535,.T.);
#5800=FACE_OUTER_BOUND('',#7536,.T.);
#5801=FACE_OUTER_BOUND('',#7537,.T.);
#5802=FACE_OUTER_BOUND('',#7538,.T.);
#5803=FACE_OUTER_BOUND('',#7539,.T.);
#5804=FACE_OUTER_BOUND('',#7540,.T.);
#5805=FACE_OUTER_BOUND('',#7541,.T.);
#5806=FACE_OUTER_BOUND('',#7542,.T.);
#5807=FACE_OUTER_BOUND('',#7543,.T.);
#5808=FACE_OUTER_BOUND('',#7544,.T.);
#5809=FACE_OUTER_BOUND('',#7545,.T.);
#5810=FACE_OUTER_BOUND('',#7546,.T.);
#5811=FACE_OUTER_BOUND('',#7547,.T.);
#5812=FACE_OUTER_BOUND('',#7548,.T.);
#5813=FACE_OUTER_BOUND('',#7549,.T.);
#5814=FACE_OUTER_BOUND('',#7550,.T.);
#5815=FACE_OUTER_BOUND('',#7551,.T.);
#5816=FACE_OUTER_BOUND('',#7552,.T.);
#5817=FACE_OUTER_BOUND('',#7553,.T.);
#5818=FACE_OUTER_BOUND('',#7554,.T.);
#5819=FACE_OUTER_BOUND('',#7555,.T.);
#5820=FACE_OUTER_BOUND('',#7556,.T.);
#5821=FACE_OUTER_BOUND('',#7557,.T.);
#5822=FACE_OUTER_BOUND('',#7558,.T.);
#5823=FACE_OUTER_BOUND('',#7559,.T.);
#5824=FACE_OUTER_BOUND('',#7560,.T.);
#5825=FACE_OUTER_BOUND('',#7561,.T.);
#5826=FACE_OUTER_BOUND('',#7562,.T.);
#5827=FACE_OUTER_BOUND('',#7563,.T.);
#5828=FACE_OUTER_BOUND('',#7564,.T.);
#5829=FACE_OUTER_BOUND('',#7565,.T.);
#5830=FACE_OUTER_BOUND('',#7566,.T.);
#5831=FACE_OUTER_BOUND('',#7567,.T.);
#5832=FACE_OUTER_BOUND('',#7568,.T.);
#5833=FACE_OUTER_BOUND('',#7569,.T.);
#5834=FACE_OUTER_BOUND('',#7570,.T.);
#5835=FACE_OUTER_BOUND('',#7571,.T.);
#5836=FACE_OUTER_BOUND('',#7572,.T.);
#5837=FACE_OUTER_BOUND('',#7573,.T.);
#5838=FACE_OUTER_BOUND('',#7574,.T.);
#5839=FACE_OUTER_BOUND('',#7575,.T.);
#5840=FACE_OUTER_BOUND('',#7576,.T.);
#5841=FACE_OUTER_BOUND('',#7577,.T.);
#5842=FACE_OUTER_BOUND('',#7578,.T.);
#5843=FACE_OUTER_BOUND('',#7579,.T.);
#5844=FACE_OUTER_BOUND('',#7580,.T.);
#5845=FACE_OUTER_BOUND('',#7581,.T.);
#5846=FACE_OUTER_BOUND('',#7582,.T.);
#5847=FACE_OUTER_BOUND('',#7583,.T.);
#5848=FACE_OUTER_BOUND('',#7584,.T.);
#5849=FACE_OUTER_BOUND('',#7585,.T.);
#5850=FACE_OUTER_BOUND('',#7586,.T.);
#5851=FACE_OUTER_BOUND('',#7587,.T.);
#5852=FACE_OUTER_BOUND('',#7588,.T.);
#5853=FACE_OUTER_BOUND('',#7589,.T.);
#5854=FACE_OUTER_BOUND('',#7590,.T.);
#5855=FACE_OUTER_BOUND('',#7591,.T.);
#5856=FACE_OUTER_BOUND('',#7592,.T.);
#5857=FACE_OUTER_BOUND('',#7593,.T.);
#5858=FACE_OUTER_BOUND('',#7594,.T.);
#5859=FACE_OUTER_BOUND('',#7595,.T.);
#5860=FACE_OUTER_BOUND('',#7596,.T.);
#5861=FACE_OUTER_BOUND('',#7597,.T.);
#5862=FACE_OUTER_BOUND('',#7598,.T.);
#5863=FACE_OUTER_BOUND('',#7599,.T.);
#5864=FACE_OUTER_BOUND('',#7600,.T.);
#5865=FACE_OUTER_BOUND('',#7601,.T.);
#5866=FACE_OUTER_BOUND('',#7602,.T.);
#5867=FACE_OUTER_BOUND('',#7603,.T.);
#5868=FACE_OUTER_BOUND('',#7604,.T.);
#5869=FACE_OUTER_BOUND('',#7605,.T.);
#5870=FACE_OUTER_BOUND('',#7606,.T.);
#5871=FACE_OUTER_BOUND('',#7607,.T.);
#5872=FACE_OUTER_BOUND('',#7608,.T.);
#5873=FACE_OUTER_BOUND('',#7609,.T.);
#5874=FACE_OUTER_BOUND('',#7610,.T.);
#5875=FACE_OUTER_BOUND('',#7611,.T.);
#5876=FACE_OUTER_BOUND('',#7612,.T.);
#5877=FACE_OUTER_BOUND('',#7613,.T.);
#5878=FACE_OUTER_BOUND('',#7614,.T.);
#5879=FACE_OUTER_BOUND('',#7615,.T.);
#5880=FACE_OUTER_BOUND('',#7616,.T.);
#5881=FACE_OUTER_BOUND('',#7617,.T.);
#5882=FACE_OUTER_BOUND('',#7618,.T.);
#5883=FACE_OUTER_BOUND('',#7619,.T.);
#5884=FACE_OUTER_BOUND('',#7620,.T.);
#5885=FACE_OUTER_BOUND('',#7621,.T.);
#5886=FACE_OUTER_BOUND('',#7622,.T.);
#5887=FACE_OUTER_BOUND('',#7623,.T.);
#5888=FACE_OUTER_BOUND('',#7624,.T.);
#5889=FACE_OUTER_BOUND('',#7625,.T.);
#5890=FACE_OUTER_BOUND('',#7626,.T.);
#5891=FACE_OUTER_BOUND('',#7627,.T.);
#5892=FACE_OUTER_BOUND('',#7628,.T.);
#5893=FACE_OUTER_BOUND('',#7629,.T.);
#5894=FACE_OUTER_BOUND('',#7630,.T.);
#5895=FACE_OUTER_BOUND('',#7631,.T.);
#5896=FACE_OUTER_BOUND('',#7632,.T.);
#5897=FACE_OUTER_BOUND('',#7633,.T.);
#5898=FACE_OUTER_BOUND('',#7634,.T.);
#5899=FACE_OUTER_BOUND('',#7635,.T.);
#5900=FACE_OUTER_BOUND('',#7636,.T.);
#5901=FACE_OUTER_BOUND('',#7637,.T.);
#5902=FACE_OUTER_BOUND('',#7638,.T.);
#5903=FACE_OUTER_BOUND('',#7639,.T.);
#5904=FACE_OUTER_BOUND('',#7640,.T.);
#5905=FACE_OUTER_BOUND('',#7641,.T.);
#5906=FACE_OUTER_BOUND('',#7642,.T.);
#5907=FACE_OUTER_BOUND('',#7643,.T.);
#5908=FACE_OUTER_BOUND('',#7644,.T.);
#5909=FACE_OUTER_BOUND('',#7645,.T.);
#5910=FACE_OUTER_BOUND('',#7646,.T.);
#5911=FACE_OUTER_BOUND('',#7647,.T.);
#5912=FACE_OUTER_BOUND('',#7648,.T.);
#5913=FACE_OUTER_BOUND('',#7649,.T.);
#5914=FACE_OUTER_BOUND('',#7650,.T.);
#5915=FACE_OUTER_BOUND('',#7651,.T.);
#5916=FACE_OUTER_BOUND('',#7652,.T.);
#5917=FACE_OUTER_BOUND('',#7653,.T.);
#5918=FACE_OUTER_BOUND('',#7654,.T.);
#5919=FACE_OUTER_BOUND('',#7655,.T.);
#5920=FACE_OUTER_BOUND('',#7656,.T.);
#5921=FACE_OUTER_BOUND('',#7657,.T.);
#5922=FACE_OUTER_BOUND('',#7658,.T.);
#5923=FACE_OUTER_BOUND('',#7659,.T.);
#5924=FACE_OUTER_BOUND('',#7660,.T.);
#5925=FACE_OUTER_BOUND('',#7661,.T.);
#5926=FACE_OUTER_BOUND('',#7662,.T.);
#5927=FACE_OUTER_BOUND('',#7663,.T.);
#5928=FACE_OUTER_BOUND('',#7664,.T.);
#5929=FACE_OUTER_BOUND('',#7665,.T.);
#5930=FACE_OUTER_BOUND('',#7666,.T.);
#5931=FACE_OUTER_BOUND('',#7667,.T.);
#5932=FACE_OUTER_BOUND('',#7668,.T.);
#5933=FACE_OUTER_BOUND('',#7669,.T.);
#5934=FACE_OUTER_BOUND('',#7670,.T.);
#5935=FACE_OUTER_BOUND('',#7671,.T.);
#5936=FACE_OUTER_BOUND('',#7672,.T.);
#5937=FACE_OUTER_BOUND('',#7673,.T.);
#5938=FACE_OUTER_BOUND('',#7674,.T.);
#5939=FACE_OUTER_BOUND('',#7675,.T.);
#5940=FACE_OUTER_BOUND('',#7676,.T.);
#5941=FACE_OUTER_BOUND('',#7677,.T.);
#5942=FACE_OUTER_BOUND('',#7678,.T.);
#5943=FACE_OUTER_BOUND('',#7679,.T.);
#5944=FACE_OUTER_BOUND('',#7680,.T.);
#5945=FACE_OUTER_BOUND('',#7681,.T.);
#5946=FACE_OUTER_BOUND('',#7682,.T.);
#5947=FACE_OUTER_BOUND('',#7683,.T.);
#5948=FACE_OUTER_BOUND('',#7684,.T.);
#5949=FACE_OUTER_BOUND('',#7685,.T.);
#5950=FACE_OUTER_BOUND('',#7686,.T.);
#5951=FACE_OUTER_BOUND('',#7687,.T.);
#5952=FACE_OUTER_BOUND('',#7688,.T.);
#5953=FACE_OUTER_BOUND('',#7689,.T.);
#5954=FACE_OUTER_BOUND('',#7690,.T.);
#5955=FACE_OUTER_BOUND('',#7691,.T.);
#5956=FACE_OUTER_BOUND('',#7692,.T.);
#5957=FACE_OUTER_BOUND('',#7693,.T.);
#5958=FACE_OUTER_BOUND('',#7694,.T.);
#5959=FACE_OUTER_BOUND('',#7695,.T.);
#5960=FACE_OUTER_BOUND('',#7696,.T.);
#5961=FACE_OUTER_BOUND('',#7697,.T.);
#5962=FACE_OUTER_BOUND('',#7698,.T.);
#5963=FACE_OUTER_BOUND('',#7699,.T.);
#5964=FACE_OUTER_BOUND('',#7700,.T.);
#5965=FACE_OUTER_BOUND('',#7701,.T.);
#5966=FACE_OUTER_BOUND('',#7702,.T.);
#5967=FACE_OUTER_BOUND('',#7703,.T.);
#5968=FACE_OUTER_BOUND('',#7704,.T.);
#5969=FACE_OUTER_BOUND('',#7705,.T.);
#5970=FACE_OUTER_BOUND('',#7706,.T.);
#5971=FACE_OUTER_BOUND('',#7707,.T.);
#5972=FACE_OUTER_BOUND('',#7708,.T.);
#5973=FACE_OUTER_BOUND('',#7709,.T.);
#5974=FACE_OUTER_BOUND('',#7710,.T.);
#5975=FACE_OUTER_BOUND('',#7711,.T.);
#5976=FACE_OUTER_BOUND('',#7712,.T.);
#5977=FACE_OUTER_BOUND('',#7713,.T.);
#5978=FACE_OUTER_BOUND('',#7714,.T.);
#5979=FACE_OUTER_BOUND('',#7715,.T.);
#5980=FACE_OUTER_BOUND('',#7716,.T.);
#5981=FACE_OUTER_BOUND('',#7717,.T.);
#5982=FACE_OUTER_BOUND('',#7718,.T.);
#5983=FACE_OUTER_BOUND('',#7719,.T.);
#5984=FACE_OUTER_BOUND('',#7720,.T.);
#5985=FACE_OUTER_BOUND('',#7721,.T.);
#5986=FACE_OUTER_BOUND('',#7722,.T.);
#5987=FACE_OUTER_BOUND('',#7723,.T.);
#5988=FACE_OUTER_BOUND('',#7724,.T.);
#5989=FACE_OUTER_BOUND('',#7725,.T.);
#5990=FACE_OUTER_BOUND('',#7726,.T.);
#5991=FACE_OUTER_BOUND('',#7727,.T.);
#5992=FACE_OUTER_BOUND('',#7728,.T.);
#5993=FACE_OUTER_BOUND('',#7729,.T.);
#5994=FACE_OUTER_BOUND('',#7730,.T.);
#5995=FACE_OUTER_BOUND('',#7731,.T.);
#5996=FACE_OUTER_BOUND('',#7732,.T.);
#5997=FACE_OUTER_BOUND('',#7733,.T.);
#5998=FACE_OUTER_BOUND('',#7734,.T.);
#5999=FACE_OUTER_BOUND('',#7735,.T.);
#6000=FACE_OUTER_BOUND('',#7736,.T.);
#6001=FACE_OUTER_BOUND('',#7737,.T.);
#6002=FACE_OUTER_BOUND('',#7738,.T.);
#6003=FACE_OUTER_BOUND('',#7739,.T.);
#6004=FACE_OUTER_BOUND('',#7740,.T.);
#6005=FACE_OUTER_BOUND('',#7741,.T.);
#6006=FACE_OUTER_BOUND('',#7742,.T.);
#6007=FACE_OUTER_BOUND('',#7743,.T.);
#6008=FACE_OUTER_BOUND('',#7744,.T.);
#6009=FACE_OUTER_BOUND('',#7745,.T.);
#6010=FACE_OUTER_BOUND('',#7746,.T.);
#6011=FACE_OUTER_BOUND('',#7747,.T.);
#6012=FACE_OUTER_BOUND('',#7748,.T.);
#6013=FACE_OUTER_BOUND('',#7749,.T.);
#6014=FACE_OUTER_BOUND('',#7750,.T.);
#6015=FACE_OUTER_BOUND('',#7751,.T.);
#6016=FACE_OUTER_BOUND('',#7752,.T.);
#6017=FACE_OUTER_BOUND('',#7753,.T.);
#6018=FACE_OUTER_BOUND('',#7754,.T.);
#6019=FACE_OUTER_BOUND('',#7755,.T.);
#6020=FACE_OUTER_BOUND('',#7756,.T.);
#6021=FACE_OUTER_BOUND('',#7757,.T.);
#6022=FACE_OUTER_BOUND('',#7758,.T.);
#6023=FACE_OUTER_BOUND('',#7759,.T.);
#6024=FACE_OUTER_BOUND('',#7760,.T.);
#6025=FACE_OUTER_BOUND('',#7761,.T.);
#6026=FACE_OUTER_BOUND('',#7762,.T.);
#6027=FACE_OUTER_BOUND('',#7763,.T.);
#6028=FACE_OUTER_BOUND('',#7764,.T.);
#6029=FACE_OUTER_BOUND('',#7765,.T.);
#6030=FACE_OUTER_BOUND('',#7766,.T.);
#6031=FACE_OUTER_BOUND('',#7767,.T.);
#6032=FACE_OUTER_BOUND('',#7768,.T.);
#6033=FACE_OUTER_BOUND('',#7769,.T.);
#6034=FACE_OUTER_BOUND('',#7770,.T.);
#6035=FACE_OUTER_BOUND('',#7771,.T.);
#6036=FACE_OUTER_BOUND('',#7772,.T.);
#6037=FACE_OUTER_BOUND('',#7773,.T.);
#6038=FACE_OUTER_BOUND('',#7774,.T.);
#6039=FACE_OUTER_BOUND('',#7775,.T.);
#6040=FACE_OUTER_BOUND('',#7776,.T.);
#6041=FACE_OUTER_BOUND('',#7777,.T.);
#6042=FACE_OUTER_BOUND('',#7778,.T.);
#6043=FACE_OUTER_BOUND('',#7779,.T.);
#6044=FACE_OUTER_BOUND('',#7780,.T.);
#6045=FACE_OUTER_BOUND('',#7781,.T.);
#6046=FACE_OUTER_BOUND('',#7782,.T.);
#6047=FACE_OUTER_BOUND('',#7783,.T.);
#6048=FACE_OUTER_BOUND('',#7784,.T.);
#6049=FACE_OUTER_BOUND('',#7785,.T.);
#6050=FACE_OUTER_BOUND('',#7786,.T.);
#6051=FACE_OUTER_BOUND('',#7787,.T.);
#6052=FACE_OUTER_BOUND('',#7788,.T.);
#6053=FACE_OUTER_BOUND('',#7789,.T.);
#6054=FACE_OUTER_BOUND('',#7790,.T.);
#6055=FACE_OUTER_BOUND('',#7791,.T.);
#6056=FACE_OUTER_BOUND('',#7792,.T.);
#6057=FACE_OUTER_BOUND('',#7793,.T.);
#6058=FACE_OUTER_BOUND('',#7794,.T.);
#6059=FACE_OUTER_BOUND('',#7796,.T.);
#6060=FACE_OUTER_BOUND('',#7797,.T.);
#6061=FACE_OUTER_BOUND('',#7798,.T.);
#6062=FACE_OUTER_BOUND('',#7799,.T.);
#6063=FACE_OUTER_BOUND('',#7801,.T.);
#6064=FACE_OUTER_BOUND('',#7802,.T.);
#6065=FACE_OUTER_BOUND('',#7803,.T.);
#6066=FACE_OUTER_BOUND('',#7804,.T.);
#6067=FACE_OUTER_BOUND('',#7805,.T.);
#6068=FACE_OUTER_BOUND('',#7806,.T.);
#6069=FACE_OUTER_BOUND('',#7807,.T.);
#6070=FACE_OUTER_BOUND('',#7808,.T.);
#6071=FACE_OUTER_BOUND('',#7809,.T.);
#6072=FACE_OUTER_BOUND('',#7810,.T.);
#6073=FACE_OUTER_BOUND('',#7811,.T.);
#6074=FACE_OUTER_BOUND('',#7812,.T.);
#6075=FACE_OUTER_BOUND('',#7813,.T.);
#6076=FACE_OUTER_BOUND('',#7814,.T.);
#6077=FACE_OUTER_BOUND('',#7815,.T.);
#6078=FACE_OUTER_BOUND('',#7816,.T.);
#6079=FACE_OUTER_BOUND('',#7817,.T.);
#6080=FACE_OUTER_BOUND('',#7818,.T.);
#6081=FACE_OUTER_BOUND('',#7819,.T.);
#6082=FACE_OUTER_BOUND('',#7820,.T.);
#6083=FACE_OUTER_BOUND('',#7821,.T.);
#6084=FACE_OUTER_BOUND('',#7822,.T.);
#6085=FACE_OUTER_BOUND('',#7823,.T.);
#6086=FACE_OUTER_BOUND('',#7824,.T.);
#6087=FACE_OUTER_BOUND('',#7825,.T.);
#6088=FACE_OUTER_BOUND('',#7826,.T.);
#6089=FACE_OUTER_BOUND('',#7827,.T.);
#6090=FACE_OUTER_BOUND('',#7828,.T.);
#6091=FACE_OUTER_BOUND('',#7829,.T.);
#6092=FACE_OUTER_BOUND('',#7830,.T.);
#6093=FACE_OUTER_BOUND('',#7831,.T.);
#6094=FACE_OUTER_BOUND('',#7832,.T.);
#6095=FACE_OUTER_BOUND('',#7833,.T.);
#6096=FACE_OUTER_BOUND('',#7834,.T.);
#6097=FACE_OUTER_BOUND('',#7835,.T.);
#6098=FACE_OUTER_BOUND('',#7836,.T.);
#6099=FACE_OUTER_BOUND('',#7837,.T.);
#6100=FACE_OUTER_BOUND('',#7838,.T.);
#6101=FACE_OUTER_BOUND('',#7839,.T.);
#6102=FACE_OUTER_BOUND('',#7840,.T.);
#6103=FACE_OUTER_BOUND('',#7841,.T.);
#6104=FACE_OUTER_BOUND('',#7842,.T.);
#6105=FACE_OUTER_BOUND('',#7843,.T.);
#6106=FACE_OUTER_BOUND('',#7844,.T.);
#6107=FACE_OUTER_BOUND('',#7845,.T.);
#6108=FACE_OUTER_BOUND('',#7846,.T.);
#6109=FACE_OUTER_BOUND('',#7847,.T.);
#6110=FACE_OUTER_BOUND('',#7848,.T.);
#6111=FACE_OUTER_BOUND('',#7849,.T.);
#6112=FACE_OUTER_BOUND('',#7850,.T.);
#6113=FACE_OUTER_BOUND('',#7851,.T.);
#6114=FACE_OUTER_BOUND('',#7852,.T.);
#6115=FACE_OUTER_BOUND('',#7853,.T.);
#6116=FACE_OUTER_BOUND('',#7854,.T.);
#6117=FACE_OUTER_BOUND('',#7855,.T.);
#6118=FACE_OUTER_BOUND('',#7856,.T.);
#6119=FACE_OUTER_BOUND('',#7857,.T.);
#6120=FACE_OUTER_BOUND('',#7858,.T.);
#6121=FACE_OUTER_BOUND('',#7859,.T.);
#6122=FACE_OUTER_BOUND('',#7860,.T.);
#6123=FACE_OUTER_BOUND('',#7861,.T.);
#6124=FACE_OUTER_BOUND('',#7862,.T.);
#6125=FACE_OUTER_BOUND('',#7863,.T.);
#6126=FACE_OUTER_BOUND('',#7864,.T.);
#6127=FACE_OUTER_BOUND('',#7865,.T.);
#6128=FACE_OUTER_BOUND('',#7866,.T.);
#6129=FACE_OUTER_BOUND('',#7867,.T.);
#6130=FACE_OUTER_BOUND('',#7868,.T.);
#6131=FACE_OUTER_BOUND('',#7869,.T.);
#6132=FACE_OUTER_BOUND('',#7870,.T.);
#6133=FACE_OUTER_BOUND('',#7871,.T.);
#6134=FACE_OUTER_BOUND('',#7872,.T.);
#6135=FACE_OUTER_BOUND('',#7873,.T.);
#6136=FACE_OUTER_BOUND('',#7874,.T.);
#6137=FACE_OUTER_BOUND('',#7875,.T.);
#6138=FACE_OUTER_BOUND('',#7876,.T.);
#6139=FACE_OUTER_BOUND('',#7877,.T.);
#6140=FACE_OUTER_BOUND('',#7878,.T.);
#6141=FACE_OUTER_BOUND('',#7879,.T.);
#6142=FACE_OUTER_BOUND('',#7880,.T.);
#6143=FACE_OUTER_BOUND('',#7881,.T.);
#6144=FACE_OUTER_BOUND('',#7882,.T.);
#6145=FACE_OUTER_BOUND('',#7883,.T.);
#6146=FACE_OUTER_BOUND('',#7884,.T.);
#6147=FACE_OUTER_BOUND('',#7885,.T.);
#6148=FACE_OUTER_BOUND('',#7886,.T.);
#6149=FACE_OUTER_BOUND('',#7887,.T.);
#6150=FACE_OUTER_BOUND('',#7888,.T.);
#6151=FACE_OUTER_BOUND('',#7889,.T.);
#6152=FACE_OUTER_BOUND('',#7890,.T.);
#6153=FACE_OUTER_BOUND('',#7891,.T.);
#6154=FACE_OUTER_BOUND('',#7892,.T.);
#6155=FACE_OUTER_BOUND('',#7893,.T.);
#6156=FACE_OUTER_BOUND('',#7894,.T.);
#6157=FACE_OUTER_BOUND('',#7895,.T.);
#6158=FACE_OUTER_BOUND('',#7896,.T.);
#6159=FACE_OUTER_BOUND('',#7897,.T.);
#6160=FACE_OUTER_BOUND('',#7898,.T.);
#6161=FACE_OUTER_BOUND('',#7899,.T.);
#6162=FACE_OUTER_BOUND('',#7900,.T.);
#6163=FACE_OUTER_BOUND('',#7901,.T.);
#6164=FACE_OUTER_BOUND('',#7902,.T.);
#6165=FACE_OUTER_BOUND('',#7903,.T.);
#6166=FACE_OUTER_BOUND('',#7904,.T.);
#6167=FACE_OUTER_BOUND('',#7905,.T.);
#6168=FACE_OUTER_BOUND('',#7906,.T.);
#6169=FACE_OUTER_BOUND('',#7907,.T.);
#6170=FACE_OUTER_BOUND('',#7908,.T.);
#6171=FACE_OUTER_BOUND('',#7909,.T.);
#6172=FACE_OUTER_BOUND('',#7910,.T.);
#6173=FACE_OUTER_BOUND('',#7911,.T.);
#6174=FACE_OUTER_BOUND('',#7912,.T.);
#6175=FACE_OUTER_BOUND('',#7913,.T.);
#6176=FACE_OUTER_BOUND('',#7914,.T.);
#6177=FACE_OUTER_BOUND('',#7915,.T.);
#6178=FACE_OUTER_BOUND('',#7916,.T.);
#6179=FACE_OUTER_BOUND('',#7917,.T.);
#6180=FACE_OUTER_BOUND('',#7918,.T.);
#6181=FACE_OUTER_BOUND('',#7919,.T.);
#6182=FACE_OUTER_BOUND('',#7920,.T.);
#6183=FACE_OUTER_BOUND('',#7921,.T.);
#6184=FACE_OUTER_BOUND('',#7922,.T.);
#6185=FACE_OUTER_BOUND('',#7923,.T.);
#6186=FACE_OUTER_BOUND('',#7924,.T.);
#6187=FACE_OUTER_BOUND('',#7925,.T.);
#6188=FACE_OUTER_BOUND('',#7926,.T.);
#6189=FACE_OUTER_BOUND('',#7927,.T.);
#6190=FACE_OUTER_BOUND('',#7928,.T.);
#6191=FACE_OUTER_BOUND('',#7929,.T.);
#6192=FACE_OUTER_BOUND('',#7930,.T.);
#6193=FACE_OUTER_BOUND('',#7931,.T.);
#6194=FACE_OUTER_BOUND('',#7932,.T.);
#6195=FACE_OUTER_BOUND('',#7933,.T.);
#6196=FACE_OUTER_BOUND('',#7934,.T.);
#6197=FACE_OUTER_BOUND('',#7935,.T.);
#6198=FACE_OUTER_BOUND('',#7936,.T.);
#6199=FACE_OUTER_BOUND('',#7937,.T.);
#6200=FACE_OUTER_BOUND('',#7938,.T.);
#6201=FACE_OUTER_BOUND('',#7939,.T.);
#6202=FACE_OUTER_BOUND('',#7940,.T.);
#6203=FACE_OUTER_BOUND('',#7941,.T.);
#6204=FACE_OUTER_BOUND('',#7942,.T.);
#6205=FACE_OUTER_BOUND('',#7943,.T.);
#6206=FACE_OUTER_BOUND('',#7944,.T.);
#6207=FACE_OUTER_BOUND('',#7945,.T.);
#6208=FACE_OUTER_BOUND('',#7946,.T.);
#6209=FACE_OUTER_BOUND('',#7947,.T.);
#6210=FACE_OUTER_BOUND('',#7948,.T.);
#6211=FACE_OUTER_BOUND('',#7949,.T.);
#6212=FACE_OUTER_BOUND('',#7950,.T.);
#6213=FACE_OUTER_BOUND('',#7951,.T.);
#6214=FACE_OUTER_BOUND('',#7952,.T.);
#6215=FACE_OUTER_BOUND('',#7953,.T.);
#6216=FACE_OUTER_BOUND('',#7954,.T.);
#6217=FACE_OUTER_BOUND('',#7955,.T.);
#6218=FACE_OUTER_BOUND('',#7956,.T.);
#6219=FACE_OUTER_BOUND('',#7957,.T.);
#6220=FACE_OUTER_BOUND('',#7958,.T.);
#6221=FACE_OUTER_BOUND('',#7959,.T.);
#6222=FACE_OUTER_BOUND('',#7960,.T.);
#6223=FACE_OUTER_BOUND('',#7961,.T.);
#6224=FACE_OUTER_BOUND('',#7962,.T.);
#6225=FACE_OUTER_BOUND('',#7963,.T.);
#6226=FACE_OUTER_BOUND('',#7964,.T.);
#6227=FACE_OUTER_BOUND('',#7965,.T.);
#6228=FACE_OUTER_BOUND('',#7966,.T.);
#6229=FACE_OUTER_BOUND('',#7967,.T.);
#6230=FACE_OUTER_BOUND('',#7968,.T.);
#6231=FACE_OUTER_BOUND('',#7969,.T.);
#6232=FACE_OUTER_BOUND('',#7970,.T.);
#6233=FACE_OUTER_BOUND('',#7971,.T.);
#6234=FACE_OUTER_BOUND('',#7972,.T.);
#6235=FACE_OUTER_BOUND('',#7973,.T.);
#6236=FACE_OUTER_BOUND('',#7974,.T.);
#6237=FACE_OUTER_BOUND('',#7975,.T.);
#6238=FACE_OUTER_BOUND('',#7976,.T.);
#6239=FACE_OUTER_BOUND('',#7977,.T.);
#6240=FACE_OUTER_BOUND('',#7978,.T.);
#6241=FACE_OUTER_BOUND('',#7979,.T.);
#6242=FACE_OUTER_BOUND('',#7980,.T.);
#6243=FACE_OUTER_BOUND('',#7981,.T.);
#6244=FACE_OUTER_BOUND('',#7982,.T.);
#6245=FACE_OUTER_BOUND('',#7983,.T.);
#6246=FACE_OUTER_BOUND('',#7984,.T.);
#6247=FACE_OUTER_BOUND('',#7985,.T.);
#6248=FACE_OUTER_BOUND('',#7986,.T.);
#6249=FACE_OUTER_BOUND('',#7987,.T.);
#6250=FACE_OUTER_BOUND('',#7988,.T.);
#6251=FACE_OUTER_BOUND('',#7989,.T.);
#6252=FACE_OUTER_BOUND('',#7990,.T.);
#6253=FACE_OUTER_BOUND('',#7991,.T.);
#6254=FACE_OUTER_BOUND('',#7992,.T.);
#6255=FACE_OUTER_BOUND('',#7993,.T.);
#6256=FACE_OUTER_BOUND('',#7994,.T.);
#6257=FACE_OUTER_BOUND('',#7995,.T.);
#6258=FACE_OUTER_BOUND('',#7996,.T.);
#6259=FACE_OUTER_BOUND('',#7997,.T.);
#6260=FACE_OUTER_BOUND('',#7998,.T.);
#6261=FACE_OUTER_BOUND('',#7999,.T.);
#6262=FACE_OUTER_BOUND('',#8000,.T.);
#6263=FACE_OUTER_BOUND('',#8001,.T.);
#6264=FACE_OUTER_BOUND('',#8002,.T.);
#6265=FACE_OUTER_BOUND('',#8003,.T.);
#6266=FACE_OUTER_BOUND('',#8004,.T.);
#6267=FACE_OUTER_BOUND('',#8005,.T.);
#6268=FACE_OUTER_BOUND('',#8006,.T.);
#6269=FACE_OUTER_BOUND('',#8007,.T.);
#6270=FACE_OUTER_BOUND('',#8008,.T.);
#6271=FACE_OUTER_BOUND('',#8009,.T.);
#6272=FACE_OUTER_BOUND('',#8010,.T.);
#6273=FACE_OUTER_BOUND('',#8011,.T.);
#6274=FACE_OUTER_BOUND('',#8012,.T.);
#6275=FACE_OUTER_BOUND('',#8013,.T.);
#6276=FACE_OUTER_BOUND('',#8014,.T.);
#6277=FACE_OUTER_BOUND('',#8015,.T.);
#6278=FACE_OUTER_BOUND('',#8016,.T.);
#6279=FACE_OUTER_BOUND('',#8017,.T.);
#6280=FACE_OUTER_BOUND('',#8018,.T.);
#6281=FACE_OUTER_BOUND('',#8019,.T.);
#6282=FACE_OUTER_BOUND('',#8020,.T.);
#6283=FACE_OUTER_BOUND('',#8021,.T.);
#6284=FACE_OUTER_BOUND('',#8022,.T.);
#6285=FACE_OUTER_BOUND('',#8023,.T.);
#6286=FACE_OUTER_BOUND('',#8024,.T.);
#6287=FACE_OUTER_BOUND('',#8025,.T.);
#6288=FACE_OUTER_BOUND('',#8026,.T.);
#6289=FACE_OUTER_BOUND('',#8027,.T.);
#6290=FACE_OUTER_BOUND('',#8028,.T.);
#6291=FACE_OUTER_BOUND('',#8029,.T.);
#6292=FACE_OUTER_BOUND('',#8030,.T.);
#6293=FACE_OUTER_BOUND('',#8031,.T.);
#6294=FACE_OUTER_BOUND('',#8032,.T.);
#6295=FACE_OUTER_BOUND('',#8033,.T.);
#6296=FACE_OUTER_BOUND('',#8034,.T.);
#6297=FACE_OUTER_BOUND('',#8035,.T.);
#7471=EDGE_LOOP('',(#23093,#23094,#23095,#23096,#23097,#23098,#23099));
#7472=EDGE_LOOP('',(#23100,#23101,#23102,#23103));
#7473=EDGE_LOOP('',(#23104,#23105,#23106,#23107));
#7474=EDGE_LOOP('',(#23108,#23109,#23110,#23111));
#7475=EDGE_LOOP('',(#23112,#23113,#23114,#23115));
#7476=EDGE_LOOP('',(#23116,#23117,#23118,#23119));
#7477=EDGE_LOOP('',(#23120,#23121,#23122,#23123));
#7478=EDGE_LOOP('',(#23124,#23125,#23126,#23127));
#7479=EDGE_LOOP('',(#23128,#23129,#23130,#23131));
#7480=EDGE_LOOP('',(#23132,#23133,#23134,#23135));
#7481=EDGE_LOOP('',(#23136,#23137,#23138,#23139));
#7482=EDGE_LOOP('',(#23140,#23141,#23142,#23143));
#7483=EDGE_LOOP('',(#23144,#23145,#23146,#23147));
#7484=EDGE_LOOP('',(#23148,#23149,#23150,#23151));
#7485=EDGE_LOOP('',(#23152,#23153,#23154,#23155));
#7486=EDGE_LOOP('',(#23156,#23157,#23158,#23159));
#7487=EDGE_LOOP('',(#23160,#23161,#23162,#23163));
#7488=EDGE_LOOP('',(#23164,#23165,#23166,#23167));
#7489=EDGE_LOOP('',(#23168,#23169,#23170,#23171));
#7490=EDGE_LOOP('',(#23172,#23173,#23174,#23175));
#7491=EDGE_LOOP('',(#23176,#23177,#23178,#23179));
#7492=EDGE_LOOP('',(#23180,#23181,#23182,#23183));
#7493=EDGE_LOOP('',(#23184,#23185,#23186,#23187));
#7494=EDGE_LOOP('',(#23188,#23189,#23190,#23191));
#7495=EDGE_LOOP('',(#23192,#23193,#23194,#23195));
#7496=EDGE_LOOP('',(#23196,#23197,#23198,#23199));
#7497=EDGE_LOOP('',(#23200,#23201,#23202,#23203));
#7498=EDGE_LOOP('',(#23204,#23205,#23206,#23207));
#7499=EDGE_LOOP('',(#23208,#23209,#23210));
#7500=EDGE_LOOP('',(#23211,#23212,#23213));
#7501=EDGE_LOOP('',(#23214,#23215,#23216,#23217));
#7502=EDGE_LOOP('',(#23218,#23219,#23220,#23221));
#7503=EDGE_LOOP('',(#23222,#23223,#23224,#23225));
#7504=EDGE_LOOP('',(#23226,#23227,#23228,#23229));
#7505=EDGE_LOOP('',(#23230,#23231,#23232,#23233));
#7506=EDGE_LOOP('',(#23234,#23235,#23236,#23237));
#7507=EDGE_LOOP('',(#23238,#23239,#23240,#23241));
#7508=EDGE_LOOP('',(#23242,#23243,#23244,#23245));
#7509=EDGE_LOOP('',(#23246,#23247,#23248,#23249));
#7510=EDGE_LOOP('',(#23250,#23251,#23252,#23253));
#7511=EDGE_LOOP('',(#23254,#23255,#23256,#23257));
#7512=EDGE_LOOP('',(#23258,#23259,#23260,#23261));
#7513=EDGE_LOOP('',(#23262,#23263,#23264,#23265));
#7514=EDGE_LOOP('',(#23266,#23267,#23268,#23269));
#7515=EDGE_LOOP('',(#23270,#23271,#23272,#23273));
#7516=EDGE_LOOP('',(#23274,#23275,#23276,#23277));
#7517=EDGE_LOOP('',(#23278,#23279,#23280,#23281));
#7518=EDGE_LOOP('',(#23282,#23283,#23284,#23285));
#7519=EDGE_LOOP('',(#23286,#23287,#23288,#23289));
#7520=EDGE_LOOP('',(#23290,#23291,#23292,#23293));
#7521=EDGE_LOOP('',(#23294,#23295,#23296,#23297));
#7522=EDGE_LOOP('',(#23298,#23299,#23300,#23301));
#7523=EDGE_LOOP('',(#23302,#23303,#23304,#23305));
#7524=EDGE_LOOP('',(#23306,#23307,#23308,#23309));
#7525=EDGE_LOOP('',(#23310,#23311,#23312,#23313));
#7526=EDGE_LOOP('',(#23314,#23315,#23316,#23317));
#7527=EDGE_LOOP('',(#23318,#23319,#23320,#23321));
#7528=EDGE_LOOP('',(#23322,#23323,#23324,#23325));
#7529=EDGE_LOOP('',(#23326,#23327,#23328,#23329));
#7530=EDGE_LOOP('',(#23330,#23331,#23332));
#7531=EDGE_LOOP('',(#23333,#23334,#23335,#23336,#23337));
#7532=EDGE_LOOP('',(#23338,#23339,#23340,#23341));
#7533=EDGE_LOOP('',(#23342,#23343,#23344,#23345));
#7534=EDGE_LOOP('',(#23346,#23347,#23348,#23349));
#7535=EDGE_LOOP('',(#23350,#23351,#23352,#23353));
#7536=EDGE_LOOP('',(#23354,#23355,#23356,#23357));
#7537=EDGE_LOOP('',(#23358,#23359,#23360,#23361));
#7538=EDGE_LOOP('',(#23362,#23363,#23364,#23365));
#7539=EDGE_LOOP('',(#23366,#23367,#23368,#23369));
#7540=EDGE_LOOP('',(#23370,#23371,#23372,#23373));
#7541=EDGE_LOOP('',(#23374,#23375,#23376,#23377));
#7542=EDGE_LOOP('',(#23378,#23379,#23380,#23381));
#7543=EDGE_LOOP('',(#23382,#23383,#23384,#23385));
#7544=EDGE_LOOP('',(#23386,#23387,#23388,#23389));
#7545=EDGE_LOOP('',(#23390,#23391,#23392,#23393));
#7546=EDGE_LOOP('',(#23394,#23395,#23396,#23397));
#7547=EDGE_LOOP('',(#23398,#23399,#23400,#23401));
#7548=EDGE_LOOP('',(#23402,#23403,#23404,#23405,#23406,#23407,#23408,#23409,
#23410,#23411));
#7549=EDGE_LOOP('',(#23412,#23413,#23414,#23415));
#7550=EDGE_LOOP('',(#23416,#23417,#23418,#23419,#23420,#23421,#23422,#23423,
#23424,#23425,#23426,#23427,#23428,#23429,#23430,#23431,#23432,#23433,#23434,
#23435,#23436,#23437,#23438,#23439,#23440,#23441,#23442,#23443,#23444,#23445,
#23446,#23447,#23448,#23449,#23450,#23451,#23452,#23453,#23454,#23455,#23456,
#23457,#23458,#23459,#23460,#23461,#23462,#23463,#23464,#23465,#23466,#23467,
#23468,#23469,#23470,#23471,#23472,#23473,#23474,#23475,#23476,#23477,#23478,
#23479,#23480,#23481,#23482,#23483,#23484,#23485,#23486,#23487,#23488,#23489,
#23490,#23491,#23492,#23493,#23494,#23495,#23496,#23497,#23498,#23499,#23500,
#23501,#23502,#23503,#23504,#23505,#23506,#23507,#23508,#23509,#23510,#23511,
#23512,#23513,#23514,#23515,#23516,#23517,#23518,#23519,#23520,#23521,#23522,
#23523,#23524,#23525,#23526,#23527,#23528,#23529,#23530,#23531,#23532,#23533,
#23534,#23535,#23536,#23537,#23538,#23539,#23540,#23541,#23542,#23543,#23544,
#23545,#23546,#23547,#23548,#23549,#23550,#23551,#23552,#23553,#23554,#23555,
#23556,#23557,#23558,#23559,#23560,#23561,#23562,#23563,#23564,#23565,#23566,
#23567,#23568,#23569,#23570,#23571,#23572,#23573,#23574,#23575,#23576,#23577,
#23578,#23579,#23580,#23581,#23582,#23583,#23584,#23585,#23586,#23587,#23588,
#23589,#23590,#23591,#23592,#23593,#23594,#23595,#23596,#23597,#23598,#23599,
#23600,#23601,#23602,#23603,#23604,#23605,#23606,#23607,#23608,#23609,#23610,
#23611,#23612,#23613,#23614,#23615,#23616,#23617,#23618,#23619,#23620,#23621,
#23622,#23623,#23624,#23625,#23626,#23627,#23628,#23629,#23630,#23631,#23632,
#23633,#23634,#23635,#23636,#23637,#23638,#23639,#23640,#23641,#23642,#23643,
#23644,#23645,#23646,#23647,#23648,#23649,#23650,#23651,#23652,#23653,#23654,
#23655,#23656,#23657,#23658,#23659,#23660,#23661,#23662,#23663,#23664,#23665,
#23666,#23667,#23668,#23669,#23670,#23671,#23672,#23673,#23674,#23675,#23676,
#23677,#23678,#23679,#23680,#23681,#23682,#23683,#23684,#23685,#23686,#23687,
#23688,#23689,#23690,#23691,#23692,#23693,#23694,#23695,#23696,#23697,#23698,
#23699,#23700,#23701,#23702,#23703,#23704,#23705,#23706,#23707,#23708,#23709,
#23710,#23711,#23712,#23713,#23714,#23715,#23716,#23717,#23718,#23719,#23720,
#23721,#23722,#23723,#23724,#23725,#23726,#23727,#23728,#23729,#23730,#23731,
#23732,#23733,#23734,#23735,#23736,#23737,#23738,#23739));
#7551=EDGE_LOOP('',(#23740,#23741,#23742,#23743,#23744,#23745,#23746,#23747,
#23748,#23749,#23750,#23751,#23752,#23753,#23754,#23755,#23756,#23757,#23758,
#23759,#23760,#23761,#23762,#23763,#23764,#23765,#23766,#23767,#23768,#23769,
#23770,#23771,#23772,#23773,#23774,#23775,#23776,#23777,#23778,#23779,#23780,
#23781,#23782,#23783,#23784,#23785,#23786,#23787,#23788,#23789,#23790,#23791,
#23792,#23793,#23794,#23795,#23796,#23797,#23798,#23799,#23800,#23801,#23802,
#23803,#23804,#23805,#23806,#23807,#23808,#23809,#23810,#23811,#23812,#23813,
#23814,#23815,#23816,#23817,#23818,#23819,#23820,#23821,#23822,#23823,#23824,
#23825,#23826,#23827,#23828,#23829,#23830,#23831,#23832,#23833,#23834,#23835,
#23836,#23837,#23838,#23839,#23840,#23841,#23842,#23843,#23844,#23845,#23846,
#23847,#23848,#23849,#23850,#23851,#23852,#23853,#23854,#23855,#23856,#23857,
#23858,#23859,#23860,#23861,#23862,#23863,#23864,#23865,#23866,#23867,#23868,
#23869,#23870,#23871,#23872,#23873,#23874,#23875,#23876,#23877,#23878,#23879,
#23880,#23881,#23882,#23883,#23884,#23885,#23886,#23887,#23888,#23889,#23890,
#23891,#23892,#23893,#23894,#23895,#23896,#23897,#23898,#23899,#23900,#23901,
#23902,#23903,#23904,#23905,#23906,#23907,#23908,#23909,#23910,#23911,#23912,
#23913,#23914,#23915,#23916,#23917,#23918,#23919,#23920,#23921,#23922,#23923,
#23924,#23925,#23926,#23927,#23928,#23929,#23930,#23931,#23932,#23933,#23934,
#23935,#23936,#23937,#23938,#23939,#23940,#23941,#23942,#23943,#23944,#23945,
#23946,#23947,#23948,#23949,#23950,#23951,#23952,#23953,#23954,#23955,#23956,
#23957,#23958,#23959,#23960,#23961,#23962,#23963,#23964,#23965,#23966,#23967,
#23968,#23969,#23970,#23971,#23972,#23973,#23974,#23975,#23976,#23977,#23978,
#23979,#23980,#23981,#23982,#23983,#23984,#23985,#23986,#23987,#23988,#23989,
#23990,#23991,#23992,#23993,#23994,#23995,#23996,#23997,#23998,#23999,#24000,
#24001,#24002,#24003,#24004,#24005,#24006,#24007,#24008,#24009,#24010,#24011,
#24012,#24013,#24014,#24015,#24016,#24017,#24018,#24019,#24020,#24021,#24022,
#24023,#24024,#24025,#24026,#24027,#24028,#24029,#24030,#24031,#24032,#24033,
#24034,#24035,#24036,#24037,#24038,#24039,#24040,#24041,#24042,#24043,#24044,
#24045,#24046,#24047,#24048,#24049,#24050,#24051,#24052,#24053,#24054,#24055,
#24056,#24057,#24058,#24059,#24060,#24061,#24062,#24063,#24064));
#7552=EDGE_LOOP('',(#24065,#24066,#24067,#24068,#24069));
#7553=EDGE_LOOP('',(#24070,#24071,#24072,#24073));
#7554=EDGE_LOOP('',(#24074,#24075,#24076,#24077));
#7555=EDGE_LOOP('',(#24078,#24079,#24080,#24081));
#7556=EDGE_LOOP('',(#24082,#24083,#24084,#24085));
#7557=EDGE_LOOP('',(#24086,#24087,#24088,#24089));
#7558=EDGE_LOOP('',(#24090,#24091,#24092,#24093));
#7559=EDGE_LOOP('',(#24094,#24095,#24096,#24097));
#7560=EDGE_LOOP('',(#24098,#24099,#24100,#24101));
#7561=EDGE_LOOP('',(#24102,#24103,#24104,#24105));
#7562=EDGE_LOOP('',(#24106,#24107,#24108,#24109));
#7563=EDGE_LOOP('',(#24110,#24111,#24112,#24113));
#7564=EDGE_LOOP('',(#24114,#24115,#24116,#24117));
#7565=EDGE_LOOP('',(#24118,#24119,#24120,#24121));
#7566=EDGE_LOOP('',(#24122,#24123,#24124,#24125));
#7567=EDGE_LOOP('',(#24126,#24127,#24128,#24129));
#7568=EDGE_LOOP('',(#24130,#24131,#24132,#24133));
#7569=EDGE_LOOP('',(#24134,#24135,#24136,#24137));
#7570=EDGE_LOOP('',(#24138,#24139,#24140,#24141));
#7571=EDGE_LOOP('',(#24142,#24143,#24144,#24145));
#7572=EDGE_LOOP('',(#24146,#24147,#24148,#24149));
#7573=EDGE_LOOP('',(#24150,#24151,#24152,#24153));
#7574=EDGE_LOOP('',(#24154,#24155,#24156,#24157));
#7575=EDGE_LOOP('',(#24158,#24159,#24160,#24161));
#7576=EDGE_LOOP('',(#24162,#24163,#24164,#24165));
#7577=EDGE_LOOP('',(#24166,#24167,#24168,#24169));
#7578=EDGE_LOOP('',(#24170,#24171,#24172,#24173));
#7579=EDGE_LOOP('',(#24174,#24175,#24176,#24177));
#7580=EDGE_LOOP('',(#24178,#24179,#24180,#24181));
#7581=EDGE_LOOP('',(#24182,#24183,#24184,#24185));
#7582=EDGE_LOOP('',(#24186,#24187,#24188,#24189));
#7583=EDGE_LOOP('',(#24190,#24191,#24192,#24193));
#7584=EDGE_LOOP('',(#24194,#24195,#24196,#24197));
#7585=EDGE_LOOP('',(#24198,#24199,#24200,#24201));
#7586=EDGE_LOOP('',(#24202,#24203,#24204,#24205));
#7587=EDGE_LOOP('',(#24206,#24207,#24208,#24209));
#7588=EDGE_LOOP('',(#24210,#24211,#24212,#24213));
#7589=EDGE_LOOP('',(#24214,#24215,#24216,#24217));
#7590=EDGE_LOOP('',(#24218,#24219,#24220,#24221));
#7591=EDGE_LOOP('',(#24222,#24223,#24224,#24225));
#7592=EDGE_LOOP('',(#24226,#24227,#24228,#24229));
#7593=EDGE_LOOP('',(#24230,#24231,#24232,#24233));
#7594=EDGE_LOOP('',(#24234,#24235,#24236,#24237));
#7595=EDGE_LOOP('',(#24238,#24239,#24240,#24241));
#7596=EDGE_LOOP('',(#24242,#24243,#24244,#24245));
#7597=EDGE_LOOP('',(#24246,#24247,#24248,#24249));
#7598=EDGE_LOOP('',(#24250,#24251,#24252,#24253));
#7599=EDGE_LOOP('',(#24254,#24255,#24256,#24257));
#7600=EDGE_LOOP('',(#24258,#24259,#24260,#24261));
#7601=EDGE_LOOP('',(#24262,#24263,#24264,#24265));
#7602=EDGE_LOOP('',(#24266,#24267,#24268,#24269));
#7603=EDGE_LOOP('',(#24270,#24271,#24272,#24273));
#7604=EDGE_LOOP('',(#24274,#24275,#24276,#24277));
#7605=EDGE_LOOP('',(#24278,#24279,#24280,#24281));
#7606=EDGE_LOOP('',(#24282,#24283,#24284,#24285));
#7607=EDGE_LOOP('',(#24286,#24287,#24288,#24289));
#7608=EDGE_LOOP('',(#24290,#24291,#24292,#24293));
#7609=EDGE_LOOP('',(#24294,#24295,#24296,#24297));
#7610=EDGE_LOOP('',(#24298,#24299,#24300,#24301));
#7611=EDGE_LOOP('',(#24302,#24303,#24304,#24305));
#7612=EDGE_LOOP('',(#24306,#24307,#24308,#24309));
#7613=EDGE_LOOP('',(#24310,#24311,#24312,#24313));
#7614=EDGE_LOOP('',(#24314,#24315,#24316,#24317));
#7615=EDGE_LOOP('',(#24318,#24319,#24320,#24321));
#7616=EDGE_LOOP('',(#24322,#24323,#24324,#24325));
#7617=EDGE_LOOP('',(#24326,#24327,#24328,#24329));
#7618=EDGE_LOOP('',(#24330,#24331,#24332,#24333));
#7619=EDGE_LOOP('',(#24334,#24335,#24336,#24337));
#7620=EDGE_LOOP('',(#24338,#24339,#24340,#24341));
#7621=EDGE_LOOP('',(#24342,#24343,#24344,#24345));
#7622=EDGE_LOOP('',(#24346,#24347,#24348,#24349));
#7623=EDGE_LOOP('',(#24350,#24351,#24352,#24353));
#7624=EDGE_LOOP('',(#24354,#24355,#24356,#24357));
#7625=EDGE_LOOP('',(#24358,#24359,#24360,#24361));
#7626=EDGE_LOOP('',(#24362,#24363,#24364,#24365));
#7627=EDGE_LOOP('',(#24366,#24367,#24368,#24369));
#7628=EDGE_LOOP('',(#24370,#24371,#24372,#24373));
#7629=EDGE_LOOP('',(#24374,#24375,#24376,#24377));
#7630=EDGE_LOOP('',(#24378,#24379,#24380,#24381));
#7631=EDGE_LOOP('',(#24382,#24383,#24384,#24385));
#7632=EDGE_LOOP('',(#24386,#24387,#24388,#24389));
#7633=EDGE_LOOP('',(#24390,#24391,#24392,#24393));
#7634=EDGE_LOOP('',(#24394,#24395,#24396,#24397));
#7635=EDGE_LOOP('',(#24398,#24399,#24400,#24401));
#7636=EDGE_LOOP('',(#24402,#24403,#24404,#24405));
#7637=EDGE_LOOP('',(#24406,#24407,#24408,#24409));
#7638=EDGE_LOOP('',(#24410,#24411,#24412,#24413));
#7639=EDGE_LOOP('',(#24414,#24415,#24416,#24417));
#7640=EDGE_LOOP('',(#24418,#24419,#24420,#24421));
#7641=EDGE_LOOP('',(#24422,#24423,#24424,#24425));
#7642=EDGE_LOOP('',(#24426,#24427,#24428,#24429));
#7643=EDGE_LOOP('',(#24430,#24431,#24432,#24433));
#7644=EDGE_LOOP('',(#24434,#24435,#24436,#24437));
#7645=EDGE_LOOP('',(#24438,#24439,#24440,#24441));
#7646=EDGE_LOOP('',(#24442,#24443,#24444,#24445));
#7647=EDGE_LOOP('',(#24446,#24447,#24448,#24449));
#7648=EDGE_LOOP('',(#24450,#24451,#24452,#24453));
#7649=EDGE_LOOP('',(#24454,#24455,#24456,#24457));
#7650=EDGE_LOOP('',(#24458,#24459,#24460,#24461));
#7651=EDGE_LOOP('',(#24462,#24463,#24464,#24465));
#7652=EDGE_LOOP('',(#24466,#24467,#24468,#24469));
#7653=EDGE_LOOP('',(#24470,#24471,#24472,#24473));
#7654=EDGE_LOOP('',(#24474,#24475,#24476,#24477));
#7655=EDGE_LOOP('',(#24478,#24479,#24480,#24481));
#7656=EDGE_LOOP('',(#24482,#24483,#24484,#24485));
#7657=EDGE_LOOP('',(#24486,#24487,#24488,#24489));
#7658=EDGE_LOOP('',(#24490,#24491,#24492,#24493));
#7659=EDGE_LOOP('',(#24494,#24495,#24496,#24497));
#7660=EDGE_LOOP('',(#24498,#24499,#24500,#24501));
#7661=EDGE_LOOP('',(#24502,#24503,#24504,#24505));
#7662=EDGE_LOOP('',(#24506,#24507,#24508,#24509));
#7663=EDGE_LOOP('',(#24510,#24511,#24512,#24513));
#7664=EDGE_LOOP('',(#24514,#24515,#24516,#24517));
#7665=EDGE_LOOP('',(#24518,#24519,#24520,#24521));
#7666=EDGE_LOOP('',(#24522,#24523,#24524,#24525));
#7667=EDGE_LOOP('',(#24526,#24527,#24528,#24529));
#7668=EDGE_LOOP('',(#24530,#24531,#24532,#24533));
#7669=EDGE_LOOP('',(#24534,#24535,#24536,#24537));
#7670=EDGE_LOOP('',(#24538,#24539,#24540,#24541));
#7671=EDGE_LOOP('',(#24542,#24543,#24544,#24545));
#7672=EDGE_LOOP('',(#24546,#24547,#24548,#24549));
#7673=EDGE_LOOP('',(#24550,#24551,#24552,#24553));
#7674=EDGE_LOOP('',(#24554,#24555,#24556,#24557));
#7675=EDGE_LOOP('',(#24558,#24559,#24560,#24561));
#7676=EDGE_LOOP('',(#24562,#24563,#24564,#24565));
#7677=EDGE_LOOP('',(#24566,#24567,#24568,#24569));
#7678=EDGE_LOOP('',(#24570,#24571,#24572,#24573));
#7679=EDGE_LOOP('',(#24574,#24575,#24576,#24577));
#7680=EDGE_LOOP('',(#24578,#24579,#24580,#24581));
#7681=EDGE_LOOP('',(#24582,#24583,#24584,#24585));
#7682=EDGE_LOOP('',(#24586,#24587,#24588,#24589));
#7683=EDGE_LOOP('',(#24590,#24591,#24592,#24593));
#7684=EDGE_LOOP('',(#24594,#24595,#24596,#24597));
#7685=EDGE_LOOP('',(#24598,#24599,#24600,#24601));
#7686=EDGE_LOOP('',(#24602,#24603,#24604,#24605));
#7687=EDGE_LOOP('',(#24606,#24607,#24608,#24609));
#7688=EDGE_LOOP('',(#24610,#24611,#24612,#24613));
#7689=EDGE_LOOP('',(#24614,#24615,#24616,#24617));
#7690=EDGE_LOOP('',(#24618,#24619,#24620,#24621));
#7691=EDGE_LOOP('',(#24622,#24623,#24624,#24625));
#7692=EDGE_LOOP('',(#24626,#24627,#24628,#24629));
#7693=EDGE_LOOP('',(#24630,#24631,#24632,#24633));
#7694=EDGE_LOOP('',(#24634,#24635,#24636,#24637));
#7695=EDGE_LOOP('',(#24638,#24639,#24640,#24641));
#7696=EDGE_LOOP('',(#24642,#24643,#24644,#24645));
#7697=EDGE_LOOP('',(#24646,#24647,#24648,#24649));
#7698=EDGE_LOOP('',(#24650,#24651,#24652,#24653));
#7699=EDGE_LOOP('',(#24654,#24655,#24656,#24657));
#7700=EDGE_LOOP('',(#24658,#24659,#24660,#24661));
#7701=EDGE_LOOP('',(#24662,#24663,#24664,#24665));
#7702=EDGE_LOOP('',(#24666,#24667,#24668,#24669));
#7703=EDGE_LOOP('',(#24670,#24671,#24672,#24673));
#7704=EDGE_LOOP('',(#24674,#24675,#24676,#24677));
#7705=EDGE_LOOP('',(#24678,#24679,#24680,#24681));
#7706=EDGE_LOOP('',(#24682,#24683,#24684,#24685));
#7707=EDGE_LOOP('',(#24686,#24687,#24688,#24689));
#7708=EDGE_LOOP('',(#24690,#24691,#24692,#24693));
#7709=EDGE_LOOP('',(#24694,#24695,#24696,#24697));
#7710=EDGE_LOOP('',(#24698,#24699,#24700,#24701));
#7711=EDGE_LOOP('',(#24702,#24703,#24704,#24705));
#7712=EDGE_LOOP('',(#24706,#24707,#24708,#24709));
#7713=EDGE_LOOP('',(#24710,#24711,#24712,#24713));
#7714=EDGE_LOOP('',(#24714,#24715,#24716,#24717));
#7715=EDGE_LOOP('',(#24718,#24719,#24720,#24721));
#7716=EDGE_LOOP('',(#24722,#24723,#24724,#24725));
#7717=EDGE_LOOP('',(#24726,#24727,#24728,#24729));
#7718=EDGE_LOOP('',(#24730,#24731,#24732,#24733));
#7719=EDGE_LOOP('',(#24734,#24735,#24736,#24737));
#7720=EDGE_LOOP('',(#24738,#24739,#24740,#24741));
#7721=EDGE_LOOP('',(#24742,#24743,#24744,#24745));
#7722=EDGE_LOOP('',(#24746,#24747,#24748,#24749));
#7723=EDGE_LOOP('',(#24750,#24751,#24752,#24753));
#7724=EDGE_LOOP('',(#24754,#24755,#24756,#24757));
#7725=EDGE_LOOP('',(#24758,#24759,#24760,#24761));
#7726=EDGE_LOOP('',(#24762,#24763,#24764,#24765));
#7727=EDGE_LOOP('',(#24766,#24767,#24768,#24769));
#7728=EDGE_LOOP('',(#24770,#24771,#24772,#24773));
#7729=EDGE_LOOP('',(#24774,#24775,#24776,#24777));
#7730=EDGE_LOOP('',(#24778,#24779,#24780,#24781));
#7731=EDGE_LOOP('',(#24782,#24783,#24784,#24785));
#7732=EDGE_LOOP('',(#24786,#24787,#24788,#24789));
#7733=EDGE_LOOP('',(#24790,#24791,#24792,#24793));
#7734=EDGE_LOOP('',(#24794,#24795,#24796,#24797));
#7735=EDGE_LOOP('',(#24798,#24799,#24800,#24801));
#7736=EDGE_LOOP('',(#24802,#24803,#24804,#24805));
#7737=EDGE_LOOP('',(#24806,#24807,#24808,#24809));
#7738=EDGE_LOOP('',(#24810,#24811,#24812,#24813));
#7739=EDGE_LOOP('',(#24814,#24815,#24816,#24817));
#7740=EDGE_LOOP('',(#24818,#24819,#24820,#24821));
#7741=EDGE_LOOP('',(#24822,#24823,#24824,#24825));
#7742=EDGE_LOOP('',(#24826,#24827,#24828,#24829));
#7743=EDGE_LOOP('',(#24830,#24831,#24832,#24833));
#7744=EDGE_LOOP('',(#24834,#24835,#24836,#24837));
#7745=EDGE_LOOP('',(#24838,#24839,#24840,#24841));
#7746=EDGE_LOOP('',(#24842,#24843,#24844,#24845));
#7747=EDGE_LOOP('',(#24846,#24847,#24848,#24849));
#7748=EDGE_LOOP('',(#24850,#24851,#24852,#24853));
#7749=EDGE_LOOP('',(#24854,#24855,#24856,#24857));
#7750=EDGE_LOOP('',(#24858,#24859,#24860,#24861));
#7751=EDGE_LOOP('',(#24862,#24863,#24864,#24865));
#7752=EDGE_LOOP('',(#24866,#24867,#24868,#24869));
#7753=EDGE_LOOP('',(#24870,#24871,#24872,#24873));
#7754=EDGE_LOOP('',(#24874,#24875,#24876,#24877));
#7755=EDGE_LOOP('',(#24878,#24879,#24880,#24881));
#7756=EDGE_LOOP('',(#24882,#24883,#24884,#24885));
#7757=EDGE_LOOP('',(#24886,#24887,#24888,#24889));
#7758=EDGE_LOOP('',(#24890,#24891,#24892,#24893));
#7759=EDGE_LOOP('',(#24894,#24895,#24896,#24897));
#7760=EDGE_LOOP('',(#24898,#24899,#24900,#24901));
#7761=EDGE_LOOP('',(#24902,#24903,#24904,#24905));
#7762=EDGE_LOOP('',(#24906,#24907,#24908,#24909));
#7763=EDGE_LOOP('',(#24910,#24911,#24912,#24913));
#7764=EDGE_LOOP('',(#24914,#24915,#24916,#24917));
#7765=EDGE_LOOP('',(#24918,#24919,#24920,#24921));
#7766=EDGE_LOOP('',(#24922,#24923,#24924,#24925));
#7767=EDGE_LOOP('',(#24926,#24927,#24928,#24929));
#7768=EDGE_LOOP('',(#24930,#24931,#24932,#24933));
#7769=EDGE_LOOP('',(#24934,#24935,#24936,#24937));
#7770=EDGE_LOOP('',(#24938,#24939,#24940,#24941));
#7771=EDGE_LOOP('',(#24942,#24943,#24944,#24945));
#7772=EDGE_LOOP('',(#24946,#24947,#24948,#24949));
#7773=EDGE_LOOP('',(#24950,#24951,#24952,#24953));
#7774=EDGE_LOOP('',(#24954,#24955,#24956,#24957));
#7775=EDGE_LOOP('',(#24958,#24959,#24960,#24961));
#7776=EDGE_LOOP('',(#24962,#24963,#24964,#24965));
#7777=EDGE_LOOP('',(#24966,#24967,#24968,#24969));
#7778=EDGE_LOOP('',(#24970,#24971,#24972,#24973));
#7779=EDGE_LOOP('',(#24974,#24975,#24976,#24977));
#7780=EDGE_LOOP('',(#24978,#24979,#24980,#24981));
#7781=EDGE_LOOP('',(#24982,#24983,#24984,#24985));
#7782=EDGE_LOOP('',(#24986,#24987,#24988,#24989));
#7783=EDGE_LOOP('',(#24990,#24991,#24992,#24993));
#7784=EDGE_LOOP('',(#24994,#24995,#24996,#24997));
#7785=EDGE_LOOP('',(#24998,#24999,#25000,#25001));
#7786=EDGE_LOOP('',(#25002,#25003,#25004,#25005));
#7787=EDGE_LOOP('',(#25006,#25007,#25008,#25009));
#7788=EDGE_LOOP('',(#25010,#25011,#25012,#25013));
#7789=EDGE_LOOP('',(#25014,#25015,#25016,#25017));
#7790=EDGE_LOOP('',(#25018,#25019,#25020,#25021));
#7791=EDGE_LOOP('',(#25022,#25023,#25024,#25025));
#7792=EDGE_LOOP('',(#25026,#25027,#25028,#25029));
#7793=EDGE_LOOP('',(#25030,#25031,#25032));
#7794=EDGE_LOOP('',(#25033));
#7795=EDGE_LOOP('',(#25034));
#7796=EDGE_LOOP('',(#25035,#25036,#25037,#25038));
#7797=EDGE_LOOP('',(#25039,#25040,#25041,#25042));
#7798=EDGE_LOOP('',(#25043,#25044,#25045,#25046));
#7799=EDGE_LOOP('',(#25047));
#7800=EDGE_LOOP('',(#25048));
#7801=EDGE_LOOP('',(#25049,#25050,#25051,#25052,#25053,#25054));
#7802=EDGE_LOOP('',(#25055,#25056,#25057,#25058));
#7803=EDGE_LOOP('',(#25059,#25060,#25061,#25062));
#7804=EDGE_LOOP('',(#25063,#25064,#25065,#25066));
#7805=EDGE_LOOP('',(#25067,#25068,#25069,#25070,#25071));
#7806=EDGE_LOOP('',(#25072,#25073,#25074,#25075));
#7807=EDGE_LOOP('',(#25076,#25077,#25078,#25079));
#7808=EDGE_LOOP('',(#25080,#25081,#25082,#25083,#25084,#25085,#25086,#25087,
#25088,#25089,#25090,#25091,#25092,#25093,#25094,#25095,#25096,#25097,#25098,
#25099,#25100,#25101,#25102,#25103,#25104,#25105,#25106,#25107,#25108,#25109,
#25110,#25111,#25112,#25113,#25114,#25115,#25116,#25117,#25118,#25119,#25120,
#25121,#25122,#25123,#25124,#25125,#25126,#25127,#25128,#25129,#25130,#25131,
#25132,#25133,#25134,#25135,#25136,#25137,#25138,#25139,#25140,#25141));
#7809=EDGE_LOOP('',(#25142,#25143,#25144,#25145,#25146,#25147,#25148,#25149,
#25150,#25151,#25152,#25153,#25154,#25155,#25156,#25157,#25158,#25159,#25160,
#25161,#25162,#25163,#25164,#25165,#25166,#25167,#25168,#25169,#25170,#25171,
#25172,#25173,#25174,#25175,#25176,#25177,#25178,#25179,#25180,#25181,#25182,
#25183,#25184,#25185,#25186,#25187,#25188,#25189,#25190,#25191,#25192,#25193,
#25194,#25195,#25196,#25197,#25198,#25199,#25200,#25201,#25202));
#7810=EDGE_LOOP('',(#25203,#25204,#25205,#25206));
#7811=EDGE_LOOP('',(#25207,#25208,#25209,#25210,#25211,#25212));
#7812=EDGE_LOOP('',(#25213,#25214,#25215,#25216,#25217));
#7813=EDGE_LOOP('',(#25218,#25219,#25220,#25221,#25222,#25223));
#7814=EDGE_LOOP('',(#25224,#25225,#25226,#25227,#25228,#25229));
#7815=EDGE_LOOP('',(#25230,#25231,#25232,#25233));
#7816=EDGE_LOOP('',(#25234,#25235,#25236,#25237,#25238,#25239));
#7817=EDGE_LOOP('',(#25240,#25241,#25242,#25243,#25244,#25245));
#7818=EDGE_LOOP('',(#25246,#25247,#25248,#25249));
#7819=EDGE_LOOP('',(#25250,#25251,#25252,#25253,#25254,#25255));
#7820=EDGE_LOOP('',(#25256,#25257,#25258,#25259,#25260,#25261));
#7821=EDGE_LOOP('',(#25262,#25263,#25264,#25265));
#7822=EDGE_LOOP('',(#25266,#25267,#25268,#25269,#25270,#25271));
#7823=EDGE_LOOP('',(#25272,#25273,#25274,#25275,#25276,#25277));
#7824=EDGE_LOOP('',(#25278,#25279,#25280,#25281));
#7825=EDGE_LOOP('',(#25282,#25283,#25284,#25285,#25286,#25287));
#7826=EDGE_LOOP('',(#25288,#25289,#25290,#25291,#25292,#25293));
#7827=EDGE_LOOP('',(#25294,#25295,#25296,#25297));
#7828=EDGE_LOOP('',(#25298,#25299,#25300,#25301,#25302,#25303));
#7829=EDGE_LOOP('',(#25304,#25305,#25306,#25307,#25308,#25309));
#7830=EDGE_LOOP('',(#25310,#25311,#25312,#25313));
#7831=EDGE_LOOP('',(#25314,#25315,#25316,#25317,#25318,#25319));
#7832=EDGE_LOOP('',(#25320,#25321,#25322,#25323,#25324,#25325));
#7833=EDGE_LOOP('',(#25326,#25327,#25328,#25329,#25330,#25331));
#7834=EDGE_LOOP('',(#25332,#25333,#25334,#25335,#25336,#25337));
#7835=EDGE_LOOP('',(#25338,#25339,#25340,#25341,#25342,#25343));
#7836=EDGE_LOOP('',(#25344,#25345,#25346,#25347,#25348,#25349));
#7837=EDGE_LOOP('',(#25350,#25351,#25352,#25353,#25354,#25355));
#7838=EDGE_LOOP('',(#25356,#25357,#25358,#25359,#25360,#25361));
#7839=EDGE_LOOP('',(#25362,#25363,#25364,#25365,#25366,#25367));
#7840=EDGE_LOOP('',(#25368,#25369,#25370,#25371,#25372,#25373));
#7841=EDGE_LOOP('',(#25374,#25375,#25376,#25377,#25378,#25379));
#7842=EDGE_LOOP('',(#25380,#25381,#25382,#25383,#25384,#25385));
#7843=EDGE_LOOP('',(#25386,#25387,#25388,#25389,#25390,#25391));
#7844=EDGE_LOOP('',(#25392,#25393,#25394,#25395,#25396,#25397));
#7845=EDGE_LOOP('',(#25398,#25399,#25400,#25401,#25402,#25403));
#7846=EDGE_LOOP('',(#25404,#25405,#25406,#25407,#25408,#25409));
#7847=EDGE_LOOP('',(#25410,#25411,#25412,#25413,#25414,#25415));
#7848=EDGE_LOOP('',(#25416,#25417,#25418,#25419,#25420,#25421));
#7849=EDGE_LOOP('',(#25422,#25423,#25424,#25425,#25426,#25427));
#7850=EDGE_LOOP('',(#25428,#25429,#25430,#25431,#25432,#25433));
#7851=EDGE_LOOP('',(#25434,#25435,#25436,#25437));
#7852=EDGE_LOOP('',(#25438,#25439,#25440,#25441,#25442,#25443));
#7853=EDGE_LOOP('',(#25444,#25445,#25446,#25447,#25448,#25449));
#7854=EDGE_LOOP('',(#25450,#25451,#25452,#25453));
#7855=EDGE_LOOP('',(#25454,#25455,#25456,#25457,#25458,#25459));
#7856=EDGE_LOOP('',(#25460,#25461,#25462,#25463,#25464,#25465));
#7857=EDGE_LOOP('',(#25466,#25467,#25468,#25469));
#7858=EDGE_LOOP('',(#25470,#25471,#25472,#25473,#25474,#25475));
#7859=EDGE_LOOP('',(#25476,#25477,#25478,#25479,#25480,#25481));
#7860=EDGE_LOOP('',(#25482,#25483,#25484,#25485));
#7861=EDGE_LOOP('',(#25486,#25487,#25488,#25489,#25490,#25491));
#7862=EDGE_LOOP('',(#25492,#25493,#25494,#25495,#25496,#25497));
#7863=EDGE_LOOP('',(#25498,#25499,#25500,#25501));
#7864=EDGE_LOOP('',(#25502,#25503,#25504,#25505,#25506,#25507));
#7865=EDGE_LOOP('',(#25508,#25509,#25510,#25511,#25512,#25513));
#7866=EDGE_LOOP('',(#25514,#25515,#25516,#25517));
#7867=EDGE_LOOP('',(#25518,#25519,#25520,#25521,#25522,#25523));
#7868=EDGE_LOOP('',(#25524,#25525,#25526,#25527,#25528,#25529));
#7869=EDGE_LOOP('',(#25530,#25531,#25532,#25533));
#7870=EDGE_LOOP('',(#25534,#25535,#25536,#25537,#25538,#25539));
#7871=EDGE_LOOP('',(#25540,#25541,#25542,#25543,#25544,#25545));
#7872=EDGE_LOOP('',(#25546,#25547,#25548,#25549));
#7873=EDGE_LOOP('',(#25550,#25551,#25552,#25553,#25554,#25555));
#7874=EDGE_LOOP('',(#25556,#25557,#25558,#25559,#25560,#25561));
#7875=EDGE_LOOP('',(#25562,#25563,#25564,#25565));
#7876=EDGE_LOOP('',(#25566,#25567,#25568,#25569,#25570,#25571));
#7877=EDGE_LOOP('',(#25572,#25573,#25574,#25575,#25576,#25577));
#7878=EDGE_LOOP('',(#25578,#25579,#25580,#25581));
#7879=EDGE_LOOP('',(#25582,#25583,#25584,#25585,#25586,#25587));
#7880=EDGE_LOOP('',(#25588,#25589,#25590,#25591,#25592,#25593));
#7881=EDGE_LOOP('',(#25594,#25595,#25596,#25597));
#7882=EDGE_LOOP('',(#25598,#25599,#25600,#25601,#25602,#25603));
#7883=EDGE_LOOP('',(#25604,#25605,#25606,#25607,#25608,#25609));
#7884=EDGE_LOOP('',(#25610,#25611,#25612,#25613));
#7885=EDGE_LOOP('',(#25614,#25615,#25616,#25617,#25618,#25619));
#7886=EDGE_LOOP('',(#25620,#25621,#25622,#25623,#25624,#25625));
#7887=EDGE_LOOP('',(#25626,#25627,#25628,#25629));
#7888=EDGE_LOOP('',(#25630,#25631,#25632,#25633,#25634,#25635));
#7889=EDGE_LOOP('',(#25636,#25637,#25638,#25639,#25640,#25641));
#7890=EDGE_LOOP('',(#25642,#25643,#25644,#25645));
#7891=EDGE_LOOP('',(#25646,#25647,#25648,#25649,#25650,#25651));
#7892=EDGE_LOOP('',(#25652,#25653,#25654,#25655,#25656,#25657));
#7893=EDGE_LOOP('',(#25658,#25659,#25660,#25661));
#7894=EDGE_LOOP('',(#25662,#25663,#25664,#25665,#25666,#25667));
#7895=EDGE_LOOP('',(#25668,#25669,#25670,#25671,#25672,#25673));
#7896=EDGE_LOOP('',(#25674,#25675,#25676,#25677));
#7897=EDGE_LOOP('',(#25678,#25679,#25680,#25681,#25682,#25683));
#7898=EDGE_LOOP('',(#25684,#25685,#25686,#25687,#25688,#25689));
#7899=EDGE_LOOP('',(#25690,#25691,#25692,#25693));
#7900=EDGE_LOOP('',(#25694,#25695,#25696,#25697,#25698,#25699));
#7901=EDGE_LOOP('',(#25700,#25701,#25702,#25703,#25704,#25705));
#7902=EDGE_LOOP('',(#25706,#25707,#25708,#25709));
#7903=EDGE_LOOP('',(#25710,#25711,#25712,#25713,#25714,#25715));
#7904=EDGE_LOOP('',(#25716,#25717,#25718,#25719,#25720,#25721));
#7905=EDGE_LOOP('',(#25722,#25723,#25724,#25725));
#7906=EDGE_LOOP('',(#25726,#25727,#25728,#25729,#25730,#25731));
#7907=EDGE_LOOP('',(#25732,#25733,#25734,#25735,#25736,#25737));
#7908=EDGE_LOOP('',(#25738,#25739,#25740,#25741));
#7909=EDGE_LOOP('',(#25742,#25743,#25744,#25745,#25746,#25747));
#7910=EDGE_LOOP('',(#25748,#25749,#25750,#25751,#25752,#25753));
#7911=EDGE_LOOP('',(#25754,#25755,#25756,#25757));
#7912=EDGE_LOOP('',(#25758,#25759,#25760,#25761,#25762,#25763));
#7913=EDGE_LOOP('',(#25764,#25765,#25766,#25767,#25768,#25769));
#7914=EDGE_LOOP('',(#25770,#25771,#25772,#25773));
#7915=EDGE_LOOP('',(#25774,#25775,#25776,#25777,#25778,#25779));
#7916=EDGE_LOOP('',(#25780,#25781,#25782,#25783,#25784,#25785));
#7917=EDGE_LOOP('',(#25786,#25787,#25788,#25789));
#7918=EDGE_LOOP('',(#25790,#25791,#25792,#25793,#25794,#25795));
#7919=EDGE_LOOP('',(#25796,#25797,#25798,#25799,#25800,#25801));
#7920=EDGE_LOOP('',(#25802,#25803,#25804,#25805));
#7921=EDGE_LOOP('',(#25806,#25807,#25808,#25809,#25810,#25811));
#7922=EDGE_LOOP('',(#25812,#25813,#25814,#25815,#25816,#25817));
#7923=EDGE_LOOP('',(#25818,#25819,#25820,#25821));
#7924=EDGE_LOOP('',(#25822,#25823,#25824,#25825,#25826,#25827));
#7925=EDGE_LOOP('',(#25828,#25829,#25830,#25831,#25832,#25833));
#7926=EDGE_LOOP('',(#25834,#25835,#25836,#25837));
#7927=EDGE_LOOP('',(#25838,#25839,#25840,#25841,#25842,#25843));
#7928=EDGE_LOOP('',(#25844,#25845,#25846,#25847,#25848,#25849));
#7929=EDGE_LOOP('',(#25850,#25851,#25852,#25853));
#7930=EDGE_LOOP('',(#25854,#25855,#25856,#25857,#25858,#25859));
#7931=EDGE_LOOP('',(#25860,#25861,#25862,#25863,#25864,#25865));
#7932=EDGE_LOOP('',(#25866,#25867,#25868,#25869));
#7933=EDGE_LOOP('',(#25870,#25871,#25872,#25873,#25874,#25875));
#7934=EDGE_LOOP('',(#25876,#25877,#25878,#25879,#25880,#25881));
#7935=EDGE_LOOP('',(#25882,#25883,#25884,#25885));
#7936=EDGE_LOOP('',(#25886,#25887,#25888,#25889,#25890,#25891));
#7937=EDGE_LOOP('',(#25892,#25893,#25894,#25895,#25896,#25897));
#7938=EDGE_LOOP('',(#25898,#25899,#25900,#25901));
#7939=EDGE_LOOP('',(#25902,#25903,#25904,#25905,#25906,#25907));
#7940=EDGE_LOOP('',(#25908,#25909,#25910,#25911,#25912,#25913));
#7941=EDGE_LOOP('',(#25914,#25915,#25916,#25917));
#7942=EDGE_LOOP('',(#25918,#25919,#25920,#25921,#25922,#25923));
#7943=EDGE_LOOP('',(#25924,#25925,#25926,#25927,#25928,#25929));
#7944=EDGE_LOOP('',(#25930,#25931,#25932,#25933));
#7945=EDGE_LOOP('',(#25934,#25935,#25936,#25937,#25938,#25939));
#7946=EDGE_LOOP('',(#25940,#25941,#25942,#25943,#25944,#25945));
#7947=EDGE_LOOP('',(#25946,#25947,#25948,#25949));
#7948=EDGE_LOOP('',(#25950,#25951,#25952,#25953,#25954,#25955));
#7949=EDGE_LOOP('',(#25956,#25957,#25958,#25959,#25960,#25961));
#7950=EDGE_LOOP('',(#25962,#25963,#25964,#25965));
#7951=EDGE_LOOP('',(#25966,#25967,#25968,#25969,#25970,#25971));
#7952=EDGE_LOOP('',(#25972,#25973,#25974,#25975,#25976,#25977));
#7953=EDGE_LOOP('',(#25978,#25979,#25980,#25981));
#7954=EDGE_LOOP('',(#25982,#25983,#25984,#25985,#25986,#25987));
#7955=EDGE_LOOP('',(#25988,#25989,#25990,#25991,#25992,#25993));
#7956=EDGE_LOOP('',(#25994,#25995,#25996,#25997));
#7957=EDGE_LOOP('',(#25998,#25999,#26000,#26001,#26002,#26003));
#7958=EDGE_LOOP('',(#26004,#26005,#26006,#26007,#26008,#26009));
#7959=EDGE_LOOP('',(#26010,#26011,#26012,#26013));
#7960=EDGE_LOOP('',(#26014,#26015,#26016,#26017,#26018,#26019));
#7961=EDGE_LOOP('',(#26020,#26021,#26022,#26023,#26024,#26025));
#7962=EDGE_LOOP('',(#26026,#26027,#26028,#26029));
#7963=EDGE_LOOP('',(#26030,#26031,#26032,#26033,#26034,#26035));
#7964=EDGE_LOOP('',(#26036,#26037,#26038,#26039,#26040,#26041));
#7965=EDGE_LOOP('',(#26042,#26043,#26044,#26045,#26046));
#7966=EDGE_LOOP('',(#26047,#26048,#26049,#26050,#26051,#26052));
#7967=EDGE_LOOP('',(#26053,#26054,#26055,#26056,#26057,#26058));
#7968=EDGE_LOOP('',(#26059,#26060,#26061,#26062));
#7969=EDGE_LOOP('',(#26063,#26064,#26065,#26066,#26067,#26068));
#7970=EDGE_LOOP('',(#26069,#26070,#26071,#26072,#26073,#26074));
#7971=EDGE_LOOP('',(#26075,#26076,#26077,#26078));
#7972=EDGE_LOOP('',(#26079,#26080,#26081,#26082,#26083,#26084));
#7973=EDGE_LOOP('',(#26085,#26086,#26087,#26088,#26089,#26090));
#7974=EDGE_LOOP('',(#26091,#26092,#26093,#26094));
#7975=EDGE_LOOP('',(#26095,#26096,#26097,#26098,#26099,#26100));
#7976=EDGE_LOOP('',(#26101,#26102,#26103,#26104,#26105,#26106));
#7977=EDGE_LOOP('',(#26107,#26108,#26109,#26110));
#7978=EDGE_LOOP('',(#26111,#26112,#26113,#26114,#26115,#26116));
#7979=EDGE_LOOP('',(#26117,#26118,#26119,#26120,#26121,#26122));
#7980=EDGE_LOOP('',(#26123,#26124,#26125,#26126));
#7981=EDGE_LOOP('',(#26127,#26128,#26129,#26130,#26131,#26132));
#7982=EDGE_LOOP('',(#26133,#26134,#26135,#26136,#26137,#26138));
#7983=EDGE_LOOP('',(#26139,#26140,#26141,#26142));
#7984=EDGE_LOOP('',(#26143,#26144,#26145,#26146,#26147,#26148));
#7985=EDGE_LOOP('',(#26149,#26150,#26151,#26152,#26153,#26154));
#7986=EDGE_LOOP('',(#26155,#26156,#26157,#26158));
#7987=EDGE_LOOP('',(#26159,#26160,#26161,#26162,#26163,#26164));
#7988=EDGE_LOOP('',(#26165,#26166,#26167,#26168,#26169,#26170));
#7989=EDGE_LOOP('',(#26171,#26172,#26173,#26174));
#7990=EDGE_LOOP('',(#26175,#26176,#26177,#26178,#26179,#26180));
#7991=EDGE_LOOP('',(#26181,#26182,#26183,#26184,#26185,#26186));
#7992=EDGE_LOOP('',(#26187,#26188,#26189,#26190));
#7993=EDGE_LOOP('',(#26191,#26192,#26193,#26194,#26195,#26196));
#7994=EDGE_LOOP('',(#26197,#26198,#26199,#26200,#26201,#26202));
#7995=EDGE_LOOP('',(#26203,#26204,#26205,#26206));
#7996=EDGE_LOOP('',(#26207,#26208,#26209,#26210,#26211,#26212));
#7997=EDGE_LOOP('',(#26213,#26214,#26215,#26216,#26217,#26218));
#7998=EDGE_LOOP('',(#26219,#26220,#26221,#26222));
#7999=EDGE_LOOP('',(#26223,#26224,#26225,#26226,#26227,#26228));
#8000=EDGE_LOOP('',(#26229,#26230,#26231,#26232,#26233,#26234));
#8001=EDGE_LOOP('',(#26235,#26236,#26237,#26238));
#8002=EDGE_LOOP('',(#26239,#26240,#26241,#26242,#26243,#26244));
#8003=EDGE_LOOP('',(#26245,#26246,#26247,#26248,#26249,#26250));
#8004=EDGE_LOOP('',(#26251,#26252,#26253,#26254));
#8005=EDGE_LOOP('',(#26255,#26256,#26257,#26258,#26259,#26260));
#8006=EDGE_LOOP('',(#26261,#26262,#26263,#26264,#26265,#26266));
#8007=EDGE_LOOP('',(#26267,#26268,#26269,#26270));
#8008=EDGE_LOOP('',(#26271,#26272,#26273,#26274,#26275,#26276));
#8009=EDGE_LOOP('',(#26277,#26278,#26279,#26280,#26281,#26282));
#8010=EDGE_LOOP('',(#26283,#26284,#26285,#26286));
#8011=EDGE_LOOP('',(#26287,#26288,#26289,#26290,#26291,#26292));
#8012=EDGE_LOOP('',(#26293,#26294,#26295,#26296,#26297,#26298));
#8013=EDGE_LOOP('',(#26299,#26300,#26301,#26302));
#8014=EDGE_LOOP('',(#26303,#26304,#26305,#26306,#26307,#26308));
#8015=EDGE_LOOP('',(#26309,#26310,#26311,#26312,#26313,#26314));
#8016=EDGE_LOOP('',(#26315,#26316,#26317,#26318));
#8017=EDGE_LOOP('',(#26319,#26320,#26321,#26322,#26323,#26324));
#8018=EDGE_LOOP('',(#26325,#26326,#26327,#26328,#26329,#26330));
#8019=EDGE_LOOP('',(#26331,#26332,#26333,#26334));
#8020=EDGE_LOOP('',(#26335,#26336,#26337,#26338,#26339,#26340));
#8021=EDGE_LOOP('',(#26341,#26342,#26343,#26344,#26345,#26346));
#8022=EDGE_LOOP('',(#26347,#26348,#26349,#26350));
#8023=EDGE_LOOP('',(#26351,#26352,#26353,#26354,#26355,#26356));
#8024=EDGE_LOOP('',(#26357,#26358,#26359,#26360,#26361,#26362));
#8025=EDGE_LOOP('',(#26363,#26364,#26365,#26366,#26367,#26368));
#8026=EDGE_LOOP('',(#26369,#26370,#26371,#26372,#26373,#26374));
#8027=EDGE_LOOP('',(#26375,#26376,#26377,#26378,#26379,#26380));
#8028=EDGE_LOOP('',(#26381,#26382,#26383,#26384,#26385,#26386));
#8029=EDGE_LOOP('',(#26387,#26388,#26389,#26390,#26391,#26392));
#8030=EDGE_LOOP('',(#26393,#26394,#26395,#26396,#26397,#26398));
#8031=EDGE_LOOP('',(#26399,#26400,#26401,#26402,#26403,#26404));
#8032=EDGE_LOOP('',(#26405,#26406,#26407,#26408,#26409,#26410));
#8033=EDGE_LOOP('',(#26411,#26412,#26413,#26414,#26415,#26416));
#8034=EDGE_LOOP('',(#26417,#26418,#26419,#26420,#26421,#26422));
#8035=EDGE_LOOP('',(#26423,#26424,#26425,#26426,#26427,#26428));
#9053=LINE('',#55935,#10299);
#9054=LINE('',#55974,#10300);
#9055=LINE('',#56015,#10301);
#9056=LINE('',#56091,#10302);
#9057=LINE('',#56169,#10303);
#9058=LINE('',#56245,#10304);
#9059=LINE('',#56321,#10305);
#9060=LINE('',#56397,#10306);
#9061=LINE('',#56473,#10307);
#9062=LINE('',#56551,#10308);
#9063=LINE('',#56629,#10309);
#9064=LINE('',#56705,#10310);
#9065=LINE('',#56781,#10311);
#9066=LINE('',#56857,#10312);
#9067=LINE('',#56933,#10313);
#9068=LINE('',#57011,#10314);
#9069=LINE('',#57087,#10315);
#9070=LINE('',#57165,#10316);
#9071=LINE('',#57241,#10317);
#9072=LINE('',#57317,#10318);
#9073=LINE('',#57393,#10319);
#9074=LINE('',#57469,#10320);
#9075=LINE('',#57547,#10321);
#9076=LINE('',#57625,#10322);
#9077=LINE('',#57701,#10323);
#9078=LINE('',#57777,#10324);
#9079=LINE('',#57853,#10325);
#9080=LINE('',#57929,#10326);
#9081=LINE('',#58007,#10327);
#9082=LINE('',#58083,#10328);
#9083=LINE('',#58108,#10329);
#9084=LINE('',#58122,#10330);
#9085=LINE('',#58198,#10331);
#9086=LINE('',#58274,#10332);
#9087=LINE('',#58352,#10333);
#9088=LINE('',#58428,#10334);
#9089=LINE('',#58506,#10335);
#9090=LINE('',#58582,#10336);
#9091=LINE('',#58658,#10337);
#9092=LINE('',#58734,#10338);
#9093=LINE('',#58810,#10339);
#9094=LINE('',#58888,#10340);
#9095=LINE('',#58964,#10341);
#9096=LINE('',#59042,#10342);
#9097=LINE('',#59118,#10343);
#9098=LINE('',#59194,#10344);
#9099=LINE('',#59270,#10345);
#9100=LINE('',#59346,#10346);
#9101=LINE('',#59422,#10347);
#9102=LINE('',#59500,#10348);
#9103=LINE('',#59576,#10349);
#9104=LINE('',#59654,#10350);
#9105=LINE('',#59730,#10351);
#9106=LINE('',#59806,#10352);
#9107=LINE('',#59882,#10353);
#9108=LINE('',#59958,#10354);
#9109=LINE('',#60036,#10355);
#9110=LINE('',#60112,#10356);
#9111=LINE('',#60190,#10357);
#9112=LINE('',#60266,#10358);
#9113=LINE('',#60461,#10359);
#9114=LINE('',#60464,#10360);
#9115=LINE('',#60470,#10361);
#9116=LINE('',#60473,#10362);
#9117=LINE('',#60479,#10363);
#9118=LINE('',#60482,#10364);
#9119=LINE('',#60488,#10365);
#9120=LINE('',#60491,#10366);
#9121=LINE('',#60497,#10367);
#9122=LINE('',#60500,#10368);
#9123=LINE('',#60506,#10369);
#9124=LINE('',#60509,#10370);
#9125=LINE('',#60515,#10371);
#9126=LINE('',#60518,#10372);
#9127=LINE('',#60524,#10373);
#9128=LINE('',#60527,#10374);
#9129=LINE('',#60533,#10375);
#9130=LINE('',#60536,#10376);
#9131=LINE('',#60542,#10377);
#9132=LINE('',#60545,#10378);
#9133=LINE('',#60551,#10379);
#9134=LINE('',#60554,#10380);
#9135=LINE('',#60560,#10381);
#9136=LINE('',#60563,#10382);
#9137=LINE('',#60569,#10383);
#9138=LINE('',#60572,#10384);
#9139=LINE('',#60578,#10385);
#9140=LINE('',#60581,#10386);
#9141=LINE('',#60587,#10387);
#9142=LINE('',#60590,#10388);
#9143=LINE('',#60621,#10389);
#9144=LINE('',#61561,#10390);
#9145=LINE('',#62495,#10391);
#9146=LINE('',#62506,#10392);
#9147=LINE('',#62991,#10393);
#9148=LINE('',#62994,#10394);
#9149=LINE('',#62997,#10395);
#9150=LINE('',#62999,#10396);
#9151=LINE('',#63003,#10397);
#9152=LINE('',#63005,#10398);
#9153=LINE('',#63009,#10399);
#9154=LINE('',#63011,#10400);
#9155=LINE('',#63015,#10401);
#9156=LINE('',#63017,#10402);
#9157=LINE('',#63021,#10403);
#9158=LINE('',#63023,#10404);
#9159=LINE('',#63027,#10405);
#9160=LINE('',#63029,#10406);
#9161=LINE('',#63033,#10407);
#9162=LINE('',#63035,#10408);
#9163=LINE('',#63039,#10409);
#9164=LINE('',#63041,#10410);
#9165=LINE('',#63045,#10411);
#9166=LINE('',#63047,#10412);
#9167=LINE('',#63051,#10413);
#9168=LINE('',#63053,#10414);
#9169=LINE('',#63057,#10415);
#9170=LINE('',#63059,#10416);
#9171=LINE('',#63063,#10417);
#9172=LINE('',#63065,#10418);
#9173=LINE('',#63069,#10419);
#9174=LINE('',#63071,#10420);
#9175=LINE('',#63075,#10421);
#9176=LINE('',#63077,#10422);
#9177=LINE('',#63081,#10423);
#9178=LINE('',#63083,#10424);
#9179=LINE('',#63087,#10425);
#9180=LINE('',#63089,#10426);
#9181=LINE('',#63093,#10427);
#9182=LINE('',#63095,#10428);
#9183=LINE('',#63099,#10429);
#9184=LINE('',#63101,#10430);
#9185=LINE('',#63105,#10431);
#9186=LINE('',#63107,#10432);
#9187=LINE('',#63111,#10433);
#9188=LINE('',#63113,#10434);
#9189=LINE('',#63117,#10435);
#9190=LINE('',#63119,#10436);
#9191=LINE('',#63123,#10437);
#9192=LINE('',#63125,#10438);
#9193=LINE('',#63129,#10439);
#9194=LINE('',#63131,#10440);
#9195=LINE('',#63135,#10441);
#9196=LINE('',#63137,#10442);
#9197=LINE('',#63141,#10443);
#9198=LINE('',#63143,#10444);
#9199=LINE('',#63147,#10445);
#9200=LINE('',#63149,#10446);
#9201=LINE('',#63153,#10447);
#9202=LINE('',#63155,#10448);
#9203=LINE('',#63159,#10449);
#9204=LINE('',#63161,#10450);
#9205=LINE('',#63165,#10451);
#9206=LINE('',#63167,#10452);
#9207=LINE('',#63171,#10453);
#9208=LINE('',#63173,#10454);
#9209=LINE('',#63177,#10455);
#9210=LINE('',#63179,#10456);
#9211=LINE('',#63183,#10457);
#9212=LINE('',#63185,#10458);
#9213=LINE('',#63189,#10459);
#9214=LINE('',#63191,#10460);
#9215=LINE('',#63195,#10461);
#9216=LINE('',#63197,#10462);
#9217=LINE('',#63201,#10463);
#9218=LINE('',#63203,#10464);
#9219=LINE('',#63207,#10465);
#9220=LINE('',#63209,#10466);
#9221=LINE('',#63213,#10467);
#9222=LINE('',#63215,#10468);
#9223=LINE('',#63219,#10469);
#9224=LINE('',#63221,#10470);
#9225=LINE('',#63225,#10471);
#9226=LINE('',#63227,#10472);
#9227=LINE('',#63231,#10473);
#9228=LINE('',#63233,#10474);
#9229=LINE('',#63237,#10475);
#9230=LINE('',#63239,#10476);
#9231=LINE('',#63243,#10477);
#9232=LINE('',#63245,#10478);
#9233=LINE('',#63249,#10479);
#9234=LINE('',#63251,#10480);
#9235=LINE('',#63255,#10481);
#9236=LINE('',#63257,#10482);
#9237=LINE('',#63261,#10483);
#9238=LINE('',#63263,#10484);
#9239=LINE('',#63267,#10485);
#9240=LINE('',#63269,#10486);
#9241=LINE('',#63273,#10487);
#9242=LINE('',#63275,#10488);
#9243=LINE('',#63279,#10489);
#9244=LINE('',#63281,#10490);
#9245=LINE('',#63285,#10491);
#9246=LINE('',#63287,#10492);
#9247=LINE('',#63291,#10493);
#9248=LINE('',#63293,#10494);
#9249=LINE('',#63297,#10495);
#9250=LINE('',#63299,#10496);
#9251=LINE('',#63303,#10497);
#9252=LINE('',#63305,#10498);
#9253=LINE('',#63309,#10499);
#9254=LINE('',#63311,#10500);
#9255=LINE('',#63315,#10501);
#9256=LINE('',#63317,#10502);
#9257=LINE('',#63321,#10503);
#9258=LINE('',#63323,#10504);
#9259=LINE('',#63327,#10505);
#9260=LINE('',#63329,#10506);
#9261=LINE('',#63333,#10507);
#9262=LINE('',#63335,#10508);
#9263=LINE('',#63339,#10509);
#9264=LINE('',#63341,#10510);
#9265=LINE('',#63345,#10511);
#9266=LINE('',#63347,#10512);
#9267=LINE('',#63351,#10513);
#9268=LINE('',#63353,#10514);
#9269=LINE('',#63357,#10515);
#9270=LINE('',#63359,#10516);
#9271=LINE('',#63363,#10517);
#9272=LINE('',#63365,#10518);
#9273=LINE('',#63369,#10519);
#9274=LINE('',#63371,#10520);
#9275=LINE('',#63375,#10521);
#9276=LINE('',#63378,#10522);
#9277=LINE('',#63381,#10523);
#9278=LINE('',#63384,#10524);
#9279=LINE('',#63387,#10525);
#9280=LINE('',#63390,#10526);
#9281=LINE('',#63393,#10527);
#9282=LINE('',#63396,#10528);
#9283=LINE('',#63399,#10529);
#9284=LINE('',#63402,#10530);
#9285=LINE('',#63405,#10531);
#9286=LINE('',#63408,#10532);
#9287=LINE('',#63411,#10533);
#9288=LINE('',#63414,#10534);
#9289=LINE('',#63417,#10535);
#9290=LINE('',#63420,#10536);
#9291=LINE('',#63423,#10537);
#9292=LINE('',#63426,#10538);
#9293=LINE('',#63429,#10539);
#9294=LINE('',#63432,#10540);
#9295=LINE('',#63435,#10541);
#9296=LINE('',#63438,#10542);
#9297=LINE('',#63441,#10543);
#9298=LINE('',#63444,#10544);
#9299=LINE('',#63447,#10545);
#9300=LINE('',#63450,#10546);
#9301=LINE('',#63453,#10547);
#9302=LINE('',#63456,#10548);
#9303=LINE('',#63459,#10549);
#9304=LINE('',#63461,#10550);
#9305=LINE('',#63710,#10551);
#9306=LINE('',#63712,#10552);
#9307=LINE('',#63721,#10553);
#9308=LINE('',#63723,#10554);
#9309=LINE('',#63725,#10555);
#9310=LINE('',#63727,#10556);
#9311=LINE('',#63729,#10557);
#9312=LINE('',#63730,#10558);
#9313=LINE('',#63732,#10559);
#9314=LINE('',#63733,#10560);
#9315=LINE('',#63735,#10561);
#9316=LINE('',#63737,#10562);
#9317=LINE('',#63739,#10563);
#9318=LINE('',#63741,#10564);
#9319=LINE('',#65263,#10565);
#9320=LINE('',#65266,#10566);
#9321=LINE('',#65268,#10567);
#9322=LINE('',#65271,#10568);
#9323=LINE('',#65273,#10569);
#9324=LINE('',#65276,#10570);
#9325=LINE('',#65278,#10571);
#9326=LINE('',#65281,#10572);
#9327=LINE('',#65283,#10573);
#9328=LINE('',#65286,#10574);
#9329=LINE('',#65288,#10575);
#9330=LINE('',#65291,#10576);
#9331=LINE('',#65293,#10577);
#9332=LINE('',#65296,#10578);
#9333=LINE('',#65298,#10579);
#9334=LINE('',#65319,#10580);
#9335=LINE('',#65321,#10581);
#9336=LINE('',#65324,#10582);
#9337=LINE('',#65326,#10583);
#9338=LINE('',#65329,#10584);
#9339=LINE('',#65331,#10585);
#9340=LINE('',#65334,#10586);
#9341=LINE('',#65336,#10587);
#9342=LINE('',#65339,#10588);
#9343=LINE('',#65341,#10589);
#9344=LINE('',#65344,#10590);
#9345=LINE('',#65346,#10591);
#9346=LINE('',#65349,#10592);
#9347=LINE('',#65351,#10593);
#9348=LINE('',#65354,#10594);
#9349=LINE('',#65356,#10595);
#9350=LINE('',#65359,#10596);
#9351=LINE('',#65361,#10597);
#9352=LINE('',#65364,#10598);
#9353=LINE('',#65366,#10599);
#9354=LINE('',#65369,#10600);
#9355=LINE('',#65371,#10601);
#9356=LINE('',#65374,#10602);
#9357=LINE('',#65376,#10603);
#9358=LINE('',#65379,#10604);
#9359=LINE('',#65381,#10605);
#9360=LINE('',#65384,#10606);
#9361=LINE('',#65386,#10607);
#9362=LINE('',#65389,#10608);
#9363=LINE('',#65391,#10609);
#9364=LINE('',#65394,#10610);
#9365=LINE('',#65396,#10611);
#9366=LINE('',#65399,#10612);
#9367=LINE('',#65401,#10613);
#9368=LINE('',#65404,#10614);
#9369=LINE('',#65406,#10615);
#9370=LINE('',#65409,#10616);
#9371=LINE('',#65411,#10617);
#9372=LINE('',#65414,#10618);
#9373=LINE('',#65416,#10619);
#9374=LINE('',#65419,#10620);
#9375=LINE('',#65421,#10621);
#9376=LINE('',#65424,#10622);
#9377=LINE('',#65426,#10623);
#9378=LINE('',#65429,#10624);
#9379=LINE('',#65431,#10625);
#9380=LINE('',#65434,#10626);
#9381=LINE('',#65436,#10627);
#9382=LINE('',#65439,#10628);
#9383=LINE('',#65441,#10629);
#9384=LINE('',#65444,#10630);
#9385=LINE('',#65446,#10631);
#9386=LINE('',#65449,#10632);
#9387=LINE('',#65451,#10633);
#9388=LINE('',#65454,#10634);
#9389=LINE('',#65456,#10635);
#9390=LINE('',#65459,#10636);
#9391=LINE('',#65461,#10637);
#9392=LINE('',#65464,#10638);
#9393=LINE('',#65466,#10639);
#9394=LINE('',#65469,#10640);
#9395=LINE('',#65471,#10641);
#9396=LINE('',#65474,#10642);
#9397=LINE('',#65476,#10643);
#9398=LINE('',#65479,#10644);
#9399=LINE('',#65481,#10645);
#9400=LINE('',#65484,#10646);
#9401=LINE('',#65486,#10647);
#9402=LINE('',#65489,#10648);
#9403=LINE('',#65491,#10649);
#9404=LINE('',#65494,#10650);
#9405=LINE('',#65496,#10651);
#9406=LINE('',#65499,#10652);
#9407=LINE('',#65501,#10653);
#9408=LINE('',#65504,#10654);
#9409=LINE('',#65506,#10655);
#9410=LINE('',#65509,#10656);
#9411=LINE('',#65511,#10657);
#9412=LINE('',#65514,#10658);
#9413=LINE('',#65516,#10659);
#9414=LINE('',#65519,#10660);
#9415=LINE('',#65521,#10661);
#9416=LINE('',#65524,#10662);
#9417=LINE('',#65526,#10663);
#9418=LINE('',#65529,#10664);
#9419=LINE('',#65531,#10665);
#9420=LINE('',#65534,#10666);
#9421=LINE('',#65536,#10667);
#9422=LINE('',#65539,#10668);
#9423=LINE('',#65541,#10669);
#9424=LINE('',#65544,#10670);
#9425=LINE('',#65546,#10671);
#9426=LINE('',#65549,#10672);
#9427=LINE('',#65551,#10673);
#9428=LINE('',#65554,#10674);
#9429=LINE('',#65556,#10675);
#9430=LINE('',#65559,#10676);
#9431=LINE('',#65561,#10677);
#9432=LINE('',#65564,#10678);
#9433=LINE('',#65566,#10679);
#9434=LINE('',#65569,#10680);
#9435=LINE('',#65571,#10681);
#9436=LINE('',#65574,#10682);
#9437=LINE('',#65576,#10683);
#9438=LINE('',#65579,#10684);
#9439=LINE('',#65581,#10685);
#9440=LINE('',#65584,#10686);
#9441=LINE('',#65586,#10687);
#9442=LINE('',#65589,#10688);
#9443=LINE('',#65591,#10689);
#9444=LINE('',#65594,#10690);
#9445=LINE('',#65596,#10691);
#9446=LINE('',#65599,#10692);
#9447=LINE('',#65601,#10693);
#9448=LINE('',#65604,#10694);
#9449=LINE('',#65606,#10695);
#10299=VECTOR('',#39719,1.5);
#10300=VECTOR('',#39720,1.5);
#10301=VECTOR('',#39727,1.5);
#10302=VECTOR('',#39730,1.5);
#10303=VECTOR('',#39733,1.5);
#10304=VECTOR('',#39736,1.5);
#10305=VECTOR('',#39739,1.5);
#10306=VECTOR('',#39742,1.5);
#10307=VECTOR('',#39745,1.5);
#10308=VECTOR('',#39748,1.5);
#10309=VECTOR('',#39751,1.5);
#10310=VECTOR('',#39754,1.5);
#10311=VECTOR('',#39757,1.5);
#10312=VECTOR('',#39760,1.5);
#10313=VECTOR('',#39763,1.5);
#10314=VECTOR('',#39766,1.5);
#10315=VECTOR('',#39769,1.5);
#10316=VECTOR('',#39772,1.5);
#10317=VECTOR('',#39775,1.5);
#10318=VECTOR('',#39778,1.5);
#10319=VECTOR('',#39781,1.5);
#10320=VECTOR('',#39784,1.5);
#10321=VECTOR('',#39787,1.5);
#10322=VECTOR('',#39790,1.5);
#10323=VECTOR('',#39793,1.5);
#10324=VECTOR('',#39796,1.5);
#10325=VECTOR('',#39799,1.5);
#10326=VECTOR('',#39802,1.5);
#10327=VECTOR('',#39805,1.5);
#10328=VECTOR('',#39808,1.17524047358084);
#10329=VECTOR('',#39813,1.17524047358084);
#10330=VECTOR('',#39818,1.17524047358084);
#10331=VECTOR('',#39821,1.17524047358084);
#10332=VECTOR('',#39824,1.17524047358084);
#10333=VECTOR('',#39827,1.17524047358084);
#10334=VECTOR('',#39830,1.17524047358084);
#10335=VECTOR('',#39833,1.17524047358084);
#10336=VECTOR('',#39836,1.17524047358084);
#10337=VECTOR('',#39839,1.17524047358084);
#10338=VECTOR('',#39842,1.17524047358084);
#10339=VECTOR('',#39845,1.17524047358084);
#10340=VECTOR('',#39848,1.17524047358084);
#10341=VECTOR('',#39851,1.17524047358084);
#10342=VECTOR('',#39854,1.17524047358084);
#10343=VECTOR('',#39857,1.17524047358084);
#10344=VECTOR('',#39860,1.17524047358084);
#10345=VECTOR('',#39863,1.17524047358084);
#10346=VECTOR('',#39866,1.17524047358084);
#10347=VECTOR('',#39869,1.17524047358084);
#10348=VECTOR('',#39872,1.17524047358084);
#10349=VECTOR('',#39875,1.17524047358084);
#10350=VECTOR('',#39878,1.17524047358084);
#10351=VECTOR('',#39881,1.17524047358084);
#10352=VECTOR('',#39884,1.17524047358084);
#10353=VECTOR('',#39887,1.17524047358084);
#10354=VECTOR('',#39890,1.17524047358084);
#10355=VECTOR('',#39893,1.17524047358084);
#10356=VECTOR('',#39896,1.17524047358084);
#10357=VECTOR('',#39899,1.17524047358084);
#10358=VECTOR('',#39902,1.17524047358084);
#10359=VECTOR('',#39919,1000.);
#10360=VECTOR('',#39922,1000.);
#10361=VECTOR('',#39927,1000.);
#10362=VECTOR('',#39930,1000.);
#10363=VECTOR('',#39935,1000.);
#10364=VECTOR('',#39938,1000.);
#10365=VECTOR('',#39943,1000.);
#10366=VECTOR('',#39946,1000.);
#10367=VECTOR('',#39951,1000.);
#10368=VECTOR('',#39954,1000.);
#10369=VECTOR('',#39959,1000.);
#10370=VECTOR('',#39962,1000.);
#10371=VECTOR('',#39967,1000.);
#10372=VECTOR('',#39970,1000.);
#10373=VECTOR('',#39975,1000.);
#10374=VECTOR('',#39978,1000.);
#10375=VECTOR('',#39983,1000.);
#10376=VECTOR('',#39986,1000.);
#10377=VECTOR('',#39991,1000.);
#10378=VECTOR('',#39994,1000.);
#10379=VECTOR('',#39999,1000.);
#10380=VECTOR('',#40002,1000.);
#10381=VECTOR('',#40007,1000.);
#10382=VECTOR('',#40010,1000.);
#10383=VECTOR('',#40015,1000.);
#10384=VECTOR('',#40018,1000.);
#10385=VECTOR('',#40023,1000.);
#10386=VECTOR('',#40026,1000.);
#10387=VECTOR('',#40031,1000.);
#10388=VECTOR('',#40034,1000.);
#10389=VECTOR('',#40037,1.55162884844711);
#10390=VECTOR('',#40338,2.73627063036812);
#10391=VECTOR('',#40629,2.68872936963188);
#10392=VECTOR('',#40644,2.675);
#10393=VECTOR('',#41291,1000.);
#10394=VECTOR('',#41294,1000.);
#10395=VECTOR('',#41297,1000.);
#10396=VECTOR('',#41298,1000.);
#10397=VECTOR('',#41303,1000.);
#10398=VECTOR('',#41304,1000.);
#10399=VECTOR('',#41309,1000.);
#10400=VECTOR('',#41310,1000.);
#10401=VECTOR('',#41315,1000.);
#10402=VECTOR('',#41316,1000.);
#10403=VECTOR('',#41321,1000.);
#10404=VECTOR('',#41322,1000.);
#10405=VECTOR('',#41327,1000.);
#10406=VECTOR('',#41328,1000.);
#10407=VECTOR('',#41333,1000.);
#10408=VECTOR('',#41334,1000.);
#10409=VECTOR('',#41339,1000.);
#10410=VECTOR('',#41340,1000.);
#10411=VECTOR('',#41345,1000.);
#10412=VECTOR('',#41346,1000.);
#10413=VECTOR('',#41351,1000.);
#10414=VECTOR('',#41352,1000.);
#10415=VECTOR('',#41357,1000.);
#10416=VECTOR('',#41358,1000.);
#10417=VECTOR('',#41363,1000.);
#10418=VECTOR('',#41364,1000.);
#10419=VECTOR('',#41369,1000.);
#10420=VECTOR('',#41370,1000.);
#10421=VECTOR('',#41375,1000.);
#10422=VECTOR('',#41376,1000.);
#10423=VECTOR('',#41381,1000.);
#10424=VECTOR('',#41382,1000.);
#10425=VECTOR('',#41387,1000.);
#10426=VECTOR('',#41388,1000.);
#10427=VECTOR('',#41393,1000.);
#10428=VECTOR('',#41394,1000.);
#10429=VECTOR('',#41399,1000.);
#10430=VECTOR('',#41400,1000.);
#10431=VECTOR('',#41405,1000.);
#10432=VECTOR('',#41406,1000.);
#10433=VECTOR('',#41411,1000.);
#10434=VECTOR('',#41412,1000.);
#10435=VECTOR('',#41417,1000.);
#10436=VECTOR('',#41418,1000.);
#10437=VECTOR('',#41423,1000.);
#10438=VECTOR('',#41424,1000.);
#10439=VECTOR('',#41429,1000.);
#10440=VECTOR('',#41430,1000.);
#10441=VECTOR('',#41435,1000.);
#10442=VECTOR('',#41436,1000.);
#10443=VECTOR('',#41441,1000.);
#10444=VECTOR('',#41442,1000.);
#10445=VECTOR('',#41447,1000.);
#10446=VECTOR('',#41448,1000.);
#10447=VECTOR('',#41453,1000.);
#10448=VECTOR('',#41454,1000.);
#10449=VECTOR('',#41459,1000.);
#10450=VECTOR('',#41460,1000.);
#10451=VECTOR('',#41465,1000.);
#10452=VECTOR('',#41466,1000.);
#10453=VECTOR('',#41471,1000.);
#10454=VECTOR('',#41472,1000.);
#10455=VECTOR('',#41477,1000.);
#10456=VECTOR('',#41478,1000.);
#10457=VECTOR('',#41483,1000.);
#10458=VECTOR('',#41484,1000.);
#10459=VECTOR('',#41489,1000.);
#10460=VECTOR('',#41490,1000.);
#10461=VECTOR('',#41495,1000.);
#10462=VECTOR('',#41496,1000.);
#10463=VECTOR('',#41501,1000.);
#10464=VECTOR('',#41502,1000.);
#10465=VECTOR('',#41507,1000.);
#10466=VECTOR('',#41508,1000.);
#10467=VECTOR('',#41513,1000.);
#10468=VECTOR('',#41514,1000.);
#10469=VECTOR('',#41519,1000.);
#10470=VECTOR('',#41520,1000.);
#10471=VECTOR('',#41525,1000.);
#10472=VECTOR('',#41526,1000.);
#10473=VECTOR('',#41531,1000.);
#10474=VECTOR('',#41532,1000.);
#10475=VECTOR('',#41537,1000.);
#10476=VECTOR('',#41538,1000.);
#10477=VECTOR('',#41543,1000.);
#10478=VECTOR('',#41544,1000.);
#10479=VECTOR('',#41549,1000.);
#10480=VECTOR('',#41550,1000.);
#10481=VECTOR('',#41555,1000.);
#10482=VECTOR('',#41556,1000.);
#10483=VECTOR('',#41561,1000.);
#10484=VECTOR('',#41562,1000.);
#10485=VECTOR('',#41567,1000.);
#10486=VECTOR('',#41568,1000.);
#10487=VECTOR('',#41573,1000.);
#10488=VECTOR('',#41574,1000.);
#10489=VECTOR('',#41579,1000.);
#10490=VECTOR('',#41580,1000.);
#10491=VECTOR('',#41585,1000.);
#10492=VECTOR('',#41586,1000.);
#10493=VECTOR('',#41591,1000.);
#10494=VECTOR('',#41592,1000.);
#10495=VECTOR('',#41597,1000.);
#10496=VECTOR('',#41598,1000.);
#10497=VECTOR('',#41603,1000.);
#10498=VECTOR('',#41604,1000.);
#10499=VECTOR('',#41609,1000.);
#10500=VECTOR('',#41610,1000.);
#10501=VECTOR('',#41615,1000.);
#10502=VECTOR('',#41616,1000.);
#10503=VECTOR('',#41621,1000.);
#10504=VECTOR('',#41622,1000.);
#10505=VECTOR('',#41627,1000.);
#10506=VECTOR('',#41628,1000.);
#10507=VECTOR('',#41633,1000.);
#10508=VECTOR('',#41634,1000.);
#10509=VECTOR('',#41639,1000.);
#10510=VECTOR('',#41640,1000.);
#10511=VECTOR('',#41645,1000.);
#10512=VECTOR('',#41646,1000.);
#10513=VECTOR('',#41651,1000.);
#10514=VECTOR('',#41652,1000.);
#10515=VECTOR('',#41657,1000.);
#10516=VECTOR('',#41658,1000.);
#10517=VECTOR('',#41663,1000.);
#10518=VECTOR('',#41664,1000.);
#10519=VECTOR('',#41669,1000.);
#10520=VECTOR('',#41670,1000.);
#10521=VECTOR('',#41675,1000.);
#10522=VECTOR('',#41678,1000.);
#10523=VECTOR('',#41681,1000.);
#10524=VECTOR('',#41684,1000.);
#10525=VECTOR('',#41687,1000.);
#10526=VECTOR('',#41690,1000.);
#10527=VECTOR('',#41693,1000.);
#10528=VECTOR('',#41696,1000.);
#10529=VECTOR('',#41699,1000.);
#10530=VECTOR('',#41702,1000.);
#10531=VECTOR('',#41705,1000.);
#10532=VECTOR('',#41708,1000.);
#10533=VECTOR('',#41711,1000.);
#10534=VECTOR('',#41714,1000.);
#10535=VECTOR('',#41717,1000.);
#10536=VECTOR('',#41720,1000.);
#10537=VECTOR('',#41723,1000.);
#10538=VECTOR('',#41726,1000.);
#10539=VECTOR('',#41729,1000.);
#10540=VECTOR('',#41732,1000.);
#10541=VECTOR('',#41735,1000.);
#10542=VECTOR('',#41738,1000.);
#10543=VECTOR('',#41741,1000.);
#10544=VECTOR('',#41744,1000.);
#10545=VECTOR('',#41747,1000.);
#10546=VECTOR('',#41750,1000.);
#10547=VECTOR('',#41753,1000.);
#10548=VECTOR('',#41756,1000.);
#10549=VECTOR('',#41759,1000.);
#10550=VECTOR('',#41760,1000.);
#10551=VECTOR('',#42251,1000.);
#10552=VECTOR('',#42252,1000.);
#10553=VECTOR('',#42265,1000.);
#10554=VECTOR('',#42266,1000.);
#10555=VECTOR('',#42267,1000.);
#10556=VECTOR('',#42268,1000.);
#10557=VECTOR('',#42269,1000.);
#10558=VECTOR('',#42270,1000.);
#10559=VECTOR('',#42273,1000.);
#10560=VECTOR('',#42274,1000.);
#10561=VECTOR('',#42277,1000.);
#10562=VECTOR('',#42280,1000.);
#10563=VECTOR('',#42283,1000.);
#10564=VECTOR('',#42286,1000.);
#10565=VECTOR('',#42289,10.);
#10566=VECTOR('',#42294,1000.);
#10567=VECTOR('',#42297,1000.);
#10568=VECTOR('',#42302,1000.);
#10569=VECTOR('',#42305,1000.);
#10570=VECTOR('',#42310,1000.);
#10571=VECTOR('',#42313,1000.);
#10572=VECTOR('',#42318,1000.);
#10573=VECTOR('',#42321,1000.);
#10574=VECTOR('',#42326,1000.);
#10575=VECTOR('',#42329,1000.);
#10576=VECTOR('',#42334,1000.);
#10577=VECTOR('',#42337,1000.);
#10578=VECTOR('',#42342,1000.);
#10579=VECTOR('',#42345,1000.);
#10580=VECTOR('',#42386,1000.);
#10581=VECTOR('',#42389,1000.);
#10582=VECTOR('',#42394,1000.);
#10583=VECTOR('',#42397,1000.);
#10584=VECTOR('',#42402,1000.);
#10585=VECTOR('',#42405,1000.);
#10586=VECTOR('',#42410,1000.);
#10587=VECTOR('',#42413,1000.);
#10588=VECTOR('',#42418,1000.);
#10589=VECTOR('',#42421,1000.);
#10590=VECTOR('',#42426,1000.);
#10591=VECTOR('',#42429,1000.);
#10592=VECTOR('',#42434,1000.);
#10593=VECTOR('',#42437,1000.);
#10594=VECTOR('',#42442,1000.);
#10595=VECTOR('',#42445,1000.);
#10596=VECTOR('',#42450,1000.);
#10597=VECTOR('',#42453,1000.);
#10598=VECTOR('',#42458,1000.);
#10599=VECTOR('',#42461,1000.);
#10600=VECTOR('',#42466,1000.);
#10601=VECTOR('',#42469,1000.);
#10602=VECTOR('',#42474,1000.);
#10603=VECTOR('',#42477,1000.);
#10604=VECTOR('',#42482,1000.);
#10605=VECTOR('',#42485,1000.);
#10606=VECTOR('',#42490,1000.);
#10607=VECTOR('',#42493,1000.);
#10608=VECTOR('',#42498,1000.);
#10609=VECTOR('',#42501,1000.);
#10610=VECTOR('',#42506,1000.);
#10611=VECTOR('',#42509,1000.);
#10612=VECTOR('',#42514,1000.);
#10613=VECTOR('',#42517,1000.);
#10614=VECTOR('',#42522,1000.);
#10615=VECTOR('',#42525,1000.);
#10616=VECTOR('',#42530,1000.);
#10617=VECTOR('',#42533,1000.);
#10618=VECTOR('',#42538,1000.);
#10619=VECTOR('',#42541,1000.);
#10620=VECTOR('',#42546,1000.);
#10621=VECTOR('',#42549,1000.);
#10622=VECTOR('',#42554,1000.);
#10623=VECTOR('',#42557,1000.);
#10624=VECTOR('',#42562,1000.);
#10625=VECTOR('',#42565,1000.);
#10626=VECTOR('',#42570,1000.);
#10627=VECTOR('',#42573,1000.);
#10628=VECTOR('',#42578,1000.);
#10629=VECTOR('',#42581,1000.);
#10630=VECTOR('',#42586,1000.);
#10631=VECTOR('',#42589,1000.);
#10632=VECTOR('',#42594,1000.);
#10633=VECTOR('',#42597,1000.);
#10634=VECTOR('',#42602,1000.);
#10635=VECTOR('',#42605,1000.);
#10636=VECTOR('',#42610,1000.);
#10637=VECTOR('',#42613,1000.);
#10638=VECTOR('',#42618,1000.);
#10639=VECTOR('',#42621,1000.);
#10640=VECTOR('',#42626,1000.);
#10641=VECTOR('',#42629,1000.);
#10642=VECTOR('',#42634,1000.);
#10643=VECTOR('',#42637,1000.);
#10644=VECTOR('',#42642,1000.);
#10645=VECTOR('',#42645,1000.);
#10646=VECTOR('',#42650,1000.);
#10647=VECTOR('',#42653,1000.);
#10648=VECTOR('',#42658,1000.);
#10649=VECTOR('',#42661,1000.);
#10650=VECTOR('',#42666,1000.);
#10651=VECTOR('',#42669,1000.);
#10652=VECTOR('',#42674,1000.);
#10653=VECTOR('',#42677,1000.);
#10654=VECTOR('',#42682,1000.);
#10655=VECTOR('',#42685,1000.);
#10656=VECTOR('',#42690,1000.);
#10657=VECTOR('',#42693,1000.);
#10658=VECTOR('',#42698,1000.);
#10659=VECTOR('',#42701,1000.);
#10660=VECTOR('',#42706,1000.);
#10661=VECTOR('',#42709,1000.);
#10662=VECTOR('',#42714,1000.);
#10663=VECTOR('',#42717,1000.);
#10664=VECTOR('',#42722,1000.);
#10665=VECTOR('',#42725,1000.);
#10666=VECTOR('',#42730,1000.);
#10667=VECTOR('',#42733,1000.);
#10668=VECTOR('',#42738,1000.);
#10669=VECTOR('',#42741,1000.);
#10670=VECTOR('',#42746,1000.);
#10671=VECTOR('',#42749,1000.);
#10672=VECTOR('',#42754,1000.);
#10673=VECTOR('',#42757,1000.);
#10674=VECTOR('',#42762,1000.);
#10675=VECTOR('',#42765,1000.);
#10676=VECTOR('',#42770,1000.);
#10677=VECTOR('',#42773,1000.);
#10678=VECTOR('',#42778,1000.);
#10679=VECTOR('',#42781,1000.);
#10680=VECTOR('',#42786,1000.);
#10681=VECTOR('',#42789,1000.);
#10682=VECTOR('',#42794,1000.);
#10683=VECTOR('',#42797,1000.);
#10684=VECTOR('',#42802,1000.);
#10685=VECTOR('',#42805,1000.);
#10686=VECTOR('',#42810,1000.);
#10687=VECTOR('',#42813,1000.);
#10688=VECTOR('',#42818,1000.);
#10689=VECTOR('',#42821,1000.);
#10690=VECTOR('',#42826,1000.);
#10691=VECTOR('',#42829,1000.);
#10692=VECTOR('',#42834,1000.);
#10693=VECTOR('',#42837,1000.);
#10694=VECTOR('',#42842,1000.);
#10695=VECTOR('',#42845,1000.);
#12265=VERTEX_POINT('',#55933);
#12266=VERTEX_POINT('',#55934);
#12267=VERTEX_POINT('',#55936);
#12268=VERTEX_POINT('',#55973);
#12269=VERTEX_POINT('',#55976);
#12270=VERTEX_POINT('',#56013);
#12271=VERTEX_POINT('',#56014);
#12272=VERTEX_POINT('',#56089);
#12273=VERTEX_POINT('',#56090);
#12274=VERTEX_POINT('',#56167);
#12275=VERTEX_POINT('',#56168);
#12276=VERTEX_POINT('',#56243);
#12277=VERTEX_POINT('',#56244);
#12278=VERTEX_POINT('',#56319);
#12279=VERTEX_POINT('',#56320);
#12280=VERTEX_POINT('',#56395);
#12281=VERTEX_POINT('',#56396);
#12282=VERTEX_POINT('',#56471);
#12283=VERTEX_POINT('',#56472);
#12284=VERTEX_POINT('',#56549);
#12285=VERTEX_POINT('',#56550);
#12286=VERTEX_POINT('',#56627);
#12287=VERTEX_POINT('',#56628);
#12288=VERTEX_POINT('',#56703);
#12289=VERTEX_POINT('',#56704);
#12290=VERTEX_POINT('',#56779);
#12291=VERTEX_POINT('',#56780);
#12292=VERTEX_POINT('',#56855);
#12293=VERTEX_POINT('',#56856);
#12294=VERTEX_POINT('',#56931);
#12295=VERTEX_POINT('',#56932);
#12296=VERTEX_POINT('',#57009);
#12297=VERTEX_POINT('',#57010);
#12298=VERTEX_POINT('',#57085);
#12299=VERTEX_POINT('',#57086);
#12300=VERTEX_POINT('',#57163);
#12301=VERTEX_POINT('',#57164);
#12302=VERTEX_POINT('',#57239);
#12303=VERTEX_POINT('',#57240);
#12304=VERTEX_POINT('',#57315);
#12305=VERTEX_POINT('',#57316);
#12306=VERTEX_POINT('',#57391);
#12307=VERTEX_POINT('',#57392);
#12308=VERTEX_POINT('',#57467);
#12309=VERTEX_POINT('',#57468);
#12310=VERTEX_POINT('',#57545);
#12311=VERTEX_POINT('',#57546);
#12312=VERTEX_POINT('',#57623);
#12313=VERTEX_POINT('',#57624);
#12314=VERTEX_POINT('',#57699);
#12315=VERTEX_POINT('',#57700);
#12316=VERTEX_POINT('',#57775);
#12317=VERTEX_POINT('',#57776);
#12318=VERTEX_POINT('',#57851);
#12319=VERTEX_POINT('',#57852);
#12320=VERTEX_POINT('',#57927);
#12321=VERTEX_POINT('',#57928);
#12322=VERTEX_POINT('',#58005);
#12323=VERTEX_POINT('',#58006);
#12324=VERTEX_POINT('',#58081);
#12325=VERTEX_POINT('',#58082);
#12326=VERTEX_POINT('',#58084);
#12327=VERTEX_POINT('',#58107);
#12328=VERTEX_POINT('',#58109);
#12329=VERTEX_POINT('',#58120);
#12330=VERTEX_POINT('',#58121);
#12331=VERTEX_POINT('',#58196);
#12332=VERTEX_POINT('',#58197);
#12333=VERTEX_POINT('',#58272);
#12334=VERTEX_POINT('',#58273);
#12335=VERTEX_POINT('',#58350);
#12336=VERTEX_POINT('',#58351);
#12337=VERTEX_POINT('',#58426);
#12338=VERTEX_POINT('',#58427);
#12339=VERTEX_POINT('',#58504);
#12340=VERTEX_POINT('',#58505);
#12341=VERTEX_POINT('',#58580);
#12342=VERTEX_POINT('',#58581);
#12343=VERTEX_POINT('',#58656);
#12344=VERTEX_POINT('',#58657);
#12345=VERTEX_POINT('',#58732);
#12346=VERTEX_POINT('',#58733);
#12347=VERTEX_POINT('',#58808);
#12348=VERTEX_POINT('',#58809);
#12349=VERTEX_POINT('',#58886);
#12350=VERTEX_POINT('',#58887);
#12351=VERTEX_POINT('',#58962);
#12352=VERTEX_POINT('',#58963);
#12353=VERTEX_POINT('',#59040);
#12354=VERTEX_POINT('',#59041);
#12355=VERTEX_POINT('',#59116);
#12356=VERTEX_POINT('',#59117);
#12357=VERTEX_POINT('',#59192);
#12358=VERTEX_POINT('',#59193);
#12359=VERTEX_POINT('',#59268);
#12360=VERTEX_POINT('',#59269);
#12361=VERTEX_POINT('',#59344);
#12362=VERTEX_POINT('',#59345);
#12363=VERTEX_POINT('',#59420);
#12364=VERTEX_POINT('',#59421);
#12365=VERTEX_POINT('',#59498);
#12366=VERTEX_POINT('',#59499);
#12367=VERTEX_POINT('',#59574);
#12368=VERTEX_POINT('',#59575);
#12369=VERTEX_POINT('',#59652);
#12370=VERTEX_POINT('',#59653);
#12371=VERTEX_POINT('',#59728);
#12372=VERTEX_POINT('',#59729);
#12373=VERTEX_POINT('',#59804);
#12374=VERTEX_POINT('',#59805);
#12375=VERTEX_POINT('',#59880);
#12376=VERTEX_POINT('',#59881);
#12377=VERTEX_POINT('',#59956);
#12378=VERTEX_POINT('',#59957);
#12379=VERTEX_POINT('',#60034);
#12380=VERTEX_POINT('',#60035);
#12381=VERTEX_POINT('',#60110);
#12382=VERTEX_POINT('',#60111);
#12383=VERTEX_POINT('',#60188);
#12384=VERTEX_POINT('',#60189);
#12385=VERTEX_POINT('',#60264);
#12386=VERTEX_POINT('',#60265);
#12387=VERTEX_POINT('',#60340);
#12388=VERTEX_POINT('',#60352);
#12389=VERTEX_POINT('',#60365);
#12390=VERTEX_POINT('',#60457);
#12391=VERTEX_POINT('',#60458);
#12392=VERTEX_POINT('',#60460);
#12393=VERTEX_POINT('',#60462);
#12394=VERTEX_POINT('',#60466);
#12395=VERTEX_POINT('',#60467);
#12396=VERTEX_POINT('',#60469);
#12397=VERTEX_POINT('',#60471);
#12398=VERTEX_POINT('',#60475);
#12399=VERTEX_POINT('',#60476);
#12400=VERTEX_POINT('',#60478);
#12401=VERTEX_POINT('',#60480);
#12402=VERTEX_POINT('',#60484);
#12403=VERTEX_POINT('',#60485);
#12404=VERTEX_POINT('',#60487);
#12405=VERTEX_POINT('',#60489);
#12406=VERTEX_POINT('',#60493);
#12407=VERTEX_POINT('',#60494);
#12408=VERTEX_POINT('',#60496);
#12409=VERTEX_POINT('',#60498);
#12410=VERTEX_POINT('',#60502);
#12411=VERTEX_POINT('',#60503);
#12412=VERTEX_POINT('',#60505);
#12413=VERTEX_POINT('',#60507);
#12414=VERTEX_POINT('',#60511);
#12415=VERTEX_POINT('',#60512);
#12416=VERTEX_POINT('',#60514);
#12417=VERTEX_POINT('',#60516);
#12418=VERTEX_POINT('',#60520);
#12419=VERTEX_POINT('',#60521);
#12420=VERTEX_POINT('',#60523);
#12421=VERTEX_POINT('',#60525);
#12422=VERTEX_POINT('',#60529);
#12423=VERTEX_POINT('',#60530);
#12424=VERTEX_POINT('',#60532);
#12425=VERTEX_POINT('',#60534);
#12426=VERTEX_POINT('',#60538);
#12427=VERTEX_POINT('',#60539);
#12428=VERTEX_POINT('',#60541);
#12429=VERTEX_POINT('',#60543);
#12430=VERTEX_POINT('',#60547);
#12431=VERTEX_POINT('',#60548);
#12432=VERTEX_POINT('',#60550);
#12433=VERTEX_POINT('',#60552);
#12434=VERTEX_POINT('',#60556);
#12435=VERTEX_POINT('',#60557);
#12436=VERTEX_POINT('',#60559);
#12437=VERTEX_POINT('',#60561);
#12438=VERTEX_POINT('',#60565);
#12439=VERTEX_POINT('',#60566);
#12440=VERTEX_POINT('',#60568);
#12441=VERTEX_POINT('',#60570);
#12442=VERTEX_POINT('',#60574);
#12443=VERTEX_POINT('',#60575);
#12444=VERTEX_POINT('',#60577);
#12445=VERTEX_POINT('',#60579);
#12446=VERTEX_POINT('',#60583);
#12447=VERTEX_POINT('',#60584);
#12448=VERTEX_POINT('',#60586);
#12449=VERTEX_POINT('',#60588);
#12450=VERTEX_POINT('',#60592);
#12451=VERTEX_POINT('',#60593);
#12452=VERTEX_POINT('',#60597);
#12453=VERTEX_POINT('',#60601);
#12454=VERTEX_POINT('',#60605);
#12455=VERTEX_POINT('',#60609);
#12456=VERTEX_POINT('',#60613);
#12457=VERTEX_POINT('',#60620);
#12458=VERTEX_POINT('',#60624);
#12459=VERTEX_POINT('',#60626);
#12460=VERTEX_POINT('',#60630);
#12461=VERTEX_POINT('',#60631);
#12462=VERTEX_POINT('',#60640);
#12463=VERTEX_POINT('',#60644);
#12464=VERTEX_POINT('',#60646);
#12465=VERTEX_POINT('',#60650);
#12466=VERTEX_POINT('',#60652);
#12467=VERTEX_POINT('',#60656);
#12468=VERTEX_POINT('',#60658);
#12469=VERTEX_POINT('',#60662);
#12470=VERTEX_POINT('',#60664);
#12471=VERTEX_POINT('',#60668);
#12472=VERTEX_POINT('',#60670);
#12473=VERTEX_POINT('',#60674);
#12474=VERTEX_POINT('',#60676);
#12475=VERTEX_POINT('',#60680);
#12476=VERTEX_POINT('',#60682);
#12477=VERTEX_POINT('',#60686);
#12478=VERTEX_POINT('',#60688);
#12479=VERTEX_POINT('',#60692);
#12480=VERTEX_POINT('',#60694);
#12481=VERTEX_POINT('',#60698);
#12482=VERTEX_POINT('',#60700);
#12483=VERTEX_POINT('',#60704);
#12484=VERTEX_POINT('',#60706);
#12485=VERTEX_POINT('',#60710);
#12486=VERTEX_POINT('',#60712);
#12487=VERTEX_POINT('',#60716);
#12488=VERTEX_POINT('',#60718);
#12489=VERTEX_POINT('',#60722);
#12490=VERTEX_POINT('',#60724);
#12491=VERTEX_POINT('',#60728);
#12492=VERTEX_POINT('',#60730);
#12493=VERTEX_POINT('',#60734);
#12494=VERTEX_POINT('',#60736);
#12495=VERTEX_POINT('',#60740);
#12496=VERTEX_POINT('',#60742);
#12497=VERTEX_POINT('',#60746);
#12498=VERTEX_POINT('',#60748);
#12499=VERTEX_POINT('',#60752);
#12500=VERTEX_POINT('',#60754);
#12501=VERTEX_POINT('',#60758);
#12502=VERTEX_POINT('',#60760);
#12503=VERTEX_POINT('',#60764);
#12504=VERTEX_POINT('',#60766);
#12505=VERTEX_POINT('',#60770);
#12506=VERTEX_POINT('',#60772);
#12507=VERTEX_POINT('',#60776);
#12508=VERTEX_POINT('',#60778);
#12509=VERTEX_POINT('',#60782);
#12510=VERTEX_POINT('',#60784);
#12511=VERTEX_POINT('',#60788);
#12512=VERTEX_POINT('',#60790);
#12513=VERTEX_POINT('',#60794);
#12514=VERTEX_POINT('',#60796);
#12515=VERTEX_POINT('',#60800);
#12516=VERTEX_POINT('',#60802);
#12517=VERTEX_POINT('',#60806);
#12518=VERTEX_POINT('',#60808);
#12519=VERTEX_POINT('',#60812);
#12520=VERTEX_POINT('',#60814);
#12521=VERTEX_POINT('',#60818);
#12522=VERTEX_POINT('',#60820);
#12523=VERTEX_POINT('',#60824);
#12524=VERTEX_POINT('',#60826);
#12525=VERTEX_POINT('',#60830);
#12526=VERTEX_POINT('',#60832);
#12527=VERTEX_POINT('',#60836);
#12528=VERTEX_POINT('',#60838);
#12529=VERTEX_POINT('',#60842);
#12530=VERTEX_POINT('',#60844);
#12531=VERTEX_POINT('',#60848);
#12532=VERTEX_POINT('',#60850);
#12533=VERTEX_POINT('',#60854);
#12534=VERTEX_POINT('',#60856);
#12535=VERTEX_POINT('',#60860);
#12536=VERTEX_POINT('',#60862);
#12537=VERTEX_POINT('',#60866);
#12538=VERTEX_POINT('',#60868);
#12539=VERTEX_POINT('',#60872);
#12540=VERTEX_POINT('',#60874);
#12541=VERTEX_POINT('',#60878);
#12542=VERTEX_POINT('',#60880);
#12543=VERTEX_POINT('',#60884);
#12544=VERTEX_POINT('',#60886);
#12545=VERTEX_POINT('',#60890);
#12546=VERTEX_POINT('',#60892);
#12547=VERTEX_POINT('',#60896);
#12548=VERTEX_POINT('',#60898);
#12549=VERTEX_POINT('',#60902);
#12550=VERTEX_POINT('',#60904);
#12551=VERTEX_POINT('',#60908);
#12552=VERTEX_POINT('',#60910);
#12553=VERTEX_POINT('',#60914);
#12554=VERTEX_POINT('',#60916);
#12555=VERTEX_POINT('',#60920);
#12556=VERTEX_POINT('',#60922);
#12557=VERTEX_POINT('',#60926);
#12558=VERTEX_POINT('',#60928);
#12559=VERTEX_POINT('',#60932);
#12560=VERTEX_POINT('',#60934);
#12561=VERTEX_POINT('',#60938);
#12562=VERTEX_POINT('',#60940);
#12563=VERTEX_POINT('',#60944);
#12564=VERTEX_POINT('',#60946);
#12565=VERTEX_POINT('',#60950);
#12566=VERTEX_POINT('',#60952);
#12567=VERTEX_POINT('',#60956);
#12568=VERTEX_POINT('',#60958);
#12569=VERTEX_POINT('',#60962);
#12570=VERTEX_POINT('',#60964);
#12571=VERTEX_POINT('',#60968);
#12572=VERTEX_POINT('',#60970);
#12573=VERTEX_POINT('',#60974);
#12574=VERTEX_POINT('',#60976);
#12575=VERTEX_POINT('',#60980);
#12576=VERTEX_POINT('',#60982);
#12577=VERTEX_POINT('',#60986);
#12578=VERTEX_POINT('',#60988);
#12579=VERTEX_POINT('',#60992);
#12580=VERTEX_POINT('',#60994);
#12581=VERTEX_POINT('',#60998);
#12582=VERTEX_POINT('',#61000);
#12583=VERTEX_POINT('',#61004);
#12584=VERTEX_POINT('',#61006);
#12585=VERTEX_POINT('',#61010);
#12586=VERTEX_POINT('',#61012);
#12587=VERTEX_POINT('',#61016);
#12588=VERTEX_POINT('',#61018);
#12589=VERTEX_POINT('',#61022);
#12590=VERTEX_POINT('',#61024);
#12591=VERTEX_POINT('',#61028);
#12592=VERTEX_POINT('',#61030);
#12593=VERTEX_POINT('',#61034);
#12594=VERTEX_POINT('',#61036);
#12595=VERTEX_POINT('',#61040);
#12596=VERTEX_POINT('',#61042);
#12597=VERTEX_POINT('',#61046);
#12598=VERTEX_POINT('',#61048);
#12599=VERTEX_POINT('',#61052);
#12600=VERTEX_POINT('',#61054);
#12601=VERTEX_POINT('',#61058);
#12602=VERTEX_POINT('',#61060);
#12603=VERTEX_POINT('',#61064);
#12604=VERTEX_POINT('',#61066);
#12605=VERTEX_POINT('',#61070);
#12606=VERTEX_POINT('',#61072);
#12607=VERTEX_POINT('',#61076);
#12608=VERTEX_POINT('',#61078);
#12609=VERTEX_POINT('',#61082);
#12610=VERTEX_POINT('',#61084);
#12611=VERTEX_POINT('',#61088);
#12612=VERTEX_POINT('',#61090);
#12613=VERTEX_POINT('',#61094);
#12614=VERTEX_POINT('',#61096);
#12615=VERTEX_POINT('',#61100);
#12616=VERTEX_POINT('',#61102);
#12617=VERTEX_POINT('',#61106);
#12618=VERTEX_POINT('',#61108);
#12619=VERTEX_POINT('',#61112);
#12620=VERTEX_POINT('',#61114);
#12621=VERTEX_POINT('',#61118);
#12622=VERTEX_POINT('',#61120);
#12623=VERTEX_POINT('',#61124);
#12624=VERTEX_POINT('',#61126);
#12625=VERTEX_POINT('',#61130);
#12626=VERTEX_POINT('',#61132);
#12627=VERTEX_POINT('',#61136);
#12628=VERTEX_POINT('',#61138);
#12629=VERTEX_POINT('',#61142);
#12630=VERTEX_POINT('',#61144);
#12631=VERTEX_POINT('',#61148);
#12632=VERTEX_POINT('',#61150);
#12633=VERTEX_POINT('',#61154);
#12634=VERTEX_POINT('',#61156);
#12635=VERTEX_POINT('',#61160);
#12636=VERTEX_POINT('',#61162);
#12637=VERTEX_POINT('',#61166);
#12638=VERTEX_POINT('',#61168);
#12639=VERTEX_POINT('',#61172);
#12640=VERTEX_POINT('',#61174);
#12641=VERTEX_POINT('',#61178);
#12642=VERTEX_POINT('',#61180);
#12643=VERTEX_POINT('',#61184);
#12644=VERTEX_POINT('',#61189);
#12645=VERTEX_POINT('',#61193);
#12646=VERTEX_POINT('',#61198);
#12647=VERTEX_POINT('',#61202);
#12648=VERTEX_POINT('',#61207);
#12649=VERTEX_POINT('',#61211);
#12650=VERTEX_POINT('',#61216);
#12651=VERTEX_POINT('',#61220);
#12652=VERTEX_POINT('',#61225);
#12653=VERTEX_POINT('',#61229);
#12654=VERTEX_POINT('',#61234);
#12655=VERTEX_POINT('',#61238);
#12656=VERTEX_POINT('',#61243);
#12657=VERTEX_POINT('',#61247);
#12658=VERTEX_POINT('',#61252);
#12659=VERTEX_POINT('',#61256);
#12660=VERTEX_POINT('',#61261);
#12661=VERTEX_POINT('',#61265);
#12662=VERTEX_POINT('',#61270);
#12663=VERTEX_POINT('',#61274);
#12664=VERTEX_POINT('',#61279);
#12665=VERTEX_POINT('',#61283);
#12666=VERTEX_POINT('',#61288);
#12667=VERTEX_POINT('',#61292);
#12668=VERTEX_POINT('',#61297);
#12669=VERTEX_POINT('',#61301);
#12670=VERTEX_POINT('',#61306);
#12671=VERTEX_POINT('',#61310);
#12672=VERTEX_POINT('',#61315);
#12673=VERTEX_POINT('',#61319);
#12674=VERTEX_POINT('',#61321);
#12675=VERTEX_POINT('',#61325);
#12676=VERTEX_POINT('',#61327);
#12677=VERTEX_POINT('',#61331);
#12678=VERTEX_POINT('',#61333);
#12679=VERTEX_POINT('',#61337);
#12680=VERTEX_POINT('',#61339);
#12681=VERTEX_POINT('',#61343);
#12682=VERTEX_POINT('',#61345);
#12683=VERTEX_POINT('',#61349);
#12684=VERTEX_POINT('',#61351);
#12685=VERTEX_POINT('',#61355);
#12686=VERTEX_POINT('',#61357);
#12687=VERTEX_POINT('',#61361);
#12688=VERTEX_POINT('',#61363);
#12689=VERTEX_POINT('',#61367);
#12690=VERTEX_POINT('',#61369);
#12691=VERTEX_POINT('',#61373);
#12692=VERTEX_POINT('',#61375);
#12693=VERTEX_POINT('',#61379);
#12694=VERTEX_POINT('',#61381);
#12695=VERTEX_POINT('',#61385);
#12696=VERTEX_POINT('',#61387);
#12697=VERTEX_POINT('',#61391);
#12698=VERTEX_POINT('',#61393);
#12699=VERTEX_POINT('',#61397);
#12700=VERTEX_POINT('',#61399);
#12701=VERTEX_POINT('',#61403);
#12702=VERTEX_POINT('',#61405);
#12703=VERTEX_POINT('',#61409);
#12704=VERTEX_POINT('',#61411);
#12705=VERTEX_POINT('',#61415);
#12706=VERTEX_POINT('',#61417);
#12707=VERTEX_POINT('',#61421);
#12708=VERTEX_POINT('',#61423);
#12709=VERTEX_POINT('',#61427);
#12710=VERTEX_POINT('',#61429);
#12711=VERTEX_POINT('',#61433);
#12712=VERTEX_POINT('',#61435);
#12713=VERTEX_POINT('',#61439);
#12714=VERTEX_POINT('',#61441);
#12715=VERTEX_POINT('',#61445);
#12716=VERTEX_POINT('',#61447);
#12717=VERTEX_POINT('',#61451);
#12718=VERTEX_POINT('',#61453);
#12719=VERTEX_POINT('',#61457);
#12720=VERTEX_POINT('',#61459);
#12721=VERTEX_POINT('',#61463);
#12722=VERTEX_POINT('',#61465);
#12723=VERTEX_POINT('',#61469);
#12724=VERTEX_POINT('',#61471);
#12725=VERTEX_POINT('',#61475);
#12726=VERTEX_POINT('',#61477);
#12727=VERTEX_POINT('',#61481);
#12728=VERTEX_POINT('',#61483);
#12729=VERTEX_POINT('',#61487);
#12730=VERTEX_POINT('',#61489);
#12731=VERTEX_POINT('',#61493);
#12732=VERTEX_POINT('',#61495);
#12733=VERTEX_POINT('',#61499);
#12734=VERTEX_POINT('',#61501);
#12735=VERTEX_POINT('',#61505);
#12736=VERTEX_POINT('',#61507);
#12737=VERTEX_POINT('',#61511);
#12738=VERTEX_POINT('',#61513);
#12739=VERTEX_POINT('',#61517);
#12740=VERTEX_POINT('',#61519);
#12741=VERTEX_POINT('',#61523);
#12742=VERTEX_POINT('',#61525);
#12743=VERTEX_POINT('',#61529);
#12744=VERTEX_POINT('',#61531);
#12745=VERTEX_POINT('',#61535);
#12746=VERTEX_POINT('',#61537);
#12747=VERTEX_POINT('',#61541);
#12748=VERTEX_POINT('',#61543);
#12749=VERTEX_POINT('',#61547);
#12750=VERTEX_POINT('',#61549);
#12751=VERTEX_POINT('',#61563);
#12752=VERTEX_POINT('',#61564);
#12753=VERTEX_POINT('',#61573);
#12754=VERTEX_POINT('',#61577);
#12755=VERTEX_POINT('',#61579);
#12756=VERTEX_POINT('',#61583);
#12757=VERTEX_POINT('',#61585);
#12758=VERTEX_POINT('',#61589);
#12759=VERTEX_POINT('',#61591);
#12760=VERTEX_POINT('',#61595);
#12761=VERTEX_POINT('',#61597);
#12762=VERTEX_POINT('',#61601);
#12763=VERTEX_POINT('',#61603);
#12764=VERTEX_POINT('',#61607);
#12765=VERTEX_POINT('',#61609);
#12766=VERTEX_POINT('',#61613);
#12767=VERTEX_POINT('',#61615);
#12768=VERTEX_POINT('',#61619);
#12769=VERTEX_POINT('',#61621);
#12770=VERTEX_POINT('',#61625);
#12771=VERTEX_POINT('',#61627);
#12772=VERTEX_POINT('',#61631);
#12773=VERTEX_POINT('',#61633);
#12774=VERTEX_POINT('',#61637);
#12775=VERTEX_POINT('',#61639);
#12776=VERTEX_POINT('',#61643);
#12777=VERTEX_POINT('',#61645);
#12778=VERTEX_POINT('',#61649);
#12779=VERTEX_POINT('',#61651);
#12780=VERTEX_POINT('',#61655);
#12781=VERTEX_POINT('',#61657);
#12782=VERTEX_POINT('',#61661);
#12783=VERTEX_POINT('',#61663);
#12784=VERTEX_POINT('',#61667);
#12785=VERTEX_POINT('',#61669);
#12786=VERTEX_POINT('',#61673);
#12787=VERTEX_POINT('',#61675);
#12788=VERTEX_POINT('',#61679);
#12789=VERTEX_POINT('',#61681);
#12790=VERTEX_POINT('',#61685);
#12791=VERTEX_POINT('',#61687);
#12792=VERTEX_POINT('',#61691);
#12793=VERTEX_POINT('',#61693);
#12794=VERTEX_POINT('',#61697);
#12795=VERTEX_POINT('',#61699);
#12796=VERTEX_POINT('',#61703);
#12797=VERTEX_POINT('',#61705);
#12798=VERTEX_POINT('',#61709);
#12799=VERTEX_POINT('',#61711);
#12800=VERTEX_POINT('',#61715);
#12801=VERTEX_POINT('',#61717);
#12802=VERTEX_POINT('',#61721);
#12803=VERTEX_POINT('',#61723);
#12804=VERTEX_POINT('',#61727);
#12805=VERTEX_POINT('',#61729);
#12806=VERTEX_POINT('',#61733);
#12807=VERTEX_POINT('',#61735);
#12808=VERTEX_POINT('',#61739);
#12809=VERTEX_POINT('',#61741);
#12810=VERTEX_POINT('',#61745);
#12811=VERTEX_POINT('',#61747);
#12812=VERTEX_POINT('',#61751);
#12813=VERTEX_POINT('',#61753);
#12814=VERTEX_POINT('',#61757);
#12815=VERTEX_POINT('',#61759);
#12816=VERTEX_POINT('',#61763);
#12817=VERTEX_POINT('',#61765);
#12818=VERTEX_POINT('',#61769);
#12819=VERTEX_POINT('',#61771);
#12820=VERTEX_POINT('',#61775);
#12821=VERTEX_POINT('',#61777);
#12822=VERTEX_POINT('',#61781);
#12823=VERTEX_POINT('',#61783);
#12824=VERTEX_POINT('',#61787);
#12825=VERTEX_POINT('',#61789);
#12826=VERTEX_POINT('',#61793);
#12827=VERTEX_POINT('',#61795);
#12828=VERTEX_POINT('',#61799);
#12829=VERTEX_POINT('',#61801);
#12830=VERTEX_POINT('',#61805);
#12831=VERTEX_POINT('',#61807);
#12832=VERTEX_POINT('',#61811);
#12833=VERTEX_POINT('',#61813);
#12834=VERTEX_POINT('',#61817);
#12835=VERTEX_POINT('',#61819);
#12836=VERTEX_POINT('',#61823);
#12837=VERTEX_POINT('',#61825);
#12838=VERTEX_POINT('',#61829);
#12839=VERTEX_POINT('',#61831);
#12840=VERTEX_POINT('',#61835);
#12841=VERTEX_POINT('',#61837);
#12842=VERTEX_POINT('',#61841);
#12843=VERTEX_POINT('',#61843);
#12844=VERTEX_POINT('',#61847);
#12845=VERTEX_POINT('',#61849);
#12846=VERTEX_POINT('',#61853);
#12847=VERTEX_POINT('',#61855);
#12848=VERTEX_POINT('',#61859);
#12849=VERTEX_POINT('',#61861);
#12850=VERTEX_POINT('',#61865);
#12851=VERTEX_POINT('',#61867);
#12852=VERTEX_POINT('',#61871);
#12853=VERTEX_POINT('',#61873);
#12854=VERTEX_POINT('',#61877);
#12855=VERTEX_POINT('',#61879);
#12856=VERTEX_POINT('',#61883);
#12857=VERTEX_POINT('',#61885);
#12858=VERTEX_POINT('',#61889);
#12859=VERTEX_POINT('',#61891);
#12860=VERTEX_POINT('',#61895);
#12861=VERTEX_POINT('',#61897);
#12862=VERTEX_POINT('',#61901);
#12863=VERTEX_POINT('',#61903);
#12864=VERTEX_POINT('',#61907);
#12865=VERTEX_POINT('',#61909);
#12866=VERTEX_POINT('',#61913);
#12867=VERTEX_POINT('',#61915);
#12868=VERTEX_POINT('',#61919);
#12869=VERTEX_POINT('',#61921);
#12870=VERTEX_POINT('',#61925);
#12871=VERTEX_POINT('',#61927);
#12872=VERTEX_POINT('',#61931);
#12873=VERTEX_POINT('',#61933);
#12874=VERTEX_POINT('',#61937);
#12875=VERTEX_POINT('',#61939);
#12876=VERTEX_POINT('',#61943);
#12877=VERTEX_POINT('',#61945);
#12878=VERTEX_POINT('',#61949);
#12879=VERTEX_POINT('',#61951);
#12880=VERTEX_POINT('',#61955);
#12881=VERTEX_POINT('',#61957);
#12882=VERTEX_POINT('',#61961);
#12883=VERTEX_POINT('',#61963);
#12884=VERTEX_POINT('',#61967);
#12885=VERTEX_POINT('',#61969);
#12886=VERTEX_POINT('',#61973);
#12887=VERTEX_POINT('',#61975);
#12888=VERTEX_POINT('',#61979);
#12889=VERTEX_POINT('',#61981);
#12890=VERTEX_POINT('',#61985);
#12891=VERTEX_POINT('',#61987);
#12892=VERTEX_POINT('',#61991);
#12893=VERTEX_POINT('',#61993);
#12894=VERTEX_POINT('',#61997);
#12895=VERTEX_POINT('',#61999);
#12896=VERTEX_POINT('',#62003);
#12897=VERTEX_POINT('',#62005);
#12898=VERTEX_POINT('',#62009);
#12899=VERTEX_POINT('',#62011);
#12900=VERTEX_POINT('',#62015);
#12901=VERTEX_POINT('',#62017);
#12902=VERTEX_POINT('',#62021);
#12903=VERTEX_POINT('',#62023);
#12904=VERTEX_POINT('',#62027);
#12905=VERTEX_POINT('',#62029);
#12906=VERTEX_POINT('',#62033);
#12907=VERTEX_POINT('',#62035);
#12908=VERTEX_POINT('',#62039);
#12909=VERTEX_POINT('',#62041);
#12910=VERTEX_POINT('',#62045);
#12911=VERTEX_POINT('',#62047);
#12912=VERTEX_POINT('',#62051);
#12913=VERTEX_POINT('',#62053);
#12914=VERTEX_POINT('',#62057);
#12915=VERTEX_POINT('',#62059);
#12916=VERTEX_POINT('',#62063);
#12917=VERTEX_POINT('',#62065);
#12918=VERTEX_POINT('',#62069);
#12919=VERTEX_POINT('',#62071);
#12920=VERTEX_POINT('',#62075);
#12921=VERTEX_POINT('',#62077);
#12922=VERTEX_POINT('',#62081);
#12923=VERTEX_POINT('',#62083);
#12924=VERTEX_POINT('',#62087);
#12925=VERTEX_POINT('',#62089);
#12926=VERTEX_POINT('',#62093);
#12927=VERTEX_POINT('',#62095);
#12928=VERTEX_POINT('',#62099);
#12929=VERTEX_POINT('',#62101);
#12930=VERTEX_POINT('',#62105);
#12931=VERTEX_POINT('',#62107);
#12932=VERTEX_POINT('',#62111);
#12933=VERTEX_POINT('',#62113);
#12934=VERTEX_POINT('',#62117);
#12935=VERTEX_POINT('',#62119);
#12936=VERTEX_POINT('',#62123);
#12937=VERTEX_POINT('',#62125);
#12938=VERTEX_POINT('',#62129);
#12939=VERTEX_POINT('',#62131);
#12940=VERTEX_POINT('',#62135);
#12941=VERTEX_POINT('',#62137);
#12942=VERTEX_POINT('',#62141);
#12943=VERTEX_POINT('',#62143);
#12944=VERTEX_POINT('',#62147);
#12945=VERTEX_POINT('',#62149);
#12946=VERTEX_POINT('',#62153);
#12947=VERTEX_POINT('',#62155);
#12948=VERTEX_POINT('',#62159);
#12949=VERTEX_POINT('',#62161);
#12950=VERTEX_POINT('',#62165);
#12951=VERTEX_POINT('',#62167);
#12952=VERTEX_POINT('',#62171);
#12953=VERTEX_POINT('',#62173);
#12954=VERTEX_POINT('',#62177);
#12955=VERTEX_POINT('',#62179);
#12956=VERTEX_POINT('',#62183);
#12957=VERTEX_POINT('',#62185);
#12958=VERTEX_POINT('',#62189);
#12959=VERTEX_POINT('',#62191);
#12960=VERTEX_POINT('',#62195);
#12961=VERTEX_POINT('',#62197);
#12962=VERTEX_POINT('',#62201);
#12963=VERTEX_POINT('',#62203);
#12964=VERTEX_POINT('',#62207);
#12965=VERTEX_POINT('',#62209);
#12966=VERTEX_POINT('',#62213);
#12967=VERTEX_POINT('',#62215);
#12968=VERTEX_POINT('',#62219);
#12969=VERTEX_POINT('',#62221);
#12970=VERTEX_POINT('',#62225);
#12971=VERTEX_POINT('',#62227);
#12972=VERTEX_POINT('',#62231);
#12973=VERTEX_POINT('',#62233);
#12974=VERTEX_POINT('',#62237);
#12975=VERTEX_POINT('',#62239);
#12976=VERTEX_POINT('',#62243);
#12977=VERTEX_POINT('',#62245);
#12978=VERTEX_POINT('',#62249);
#12979=VERTEX_POINT('',#62251);
#12980=VERTEX_POINT('',#62255);
#12981=VERTEX_POINT('',#62257);
#12982=VERTEX_POINT('',#62261);
#12983=VERTEX_POINT('',#62263);
#12984=VERTEX_POINT('',#62267);
#12985=VERTEX_POINT('',#62269);
#12986=VERTEX_POINT('',#62273);
#12987=VERTEX_POINT('',#62275);
#12988=VERTEX_POINT('',#62279);
#12989=VERTEX_POINT('',#62281);
#12990=VERTEX_POINT('',#62285);
#12991=VERTEX_POINT('',#62290);
#12992=VERTEX_POINT('',#62294);
#12993=VERTEX_POINT('',#62299);
#12994=VERTEX_POINT('',#62303);
#12995=VERTEX_POINT('',#62308);
#12996=VERTEX_POINT('',#62312);
#12997=VERTEX_POINT('',#62317);
#12998=VERTEX_POINT('',#62321);
#12999=VERTEX_POINT('',#62326);
#13000=VERTEX_POINT('',#62330);
#13001=VERTEX_POINT('',#62335);
#13002=VERTEX_POINT('',#62339);
#13003=VERTEX_POINT('',#62344);
#13004=VERTEX_POINT('',#62348);
#13005=VERTEX_POINT('',#62353);
#13006=VERTEX_POINT('',#62357);
#13007=VERTEX_POINT('',#62362);
#13008=VERTEX_POINT('',#62366);
#13009=VERTEX_POINT('',#62371);
#13010=VERTEX_POINT('',#62375);
#13011=VERTEX_POINT('',#62380);
#13012=VERTEX_POINT('',#62384);
#13013=VERTEX_POINT('',#62389);
#13014=VERTEX_POINT('',#62393);
#13015=VERTEX_POINT('',#62398);
#13016=VERTEX_POINT('',#62402);
#13017=VERTEX_POINT('',#62407);
#13018=VERTEX_POINT('',#62411);
#13019=VERTEX_POINT('',#62416);
#13020=VERTEX_POINT('',#62420);
#13021=VERTEX_POINT('',#62422);
#13022=VERTEX_POINT('',#62426);
#13023=VERTEX_POINT('',#62428);
#13024=VERTEX_POINT('',#62432);
#13025=VERTEX_POINT('',#62434);
#13026=VERTEX_POINT('',#62438);
#13027=VERTEX_POINT('',#62440);
#13028=VERTEX_POINT('',#62444);
#13029=VERTEX_POINT('',#62446);
#13030=VERTEX_POINT('',#62450);
#13031=VERTEX_POINT('',#62452);
#13032=VERTEX_POINT('',#62456);
#13033=VERTEX_POINT('',#62458);
#13034=VERTEX_POINT('',#62462);
#13035=VERTEX_POINT('',#62464);
#13036=VERTEX_POINT('',#62468);
#13037=VERTEX_POINT('',#62470);
#13038=VERTEX_POINT('',#62474);
#13039=VERTEX_POINT('',#62476);
#13040=VERTEX_POINT('',#62480);
#13041=VERTEX_POINT('',#62482);
#13042=VERTEX_POINT('',#62494);
#13043=VERTEX_POINT('',#62496);
#13044=VERTEX_POINT('',#62500);
#13045=VERTEX_POINT('',#62504);
#13046=VERTEX_POINT('',#62508);
#13047=VERTEX_POINT('',#62512);
#13048=VERTEX_POINT('',#62516);
#13049=VERTEX_POINT('',#62518);
#13050=VERTEX_POINT('',#62522);
#13051=VERTEX_POINT('',#62524);
#13052=VERTEX_POINT('',#62528);
#13053=VERTEX_POINT('',#62530);
#13054=VERTEX_POINT('',#62534);
#13055=VERTEX_POINT('',#62536);
#13056=VERTEX_POINT('',#62540);
#13057=VERTEX_POINT('',#62542);
#13058=VERTEX_POINT('',#62546);
#13059=VERTEX_POINT('',#62548);
#13060=VERTEX_POINT('',#62552);
#13061=VERTEX_POINT('',#62554);
#13062=VERTEX_POINT('',#62558);
#13063=VERTEX_POINT('',#62560);
#13064=VERTEX_POINT('',#62564);
#13065=VERTEX_POINT('',#62566);
#13066=VERTEX_POINT('',#62570);
#13067=VERTEX_POINT('',#62572);
#13068=VERTEX_POINT('',#62576);
#13069=VERTEX_POINT('',#62578);
#13070=VERTEX_POINT('',#62582);
#13071=VERTEX_POINT('',#62584);
#13072=VERTEX_POINT('',#62588);
#13073=VERTEX_POINT('',#62590);
#13074=VERTEX_POINT('',#62594);
#13075=VERTEX_POINT('',#62596);
#13076=VERTEX_POINT('',#62600);
#13077=VERTEX_POINT('',#62602);
#13078=VERTEX_POINT('',#62606);
#13079=VERTEX_POINT('',#62608);
#13080=VERTEX_POINT('',#62612);
#13081=VERTEX_POINT('',#62614);
#13082=VERTEX_POINT('',#62618);
#13083=VERTEX_POINT('',#62620);
#13084=VERTEX_POINT('',#62624);
#13085=VERTEX_POINT('',#62626);
#13086=VERTEX_POINT('',#62630);
#13087=VERTEX_POINT('',#62632);
#13088=VERTEX_POINT('',#62636);
#13089=VERTEX_POINT('',#62638);
#13090=VERTEX_POINT('',#62642);
#13091=VERTEX_POINT('',#62644);
#13092=VERTEX_POINT('',#62648);
#13093=VERTEX_POINT('',#62650);
#13094=VERTEX_POINT('',#62654);
#13095=VERTEX_POINT('',#62656);
#13096=VERTEX_POINT('',#62660);
#13097=VERTEX_POINT('',#62662);
#13098=VERTEX_POINT('',#62666);
#13099=VERTEX_POINT('',#62668);
#13100=VERTEX_POINT('',#62672);
#13101=VERTEX_POINT('',#62674);
#13102=VERTEX_POINT('',#62678);
#13103=VERTEX_POINT('',#62680);
#13104=VERTEX_POINT('',#62684);
#13105=VERTEX_POINT('',#62686);
#13106=VERTEX_POINT('',#62690);
#13107=VERTEX_POINT('',#62692);
#13108=VERTEX_POINT('',#62696);
#13109=VERTEX_POINT('',#62698);
#13110=VERTEX_POINT('',#62702);
#13111=VERTEX_POINT('',#62704);
#13112=VERTEX_POINT('',#62708);
#13113=VERTEX_POINT('',#62710);
#13114=VERTEX_POINT('',#62714);
#13115=VERTEX_POINT('',#62716);
#13116=VERTEX_POINT('',#62720);
#13117=VERTEX_POINT('',#62722);
#13118=VERTEX_POINT('',#62726);
#13119=VERTEX_POINT('',#62728);
#13120=VERTEX_POINT('',#62732);
#13121=VERTEX_POINT('',#62734);
#13122=VERTEX_POINT('',#62738);
#13123=VERTEX_POINT('',#62740);
#13124=VERTEX_POINT('',#62744);
#13125=VERTEX_POINT('',#62746);
#13126=VERTEX_POINT('',#62750);
#13127=VERTEX_POINT('',#62752);
#13128=VERTEX_POINT('',#62756);
#13129=VERTEX_POINT('',#62758);
#13130=VERTEX_POINT('',#62762);
#13131=VERTEX_POINT('',#62764);
#13132=VERTEX_POINT('',#62768);
#13133=VERTEX_POINT('',#62770);
#13134=VERTEX_POINT('',#62774);
#13135=VERTEX_POINT('',#62776);
#13136=VERTEX_POINT('',#62780);
#13137=VERTEX_POINT('',#62782);
#13138=VERTEX_POINT('',#62786);
#13139=VERTEX_POINT('',#62788);
#13140=VERTEX_POINT('',#62792);
#13141=VERTEX_POINT('',#62794);
#13142=VERTEX_POINT('',#62798);
#13143=VERTEX_POINT('',#62800);
#13144=VERTEX_POINT('',#62804);
#13145=VERTEX_POINT('',#62806);
#13146=VERTEX_POINT('',#62810);
#13147=VERTEX_POINT('',#62812);
#13148=VERTEX_POINT('',#62816);
#13149=VERTEX_POINT('',#62818);
#13150=VERTEX_POINT('',#62822);
#13151=VERTEX_POINT('',#62824);
#13152=VERTEX_POINT('',#62828);
#13153=VERTEX_POINT('',#62830);
#13154=VERTEX_POINT('',#62834);
#13155=VERTEX_POINT('',#62836);
#13156=VERTEX_POINT('',#62840);
#13157=VERTEX_POINT('',#62842);
#13158=VERTEX_POINT('',#62846);
#13159=VERTEX_POINT('',#62848);
#13160=VERTEX_POINT('',#62852);
#13161=VERTEX_POINT('',#62854);
#13162=VERTEX_POINT('',#62858);
#13163=VERTEX_POINT('',#62860);
#13164=VERTEX_POINT('',#62864);
#13165=VERTEX_POINT('',#62866);
#13166=VERTEX_POINT('',#62870);
#13167=VERTEX_POINT('',#62872);
#13168=VERTEX_POINT('',#62876);
#13169=VERTEX_POINT('',#62878);
#13170=VERTEX_POINT('',#62882);
#13171=VERTEX_POINT('',#62884);
#13172=VERTEX_POINT('',#62888);
#13173=VERTEX_POINT('',#62890);
#13174=VERTEX_POINT('',#62894);
#13175=VERTEX_POINT('',#62896);
#13176=VERTEX_POINT('',#62900);
#13177=VERTEX_POINT('',#62902);
#13178=VERTEX_POINT('',#62906);
#13179=VERTEX_POINT('',#62908);
#13180=VERTEX_POINT('',#62912);
#13181=VERTEX_POINT('',#62914);
#13182=VERTEX_POINT('',#62918);
#13183=VERTEX_POINT('',#62920);
#13184=VERTEX_POINT('',#62924);
#13185=VERTEX_POINT('',#62926);
#13186=VERTEX_POINT('',#62930);
#13187=VERTEX_POINT('',#62932);
#13188=VERTEX_POINT('',#62936);
#13189=VERTEX_POINT('',#62938);
#13190=VERTEX_POINT('',#62942);
#13191=VERTEX_POINT('',#62944);
#13192=VERTEX_POINT('',#62948);
#13193=VERTEX_POINT('',#62950);
#13194=VERTEX_POINT('',#62954);
#13195=VERTEX_POINT('',#62956);
#13196=VERTEX_POINT('',#62960);
#13197=VERTEX_POINT('',#62962);
#13198=VERTEX_POINT('',#62966);
#13199=VERTEX_POINT('',#62968);
#13200=VERTEX_POINT('',#62972);
#13201=VERTEX_POINT('',#62974);
#13202=VERTEX_POINT('',#62978);
#13203=VERTEX_POINT('',#62980);
#13204=VERTEX_POINT('',#62984);
#13205=VERTEX_POINT('',#62986);
#13206=VERTEX_POINT('',#62990);
#13207=VERTEX_POINT('',#62992);
#13208=VERTEX_POINT('',#62996);
#13209=VERTEX_POINT('',#62998);
#13210=VERTEX_POINT('',#63002);
#13211=VERTEX_POINT('',#63004);
#13212=VERTEX_POINT('',#63008);
#13213=VERTEX_POINT('',#63010);
#13214=VERTEX_POINT('',#63014);
#13215=VERTEX_POINT('',#63016);
#13216=VERTEX_POINT('',#63020);
#13217=VERTEX_POINT('',#63022);
#13218=VERTEX_POINT('',#63026);
#13219=VERTEX_POINT('',#63028);
#13220=VERTEX_POINT('',#63032);
#13221=VERTEX_POINT('',#63034);
#13222=VERTEX_POINT('',#63038);
#13223=VERTEX_POINT('',#63040);
#13224=VERTEX_POINT('',#63044);
#13225=VERTEX_POINT('',#63046);
#13226=VERTEX_POINT('',#63050);
#13227=VERTEX_POINT('',#63052);
#13228=VERTEX_POINT('',#63056);
#13229=VERTEX_POINT('',#63058);
#13230=VERTEX_POINT('',#63062);
#13231=VERTEX_POINT('',#63064);
#13232=VERTEX_POINT('',#63068);
#13233=VERTEX_POINT('',#63070);
#13234=VERTEX_POINT('',#63074);
#13235=VERTEX_POINT('',#63076);
#13236=VERTEX_POINT('',#63080);
#13237=VERTEX_POINT('',#63082);
#13238=VERTEX_POINT('',#63086);
#13239=VERTEX_POINT('',#63088);
#13240=VERTEX_POINT('',#63092);
#13241=VERTEX_POINT('',#63094);
#13242=VERTEX_POINT('',#63098);
#13243=VERTEX_POINT('',#63100);
#13244=VERTEX_POINT('',#63104);
#13245=VERTEX_POINT('',#63106);
#13246=VERTEX_POINT('',#63110);
#13247=VERTEX_POINT('',#63112);
#13248=VERTEX_POINT('',#63116);
#13249=VERTEX_POINT('',#63118);
#13250=VERTEX_POINT('',#63122);
#13251=VERTEX_POINT('',#63124);
#13252=VERTEX_POINT('',#63128);
#13253=VERTEX_POINT('',#63130);
#13254=VERTEX_POINT('',#63134);
#13255=VERTEX_POINT('',#63136);
#13256=VERTEX_POINT('',#63140);
#13257=VERTEX_POINT('',#63142);
#13258=VERTEX_POINT('',#63146);
#13259=VERTEX_POINT('',#63148);
#13260=VERTEX_POINT('',#63152);
#13261=VERTEX_POINT('',#63154);
#13262=VERTEX_POINT('',#63158);
#13263=VERTEX_POINT('',#63160);
#13264=VERTEX_POINT('',#63164);
#13265=VERTEX_POINT('',#63166);
#13266=VERTEX_POINT('',#63170);
#13267=VERTEX_POINT('',#63172);
#13268=VERTEX_POINT('',#63176);
#13269=VERTEX_POINT('',#63178);
#13270=VERTEX_POINT('',#63182);
#13271=VERTEX_POINT('',#63184);
#13272=VERTEX_POINT('',#63188);
#13273=VERTEX_POINT('',#63190);
#13274=VERTEX_POINT('',#63194);
#13275=VERTEX_POINT('',#63196);
#13276=VERTEX_POINT('',#63200);
#13277=VERTEX_POINT('',#63202);
#13278=VERTEX_POINT('',#63206);
#13279=VERTEX_POINT('',#63208);
#13280=VERTEX_POINT('',#63212);
#13281=VERTEX_POINT('',#63214);
#13282=VERTEX_POINT('',#63218);
#13283=VERTEX_POINT('',#63220);
#13284=VERTEX_POINT('',#63224);
#13285=VERTEX_POINT('',#63226);
#13286=VERTEX_POINT('',#63230);
#13287=VERTEX_POINT('',#63232);
#13288=VERTEX_POINT('',#63236);
#13289=VERTEX_POINT('',#63238);
#13290=VERTEX_POINT('',#63242);
#13291=VERTEX_POINT('',#63244);
#13292=VERTEX_POINT('',#63248);
#13293=VERTEX_POINT('',#63250);
#13294=VERTEX_POINT('',#63254);
#13295=VERTEX_POINT('',#63256);
#13296=VERTEX_POINT('',#63260);
#13297=VERTEX_POINT('',#63262);
#13298=VERTEX_POINT('',#63266);
#13299=VERTEX_POINT('',#63268);
#13300=VERTEX_POINT('',#63272);
#13301=VERTEX_POINT('',#63274);
#13302=VERTEX_POINT('',#63278);
#13303=VERTEX_POINT('',#63280);
#13304=VERTEX_POINT('',#63284);
#13305=VERTEX_POINT('',#63286);
#13306=VERTEX_POINT('',#63290);
#13307=VERTEX_POINT('',#63292);
#13308=VERTEX_POINT('',#63296);
#13309=VERTEX_POINT('',#63298);
#13310=VERTEX_POINT('',#63302);
#13311=VERTEX_POINT('',#63304);
#13312=VERTEX_POINT('',#63308);
#13313=VERTEX_POINT('',#63310);
#13314=VERTEX_POINT('',#63314);
#13315=VERTEX_POINT('',#63316);
#13316=VERTEX_POINT('',#63320);
#13317=VERTEX_POINT('',#63322);
#13318=VERTEX_POINT('',#63326);
#13319=VERTEX_POINT('',#63328);
#13320=VERTEX_POINT('',#63332);
#13321=VERTEX_POINT('',#63334);
#13322=VERTEX_POINT('',#63338);
#13323=VERTEX_POINT('',#63340);
#13324=VERTEX_POINT('',#63344);
#13325=VERTEX_POINT('',#63346);
#13326=VERTEX_POINT('',#63350);
#13327=VERTEX_POINT('',#63352);
#13328=VERTEX_POINT('',#63356);
#13329=VERTEX_POINT('',#63358);
#13330=VERTEX_POINT('',#63362);
#13331=VERTEX_POINT('',#63364);
#13332=VERTEX_POINT('',#63368);
#13333=VERTEX_POINT('',#63370);
#13334=VERTEX_POINT('',#63374);
#13335=VERTEX_POINT('',#63376);
#13336=VERTEX_POINT('',#63380);
#13337=VERTEX_POINT('',#63382);
#13338=VERTEX_POINT('',#63386);
#13339=VERTEX_POINT('',#63388);
#13340=VERTEX_POINT('',#63392);
#13341=VERTEX_POINT('',#63394);
#13342=VERTEX_POINT('',#63398);
#13343=VERTEX_POINT('',#63400);
#13344=VERTEX_POINT('',#63404);
#13345=VERTEX_POINT('',#63406);
#13346=VERTEX_POINT('',#63410);
#13347=VERTEX_POINT('',#63412);
#13348=VERTEX_POINT('',#63416);
#13349=VERTEX_POINT('',#63418);
#13350=VERTEX_POINT('',#63422);
#13351=VERTEX_POINT('',#63424);
#13352=VERTEX_POINT('',#63428);
#13353=VERTEX_POINT('',#63430);
#13354=VERTEX_POINT('',#63434);
#13355=VERTEX_POINT('',#63436);
#13356=VERTEX_POINT('',#63440);
#13357=VERTEX_POINT('',#63442);
#13358=VERTEX_POINT('',#63446);
#13359=VERTEX_POINT('',#63448);
#13360=VERTEX_POINT('',#63452);
#13361=VERTEX_POINT('',#63454);
#13362=VERTEX_POINT('',#63458);
#13363=VERTEX_POINT('',#63460);
#13364=VERTEX_POINT('',#63703);
#13365=VERTEX_POINT('',#63705);
#13366=VERTEX_POINT('',#63709);
#13367=VERTEX_POINT('',#63711);
#13368=VERTEX_POINT('',#63719);
#13369=VERTEX_POINT('',#63720);
#13370=VERTEX_POINT('',#63722);
#13371=VERTEX_POINT('',#63724);
#13372=VERTEX_POINT('',#63726);
#13373=VERTEX_POINT('',#63728);
#16241=EDGE_CURVE('',#12265,#12266,#9053,.T.);
#16242=EDGE_CURVE('',#12267,#12265,#3100,.F.);
#16243=EDGE_CURVE('',#12267,#12268,#9054,.T.);
#16244=EDGE_CURVE('',#12268,#12268,#3775,.T.);
#16245=EDGE_CURVE('',#12269,#12267,#3776,.T.);
#16246=EDGE_CURVE('',#12266,#12269,#3101,.F.);
#16247=EDGE_CURVE('',#12270,#12271,#9055,.T.);
#16248=EDGE_CURVE('',#12265,#12270,#3102,.F.);
#16249=EDGE_CURVE('',#12271,#12266,#3103,.F.);
#16250=EDGE_CURVE('',#12272,#12273,#9056,.T.);
#16251=EDGE_CURVE('',#12270,#12272,#3104,.F.);
#16252=EDGE_CURVE('',#12273,#12271,#3105,.F.);
#16253=EDGE_CURVE('',#12274,#12275,#9057,.T.);
#16254=EDGE_CURVE('',#12272,#12274,#3106,.F.);
#16255=EDGE_CURVE('',#12275,#12273,#3107,.F.);
#16256=EDGE_CURVE('',#12276,#12277,#9058,.T.);
#16257=EDGE_CURVE('',#12274,#12276,#3108,.F.);
#16258=EDGE_CURVE('',#12277,#12275,#3109,.F.);
#16259=EDGE_CURVE('',#12278,#12279,#9059,.T.);
#16260=EDGE_CURVE('',#12276,#12278,#3110,.F.);
#16261=EDGE_CURVE('',#12279,#12277,#3111,.F.);
#16262=EDGE_CURVE('',#12280,#12281,#9060,.T.);
#16263=EDGE_CURVE('',#12278,#12280,#3112,.F.);
#16264=EDGE_CURVE('',#12281,#12279,#3113,.F.);
#16265=EDGE_CURVE('',#12282,#12283,#9061,.T.);
#16266=EDGE_CURVE('',#12280,#12282,#3114,.F.);
#16267=EDGE_CURVE('',#12283,#12281,#3115,.F.);
#16268=EDGE_CURVE('',#12284,#12285,#9062,.T.);
#16269=EDGE_CURVE('',#12282,#12284,#3116,.F.);
#16270=EDGE_CURVE('',#12285,#12283,#3117,.F.);
#16271=EDGE_CURVE('',#12286,#12287,#9063,.T.);
#16272=EDGE_CURVE('',#12284,#12286,#3118,.F.);
#16273=EDGE_CURVE('',#12287,#12285,#3119,.F.);
#16274=EDGE_CURVE('',#12288,#12289,#9064,.T.);
#16275=EDGE_CURVE('',#12286,#12288,#3120,.F.);
#16276=EDGE_CURVE('',#12289,#12287,#3121,.F.);
#16277=EDGE_CURVE('',#12290,#12291,#9065,.T.);
#16278=EDGE_CURVE('',#12288,#12290,#3122,.F.);
#16279=EDGE_CURVE('',#12291,#12289,#3123,.F.);
#16280=EDGE_CURVE('',#12292,#12293,#9066,.T.);
#16281=EDGE_CURVE('',#12290,#12292,#3124,.F.);
#16282=EDGE_CURVE('',#12293,#12291,#3125,.F.);
#16283=EDGE_CURVE('',#12294,#12295,#9067,.T.);
#16284=EDGE_CURVE('',#12292,#12294,#3126,.F.);
#16285=EDGE_CURVE('',#12295,#12293,#3127,.F.);
#16286=EDGE_CURVE('',#12296,#12297,#9068,.T.);
#16287=EDGE_CURVE('',#12294,#12296,#3128,.F.);
#16288=EDGE_CURVE('',#12297,#12295,#3129,.F.);
#16289=EDGE_CURVE('',#12298,#12299,#9069,.T.);
#16290=EDGE_CURVE('',#12296,#12298,#3130,.F.);
#16291=EDGE_CURVE('',#12299,#12297,#3131,.F.);
#16292=EDGE_CURVE('',#12300,#12301,#9070,.T.);
#16293=EDGE_CURVE('',#12298,#12300,#3132,.F.);
#16294=EDGE_CURVE('',#12301,#12299,#3133,.F.);
#16295=EDGE_CURVE('',#12302,#12303,#9071,.T.);
#16296=EDGE_CURVE('',#12300,#12302,#3134,.F.);
#16297=EDGE_CURVE('',#12303,#12301,#3135,.F.);
#16298=EDGE_CURVE('',#12304,#12305,#9072,.T.);
#16299=EDGE_CURVE('',#12302,#12304,#3136,.F.);
#16300=EDGE_CURVE('',#12305,#12303,#3137,.F.);
#16301=EDGE_CURVE('',#12306,#12307,#9073,.T.);
#16302=EDGE_CURVE('',#12304,#12306,#3138,.F.);
#16303=EDGE_CURVE('',#12307,#12305,#3139,.F.);
#16304=EDGE_CURVE('',#12308,#12309,#9074,.T.);
#16305=EDGE_CURVE('',#12306,#12308,#3140,.F.);
#16306=EDGE_CURVE('',#12309,#12307,#3141,.F.);
#16307=EDGE_CURVE('',#12310,#12311,#9075,.T.);
#16308=EDGE_CURVE('',#12308,#12310,#3142,.F.);
#16309=EDGE_CURVE('',#12311,#12309,#3143,.F.);
#16310=EDGE_CURVE('',#12312,#12313,#9076,.T.);
#16311=EDGE_CURVE('',#12310,#12312,#3144,.F.);
#16312=EDGE_CURVE('',#12313,#12311,#3145,.F.);
#16313=EDGE_CURVE('',#12314,#12315,#9077,.T.);
#16314=EDGE_CURVE('',#12312,#12314,#3146,.F.);
#16315=EDGE_CURVE('',#12315,#12313,#3147,.F.);
#16316=EDGE_CURVE('',#12316,#12317,#9078,.T.);
#16317=EDGE_CURVE('',#12314,#12316,#3148,.F.);
#16318=EDGE_CURVE('',#12317,#12315,#3149,.F.);
#16319=EDGE_CURVE('',#12318,#12319,#9079,.T.);
#16320=EDGE_CURVE('',#12316,#12318,#3150,.F.);
#16321=EDGE_CURVE('',#12319,#12317,#3151,.F.);
#16322=EDGE_CURVE('',#12320,#12321,#9080,.T.);
#16323=EDGE_CURVE('',#12318,#12320,#3152,.F.);
#16324=EDGE_CURVE('',#12321,#12319,#3153,.F.);
#16325=EDGE_CURVE('',#12322,#12323,#9081,.T.);
#16326=EDGE_CURVE('',#12320,#12322,#3154,.F.);
#16327=EDGE_CURVE('',#12323,#12321,#3155,.F.);
#16328=EDGE_CURVE('',#12324,#12325,#9082,.T.);
#16329=EDGE_CURVE('',#12324,#12326,#3156,.F.);
#16330=EDGE_CURVE('',#12325,#12326,#3777,.T.);
#16331=EDGE_CURVE('',#12327,#12326,#9083,.T.);
#16332=EDGE_CURVE('',#12328,#12327,#3157,.F.);
#16333=EDGE_CURVE('',#12326,#12328,#3778,.T.);
#16334=EDGE_CURVE('',#12329,#12330,#9084,.T.);
#16335=EDGE_CURVE('',#12327,#12329,#3158,.F.);
#16336=EDGE_CURVE('',#12326,#12330,#3159,.T.);
#16337=EDGE_CURVE('',#12331,#12332,#9085,.T.);
#16338=EDGE_CURVE('',#12329,#12331,#3160,.F.);
#16339=EDGE_CURVE('',#12330,#12332,#3161,.T.);
#16340=EDGE_CURVE('',#12333,#12334,#9086,.T.);
#16341=EDGE_CURVE('',#12331,#12333,#3162,.F.);
#16342=EDGE_CURVE('',#12332,#12334,#3163,.T.);
#16343=EDGE_CURVE('',#12335,#12336,#9087,.T.);
#16344=EDGE_CURVE('',#12333,#12335,#3164,.F.);
#16345=EDGE_CURVE('',#12334,#12336,#3165,.T.);
#16346=EDGE_CURVE('',#12337,#12338,#9088,.T.);
#16347=EDGE_CURVE('',#12335,#12337,#3166,.F.);
#16348=EDGE_CURVE('',#12336,#12338,#3167,.T.);
#16349=EDGE_CURVE('',#12339,#12340,#9089,.T.);
#16350=EDGE_CURVE('',#12337,#12339,#3168,.F.);
#16351=EDGE_CURVE('',#12338,#12340,#3169,.T.);
#16352=EDGE_CURVE('',#12341,#12342,#9090,.T.);
#16353=EDGE_CURVE('',#12339,#12341,#3170,.F.);
#16354=EDGE_CURVE('',#12340,#12342,#3171,.T.);
#16355=EDGE_CURVE('',#12343,#12344,#9091,.T.);
#16356=EDGE_CURVE('',#12341,#12343,#3172,.F.);
#16357=EDGE_CURVE('',#12342,#12344,#3173,.T.);
#16358=EDGE_CURVE('',#12345,#12346,#9092,.T.);
#16359=EDGE_CURVE('',#12343,#12345,#3174,.F.);
#16360=EDGE_CURVE('',#12344,#12346,#3175,.T.);
#16361=EDGE_CURVE('',#12347,#12348,#9093,.T.);
#16362=EDGE_CURVE('',#12345,#12347,#3176,.F.);
#16363=EDGE_CURVE('',#12346,#12348,#3177,.T.);
#16364=EDGE_CURVE('',#12349,#12350,#9094,.T.);
#16365=EDGE_CURVE('',#12347,#12349,#3178,.F.);
#16366=EDGE_CURVE('',#12348,#12350,#3179,.T.);
#16367=EDGE_CURVE('',#12351,#12352,#9095,.T.);
#16368=EDGE_CURVE('',#12349,#12351,#3180,.F.);
#16369=EDGE_CURVE('',#12350,#12352,#3181,.T.);
#16370=EDGE_CURVE('',#12353,#12354,#9096,.T.);
#16371=EDGE_CURVE('',#12351,#12353,#3182,.F.);
#16372=EDGE_CURVE('',#12352,#12354,#3183,.T.);
#16373=EDGE_CURVE('',#12355,#12356,#9097,.T.);
#16374=EDGE_CURVE('',#12353,#12355,#3184,.F.);
#16375=EDGE_CURVE('',#12354,#12356,#3185,.T.);
#16376=EDGE_CURVE('',#12357,#12358,#9098,.T.);
#16377=EDGE_CURVE('',#12355,#12357,#3186,.F.);
#16378=EDGE_CURVE('',#12356,#12358,#3187,.T.);
#16379=EDGE_CURVE('',#12359,#12360,#9099,.T.);
#16380=EDGE_CURVE('',#12357,#12359,#3188,.F.);
#16381=EDGE_CURVE('',#12358,#12360,#3189,.T.);
#16382=EDGE_CURVE('',#12361,#12362,#9100,.T.);
#16383=EDGE_CURVE('',#12359,#12361,#3190,.F.);
#16384=EDGE_CURVE('',#12360,#12362,#3191,.T.);
#16385=EDGE_CURVE('',#12363,#12364,#9101,.T.);
#16386=EDGE_CURVE('',#12361,#12363,#3192,.F.);
#16387=EDGE_CURVE('',#12362,#12364,#3193,.T.);
#16388=EDGE_CURVE('',#12365,#12366,#9102,.T.);
#16389=EDGE_CURVE('',#12363,#12365,#3194,.F.);
#16390=EDGE_CURVE('',#12364,#12366,#3195,.T.);
#16391=EDGE_CURVE('',#12367,#12368,#9103,.T.);
#16392=EDGE_CURVE('',#12365,#12367,#3196,.F.);
#16393=EDGE_CURVE('',#12366,#12368,#3197,.T.);
#16394=EDGE_CURVE('',#12369,#12370,#9104,.T.);
#16395=EDGE_CURVE('',#12367,#12369,#3198,.F.);
#16396=EDGE_CURVE('',#12368,#12370,#3199,.T.);
#16397=EDGE_CURVE('',#12371,#12372,#9105,.T.);
#16398=EDGE_CURVE('',#12369,#12371,#3200,.F.);
#16399=EDGE_CURVE('',#12370,#12372,#3201,.T.);
#16400=EDGE_CURVE('',#12373,#12374,#9106,.T.);
#16401=EDGE_CURVE('',#12371,#12373,#3202,.F.);
#16402=EDGE_CURVE('',#12372,#12374,#3203,.T.);
#16403=EDGE_CURVE('',#12375,#12376,#9107,.T.);
#16404=EDGE_CURVE('',#12373,#12375,#3204,.F.);
#16405=EDGE_CURVE('',#12374,#12376,#3205,.T.);
#16406=EDGE_CURVE('',#12377,#12378,#9108,.T.);
#16407=EDGE_CURVE('',#12375,#12377,#3206,.F.);
#16408=EDGE_CURVE('',#12376,#12378,#3207,.T.);
#16409=EDGE_CURVE('',#12379,#12380,#9109,.T.);
#16410=EDGE_CURVE('',#12377,#12379,#3208,.F.);
#16411=EDGE_CURVE('',#12378,#12380,#3209,.T.);
#16412=EDGE_CURVE('',#12381,#12382,#9110,.T.);
#16413=EDGE_CURVE('',#12379,#12381,#3210,.F.);
#16414=EDGE_CURVE('',#12380,#12382,#3211,.T.);
#16415=EDGE_CURVE('',#12383,#12384,#9111,.T.);
#16416=EDGE_CURVE('',#12381,#12383,#3212,.F.);
#16417=EDGE_CURVE('',#12382,#12384,#3213,.T.);
#16418=EDGE_CURVE('',#12385,#12386,#9112,.T.);
#16419=EDGE_CURVE('',#12383,#12385,#3214,.F.);
#16420=EDGE_CURVE('',#12384,#12386,#3215,.T.);
#16421=EDGE_CURVE('',#12386,#12387,#3216,.T.);
#16422=EDGE_CURVE('',#12385,#12387,#3779,.T.);
#16423=EDGE_CURVE('',#12328,#12325,#3780,.T.);
#16424=EDGE_CURVE('',#12328,#12388,#3217,.T.);
#16425=EDGE_CURVE('',#12388,#12389,#3781,.T.);
#16426=EDGE_CURVE('',#12389,#12324,#3218,.F.);
#16427=EDGE_CURVE('',#12389,#12323,#3219,.F.);
#16428=EDGE_CURVE('',#12322,#12388,#3220,.F.);
#16429=EDGE_CURVE('',#12390,#12391,#2000,.T.);
#16430=EDGE_CURVE('',#12391,#12392,#9113,.T.);
#16431=EDGE_CURVE('',#12392,#12393,#2001,.T.);
#16432=EDGE_CURVE('',#12390,#12393,#9114,.T.);
#16433=EDGE_CURVE('',#12394,#12395,#2002,.T.);
#16434=EDGE_CURVE('',#12395,#12396,#9115,.T.);
#16435=EDGE_CURVE('',#12396,#12397,#2003,.T.);
#16436=EDGE_CURVE('',#12394,#12397,#9116,.T.);
#16437=EDGE_CURVE('',#12398,#12399,#2004,.T.);
#16438=EDGE_CURVE('',#12399,#12400,#9117,.T.);
#16439=EDGE_CURVE('',#12400,#12401,#2005,.T.);
#16440=EDGE_CURVE('',#12398,#12401,#9118,.T.);
#16441=EDGE_CURVE('',#12402,#12403,#2006,.T.);
#16442=EDGE_CURVE('',#12403,#12404,#9119,.T.);
#16443=EDGE_CURVE('',#12404,#12405,#2007,.T.);
#16444=EDGE_CURVE('',#12402,#12405,#9120,.T.);
#16445=EDGE_CURVE('',#12406,#12407,#2008,.T.);
#16446=EDGE_CURVE('',#12407,#12408,#9121,.T.);
#16447=EDGE_CURVE('',#12408,#12409,#2009,.T.);
#16448=EDGE_CURVE('',#12406,#12409,#9122,.T.);
#16449=EDGE_CURVE('',#12410,#12411,#2010,.T.);
#16450=EDGE_CURVE('',#12411,#12412,#9123,.T.);
#16451=EDGE_CURVE('',#12412,#12413,#2011,.T.);
#16452=EDGE_CURVE('',#12410,#12413,#9124,.T.);
#16453=EDGE_CURVE('',#12414,#12415,#2012,.T.);
#16454=EDGE_CURVE('',#12415,#12416,#9125,.T.);
#16455=EDGE_CURVE('',#12416,#12417,#2013,.T.);
#16456=EDGE_CURVE('',#12414,#12417,#9126,.T.);
#16457=EDGE_CURVE('',#12418,#12419,#2014,.T.);
#16458=EDGE_CURVE('',#12419,#12420,#9127,.T.);
#16459=EDGE_CURVE('',#12420,#12421,#2015,.T.);
#16460=EDGE_CURVE('',#12418,#12421,#9128,.T.);
#16461=EDGE_CURVE('',#12422,#12423,#2016,.T.);
#16462=EDGE_CURVE('',#12423,#12424,#9129,.T.);
#16463=EDGE_CURVE('',#12424,#12425,#2017,.T.);
#16464=EDGE_CURVE('',#12422,#12425,#9130,.T.);
#16465=EDGE_CURVE('',#12426,#12427,#2018,.T.);
#16466=EDGE_CURVE('',#12427,#12428,#9131,.T.);
#16467=EDGE_CURVE('',#12428,#12429,#2019,.T.);
#16468=EDGE_CURVE('',#12426,#12429,#9132,.T.);
#16469=EDGE_CURVE('',#12430,#12431,#2020,.T.);
#16470=EDGE_CURVE('',#12431,#12432,#9133,.T.);
#16471=EDGE_CURVE('',#12432,#12433,#2021,.T.);
#16472=EDGE_CURVE('',#12430,#12433,#9134,.T.);
#16473=EDGE_CURVE('',#12434,#12435,#2022,.T.);
#16474=EDGE_CURVE('',#12435,#12436,#9135,.T.);
#16475=EDGE_CURVE('',#12436,#12437,#2023,.T.);
#16476=EDGE_CURVE('',#12434,#12437,#9136,.T.);
#16477=EDGE_CURVE('',#12438,#12439,#2024,.T.);
#16478=EDGE_CURVE('',#12439,#12440,#9137,.T.);
#16479=EDGE_CURVE('',#12440,#12441,#2025,.T.);
#16480=EDGE_CURVE('',#12438,#12441,#9138,.T.);
#16481=EDGE_CURVE('',#12442,#12443,#2026,.T.);
#16482=EDGE_CURVE('',#12443,#12444,#9139,.T.);
#16483=EDGE_CURVE('',#12444,#12445,#2027,.T.);
#16484=EDGE_CURVE('',#12442,#12445,#9140,.T.);
#16485=EDGE_CURVE('',#12446,#12447,#2028,.T.);
#16486=EDGE_CURVE('',#12447,#12448,#9141,.T.);
#16487=EDGE_CURVE('',#12448,#12449,#2029,.T.);
#16488=EDGE_CURVE('',#12446,#12449,#9142,.T.);
#16489=EDGE_CURVE('',#12450,#12451,#868,.T.);
#16490=EDGE_CURVE('',#12452,#12450,#869,.T.);
#16491=EDGE_CURVE('',#12453,#12452,#870,.T.);
#16492=EDGE_CURVE('',#12454,#12453,#871,.T.);
#16493=EDGE_CURVE('',#12455,#12454,#872,.T.);
#16494=EDGE_CURVE('',#12456,#12455,#873,.T.);
#16495=EDGE_CURVE('',#12451,#12456,#874,.T.);
#16496=EDGE_CURVE('',#12451,#12457,#9143,.T.);
#16497=EDGE_CURVE('',#12457,#12457,#3782,.T.);
#16498=EDGE_CURVE('',#12458,#12458,#3783,.T.);
#16499=EDGE_CURVE('',#12458,#12459,#3784,.T.);
#16500=EDGE_CURVE('',#12459,#12459,#3785,.T.);
#16501=EDGE_CURVE('',#12460,#12461,#3221,.T.);
#16502=EDGE_CURVE('',#12462,#12460,#875,.T.);
#16503=EDGE_CURVE('',#12463,#12462,#3786,.T.);
#16504=EDGE_CURVE('',#12464,#12463,#876,.T.);
#16505=EDGE_CURVE('',#12465,#12464,#2030,.T.);
#16506=EDGE_CURVE('',#12466,#12465,#877,.T.);
#16507=EDGE_CURVE('',#12467,#12466,#3787,.T.);
#16508=EDGE_CURVE('',#12468,#12467,#878,.T.);
#16509=EDGE_CURVE('',#12469,#12468,#2031,.T.);
#16510=EDGE_CURVE('',#12470,#12469,#879,.T.);
#16511=EDGE_CURVE('',#12471,#12470,#3788,.T.);
#16512=EDGE_CURVE('',#12472,#12471,#880,.T.);
#16513=EDGE_CURVE('',#12473,#12472,#2032,.T.);
#16514=EDGE_CURVE('',#12474,#12473,#881,.T.);
#16515=EDGE_CURVE('',#12475,#12474,#3789,.T.);
#16516=EDGE_CURVE('',#12476,#12475,#882,.T.);
#16517=EDGE_CURVE('',#12477,#12476,#2033,.T.);
#16518=EDGE_CURVE('',#12478,#12477,#883,.T.);
#16519=EDGE_CURVE('',#12479,#12478,#3790,.T.);
#16520=EDGE_CURVE('',#12480,#12479,#884,.T.);
#16521=EDGE_CURVE('',#12481,#12480,#2034,.T.);
#16522=EDGE_CURVE('',#12482,#12481,#885,.T.);
#16523=EDGE_CURVE('',#12483,#12482,#3791,.T.);
#16524=EDGE_CURVE('',#12484,#12483,#886,.T.);
#16525=EDGE_CURVE('',#12485,#12484,#2035,.T.);
#16526=EDGE_CURVE('',#12486,#12485,#887,.T.);
#16527=EDGE_CURVE('',#12487,#12486,#3792,.T.);
#16528=EDGE_CURVE('',#12488,#12487,#888,.T.);
#16529=EDGE_CURVE('',#12489,#12488,#2036,.T.);
#16530=EDGE_CURVE('',#12490,#12489,#889,.T.);
#16531=EDGE_CURVE('',#12491,#12490,#3793,.T.);
#16532=EDGE_CURVE('',#12492,#12491,#890,.T.);
#16533=EDGE_CURVE('',#12493,#12492,#2037,.T.);
#16534=EDGE_CURVE('',#12494,#12493,#891,.T.);
#16535=EDGE_CURVE('',#12495,#12494,#3794,.T.);
#16536=EDGE_CURVE('',#12496,#12495,#892,.T.);
#16537=EDGE_CURVE('',#12497,#12496,#2038,.T.);
#16538=EDGE_CURVE('',#12498,#12497,#893,.T.);
#16539=EDGE_CURVE('',#12499,#12498,#3795,.T.);
#16540=EDGE_CURVE('',#12500,#12499,#894,.T.);
#16541=EDGE_CURVE('',#12501,#12500,#2039,.T.);
#16542=EDGE_CURVE('',#12502,#12501,#895,.T.);
#16543=EDGE_CURVE('',#12503,#12502,#3796,.T.);
#16544=EDGE_CURVE('',#12504,#12503,#896,.T.);
#16545=EDGE_CURVE('',#12505,#12504,#2040,.T.);
#16546=EDGE_CURVE('',#12506,#12505,#897,.T.);
#16547=EDGE_CURVE('',#12507,#12506,#3797,.T.);
#16548=EDGE_CURVE('',#12508,#12507,#898,.T.);
#16549=EDGE_CURVE('',#12509,#12508,#2041,.T.);
#16550=EDGE_CURVE('',#12510,#12509,#899,.T.);
#16551=EDGE_CURVE('',#12511,#12510,#3798,.T.);
#16552=EDGE_CURVE('',#12512,#12511,#900,.T.);
#16553=EDGE_CURVE('',#12513,#12512,#2042,.T.);
#16554=EDGE_CURVE('',#12514,#12513,#901,.T.);
#16555=EDGE_CURVE('',#12515,#12514,#3799,.T.);
#16556=EDGE_CURVE('',#12516,#12515,#902,.T.);
#16557=EDGE_CURVE('',#12517,#12516,#2043,.T.);
#16558=EDGE_CURVE('',#12518,#12517,#903,.T.);
#16559=EDGE_CURVE('',#12519,#12518,#3800,.T.);
#16560=EDGE_CURVE('',#12520,#12519,#904,.T.);
#16561=EDGE_CURVE('',#12521,#12520,#2044,.T.);
#16562=EDGE_CURVE('',#12522,#12521,#905,.T.);
#16563=EDGE_CURVE('',#12523,#12522,#3801,.T.);
#16564=EDGE_CURVE('',#12524,#12523,#906,.T.);
#16565=EDGE_CURVE('',#12525,#12524,#2045,.T.);
#16566=EDGE_CURVE('',#12526,#12525,#907,.T.);
#16567=EDGE_CURVE('',#12527,#12526,#3802,.T.);
#16568=EDGE_CURVE('',#12528,#12527,#908,.T.);
#16569=EDGE_CURVE('',#12529,#12528,#2046,.T.);
#16570=EDGE_CURVE('',#12530,#12529,#909,.T.);
#16571=EDGE_CURVE('',#12531,#12530,#3803,.T.);
#16572=EDGE_CURVE('',#12532,#12531,#910,.T.);
#16573=EDGE_CURVE('',#12533,#12532,#2047,.T.);
#16574=EDGE_CURVE('',#12534,#12533,#911,.T.);
#16575=EDGE_CURVE('',#12535,#12534,#3804,.T.);
#16576=EDGE_CURVE('',#12536,#12535,#912,.T.);
#16577=EDGE_CURVE('',#12537,#12536,#2048,.T.);
#16578=EDGE_CURVE('',#12538,#12537,#913,.T.);
#16579=EDGE_CURVE('',#12539,#12538,#3805,.T.);
#16580=EDGE_CURVE('',#12540,#12539,#914,.T.);
#16581=EDGE_CURVE('',#12541,#12540,#2049,.T.);
#16582=EDGE_CURVE('',#12542,#12541,#915,.T.);
#16583=EDGE_CURVE('',#12543,#12542,#3806,.T.);
#16584=EDGE_CURVE('',#12544,#12543,#916,.T.);
#16585=EDGE_CURVE('',#12545,#12544,#2050,.T.);
#16586=EDGE_CURVE('',#12546,#12545,#917,.T.);
#16587=EDGE_CURVE('',#12547,#12546,#3807,.T.);
#16588=EDGE_CURVE('',#12548,#12547,#918,.T.);
#16589=EDGE_CURVE('',#12549,#12548,#2051,.T.);
#16590=EDGE_CURVE('',#12550,#12549,#919,.T.);
#16591=EDGE_CURVE('',#12551,#12550,#3808,.T.);
#16592=EDGE_CURVE('',#12552,#12551,#920,.T.);
#16593=EDGE_CURVE('',#12553,#12552,#2052,.T.);
#16594=EDGE_CURVE('',#12554,#12553,#921,.T.);
#16595=EDGE_CURVE('',#12555,#12554,#3809,.T.);
#16596=EDGE_CURVE('',#12556,#12555,#922,.T.);
#16597=EDGE_CURVE('',#12557,#12556,#2053,.T.);
#16598=EDGE_CURVE('',#12558,#12557,#923,.T.);
#16599=EDGE_CURVE('',#12559,#12558,#3810,.T.);
#16600=EDGE_CURVE('',#12560,#12559,#924,.T.);
#16601=EDGE_CURVE('',#12561,#12560,#2054,.T.);
#16602=EDGE_CURVE('',#12562,#12561,#925,.T.);
#16603=EDGE_CURVE('',#12563,#12562,#3811,.T.);
#16604=EDGE_CURVE('',#12564,#12563,#926,.T.);
#16605=EDGE_CURVE('',#12565,#12564,#2055,.T.);
#16606=EDGE_CURVE('',#12566,#12565,#927,.T.);
#16607=EDGE_CURVE('',#12567,#12566,#3812,.T.);
#16608=EDGE_CURVE('',#12568,#12567,#928,.T.);
#16609=EDGE_CURVE('',#12569,#12568,#2056,.T.);
#16610=EDGE_CURVE('',#12570,#12569,#929,.T.);
#16611=EDGE_CURVE('',#12571,#12570,#3813,.T.);
#16612=EDGE_CURVE('',#12572,#12571,#930,.T.);
#16613=EDGE_CURVE('',#12573,#12572,#2057,.T.);
#16614=EDGE_CURVE('',#12574,#12573,#931,.T.);
#16615=EDGE_CURVE('',#12575,#12574,#3814,.T.);
#16616=EDGE_CURVE('',#12576,#12575,#932,.T.);
#16617=EDGE_CURVE('',#12577,#12576,#2058,.T.);
#16618=EDGE_CURVE('',#12578,#12577,#933,.T.);
#16619=EDGE_CURVE('',#12579,#12578,#3815,.T.);
#16620=EDGE_CURVE('',#12580,#12579,#934,.T.);
#16621=EDGE_CURVE('',#12581,#12580,#2059,.T.);
#16622=EDGE_CURVE('',#12582,#12581,#935,.T.);
#16623=EDGE_CURVE('',#12583,#12582,#3816,.T.);
#16624=EDGE_CURVE('',#12584,#12583,#936,.T.);
#16625=EDGE_CURVE('',#12585,#12584,#2060,.T.);
#16626=EDGE_CURVE('',#12586,#12585,#937,.T.);
#16627=EDGE_CURVE('',#12587,#12586,#3817,.T.);
#16628=EDGE_CURVE('',#12588,#12587,#938,.T.);
#16629=EDGE_CURVE('',#12589,#12588,#2061,.T.);
#16630=EDGE_CURVE('',#12590,#12589,#939,.T.);
#16631=EDGE_CURVE('',#12591,#12590,#3818,.T.);
#16632=EDGE_CURVE('',#12592,#12591,#940,.T.);
#16633=EDGE_CURVE('',#12593,#12592,#2062,.T.);
#16634=EDGE_CURVE('',#12594,#12593,#941,.T.);
#16635=EDGE_CURVE('',#12595,#12594,#3819,.T.);
#16636=EDGE_CURVE('',#12596,#12595,#942,.T.);
#16637=EDGE_CURVE('',#12597,#12596,#2063,.T.);
#16638=EDGE_CURVE('',#12598,#12597,#943,.T.);
#16639=EDGE_CURVE('',#12599,#12598,#3820,.T.);
#16640=EDGE_CURVE('',#12600,#12599,#944,.T.);
#16641=EDGE_CURVE('',#12601,#12600,#2064,.T.);
#16642=EDGE_CURVE('',#12602,#12601,#945,.T.);
#16643=EDGE_CURVE('',#12603,#12602,#3821,.T.);
#16644=EDGE_CURVE('',#12604,#12603,#946,.T.);
#16645=EDGE_CURVE('',#12605,#12604,#2065,.T.);
#16646=EDGE_CURVE('',#12606,#12605,#947,.T.);
#16647=EDGE_CURVE('',#12607,#12606,#3822,.T.);
#16648=EDGE_CURVE('',#12608,#12607,#948,.T.);
#16649=EDGE_CURVE('',#12609,#12608,#2066,.T.);
#16650=EDGE_CURVE('',#12610,#12609,#949,.T.);
#16651=EDGE_CURVE('',#12611,#12610,#3823,.T.);
#16652=EDGE_CURVE('',#12612,#12611,#950,.T.);
#16653=EDGE_CURVE('',#12613,#12612,#2067,.T.);
#16654=EDGE_CURVE('',#12614,#12613,#951,.T.);
#16655=EDGE_CURVE('',#12615,#12614,#3824,.T.);
#16656=EDGE_CURVE('',#12616,#12615,#952,.T.);
#16657=EDGE_CURVE('',#12617,#12616,#2068,.T.);
#16658=EDGE_CURVE('',#12618,#12617,#953,.T.);
#16659=EDGE_CURVE('',#12619,#12618,#3825,.T.);
#16660=EDGE_CURVE('',#12620,#12619,#954,.T.);
#16661=EDGE_CURVE('',#12621,#12620,#2069,.T.);
#16662=EDGE_CURVE('',#12622,#12621,#955,.T.);
#16663=EDGE_CURVE('',#12623,#12622,#3826,.T.);
#16664=EDGE_CURVE('',#12624,#12623,#956,.T.);
#16665=EDGE_CURVE('',#12625,#12624,#2070,.T.);
#16666=EDGE_CURVE('',#12626,#12625,#957,.T.);
#16667=EDGE_CURVE('',#12627,#12626,#3827,.T.);
#16668=EDGE_CURVE('',#12628,#12627,#958,.T.);
#16669=EDGE_CURVE('',#12629,#12628,#2071,.T.);
#16670=EDGE_CURVE('',#12630,#12629,#959,.T.);
#16671=EDGE_CURVE('',#12631,#12630,#3828,.T.);
#16672=EDGE_CURVE('',#12632,#12631,#960,.T.);
#16673=EDGE_CURVE('',#12633,#12632,#2072,.T.);
#16674=EDGE_CURVE('',#12634,#12633,#961,.T.);
#16675=EDGE_CURVE('',#12635,#12634,#3829,.T.);
#16676=EDGE_CURVE('',#12636,#12635,#962,.T.);
#16677=EDGE_CURVE('',#12637,#12636,#2073,.T.);
#16678=EDGE_CURVE('',#12638,#12637,#963,.T.);
#16679=EDGE_CURVE('',#12639,#12638,#3830,.T.);
#16680=EDGE_CURVE('',#12640,#12639,#964,.T.);
#16681=EDGE_CURVE('',#12641,#12640,#2074,.T.);
#16682=EDGE_CURVE('',#12642,#12641,#965,.T.);
#16683=EDGE_CURVE('',#12643,#12642,#3831,.T.);
#16684=EDGE_CURVE('',#12449,#12643,#966,.T.);
#16685=EDGE_CURVE('',#12644,#12448,#967,.T.);
#16686=EDGE_CURVE('',#12645,#12644,#3832,.T.);
#16687=EDGE_CURVE('',#12445,#12645,#968,.T.);
#16688=EDGE_CURVE('',#12646,#12444,#969,.T.);
#16689=EDGE_CURVE('',#12647,#12646,#3833,.T.);
#16690=EDGE_CURVE('',#12441,#12647,#970,.T.);
#16691=EDGE_CURVE('',#12648,#12440,#971,.T.);
#16692=EDGE_CURVE('',#12649,#12648,#3834,.T.);
#16693=EDGE_CURVE('',#12437,#12649,#972,.T.);
#16694=EDGE_CURVE('',#12650,#12436,#973,.T.);
#16695=EDGE_CURVE('',#12651,#12650,#3835,.T.);
#16696=EDGE_CURVE('',#12433,#12651,#974,.T.);
#16697=EDGE_CURVE('',#12652,#12432,#975,.T.);
#16698=EDGE_CURVE('',#12653,#12652,#3836,.T.);
#16699=EDGE_CURVE('',#12429,#12653,#976,.T.);
#16700=EDGE_CURVE('',#12654,#12428,#977,.T.);
#16701=EDGE_CURVE('',#12655,#12654,#3837,.T.);
#16702=EDGE_CURVE('',#12425,#12655,#978,.T.);
#16703=EDGE_CURVE('',#12656,#12424,#979,.T.);
#16704=EDGE_CURVE('',#12657,#12656,#3838,.T.);
#16705=EDGE_CURVE('',#12421,#12657,#980,.T.);
#16706=EDGE_CURVE('',#12658,#12420,#981,.T.);
#16707=EDGE_CURVE('',#12659,#12658,#3839,.T.);
#16708=EDGE_CURVE('',#12417,#12659,#982,.T.);
#16709=EDGE_CURVE('',#12660,#12416,#983,.T.);
#16710=EDGE_CURVE('',#12661,#12660,#3840,.T.);
#16711=EDGE_CURVE('',#12393,#12661,#984,.T.);
#16712=EDGE_CURVE('',#12662,#12392,#985,.T.);
#16713=EDGE_CURVE('',#12663,#12662,#3841,.T.);
#16714=EDGE_CURVE('',#12397,#12663,#986,.T.);
#16715=EDGE_CURVE('',#12664,#12396,#987,.T.);
#16716=EDGE_CURVE('',#12665,#12664,#3842,.T.);
#16717=EDGE_CURVE('',#12401,#12665,#988,.T.);
#16718=EDGE_CURVE('',#12666,#12400,#989,.T.);
#16719=EDGE_CURVE('',#12667,#12666,#3843,.T.);
#16720=EDGE_CURVE('',#12405,#12667,#990,.T.);
#16721=EDGE_CURVE('',#12668,#12404,#991,.T.);
#16722=EDGE_CURVE('',#12669,#12668,#3844,.T.);
#16723=EDGE_CURVE('',#12409,#12669,#992,.T.);
#16724=EDGE_CURVE('',#12670,#12408,#993,.T.);
#16725=EDGE_CURVE('',#12671,#12670,#3845,.T.);
#16726=EDGE_CURVE('',#12413,#12671,#994,.T.);
#16727=EDGE_CURVE('',#12672,#12412,#995,.T.);
#16728=EDGE_CURVE('',#12673,#12672,#3846,.T.);
#16729=EDGE_CURVE('',#12674,#12673,#996,.T.);
#16730=EDGE_CURVE('',#12675,#12674,#2075,.T.);
#16731=EDGE_CURVE('',#12676,#12675,#997,.T.);
#16732=EDGE_CURVE('',#12677,#12676,#3847,.T.);
#16733=EDGE_CURVE('',#12678,#12677,#998,.T.);
#16734=EDGE_CURVE('',#12679,#12678,#2076,.T.);
#16735=EDGE_CURVE('',#12680,#12679,#999,.T.);
#16736=EDGE_CURVE('',#12681,#12680,#3848,.T.);
#16737=EDGE_CURVE('',#12682,#12681,#1000,.T.);
#16738=EDGE_CURVE('',#12683,#12682,#2077,.T.);
#16739=EDGE_CURVE('',#12684,#12683,#1001,.T.);
#16740=EDGE_CURVE('',#12685,#12684,#3849,.T.);
#16741=EDGE_CURVE('',#12686,#12685,#1002,.T.);
#16742=EDGE_CURVE('',#12687,#12686,#2078,.T.);
#16743=EDGE_CURVE('',#12688,#12687,#1003,.T.);
#16744=EDGE_CURVE('',#12689,#12688,#3850,.T.);
#16745=EDGE_CURVE('',#12690,#12689,#1004,.T.);
#16746=EDGE_CURVE('',#12691,#12690,#2079,.T.);
#16747=EDGE_CURVE('',#12692,#12691,#1005,.T.);
#16748=EDGE_CURVE('',#12693,#12692,#3851,.T.);
#16749=EDGE_CURVE('',#12694,#12693,#1006,.T.);
#16750=EDGE_CURVE('',#12695,#12694,#2080,.T.);
#16751=EDGE_CURVE('',#12696,#12695,#1007,.T.);
#16752=EDGE_CURVE('',#12697,#12696,#3852,.T.);
#16753=EDGE_CURVE('',#12698,#12697,#1008,.T.);
#16754=EDGE_CURVE('',#12699,#12698,#2081,.T.);
#16755=EDGE_CURVE('',#12700,#12699,#1009,.T.);
#16756=EDGE_CURVE('',#12701,#12700,#3853,.T.);
#16757=EDGE_CURVE('',#12702,#12701,#1010,.T.);
#16758=EDGE_CURVE('',#12703,#12702,#2082,.T.);
#16759=EDGE_CURVE('',#12704,#12703,#1011,.T.);
#16760=EDGE_CURVE('',#12705,#12704,#3854,.T.);
#16761=EDGE_CURVE('',#12706,#12705,#1012,.T.);
#16762=EDGE_CURVE('',#12707,#12706,#2083,.T.);
#16763=EDGE_CURVE('',#12708,#12707,#1013,.T.);
#16764=EDGE_CURVE('',#12709,#12708,#3855,.T.);
#16765=EDGE_CURVE('',#12710,#12709,#1014,.T.);
#16766=EDGE_CURVE('',#12711,#12710,#2084,.T.);
#16767=EDGE_CURVE('',#12712,#12711,#1015,.T.);
#16768=EDGE_CURVE('',#12713,#12712,#3856,.T.);
#16769=EDGE_CURVE('',#12714,#12713,#1016,.T.);
#16770=EDGE_CURVE('',#12715,#12714,#2085,.T.);
#16771=EDGE_CURVE('',#12716,#12715,#1017,.T.);
#16772=EDGE_CURVE('',#12717,#12716,#3857,.T.);
#16773=EDGE_CURVE('',#12718,#12717,#1018,.T.);
#16774=EDGE_CURVE('',#12719,#12718,#2086,.T.);
#16775=EDGE_CURVE('',#12720,#12719,#1019,.T.);
#16776=EDGE_CURVE('',#12721,#12720,#3858,.T.);
#16777=EDGE_CURVE('',#12722,#12721,#1020,.T.);
#16778=EDGE_CURVE('',#12723,#12722,#2087,.T.);
#16779=EDGE_CURVE('',#12724,#12723,#1021,.T.);
#16780=EDGE_CURVE('',#12725,#12724,#3859,.T.);
#16781=EDGE_CURVE('',#12726,#12725,#1022,.T.);
#16782=EDGE_CURVE('',#12727,#12726,#2088,.T.);
#16783=EDGE_CURVE('',#12728,#12727,#1023,.T.);
#16784=EDGE_CURVE('',#12729,#12728,#3860,.T.);
#16785=EDGE_CURVE('',#12730,#12729,#1024,.T.);
#16786=EDGE_CURVE('',#12731,#12730,#2089,.T.);
#16787=EDGE_CURVE('',#12732,#12731,#1025,.T.);
#16788=EDGE_CURVE('',#12733,#12732,#3861,.T.);
#16789=EDGE_CURVE('',#12734,#12733,#1026,.T.);
#16790=EDGE_CURVE('',#12735,#12734,#2090,.T.);
#16791=EDGE_CURVE('',#12736,#12735,#1027,.T.);
#16792=EDGE_CURVE('',#12737,#12736,#3862,.T.);
#16793=EDGE_CURVE('',#12738,#12737,#1028,.T.);
#16794=EDGE_CURVE('',#12739,#12738,#2091,.T.);
#16795=EDGE_CURVE('',#12740,#12739,#1029,.T.);
#16796=EDGE_CURVE('',#12741,#12740,#3863,.T.);
#16797=EDGE_CURVE('',#12742,#12741,#1030,.T.);
#16798=EDGE_CURVE('',#12743,#12742,#2092,.T.);
#16799=EDGE_CURVE('',#12744,#12743,#1031,.T.);
#16800=EDGE_CURVE('',#12745,#12744,#3864,.T.);
#16801=EDGE_CURVE('',#12746,#12745,#1032,.T.);
#16802=EDGE_CURVE('',#12747,#12746,#2093,.T.);
#16803=EDGE_CURVE('',#12748,#12747,#1033,.T.);
#16804=EDGE_CURVE('',#12749,#12748,#3865,.T.);
#16805=EDGE_CURVE('',#12750,#12749,#1034,.T.);
#16806=EDGE_CURVE('',#12461,#12750,#3222,.T.);
#16807=EDGE_CURVE('',#12461,#12458,#9144,.T.);
#16808=EDGE_CURVE('',#12751,#12752,#3223,.T.);
#16809=EDGE_CURVE('',#12753,#12751,#1035,.T.);
#16810=EDGE_CURVE('',#12753,#12754,#3866,.T.);
#16811=EDGE_CURVE('',#12755,#12754,#1036,.T.);
#16812=EDGE_CURVE('',#12756,#12755,#2094,.T.);
#16813=EDGE_CURVE('',#12757,#12756,#1037,.T.);
#16814=EDGE_CURVE('',#12757,#12758,#3867,.T.);
#16815=EDGE_CURVE('',#12759,#12758,#1038,.T.);
#16816=EDGE_CURVE('',#12760,#12759,#2095,.T.);
#16817=EDGE_CURVE('',#12761,#12760,#1039,.T.);
#16818=EDGE_CURVE('',#12761,#12762,#3868,.T.);
#16819=EDGE_CURVE('',#12763,#12762,#1040,.T.);
#16820=EDGE_CURVE('',#12764,#12763,#2096,.T.);
#16821=EDGE_CURVE('',#12765,#12764,#1041,.T.);
#16822=EDGE_CURVE('',#12765,#12766,#3869,.T.);
#16823=EDGE_CURVE('',#12767,#12766,#1042,.T.);
#16824=EDGE_CURVE('',#12768,#12767,#2097,.T.);
#16825=EDGE_CURVE('',#12769,#12768,#1043,.T.);
#16826=EDGE_CURVE('',#12769,#12770,#3870,.T.);
#16827=EDGE_CURVE('',#12771,#12770,#1044,.T.);
#16828=EDGE_CURVE('',#12772,#12771,#2098,.T.);
#16829=EDGE_CURVE('',#12773,#12772,#1045,.T.);
#16830=EDGE_CURVE('',#12773,#12774,#3871,.T.);
#16831=EDGE_CURVE('',#12775,#12774,#1046,.T.);
#16832=EDGE_CURVE('',#12776,#12775,#2099,.T.);
#16833=EDGE_CURVE('',#12777,#12776,#1047,.T.);
#16834=EDGE_CURVE('',#12777,#12778,#3872,.T.);
#16835=EDGE_CURVE('',#12779,#12778,#1048,.T.);
#16836=EDGE_CURVE('',#12780,#12779,#2100,.T.);
#16837=EDGE_CURVE('',#12781,#12780,#1049,.T.);
#16838=EDGE_CURVE('',#12781,#12782,#3873,.T.);
#16839=EDGE_CURVE('',#12783,#12782,#1050,.T.);
#16840=EDGE_CURVE('',#12784,#12783,#2101,.T.);
#16841=EDGE_CURVE('',#12785,#12784,#1051,.T.);
#16842=EDGE_CURVE('',#12785,#12786,#3874,.T.);
#16843=EDGE_CURVE('',#12787,#12786,#1052,.T.);
#16844=EDGE_CURVE('',#12788,#12787,#2102,.T.);
#16845=EDGE_CURVE('',#12789,#12788,#1053,.T.);
#16846=EDGE_CURVE('',#12789,#12790,#3875,.T.);
#16847=EDGE_CURVE('',#12791,#12790,#1054,.T.);
#16848=EDGE_CURVE('',#12792,#12791,#2103,.T.);
#16849=EDGE_CURVE('',#12793,#12792,#1055,.T.);
#16850=EDGE_CURVE('',#12793,#12794,#3876,.T.);
#16851=EDGE_CURVE('',#12795,#12794,#1056,.T.);
#16852=EDGE_CURVE('',#12796,#12795,#2104,.T.);
#16853=EDGE_CURVE('',#12797,#12796,#1057,.T.);
#16854=EDGE_CURVE('',#12797,#12798,#3877,.T.);
#16855=EDGE_CURVE('',#12799,#12798,#1058,.T.);
#16856=EDGE_CURVE('',#12800,#12799,#2105,.T.);
#16857=EDGE_CURVE('',#12801,#12800,#1059,.T.);
#16858=EDGE_CURVE('',#12801,#12802,#3878,.T.);
#16859=EDGE_CURVE('',#12803,#12802,#1060,.T.);
#16860=EDGE_CURVE('',#12804,#12803,#2106,.T.);
#16861=EDGE_CURVE('',#12805,#12804,#1061,.T.);
#16862=EDGE_CURVE('',#12805,#12806,#3879,.T.);
#16863=EDGE_CURVE('',#12807,#12806,#1062,.T.);
#16864=EDGE_CURVE('',#12808,#12807,#2107,.T.);
#16865=EDGE_CURVE('',#12809,#12808,#1063,.T.);
#16866=EDGE_CURVE('',#12809,#12810,#3880,.T.);
#16867=EDGE_CURVE('',#12811,#12810,#1064,.T.);
#16868=EDGE_CURVE('',#12812,#12811,#2108,.T.);
#16869=EDGE_CURVE('',#12813,#12812,#1065,.T.);
#16870=EDGE_CURVE('',#12813,#12814,#3881,.T.);
#16871=EDGE_CURVE('',#12815,#12814,#1066,.T.);
#16872=EDGE_CURVE('',#12816,#12815,#2109,.T.);
#16873=EDGE_CURVE('',#12817,#12816,#1067,.T.);
#16874=EDGE_CURVE('',#12817,#12818,#3882,.T.);
#16875=EDGE_CURVE('',#12819,#12818,#1068,.T.);
#16876=EDGE_CURVE('',#12820,#12819,#2110,.T.);
#16877=EDGE_CURVE('',#12821,#12820,#1069,.T.);
#16878=EDGE_CURVE('',#12821,#12822,#3883,.T.);
#16879=EDGE_CURVE('',#12823,#12822,#1070,.T.);
#16880=EDGE_CURVE('',#12824,#12823,#2111,.T.);
#16881=EDGE_CURVE('',#12825,#12824,#1071,.T.);
#16882=EDGE_CURVE('',#12825,#12826,#3884,.T.);
#16883=EDGE_CURVE('',#12827,#12826,#1072,.T.);
#16884=EDGE_CURVE('',#12828,#12827,#2112,.T.);
#16885=EDGE_CURVE('',#12829,#12828,#1073,.T.);
#16886=EDGE_CURVE('',#12829,#12830,#3885,.T.);
#16887=EDGE_CURVE('',#12831,#12830,#1074,.T.);
#16888=EDGE_CURVE('',#12832,#12831,#2113,.T.);
#16889=EDGE_CURVE('',#12833,#12832,#1075,.T.);
#16890=EDGE_CURVE('',#12833,#12834,#3886,.T.);
#16891=EDGE_CURVE('',#12835,#12834,#1076,.T.);
#16892=EDGE_CURVE('',#12836,#12835,#2114,.T.);
#16893=EDGE_CURVE('',#12837,#12836,#1077,.T.);
#16894=EDGE_CURVE('',#12837,#12838,#3887,.T.);
#16895=EDGE_CURVE('',#12839,#12838,#1078,.T.);
#16896=EDGE_CURVE('',#12840,#12839,#2115,.T.);
#16897=EDGE_CURVE('',#12841,#12840,#1079,.T.);
#16898=EDGE_CURVE('',#12841,#12842,#3888,.T.);
#16899=EDGE_CURVE('',#12843,#12842,#1080,.T.);
#16900=EDGE_CURVE('',#12844,#12843,#2116,.T.);
#16901=EDGE_CURVE('',#12845,#12844,#1081,.T.);
#16902=EDGE_CURVE('',#12845,#12846,#3889,.T.);
#16903=EDGE_CURVE('',#12847,#12846,#1082,.T.);
#16904=EDGE_CURVE('',#12848,#12847,#2117,.T.);
#16905=EDGE_CURVE('',#12849,#12848,#1083,.T.);
#16906=EDGE_CURVE('',#12849,#12850,#3890,.T.);
#16907=EDGE_CURVE('',#12851,#12850,#1084,.T.);
#16908=EDGE_CURVE('',#12852,#12851,#2118,.T.);
#16909=EDGE_CURVE('',#12853,#12852,#1085,.T.);
#16910=EDGE_CURVE('',#12853,#12854,#3891,.T.);
#16911=EDGE_CURVE('',#12855,#12854,#1086,.T.);
#16912=EDGE_CURVE('',#12856,#12855,#2119,.T.);
#16913=EDGE_CURVE('',#12857,#12856,#1087,.T.);
#16914=EDGE_CURVE('',#12857,#12858,#3892,.T.);
#16915=EDGE_CURVE('',#12859,#12858,#1088,.T.);
#16916=EDGE_CURVE('',#12860,#12859,#2120,.T.);
#16917=EDGE_CURVE('',#12861,#12860,#1089,.T.);
#16918=EDGE_CURVE('',#12861,#12862,#3893,.T.);
#16919=EDGE_CURVE('',#12863,#12862,#1090,.T.);
#16920=EDGE_CURVE('',#12864,#12863,#2121,.T.);
#16921=EDGE_CURVE('',#12865,#12864,#1091,.T.);
#16922=EDGE_CURVE('',#12865,#12866,#3894,.T.);
#16923=EDGE_CURVE('',#12867,#12866,#1092,.T.);
#16924=EDGE_CURVE('',#12868,#12867,#2122,.T.);
#16925=EDGE_CURVE('',#12869,#12868,#1093,.T.);
#16926=EDGE_CURVE('',#12869,#12870,#3895,.T.);
#16927=EDGE_CURVE('',#12871,#12870,#1094,.T.);
#16928=EDGE_CURVE('',#12872,#12871,#2123,.T.);
#16929=EDGE_CURVE('',#12873,#12872,#1095,.T.);
#16930=EDGE_CURVE('',#12873,#12874,#3896,.T.);
#16931=EDGE_CURVE('',#12875,#12874,#1096,.T.);
#16932=EDGE_CURVE('',#12876,#12875,#2124,.T.);
#16933=EDGE_CURVE('',#12877,#12876,#1097,.T.);
#16934=EDGE_CURVE('',#12877,#12878,#3897,.T.);
#16935=EDGE_CURVE('',#12879,#12878,#1098,.T.);
#16936=EDGE_CURVE('',#12880,#12879,#2125,.T.);
#16937=EDGE_CURVE('',#12881,#12880,#1099,.T.);
#16938=EDGE_CURVE('',#12881,#12882,#3898,.T.);
#16939=EDGE_CURVE('',#12883,#12882,#1100,.T.);
#16940=EDGE_CURVE('',#12884,#12883,#2126,.T.);
#16941=EDGE_CURVE('',#12885,#12884,#1101,.T.);
#16942=EDGE_CURVE('',#12885,#12886,#3899,.T.);
#16943=EDGE_CURVE('',#12887,#12886,#1102,.T.);
#16944=EDGE_CURVE('',#12888,#12887,#2127,.T.);
#16945=EDGE_CURVE('',#12889,#12888,#1103,.T.);
#16946=EDGE_CURVE('',#12889,#12890,#3900,.T.);
#16947=EDGE_CURVE('',#12891,#12890,#1104,.T.);
#16948=EDGE_CURVE('',#12892,#12891,#2128,.T.);
#16949=EDGE_CURVE('',#12893,#12892,#1105,.T.);
#16950=EDGE_CURVE('',#12893,#12894,#3901,.T.);
#16951=EDGE_CURVE('',#12895,#12894,#1106,.T.);
#16952=EDGE_CURVE('',#12896,#12895,#2129,.T.);
#16953=EDGE_CURVE('',#12897,#12896,#1107,.T.);
#16954=EDGE_CURVE('',#12897,#12898,#3902,.T.);
#16955=EDGE_CURVE('',#12899,#12898,#1108,.T.);
#16956=EDGE_CURVE('',#12900,#12899,#2130,.T.);
#16957=EDGE_CURVE('',#12901,#12900,#1109,.T.);
#16958=EDGE_CURVE('',#12901,#12902,#3903,.T.);
#16959=EDGE_CURVE('',#12903,#12902,#1110,.T.);
#16960=EDGE_CURVE('',#12904,#12903,#2131,.T.);
#16961=EDGE_CURVE('',#12905,#12904,#1111,.T.);
#16962=EDGE_CURVE('',#12905,#12906,#3904,.T.);
#16963=EDGE_CURVE('',#12907,#12906,#1112,.T.);
#16964=EDGE_CURVE('',#12908,#12907,#2132,.T.);
#16965=EDGE_CURVE('',#12909,#12908,#1113,.T.);
#16966=EDGE_CURVE('',#12909,#12910,#3905,.T.);
#16967=EDGE_CURVE('',#12911,#12910,#1114,.T.);
#16968=EDGE_CURVE('',#12912,#12911,#2133,.T.);
#16969=EDGE_CURVE('',#12913,#12912,#1115,.T.);
#16970=EDGE_CURVE('',#12913,#12914,#3906,.T.);
#16971=EDGE_CURVE('',#12915,#12914,#1116,.T.);
#16972=EDGE_CURVE('',#12916,#12915,#2134,.T.);
#16973=EDGE_CURVE('',#12917,#12916,#1117,.T.);
#16974=EDGE_CURVE('',#12917,#12918,#3907,.T.);
#16975=EDGE_CURVE('',#12919,#12918,#1118,.T.);
#16976=EDGE_CURVE('',#12920,#12919,#2135,.T.);
#16977=EDGE_CURVE('',#12921,#12920,#1119,.T.);
#16978=EDGE_CURVE('',#12921,#12922,#3908,.T.);
#16979=EDGE_CURVE('',#12923,#12922,#1120,.T.);
#16980=EDGE_CURVE('',#12924,#12923,#2136,.T.);
#16981=EDGE_CURVE('',#12925,#12924,#1121,.T.);
#16982=EDGE_CURVE('',#12925,#12926,#3909,.T.);
#16983=EDGE_CURVE('',#12927,#12926,#1122,.T.);
#16984=EDGE_CURVE('',#12928,#12927,#2137,.T.);
#16985=EDGE_CURVE('',#12929,#12928,#1123,.T.);
#16986=EDGE_CURVE('',#12929,#12930,#3910,.T.);
#16987=EDGE_CURVE('',#12931,#12930,#1124,.T.);
#16988=EDGE_CURVE('',#12932,#12931,#2138,.T.);
#16989=EDGE_CURVE('',#12933,#12932,#1125,.T.);
#16990=EDGE_CURVE('',#12933,#12934,#3911,.T.);
#16991=EDGE_CURVE('',#12935,#12934,#1126,.T.);
#16992=EDGE_CURVE('',#12936,#12935,#2139,.T.);
#16993=EDGE_CURVE('',#12937,#12936,#1127,.T.);
#16994=EDGE_CURVE('',#12937,#12938,#3912,.T.);
#16995=EDGE_CURVE('',#12939,#12938,#1128,.T.);
#16996=EDGE_CURVE('',#12940,#12939,#2140,.T.);
#16997=EDGE_CURVE('',#12941,#12940,#1129,.T.);
#16998=EDGE_CURVE('',#12941,#12942,#3913,.T.);
#16999=EDGE_CURVE('',#12943,#12942,#1130,.T.);
#17000=EDGE_CURVE('',#12944,#12943,#2141,.T.);
#17001=EDGE_CURVE('',#12945,#12944,#1131,.T.);
#17002=EDGE_CURVE('',#12945,#12946,#3914,.T.);
#17003=EDGE_CURVE('',#12947,#12946,#1132,.T.);
#17004=EDGE_CURVE('',#12948,#12947,#2142,.T.);
#17005=EDGE_CURVE('',#12949,#12948,#1133,.T.);
#17006=EDGE_CURVE('',#12949,#12950,#3915,.T.);
#17007=EDGE_CURVE('',#12951,#12950,#1134,.T.);
#17008=EDGE_CURVE('',#12952,#12951,#2143,.T.);
#17009=EDGE_CURVE('',#12953,#12952,#1135,.T.);
#17010=EDGE_CURVE('',#12953,#12954,#3916,.T.);
#17011=EDGE_CURVE('',#12955,#12954,#1136,.T.);
#17012=EDGE_CURVE('',#12956,#12955,#2144,.T.);
#17013=EDGE_CURVE('',#12957,#12956,#1137,.T.);
#17014=EDGE_CURVE('',#12957,#12958,#3917,.T.);
#17015=EDGE_CURVE('',#12959,#12958,#1138,.T.);
#17016=EDGE_CURVE('',#12960,#12959,#2145,.T.);
#17017=EDGE_CURVE('',#12961,#12960,#1139,.T.);
#17018=EDGE_CURVE('',#12961,#12962,#3918,.T.);
#17019=EDGE_CURVE('',#12963,#12962,#1140,.T.);
#17020=EDGE_CURVE('',#12964,#12963,#2146,.T.);
#17021=EDGE_CURVE('',#12965,#12964,#1141,.T.);
#17022=EDGE_CURVE('',#12965,#12966,#3919,.T.);
#17023=EDGE_CURVE('',#12967,#12966,#1142,.T.);
#17024=EDGE_CURVE('',#12968,#12967,#2147,.T.);
#17025=EDGE_CURVE('',#12969,#12968,#1143,.T.);
#17026=EDGE_CURVE('',#12969,#12970,#3920,.T.);
#17027=EDGE_CURVE('',#12971,#12970,#1144,.T.);
#17028=EDGE_CURVE('',#12972,#12971,#2148,.T.);
#17029=EDGE_CURVE('',#12973,#12972,#1145,.T.);
#17030=EDGE_CURVE('',#12973,#12974,#3921,.T.);
#17031=EDGE_CURVE('',#12975,#12974,#1146,.T.);
#17032=EDGE_CURVE('',#12976,#12975,#2149,.T.);
#17033=EDGE_CURVE('',#12977,#12976,#1147,.T.);
#17034=EDGE_CURVE('',#12977,#12978,#3922,.T.);
#17035=EDGE_CURVE('',#12979,#12978,#1148,.T.);
#17036=EDGE_CURVE('',#12980,#12979,#2150,.T.);
#17037=EDGE_CURVE('',#12981,#12980,#1149,.T.);
#17038=EDGE_CURVE('',#12981,#12982,#3923,.T.);
#17039=EDGE_CURVE('',#12983,#12982,#1150,.T.);
#17040=EDGE_CURVE('',#12984,#12983,#2151,.T.);
#17041=EDGE_CURVE('',#12985,#12984,#1151,.T.);
#17042=EDGE_CURVE('',#12985,#12986,#3924,.T.);
#17043=EDGE_CURVE('',#12987,#12986,#1152,.T.);
#17044=EDGE_CURVE('',#12988,#12987,#2152,.T.);
#17045=EDGE_CURVE('',#12989,#12988,#1153,.T.);
#17046=EDGE_CURVE('',#12989,#12990,#3925,.T.);
#17047=EDGE_CURVE('',#12411,#12990,#1154,.T.);
#17048=EDGE_CURVE('',#12991,#12410,#1155,.T.);
#17049=EDGE_CURVE('',#12991,#12992,#3926,.T.);
#17050=EDGE_CURVE('',#12407,#12992,#1156,.T.);
#17051=EDGE_CURVE('',#12993,#12406,#1157,.T.);
#17052=EDGE_CURVE('',#12993,#12994,#3927,.T.);
#17053=EDGE_CURVE('',#12403,#12994,#1158,.T.);
#17054=EDGE_CURVE('',#12995,#12402,#1159,.T.);
#17055=EDGE_CURVE('',#12995,#12996,#3928,.T.);
#17056=EDGE_CURVE('',#12399,#12996,#1160,.T.);
#17057=EDGE_CURVE('',#12997,#12398,#1161,.T.);
#17058=EDGE_CURVE('',#12997,#12998,#3929,.T.);
#17059=EDGE_CURVE('',#12395,#12998,#1162,.T.);
#17060=EDGE_CURVE('',#12999,#12394,#1163,.T.);
#17061=EDGE_CURVE('',#12999,#13000,#3930,.T.);
#17062=EDGE_CURVE('',#12391,#13000,#1164,.T.);
#17063=EDGE_CURVE('',#13001,#12390,#1165,.T.);
#17064=EDGE_CURVE('',#13001,#13002,#3931,.T.);
#17065=EDGE_CURVE('',#12415,#13002,#1166,.T.);
#17066=EDGE_CURVE('',#13003,#12414,#1167,.T.);
#17067=EDGE_CURVE('',#13003,#13004,#3932,.T.);
#17068=EDGE_CURVE('',#12419,#13004,#1168,.T.);
#17069=EDGE_CURVE('',#13005,#12418,#1169,.T.);
#17070=EDGE_CURVE('',#13005,#13006,#3933,.T.);
#17071=EDGE_CURVE('',#12423,#13006,#1170,.T.);
#17072=EDGE_CURVE('',#13007,#12422,#1171,.T.);
#17073=EDGE_CURVE('',#13007,#13008,#3934,.T.);
#17074=EDGE_CURVE('',#12427,#13008,#1172,.T.);
#17075=EDGE_CURVE('',#13009,#12426,#1173,.T.);
#17076=EDGE_CURVE('',#13009,#13010,#3935,.T.);
#17077=EDGE_CURVE('',#12431,#13010,#1174,.T.);
#17078=EDGE_CURVE('',#13011,#12430,#1175,.T.);
#17079=EDGE_CURVE('',#13011,#13012,#3936,.T.);
#17080=EDGE_CURVE('',#12435,#13012,#1176,.T.);
#17081=EDGE_CURVE('',#13013,#12434,#1177,.T.);
#17082=EDGE_CURVE('',#13013,#13014,#3937,.T.);
#17083=EDGE_CURVE('',#12439,#13014,#1178,.T.);
#17084=EDGE_CURVE('',#13015,#12438,#1179,.T.);
#17085=EDGE_CURVE('',#13015,#13016,#3938,.T.);
#17086=EDGE_CURVE('',#12443,#13016,#1180,.T.);
#17087=EDGE_CURVE('',#13017,#12442,#1181,.T.);
#17088=EDGE_CURVE('',#13017,#13018,#3939,.T.);
#17089=EDGE_CURVE('',#12447,#13018,#1182,.T.);
#17090=EDGE_CURVE('',#13019,#12446,#1183,.T.);
#17091=EDGE_CURVE('',#13019,#13020,#3940,.T.);
#17092=EDGE_CURVE('',#13021,#13020,#1184,.T.);
#17093=EDGE_CURVE('',#13022,#13021,#2153,.T.);
#17094=EDGE_CURVE('',#13023,#13022,#1185,.T.);
#17095=EDGE_CURVE('',#13023,#13024,#3941,.T.);
#17096=EDGE_CURVE('',#13025,#13024,#1186,.T.);
#17097=EDGE_CURVE('',#13026,#13025,#2154,.T.);
#17098=EDGE_CURVE('',#13027,#13026,#1187,.T.);
#17099=EDGE_CURVE('',#13027,#13028,#3942,.T.);
#17100=EDGE_CURVE('',#13029,#13028,#1188,.T.);
#17101=EDGE_CURVE('',#13030,#13029,#2155,.T.);
#17102=EDGE_CURVE('',#13031,#13030,#1189,.T.);
#17103=EDGE_CURVE('',#13031,#13032,#3943,.T.);
#17104=EDGE_CURVE('',#13033,#13032,#1190,.T.);
#17105=EDGE_CURVE('',#13034,#13033,#2156,.T.);
#17106=EDGE_CURVE('',#13035,#13034,#1191,.T.);
#17107=EDGE_CURVE('',#13035,#13036,#3944,.T.);
#17108=EDGE_CURVE('',#13037,#13036,#1192,.T.);
#17109=EDGE_CURVE('',#13038,#13037,#2157,.T.);
#17110=EDGE_CURVE('',#13039,#13038,#1193,.T.);
#17111=EDGE_CURVE('',#13039,#13040,#3945,.T.);
#17112=EDGE_CURVE('',#13041,#13040,#1194,.T.);
#17113=EDGE_CURVE('',#12752,#13041,#3224,.T.);
#17114=EDGE_CURVE('',#12752,#13042,#9145,.T.);
#17115=EDGE_CURVE('',#13043,#13042,#3946,.T.);
#17116=EDGE_CURVE('',#13042,#13043,#3947,.T.);
#17117=EDGE_CURVE('',#13044,#13044,#3948,.T.);
#17118=EDGE_CURVE('',#13044,#13043,#3949,.T.);
#17119=EDGE_CURVE('',#13045,#13045,#3950,.T.);
#17120=EDGE_CURVE('',#13045,#13044,#9146,.T.);
#17121=EDGE_CURVE('',#13046,#13046,#3951,.T.);
#17122=EDGE_CURVE('',#13046,#13045,#3952,.T.);
#17123=EDGE_CURVE('',#12268,#13047,#3953,.T.);
#17124=EDGE_CURVE('',#13047,#13047,#3954,.T.);
#17125=EDGE_CURVE('',#13048,#13001,#2158,.T.);
#17126=EDGE_CURVE('',#13048,#13049,#3955,.T.);
#17127=EDGE_CURVE('',#13002,#13049,#2159,.T.);
#17128=EDGE_CURVE('',#13000,#13050,#2160,.T.);
#17129=EDGE_CURVE('',#13051,#12999,#2161,.T.);
#17130=EDGE_CURVE('',#13051,#13050,#3956,.T.);
#17131=EDGE_CURVE('',#12998,#13052,#2162,.T.);
#17132=EDGE_CURVE('',#13053,#12997,#2163,.T.);
#17133=EDGE_CURVE('',#13053,#13052,#3957,.T.);
#17134=EDGE_CURVE('',#12996,#13054,#2164,.T.);
#17135=EDGE_CURVE('',#13055,#12995,#2165,.T.);
#17136=EDGE_CURVE('',#13055,#13054,#3958,.T.);
#17137=EDGE_CURVE('',#12994,#13056,#2166,.T.);
#17138=EDGE_CURVE('',#13057,#12993,#2167,.T.);
#17139=EDGE_CURVE('',#13057,#13056,#3959,.T.);
#17140=EDGE_CURVE('',#12992,#13058,#2168,.T.);
#17141=EDGE_CURVE('',#13059,#12991,#2169,.T.);
#17142=EDGE_CURVE('',#13059,#13058,#3960,.T.);
#17143=EDGE_CURVE('',#12990,#13060,#2170,.T.);
#17144=EDGE_CURVE('',#13061,#12989,#2171,.T.);
#17145=EDGE_CURVE('',#13061,#13060,#3961,.T.);
#17146=EDGE_CURVE('',#12986,#13062,#2172,.T.);
#17147=EDGE_CURVE('',#13063,#12985,#2173,.T.);
#17148=EDGE_CURVE('',#13063,#13062,#3962,.T.);
#17149=EDGE_CURVE('',#12982,#13064,#2174,.T.);
#17150=EDGE_CURVE('',#13065,#12981,#2175,.T.);
#17151=EDGE_CURVE('',#13065,#13064,#3963,.T.);
#17152=EDGE_CURVE('',#12978,#13066,#2176,.T.);
#17153=EDGE_CURVE('',#13067,#12977,#2177,.T.);
#17154=EDGE_CURVE('',#13067,#13066,#3964,.T.);
#17155=EDGE_CURVE('',#12974,#13068,#2178,.T.);
#17156=EDGE_CURVE('',#13069,#12973,#2179,.T.);
#17157=EDGE_CURVE('',#13069,#13068,#3965,.T.);
#17158=EDGE_CURVE('',#12970,#13070,#2180,.T.);
#17159=EDGE_CURVE('',#13071,#12969,#2181,.T.);
#17160=EDGE_CURVE('',#13071,#13070,#3966,.T.);
#17161=EDGE_CURVE('',#12966,#13072,#2182,.T.);
#17162=EDGE_CURVE('',#13073,#12965,#2183,.T.);
#17163=EDGE_CURVE('',#13073,#13072,#3967,.T.);
#17164=EDGE_CURVE('',#12962,#13074,#2184,.T.);
#17165=EDGE_CURVE('',#13075,#12961,#2185,.T.);
#17166=EDGE_CURVE('',#13075,#13074,#3968,.T.);
#17167=EDGE_CURVE('',#12958,#13076,#2186,.T.);
#17168=EDGE_CURVE('',#13077,#12957,#2187,.T.);
#17169=EDGE_CURVE('',#13077,#13076,#3969,.T.);
#17170=EDGE_CURVE('',#12954,#13078,#2188,.T.);
#17171=EDGE_CURVE('',#13079,#12953,#2189,.T.);
#17172=EDGE_CURVE('',#13079,#13078,#3970,.T.);
#17173=EDGE_CURVE('',#12950,#13080,#2190,.T.);
#17174=EDGE_CURVE('',#13081,#12949,#2191,.T.);
#17175=EDGE_CURVE('',#13081,#13080,#3971,.T.);
#17176=EDGE_CURVE('',#12946,#13082,#2192,.T.);
#17177=EDGE_CURVE('',#13083,#12945,#2193,.T.);
#17178=EDGE_CURVE('',#13083,#13082,#3972,.T.);
#17179=EDGE_CURVE('',#12942,#13084,#2194,.T.);
#17180=EDGE_CURVE('',#13085,#12941,#2195,.T.);
#17181=EDGE_CURVE('',#13085,#13084,#3973,.T.);
#17182=EDGE_CURVE('',#12938,#13086,#2196,.T.);
#17183=EDGE_CURVE('',#13087,#12937,#2197,.T.);
#17184=EDGE_CURVE('',#13087,#13086,#3974,.T.);
#17185=EDGE_CURVE('',#12934,#13088,#2198,.T.);
#17186=EDGE_CURVE('',#13089,#12933,#2199,.T.);
#17187=EDGE_CURVE('',#13089,#13088,#3975,.T.);
#17188=EDGE_CURVE('',#12930,#13090,#2200,.T.);
#17189=EDGE_CURVE('',#13091,#12929,#2201,.T.);
#17190=EDGE_CURVE('',#13091,#13090,#3976,.T.);
#17191=EDGE_CURVE('',#12926,#13092,#2202,.T.);
#17192=EDGE_CURVE('',#13093,#12925,#2203,.T.);
#17193=EDGE_CURVE('',#13093,#13092,#3977,.T.);
#17194=EDGE_CURVE('',#12922,#13094,#2204,.T.);
#17195=EDGE_CURVE('',#13095,#12921,#2205,.T.);
#17196=EDGE_CURVE('',#13095,#13094,#3978,.T.);
#17197=EDGE_CURVE('',#12918,#13096,#2206,.T.);
#17198=EDGE_CURVE('',#13097,#12917,#2207,.T.);
#17199=EDGE_CURVE('',#13097,#13096,#3979,.T.);
#17200=EDGE_CURVE('',#12914,#13098,#2208,.T.);
#17201=EDGE_CURVE('',#13099,#12913,#2209,.T.);
#17202=EDGE_CURVE('',#13099,#13098,#3980,.T.);
#17203=EDGE_CURVE('',#12910,#13100,#2210,.T.);
#17204=EDGE_CURVE('',#13101,#12909,#2211,.T.);
#17205=EDGE_CURVE('',#13101,#13100,#3981,.T.);
#17206=EDGE_CURVE('',#12906,#13102,#2212,.T.);
#17207=EDGE_CURVE('',#13103,#12905,#2213,.T.);
#17208=EDGE_CURVE('',#13103,#13102,#3982,.T.);
#17209=EDGE_CURVE('',#12902,#13104,#2214,.T.);
#17210=EDGE_CURVE('',#13105,#12901,#2215,.T.);
#17211=EDGE_CURVE('',#13105,#13104,#3983,.T.);
#17212=EDGE_CURVE('',#12898,#13106,#2216,.T.);
#17213=EDGE_CURVE('',#13107,#12897,#2217,.T.);
#17214=EDGE_CURVE('',#13107,#13106,#3984,.T.);
#17215=EDGE_CURVE('',#12894,#13108,#2218,.T.);
#17216=EDGE_CURVE('',#13109,#12893,#2219,.T.);
#17217=EDGE_CURVE('',#13109,#13108,#3985,.T.);
#17218=EDGE_CURVE('',#12890,#13110,#2220,.T.);
#17219=EDGE_CURVE('',#13111,#12889,#2221,.T.);
#17220=EDGE_CURVE('',#13111,#13110,#3986,.T.);
#17221=EDGE_CURVE('',#12886,#13112,#2222,.T.);
#17222=EDGE_CURVE('',#13113,#12885,#2223,.T.);
#17223=EDGE_CURVE('',#13113,#13112,#3987,.T.);
#17224=EDGE_CURVE('',#12882,#13114,#2224,.T.);
#17225=EDGE_CURVE('',#13115,#12881,#2225,.T.);
#17226=EDGE_CURVE('',#13115,#13114,#3988,.T.);
#17227=EDGE_CURVE('',#12878,#13116,#2226,.T.);
#17228=EDGE_CURVE('',#13117,#12877,#2227,.T.);
#17229=EDGE_CURVE('',#13117,#13116,#3989,.T.);
#17230=EDGE_CURVE('',#12874,#13118,#2228,.T.);
#17231=EDGE_CURVE('',#13119,#12873,#2229,.T.);
#17232=EDGE_CURVE('',#13119,#13118,#3990,.T.);
#17233=EDGE_CURVE('',#12870,#13120,#2230,.T.);
#17234=EDGE_CURVE('',#13121,#12869,#2231,.T.);
#17235=EDGE_CURVE('',#13121,#13120,#3991,.T.);
#17236=EDGE_CURVE('',#12866,#13122,#2232,.T.);
#17237=EDGE_CURVE('',#13123,#12865,#2233,.T.);
#17238=EDGE_CURVE('',#13123,#13122,#3992,.T.);
#17239=EDGE_CURVE('',#12862,#13124,#2234,.T.);
#17240=EDGE_CURVE('',#13125,#12861,#2235,.T.);
#17241=EDGE_CURVE('',#13125,#13124,#3993,.T.);
#17242=EDGE_CURVE('',#12858,#13126,#2236,.T.);
#17243=EDGE_CURVE('',#13127,#12857,#2237,.T.);
#17244=EDGE_CURVE('',#13127,#13126,#3994,.T.);
#17245=EDGE_CURVE('',#12854,#13128,#2238,.T.);
#17246=EDGE_CURVE('',#13129,#12853,#2239,.T.);
#17247=EDGE_CURVE('',#13129,#13128,#3995,.T.);
#17248=EDGE_CURVE('',#12850,#13130,#2240,.T.);
#17249=EDGE_CURVE('',#13131,#12849,#2241,.T.);
#17250=EDGE_CURVE('',#13131,#13130,#3996,.T.);
#17251=EDGE_CURVE('',#12846,#13132,#2242,.T.);
#17252=EDGE_CURVE('',#13133,#12845,#2243,.T.);
#17253=EDGE_CURVE('',#13133,#13132,#3997,.T.);
#17254=EDGE_CURVE('',#12842,#13134,#2244,.T.);
#17255=EDGE_CURVE('',#13135,#12841,#2245,.T.);
#17256=EDGE_CURVE('',#13135,#13134,#3998,.T.);
#17257=EDGE_CURVE('',#12838,#13136,#2246,.T.);
#17258=EDGE_CURVE('',#13137,#12837,#2247,.T.);
#17259=EDGE_CURVE('',#13137,#13136,#3999,.T.);
#17260=EDGE_CURVE('',#12834,#13138,#2248,.T.);
#17261=EDGE_CURVE('',#13139,#12833,#2249,.T.);
#17262=EDGE_CURVE('',#13139,#13138,#4000,.T.);
#17263=EDGE_CURVE('',#12830,#13140,#2250,.T.);
#17264=EDGE_CURVE('',#13141,#12829,#2251,.T.);
#17265=EDGE_CURVE('',#13141,#13140,#4001,.T.);
#17266=EDGE_CURVE('',#12826,#13142,#2252,.T.);
#17267=EDGE_CURVE('',#13143,#12825,#2253,.T.);
#17268=EDGE_CURVE('',#13143,#13142,#4002,.T.);
#17269=EDGE_CURVE('',#12822,#13144,#2254,.T.);
#17270=EDGE_CURVE('',#13145,#12821,#2255,.T.);
#17271=EDGE_CURVE('',#13145,#13144,#4003,.T.);
#17272=EDGE_CURVE('',#12818,#13146,#2256,.T.);
#17273=EDGE_CURVE('',#13147,#12817,#2257,.T.);
#17274=EDGE_CURVE('',#13147,#13146,#4004,.T.);
#17275=EDGE_CURVE('',#12814,#13148,#2258,.T.);
#17276=EDGE_CURVE('',#13149,#12813,#2259,.T.);
#17277=EDGE_CURVE('',#13149,#13148,#4005,.T.);
#17278=EDGE_CURVE('',#12810,#13150,#2260,.T.);
#17279=EDGE_CURVE('',#13151,#12809,#2261,.T.);
#17280=EDGE_CURVE('',#13151,#13150,#4006,.T.);
#17281=EDGE_CURVE('',#12806,#13152,#2262,.T.);
#17282=EDGE_CURVE('',#13153,#12805,#2263,.T.);
#17283=EDGE_CURVE('',#13153,#13152,#4007,.T.);
#17284=EDGE_CURVE('',#12802,#13154,#2264,.T.);
#17285=EDGE_CURVE('',#13155,#12801,#2265,.T.);
#17286=EDGE_CURVE('',#13155,#13154,#4008,.T.);
#17287=EDGE_CURVE('',#12798,#13156,#2266,.T.);
#17288=EDGE_CURVE('',#13157,#12797,#2267,.T.);
#17289=EDGE_CURVE('',#13157,#13156,#4009,.T.);
#17290=EDGE_CURVE('',#12794,#13158,#2268,.T.);
#17291=EDGE_CURVE('',#13159,#12793,#2269,.T.);
#17292=EDGE_CURVE('',#13159,#13158,#4010,.T.);
#17293=EDGE_CURVE('',#12790,#13160,#2270,.T.);
#17294=EDGE_CURVE('',#13161,#12789,#2271,.T.);
#17295=EDGE_CURVE('',#13161,#13160,#4011,.T.);
#17296=EDGE_CURVE('',#12786,#13162,#2272,.T.);
#17297=EDGE_CURVE('',#13163,#12785,#2273,.T.);
#17298=EDGE_CURVE('',#13163,#13162,#4012,.T.);
#17299=EDGE_CURVE('',#12782,#13164,#2274,.T.);
#17300=EDGE_CURVE('',#13165,#12781,#2275,.T.);
#17301=EDGE_CURVE('',#13165,#13164,#4013,.T.);
#17302=EDGE_CURVE('',#12778,#13166,#2276,.T.);
#17303=EDGE_CURVE('',#13167,#12777,#2277,.T.);
#17304=EDGE_CURVE('',#13167,#13166,#4014,.T.);
#17305=EDGE_CURVE('',#12774,#13168,#2278,.T.);
#17306=EDGE_CURVE('',#13169,#12773,#2279,.T.);
#17307=EDGE_CURVE('',#13169,#13168,#4015,.T.);
#17308=EDGE_CURVE('',#12770,#13170,#2280,.T.);
#17309=EDGE_CURVE('',#13171,#12769,#2281,.T.);
#17310=EDGE_CURVE('',#13171,#13170,#4016,.T.);
#17311=EDGE_CURVE('',#12766,#13172,#2282,.T.);
#17312=EDGE_CURVE('',#13173,#12765,#2283,.T.);
#17313=EDGE_CURVE('',#13173,#13172,#4017,.T.);
#17314=EDGE_CURVE('',#12762,#13174,#2284,.T.);
#17315=EDGE_CURVE('',#13175,#12761,#2285,.T.);
#17316=EDGE_CURVE('',#13175,#13174,#4018,.T.);
#17317=EDGE_CURVE('',#13176,#13003,#2286,.T.);
#17318=EDGE_CURVE('',#13176,#13177,#4019,.T.);
#17319=EDGE_CURVE('',#13004,#13177,#2287,.T.);
#17320=EDGE_CURVE('',#13178,#13005,#2288,.T.);
#17321=EDGE_CURVE('',#13178,#13179,#4020,.T.);
#17322=EDGE_CURVE('',#13006,#13179,#2289,.T.);
#17323=EDGE_CURVE('',#13180,#13007,#2290,.T.);
#17324=EDGE_CURVE('',#13180,#13181,#4021,.T.);
#17325=EDGE_CURVE('',#13008,#13181,#2291,.T.);
#17326=EDGE_CURVE('',#13182,#13009,#2292,.T.);
#17327=EDGE_CURVE('',#13182,#13183,#4022,.T.);
#17328=EDGE_CURVE('',#13010,#13183,#2293,.T.);
#17329=EDGE_CURVE('',#13184,#13011,#2294,.T.);
#17330=EDGE_CURVE('',#13184,#13185,#4023,.T.);
#17331=EDGE_CURVE('',#13012,#13185,#2295,.T.);
#17332=EDGE_CURVE('',#13186,#13013,#2296,.T.);
#17333=EDGE_CURVE('',#13186,#13187,#4024,.T.);
#17334=EDGE_CURVE('',#13014,#13187,#2297,.T.);
#17335=EDGE_CURVE('',#13188,#13015,#2298,.T.);
#17336=EDGE_CURVE('',#13188,#13189,#4025,.T.);
#17337=EDGE_CURVE('',#13016,#13189,#2299,.T.);
#17338=EDGE_CURVE('',#13190,#13017,#2300,.T.);
#17339=EDGE_CURVE('',#13190,#13191,#4026,.T.);
#17340=EDGE_CURVE('',#13018,#13191,#2301,.T.);
#17341=EDGE_CURVE('',#13192,#13019,#2302,.T.);
#17342=EDGE_CURVE('',#13192,#13193,#4027,.T.);
#17343=EDGE_CURVE('',#13020,#13193,#2303,.T.);
#17344=EDGE_CURVE('',#13194,#13023,#2304,.T.);
#17345=EDGE_CURVE('',#13194,#13195,#4028,.T.);
#17346=EDGE_CURVE('',#13024,#13195,#2305,.T.);
#17347=EDGE_CURVE('',#13196,#13027,#2306,.T.);
#17348=EDGE_CURVE('',#13196,#13197,#4029,.T.);
#17349=EDGE_CURVE('',#13028,#13197,#2307,.T.);
#17350=EDGE_CURVE('',#13198,#13031,#2308,.T.);
#17351=EDGE_CURVE('',#13198,#13199,#4030,.T.);
#17352=EDGE_CURVE('',#13032,#13199,#2309,.T.);
#17353=EDGE_CURVE('',#13200,#13035,#2310,.T.);
#17354=EDGE_CURVE('',#13200,#13201,#4031,.T.);
#17355=EDGE_CURVE('',#13036,#13201,#2311,.T.);
#17356=EDGE_CURVE('',#13202,#13039,#2312,.T.);
#17357=EDGE_CURVE('',#13202,#13203,#4032,.T.);
#17358=EDGE_CURVE('',#13040,#13203,#2313,.T.);
#17359=EDGE_CURVE('',#12758,#13204,#2314,.T.);
#17360=EDGE_CURVE('',#13205,#12757,#2315,.T.);
#17361=EDGE_CURVE('',#13205,#13204,#4033,.T.);
#17362=EDGE_CURVE('',#13206,#13048,#9147,.T.);
#17363=EDGE_CURVE('',#13206,#13207,#4034,.T.);
#17364=EDGE_CURVE('',#13049,#13207,#9148,.T.);
#17365=EDGE_CURVE('',#13050,#13208,#9149,.T.);
#17366=EDGE_CURVE('',#13209,#13051,#9150,.T.);
#17367=EDGE_CURVE('',#13209,#13208,#4035,.T.);
#17368=EDGE_CURVE('',#13052,#13210,#9151,.T.);
#17369=EDGE_CURVE('',#13211,#13053,#9152,.T.);
#17370=EDGE_CURVE('',#13211,#13210,#4036,.T.);
#17371=EDGE_CURVE('',#13054,#13212,#9153,.T.);
#17372=EDGE_CURVE('',#13213,#13055,#9154,.T.);
#17373=EDGE_CURVE('',#13213,#13212,#4037,.T.);
#17374=EDGE_CURVE('',#13056,#13214,#9155,.T.);
#17375=EDGE_CURVE('',#13215,#13057,#9156,.T.);
#17376=EDGE_CURVE('',#13215,#13214,#4038,.T.);
#17377=EDGE_CURVE('',#13058,#13216,#9157,.T.);
#17378=EDGE_CURVE('',#13217,#13059,#9158,.T.);
#17379=EDGE_CURVE('',#13217,#13216,#4039,.T.);
#17380=EDGE_CURVE('',#13060,#13218,#9159,.T.);
#17381=EDGE_CURVE('',#13219,#13061,#9160,.T.);
#17382=EDGE_CURVE('',#13219,#13218,#4040,.T.);
#17383=EDGE_CURVE('',#13062,#13220,#9161,.T.);
#17384=EDGE_CURVE('',#13221,#13063,#9162,.T.);
#17385=EDGE_CURVE('',#13221,#13220,#4041,.T.);
#17386=EDGE_CURVE('',#13064,#13222,#9163,.T.);
#17387=EDGE_CURVE('',#13223,#13065,#9164,.T.);
#17388=EDGE_CURVE('',#13223,#13222,#4042,.T.);
#17389=EDGE_CURVE('',#13066,#13224,#9165,.T.);
#17390=EDGE_CURVE('',#13225,#13067,#9166,.T.);
#17391=EDGE_CURVE('',#13225,#13224,#4043,.T.);
#17392=EDGE_CURVE('',#13068,#13226,#9167,.T.);
#17393=EDGE_CURVE('',#13227,#13069,#9168,.T.);
#17394=EDGE_CURVE('',#13227,#13226,#4044,.T.);
#17395=EDGE_CURVE('',#13070,#13228,#9169,.T.);
#17396=EDGE_CURVE('',#13229,#13071,#9170,.T.);
#17397=EDGE_CURVE('',#13229,#13228,#4045,.T.);
#17398=EDGE_CURVE('',#13072,#13230,#9171,.T.);
#17399=EDGE_CURVE('',#13231,#13073,#9172,.T.);
#17400=EDGE_CURVE('',#13231,#13230,#4046,.T.);
#17401=EDGE_CURVE('',#13074,#13232,#9173,.T.);
#17402=EDGE_CURVE('',#13233,#13075,#9174,.T.);
#17403=EDGE_CURVE('',#13233,#13232,#4047,.T.);
#17404=EDGE_CURVE('',#13076,#13234,#9175,.T.);
#17405=EDGE_CURVE('',#13235,#13077,#9176,.T.);
#17406=EDGE_CURVE('',#13235,#13234,#4048,.T.);
#17407=EDGE_CURVE('',#13078,#13236,#9177,.T.);
#17408=EDGE_CURVE('',#13237,#13079,#9178,.T.);
#17409=EDGE_CURVE('',#13237,#13236,#4049,.T.);
#17410=EDGE_CURVE('',#13080,#13238,#9179,.T.);
#17411=EDGE_CURVE('',#13239,#13081,#9180,.T.);
#17412=EDGE_CURVE('',#13239,#13238,#4050,.T.);
#17413=EDGE_CURVE('',#13082,#13240,#9181,.T.);
#17414=EDGE_CURVE('',#13241,#13083,#9182,.T.);
#17415=EDGE_CURVE('',#13241,#13240,#4051,.T.);
#17416=EDGE_CURVE('',#13084,#13242,#9183,.T.);
#17417=EDGE_CURVE('',#13243,#13085,#9184,.T.);
#17418=EDGE_CURVE('',#13243,#13242,#4052,.T.);
#17419=EDGE_CURVE('',#13086,#13244,#9185,.T.);
#17420=EDGE_CURVE('',#13245,#13087,#9186,.T.);
#17421=EDGE_CURVE('',#13245,#13244,#4053,.T.);
#17422=EDGE_CURVE('',#13088,#13246,#9187,.T.);
#17423=EDGE_CURVE('',#13247,#13089,#9188,.T.);
#17424=EDGE_CURVE('',#13247,#13246,#4054,.T.);
#17425=EDGE_CURVE('',#13090,#13248,#9189,.T.);
#17426=EDGE_CURVE('',#13249,#13091,#9190,.T.);
#17427=EDGE_CURVE('',#13249,#13248,#4055,.T.);
#17428=EDGE_CURVE('',#13092,#13250,#9191,.T.);
#17429=EDGE_CURVE('',#13251,#13093,#9192,.T.);
#17430=EDGE_CURVE('',#13251,#13250,#4056,.T.);
#17431=EDGE_CURVE('',#13094,#13252,#9193,.T.);
#17432=EDGE_CURVE('',#13253,#13095,#9194,.T.);
#17433=EDGE_CURVE('',#13253,#13252,#4057,.T.);
#17434=EDGE_CURVE('',#13096,#13254,#9195,.T.);
#17435=EDGE_CURVE('',#13255,#13097,#9196,.T.);
#17436=EDGE_CURVE('',#13255,#13254,#4058,.T.);
#17437=EDGE_CURVE('',#13098,#13256,#9197,.T.);
#17438=EDGE_CURVE('',#13257,#13099,#9198,.T.);
#17439=EDGE_CURVE('',#13257,#13256,#4059,.T.);
#17440=EDGE_CURVE('',#13100,#13258,#9199,.T.);
#17441=EDGE_CURVE('',#13259,#13101,#9200,.T.);
#17442=EDGE_CURVE('',#13259,#13258,#4060,.T.);
#17443=EDGE_CURVE('',#13102,#13260,#9201,.T.);
#17444=EDGE_CURVE('',#13261,#13103,#9202,.T.);
#17445=EDGE_CURVE('',#13261,#13260,#4061,.T.);
#17446=EDGE_CURVE('',#13104,#13262,#9203,.T.);
#17447=EDGE_CURVE('',#13263,#13105,#9204,.T.);
#17448=EDGE_CURVE('',#13263,#13262,#4062,.T.);
#17449=EDGE_CURVE('',#13106,#13264,#9205,.T.);
#17450=EDGE_CURVE('',#13265,#13107,#9206,.T.);
#17451=EDGE_CURVE('',#13265,#13264,#4063,.T.);
#17452=EDGE_CURVE('',#13108,#13266,#9207,.T.);
#17453=EDGE_CURVE('',#13267,#13109,#9208,.T.);
#17454=EDGE_CURVE('',#13267,#13266,#4064,.T.);
#17455=EDGE_CURVE('',#13110,#13268,#9209,.T.);
#17456=EDGE_CURVE('',#13269,#13111,#9210,.T.);
#17457=EDGE_CURVE('',#13269,#13268,#4065,.T.);
#17458=EDGE_CURVE('',#13112,#13270,#9211,.T.);
#17459=EDGE_CURVE('',#13271,#13113,#9212,.T.);
#17460=EDGE_CURVE('',#13271,#13270,#4066,.T.);
#17461=EDGE_CURVE('',#13114,#13272,#9213,.T.);
#17462=EDGE_CURVE('',#13273,#13115,#9214,.T.);
#17463=EDGE_CURVE('',#13273,#13272,#4067,.T.);
#17464=EDGE_CURVE('',#13116,#13274,#9215,.T.);
#17465=EDGE_CURVE('',#13275,#13117,#9216,.T.);
#17466=EDGE_CURVE('',#13275,#13274,#4068,.T.);
#17467=EDGE_CURVE('',#13118,#13276,#9217,.T.);
#17468=EDGE_CURVE('',#13277,#13119,#9218,.T.);
#17469=EDGE_CURVE('',#13277,#13276,#4069,.T.);
#17470=EDGE_CURVE('',#13120,#13278,#9219,.T.);
#17471=EDGE_CURVE('',#13279,#13121,#9220,.T.);
#17472=EDGE_CURVE('',#13279,#13278,#4070,.T.);
#17473=EDGE_CURVE('',#13122,#13280,#9221,.T.);
#17474=EDGE_CURVE('',#13281,#13123,#9222,.T.);
#17475=EDGE_CURVE('',#13281,#13280,#4071,.T.);
#17476=EDGE_CURVE('',#13124,#13282,#9223,.T.);
#17477=EDGE_CURVE('',#13283,#13125,#9224,.T.);
#17478=EDGE_CURVE('',#13283,#13282,#4072,.T.);
#17479=EDGE_CURVE('',#13126,#13284,#9225,.T.);
#17480=EDGE_CURVE('',#13285,#13127,#9226,.T.);
#17481=EDGE_CURVE('',#13285,#13284,#4073,.T.);
#17482=EDGE_CURVE('',#13128,#13286,#9227,.T.);
#17483=EDGE_CURVE('',#13287,#13129,#9228,.T.);
#17484=EDGE_CURVE('',#13287,#13286,#4074,.T.);
#17485=EDGE_CURVE('',#13130,#13288,#9229,.T.);
#17486=EDGE_CURVE('',#13289,#13131,#9230,.T.);
#17487=EDGE_CURVE('',#13289,#13288,#4075,.T.);
#17488=EDGE_CURVE('',#13132,#13290,#9231,.T.);
#17489=EDGE_CURVE('',#13291,#13133,#9232,.T.);
#17490=EDGE_CURVE('',#13291,#13290,#4076,.T.);
#17491=EDGE_CURVE('',#13134,#13292,#9233,.T.);
#17492=EDGE_CURVE('',#13293,#13135,#9234,.T.);
#17493=EDGE_CURVE('',#13293,#13292,#4077,.T.);
#17494=EDGE_CURVE('',#13136,#13294,#9235,.T.);
#17495=EDGE_CURVE('',#13295,#13137,#9236,.T.);
#17496=EDGE_CURVE('',#13295,#13294,#4078,.T.);
#17497=EDGE_CURVE('',#13138,#13296,#9237,.T.);
#17498=EDGE_CURVE('',#13297,#13139,#9238,.T.);
#17499=EDGE_CURVE('',#13297,#13296,#4079,.T.);
#17500=EDGE_CURVE('',#13140,#13298,#9239,.T.);
#17501=EDGE_CURVE('',#13299,#13141,#9240,.T.);
#17502=EDGE_CURVE('',#13299,#13298,#4080,.T.);
#17503=EDGE_CURVE('',#13142,#13300,#9241,.T.);
#17504=EDGE_CURVE('',#13301,#13143,#9242,.T.);
#17505=EDGE_CURVE('',#13301,#13300,#4081,.T.);
#17506=EDGE_CURVE('',#13144,#13302,#9243,.T.);
#17507=EDGE_CURVE('',#13303,#13145,#9244,.T.);
#17508=EDGE_CURVE('',#13303,#13302,#4082,.T.);
#17509=EDGE_CURVE('',#13146,#13304,#9245,.T.);
#17510=EDGE_CURVE('',#13305,#13147,#9246,.T.);
#17511=EDGE_CURVE('',#13305,#13304,#4083,.T.);
#17512=EDGE_CURVE('',#13148,#13306,#9247,.T.);
#17513=EDGE_CURVE('',#13307,#13149,#9248,.T.);
#17514=EDGE_CURVE('',#13307,#13306,#4084,.T.);
#17515=EDGE_CURVE('',#13150,#13308,#9249,.T.);
#17516=EDGE_CURVE('',#13309,#13151,#9250,.T.);
#17517=EDGE_CURVE('',#13309,#13308,#4085,.T.);
#17518=EDGE_CURVE('',#13152,#13310,#9251,.T.);
#17519=EDGE_CURVE('',#13311,#13153,#9252,.T.);
#17520=EDGE_CURVE('',#13311,#13310,#4086,.T.);
#17521=EDGE_CURVE('',#13154,#13312,#9253,.T.);
#17522=EDGE_CURVE('',#13313,#13155,#9254,.T.);
#17523=EDGE_CURVE('',#13313,#13312,#4087,.T.);
#17524=EDGE_CURVE('',#13156,#13314,#9255,.T.);
#17525=EDGE_CURVE('',#13315,#13157,#9256,.T.);
#17526=EDGE_CURVE('',#13315,#13314,#4088,.T.);
#17527=EDGE_CURVE('',#13158,#13316,#9257,.T.);
#17528=EDGE_CURVE('',#13317,#13159,#9258,.T.);
#17529=EDGE_CURVE('',#13317,#13316,#4089,.T.);
#17530=EDGE_CURVE('',#13160,#13318,#9259,.T.);
#17531=EDGE_CURVE('',#13319,#13161,#9260,.T.);
#17532=EDGE_CURVE('',#13319,#13318,#4090,.T.);
#17533=EDGE_CURVE('',#13162,#13320,#9261,.T.);
#17534=EDGE_CURVE('',#13321,#13163,#9262,.T.);
#17535=EDGE_CURVE('',#13321,#13320,#4091,.T.);
#17536=EDGE_CURVE('',#13164,#13322,#9263,.T.);
#17537=EDGE_CURVE('',#13323,#13165,#9264,.T.);
#17538=EDGE_CURVE('',#13323,#13322,#4092,.T.);
#17539=EDGE_CURVE('',#13166,#13324,#9265,.T.);
#17540=EDGE_CURVE('',#13325,#13167,#9266,.T.);
#17541=EDGE_CURVE('',#13325,#13324,#4093,.T.);
#17542=EDGE_CURVE('',#13168,#13326,#9267,.T.);
#17543=EDGE_CURVE('',#13327,#13169,#9268,.T.);
#17544=EDGE_CURVE('',#13327,#13326,#4094,.T.);
#17545=EDGE_CURVE('',#13170,#13328,#9269,.T.);
#17546=EDGE_CURVE('',#13329,#13171,#9270,.T.);
#17547=EDGE_CURVE('',#13329,#13328,#4095,.T.);
#17548=EDGE_CURVE('',#13172,#13330,#9271,.T.);
#17549=EDGE_CURVE('',#13331,#13173,#9272,.T.);
#17550=EDGE_CURVE('',#13331,#13330,#4096,.T.);
#17551=EDGE_CURVE('',#13174,#13332,#9273,.T.);
#17552=EDGE_CURVE('',#13333,#13175,#9274,.T.);
#17553=EDGE_CURVE('',#13333,#13332,#4097,.T.);
#17554=EDGE_CURVE('',#13334,#13176,#9275,.T.);
#17555=EDGE_CURVE('',#13334,#13335,#4098,.T.);
#17556=EDGE_CURVE('',#13177,#13335,#9276,.T.);
#17557=EDGE_CURVE('',#13336,#13178,#9277,.T.);
#17558=EDGE_CURVE('',#13336,#13337,#4099,.T.);
#17559=EDGE_CURVE('',#13179,#13337,#9278,.T.);
#17560=EDGE_CURVE('',#13338,#13180,#9279,.T.);
#17561=EDGE_CURVE('',#13338,#13339,#4100,.T.);
#17562=EDGE_CURVE('',#13181,#13339,#9280,.T.);
#17563=EDGE_CURVE('',#13340,#13182,#9281,.T.);
#17564=EDGE_CURVE('',#13340,#13341,#4101,.T.);
#17565=EDGE_CURVE('',#13183,#13341,#9282,.T.);
#17566=EDGE_CURVE('',#13342,#13184,#9283,.T.);
#17567=EDGE_CURVE('',#13342,#13343,#4102,.T.);
#17568=EDGE_CURVE('',#13185,#13343,#9284,.T.);
#17569=EDGE_CURVE('',#13344,#13186,#9285,.T.);
#17570=EDGE_CURVE('',#13344,#13345,#4103,.T.);
#17571=EDGE_CURVE('',#13187,#13345,#9286,.T.);
#17572=EDGE_CURVE('',#13346,#13188,#9287,.T.);
#17573=EDGE_CURVE('',#13346,#13347,#4104,.T.);
#17574=EDGE_CURVE('',#13189,#13347,#9288,.T.);
#17575=EDGE_CURVE('',#13348,#13190,#9289,.T.);
#17576=EDGE_CURVE('',#13348,#13349,#4105,.T.);
#17577=EDGE_CURVE('',#13191,#13349,#9290,.T.);
#17578=EDGE_CURVE('',#13350,#13192,#9291,.T.);
#17579=EDGE_CURVE('',#13350,#13351,#4106,.T.);
#17580=EDGE_CURVE('',#13193,#13351,#9292,.T.);
#17581=EDGE_CURVE('',#13352,#13194,#9293,.T.);
#17582=EDGE_CURVE('',#13352,#13353,#4107,.T.);
#17583=EDGE_CURVE('',#13195,#13353,#9294,.T.);
#17584=EDGE_CURVE('',#13354,#13196,#9295,.T.);
#17585=EDGE_CURVE('',#13354,#13355,#4108,.T.);
#17586=EDGE_CURVE('',#13197,#13355,#9296,.T.);
#17587=EDGE_CURVE('',#13356,#13198,#9297,.T.);
#17588=EDGE_CURVE('',#13356,#13357,#4109,.T.);
#17589=EDGE_CURVE('',#13199,#13357,#9298,.T.);
#17590=EDGE_CURVE('',#13358,#13200,#9299,.T.);
#17591=EDGE_CURVE('',#13358,#13359,#4110,.T.);
#17592=EDGE_CURVE('',#13201,#13359,#9300,.T.);
#17593=EDGE_CURVE('',#13360,#13202,#9301,.T.);
#17594=EDGE_CURVE('',#13360,#13361,#4111,.T.);
#17595=EDGE_CURVE('',#13203,#13361,#9302,.T.);
#17596=EDGE_CURVE('',#13204,#13362,#9303,.T.);
#17597=EDGE_CURVE('',#13363,#13205,#9304,.T.);
#17598=EDGE_CURVE('',#13363,#13362,#4112,.T.);
#17599=EDGE_CURVE('',#12661,#13206,#2316,.T.);
#17600=EDGE_CURVE('',#13207,#12660,#2317,.T.);
#17601=EDGE_CURVE('',#13208,#12662,#2318,.T.);
#17602=EDGE_CURVE('',#12663,#13209,#2319,.T.);
#17603=EDGE_CURVE('',#13210,#12664,#2320,.T.);
#17604=EDGE_CURVE('',#12665,#13211,#2321,.T.);
#17605=EDGE_CURVE('',#13212,#12666,#2322,.T.);
#17606=EDGE_CURVE('',#12667,#13213,#2323,.T.);
#17607=EDGE_CURVE('',#13214,#12668,#2324,.T.);
#17608=EDGE_CURVE('',#12669,#13215,#2325,.T.);
#17609=EDGE_CURVE('',#13216,#12670,#2326,.T.);
#17610=EDGE_CURVE('',#12671,#13217,#2327,.T.);
#17611=EDGE_CURVE('',#13218,#12672,#2328,.T.);
#17612=EDGE_CURVE('',#12673,#13219,#2329,.T.);
#17613=EDGE_CURVE('',#13220,#12676,#2330,.T.);
#17614=EDGE_CURVE('',#12677,#13221,#2331,.T.);
#17615=EDGE_CURVE('',#13222,#12680,#2332,.T.);
#17616=EDGE_CURVE('',#12681,#13223,#2333,.T.);
#17617=EDGE_CURVE('',#13224,#12684,#2334,.T.);
#17618=EDGE_CURVE('',#12685,#13225,#2335,.T.);
#17619=EDGE_CURVE('',#13226,#12688,#2336,.T.);
#17620=EDGE_CURVE('',#12689,#13227,#2337,.T.);
#17621=EDGE_CURVE('',#13228,#12692,#2338,.T.);
#17622=EDGE_CURVE('',#12693,#13229,#2339,.T.);
#17623=EDGE_CURVE('',#13230,#12696,#2340,.T.);
#17624=EDGE_CURVE('',#12697,#13231,#2341,.T.);
#17625=EDGE_CURVE('',#13232,#12700,#2342,.T.);
#17626=EDGE_CURVE('',#12701,#13233,#2343,.T.);
#17627=EDGE_CURVE('',#13234,#12704,#2344,.T.);
#17628=EDGE_CURVE('',#12705,#13235,#2345,.T.);
#17629=EDGE_CURVE('',#13236,#12708,#2346,.T.);
#17630=EDGE_CURVE('',#12709,#13237,#2347,.T.);
#17631=EDGE_CURVE('',#13238,#12712,#2348,.T.);
#17632=EDGE_CURVE('',#12713,#13239,#2349,.T.);
#17633=EDGE_CURVE('',#13240,#12716,#2350,.T.);
#17634=EDGE_CURVE('',#12717,#13241,#2351,.T.);
#17635=EDGE_CURVE('',#13242,#12720,#2352,.T.);
#17636=EDGE_CURVE('',#12721,#13243,#2353,.T.);
#17637=EDGE_CURVE('',#13244,#12724,#2354,.T.);
#17638=EDGE_CURVE('',#12725,#13245,#2355,.T.);
#17639=EDGE_CURVE('',#13246,#12728,#2356,.T.);
#17640=EDGE_CURVE('',#12729,#13247,#2357,.T.);
#17641=EDGE_CURVE('',#13248,#12732,#2358,.T.);
#17642=EDGE_CURVE('',#12733,#13249,#2359,.T.);
#17643=EDGE_CURVE('',#13250,#12736,#2360,.T.);
#17644=EDGE_CURVE('',#12737,#13251,#2361,.T.);
#17645=EDGE_CURVE('',#13252,#12740,#2362,.T.);
#17646=EDGE_CURVE('',#12741,#13253,#2363,.T.);
#17647=EDGE_CURVE('',#13254,#12744,#2364,.T.);
#17648=EDGE_CURVE('',#12745,#13255,#2365,.T.);
#17649=EDGE_CURVE('',#13256,#12748,#2366,.T.);
#17650=EDGE_CURVE('',#12749,#13257,#2367,.T.);
#17651=EDGE_CURVE('',#13258,#12462,#2368,.T.);
#17652=EDGE_CURVE('',#12463,#13259,#2369,.T.);
#17653=EDGE_CURVE('',#13260,#12466,#2370,.T.);
#17654=EDGE_CURVE('',#12467,#13261,#2371,.T.);
#17655=EDGE_CURVE('',#13262,#12470,#2372,.T.);
#17656=EDGE_CURVE('',#12471,#13263,#2373,.T.);
#17657=EDGE_CURVE('',#13264,#12474,#2374,.T.);
#17658=EDGE_CURVE('',#12475,#13265,#2375,.T.);
#17659=EDGE_CURVE('',#13266,#12478,#2376,.T.);
#17660=EDGE_CURVE('',#12479,#13267,#2377,.T.);
#17661=EDGE_CURVE('',#13268,#12482,#2378,.T.);
#17662=EDGE_CURVE('',#12483,#13269,#2379,.T.);
#17663=EDGE_CURVE('',#13270,#12486,#2380,.T.);
#17664=EDGE_CURVE('',#12487,#13271,#2381,.T.);
#17665=EDGE_CURVE('',#13272,#12490,#2382,.T.);
#17666=EDGE_CURVE('',#12491,#13273,#2383,.T.);
#17667=EDGE_CURVE('',#13274,#12494,#2384,.T.);
#17668=EDGE_CURVE('',#12495,#13275,#2385,.T.);
#17669=EDGE_CURVE('',#13276,#12498,#2386,.T.);
#17670=EDGE_CURVE('',#12499,#13277,#2387,.T.);
#17671=EDGE_CURVE('',#13278,#12502,#2388,.T.);
#17672=EDGE_CURVE('',#12503,#13279,#2389,.T.);
#17673=EDGE_CURVE('',#13280,#12506,#2390,.T.);
#17674=EDGE_CURVE('',#12507,#13281,#2391,.T.);
#17675=EDGE_CURVE('',#13282,#12510,#2392,.T.);
#17676=EDGE_CURVE('',#12511,#13283,#2393,.T.);
#17677=EDGE_CURVE('',#13284,#12514,#2394,.T.);
#17678=EDGE_CURVE('',#12515,#13285,#2395,.T.);
#17679=EDGE_CURVE('',#13286,#12518,#2396,.T.);
#17680=EDGE_CURVE('',#12519,#13287,#2397,.T.);
#17681=EDGE_CURVE('',#13288,#12522,#2398,.T.);
#17682=EDGE_CURVE('',#12523,#13289,#2399,.T.);
#17683=EDGE_CURVE('',#13290,#12526,#2400,.T.);
#17684=EDGE_CURVE('',#12527,#13291,#2401,.T.);
#17685=EDGE_CURVE('',#13292,#12530,#2402,.T.);
#17686=EDGE_CURVE('',#12531,#13293,#2403,.T.);
#17687=EDGE_CURVE('',#13294,#12534,#2404,.T.);
#17688=EDGE_CURVE('',#12535,#13295,#2405,.T.);
#17689=EDGE_CURVE('',#13296,#12538,#2406,.T.);
#17690=EDGE_CURVE('',#12539,#13297,#2407,.T.);
#17691=EDGE_CURVE('',#13298,#12542,#2408,.T.);
#17692=EDGE_CURVE('',#12543,#13299,#2409,.T.);
#17693=EDGE_CURVE('',#13300,#12546,#2410,.T.);
#17694=EDGE_CURVE('',#12547,#13301,#2411,.T.);
#17695=EDGE_CURVE('',#13302,#12550,#2412,.T.);
#17696=EDGE_CURVE('',#12551,#13303,#2413,.T.);
#17697=EDGE_CURVE('',#13304,#12554,#2414,.T.);
#17698=EDGE_CURVE('',#12555,#13305,#2415,.T.);
#17699=EDGE_CURVE('',#13306,#12558,#2416,.T.);
#17700=EDGE_CURVE('',#12559,#13307,#2417,.T.);
#17701=EDGE_CURVE('',#13308,#12562,#2418,.T.);
#17702=EDGE_CURVE('',#12563,#13309,#2419,.T.);
#17703=EDGE_CURVE('',#13310,#12566,#2420,.T.);
#17704=EDGE_CURVE('',#12567,#13311,#2421,.T.);
#17705=EDGE_CURVE('',#13312,#12570,#2422,.T.);
#17706=EDGE_CURVE('',#12571,#13313,#2423,.T.);
#17707=EDGE_CURVE('',#13314,#12574,#2424,.T.);
#17708=EDGE_CURVE('',#12575,#13315,#2425,.T.);
#17709=EDGE_CURVE('',#13316,#12578,#2426,.T.);
#17710=EDGE_CURVE('',#12579,#13317,#2427,.T.);
#17711=EDGE_CURVE('',#13318,#12582,#2428,.T.);
#17712=EDGE_CURVE('',#12583,#13319,#2429,.T.);
#17713=EDGE_CURVE('',#13320,#12586,#2430,.T.);
#17714=EDGE_CURVE('',#12587,#13321,#2431,.T.);
#17715=EDGE_CURVE('',#13322,#12590,#2432,.T.);
#17716=EDGE_CURVE('',#12591,#13323,#2433,.T.);
#17717=EDGE_CURVE('',#13324,#12594,#2434,.T.);
#17718=EDGE_CURVE('',#12595,#13325,#2435,.T.);
#17719=EDGE_CURVE('',#13326,#12598,#2436,.T.);
#17720=EDGE_CURVE('',#12599,#13327,#2437,.T.);
#17721=EDGE_CURVE('',#13328,#12602,#2438,.T.);
#17722=EDGE_CURVE('',#12603,#13329,#2439,.T.);
#17723=EDGE_CURVE('',#13330,#12606,#2440,.T.);
#17724=EDGE_CURVE('',#12607,#13331,#2441,.T.);
#17725=EDGE_CURVE('',#13332,#12610,#2442,.T.);
#17726=EDGE_CURVE('',#12611,#13333,#2443,.T.);
#17727=EDGE_CURVE('',#12659,#13334,#2444,.T.);
#17728=EDGE_CURVE('',#13335,#12658,#2445,.T.);
#17729=EDGE_CURVE('',#12657,#13336,#2446,.T.);
#17730=EDGE_CURVE('',#13337,#12656,#2447,.T.);
#17731=EDGE_CURVE('',#12655,#13338,#2448,.T.);
#17732=EDGE_CURVE('',#13339,#12654,#2449,.T.);
#17733=EDGE_CURVE('',#12653,#13340,#2450,.T.);
#17734=EDGE_CURVE('',#13341,#12652,#2451,.T.);
#17735=EDGE_CURVE('',#12651,#13342,#2452,.T.);
#17736=EDGE_CURVE('',#13343,#12650,#2453,.T.);
#17737=EDGE_CURVE('',#12649,#13344,#2454,.T.);
#17738=EDGE_CURVE('',#13345,#12648,#2455,.T.);
#17739=EDGE_CURVE('',#12647,#13346,#2456,.T.);
#17740=EDGE_CURVE('',#13347,#12646,#2457,.T.);
#17741=EDGE_CURVE('',#12645,#13348,#2458,.T.);
#17742=EDGE_CURVE('',#13349,#12644,#2459,.T.);
#17743=EDGE_CURVE('',#12643,#13350,#2460,.T.);
#17744=EDGE_CURVE('',#13351,#12642,#2461,.T.);
#17745=EDGE_CURVE('',#12639,#13352,#2462,.T.);
#17746=EDGE_CURVE('',#13353,#12638,#2463,.T.);
#17747=EDGE_CURVE('',#12635,#13354,#2464,.T.);
#17748=EDGE_CURVE('',#13355,#12634,#2465,.T.);
#17749=EDGE_CURVE('',#12631,#13356,#2466,.T.);
#17750=EDGE_CURVE('',#13357,#12630,#2467,.T.);
#17751=EDGE_CURVE('',#12627,#13358,#2468,.T.);
#17752=EDGE_CURVE('',#13359,#12626,#2469,.T.);
#17753=EDGE_CURVE('',#12623,#13360,#2470,.T.);
#17754=EDGE_CURVE('',#13361,#12622,#2471,.T.);
#17755=EDGE_CURVE('',#13362,#12614,#2472,.T.);
#17756=EDGE_CURVE('',#12615,#13363,#2473,.T.);
#17757=EDGE_CURVE('',#12754,#13364,#2474,.T.);
#17758=EDGE_CURVE('',#13365,#12753,#2475,.T.);
#17759=EDGE_CURVE('',#13365,#13364,#4113,.T.);
#17760=EDGE_CURVE('',#13364,#13366,#9305,.T.);
#17761=EDGE_CURVE('',#13367,#13365,#9306,.T.);
#17762=EDGE_CURVE('',#13367,#13366,#4114,.T.);
#17763=EDGE_CURVE('',#13366,#12618,#2476,.T.);
#17764=EDGE_CURVE('',#12619,#13367,#2477,.T.);
#17765=EDGE_CURVE('',#13368,#13369,#9307,.T.);
#17766=EDGE_CURVE('',#13369,#13370,#9308,.T.);
#17767=EDGE_CURVE('',#13370,#13371,#9309,.T.);
#17768=EDGE_CURVE('',#13371,#13372,#9310,.T.);
#17769=EDGE_CURVE('',#13372,#13373,#9311,.T.);
#17770=EDGE_CURVE('',#13373,#13368,#9312,.T.);
#17771=EDGE_CURVE('',#13369,#12454,#9313,.T.);
#17772=EDGE_CURVE('',#13370,#12453,#9314,.T.);
#17773=EDGE_CURVE('',#13371,#12452,#9315,.T.);
#17774=EDGE_CURVE('',#13372,#12450,#9316,.T.);
#17775=EDGE_CURVE('',#13373,#12456,#9317,.T.);
#17776=EDGE_CURVE('',#13368,#12455,#9318,.T.);
#17777=EDGE_CURVE('',#12387,#12269,#3225,.T.);
#17778=EDGE_CURVE('',#12267,#12385,#9319,.T.);
#17779=EDGE_CURVE('',#12751,#12620,#9320,.T.);
#17780=EDGE_CURVE('',#13041,#12621,#9321,.T.);
#17781=EDGE_CURVE('',#12756,#12616,#9322,.T.);
#17782=EDGE_CURVE('',#12755,#12617,#9323,.T.);
#17783=EDGE_CURVE('',#13038,#12624,#9324,.T.);
#17784=EDGE_CURVE('',#13037,#12625,#9325,.T.);
#17785=EDGE_CURVE('',#13034,#12628,#9326,.T.);
#17786=EDGE_CURVE('',#13033,#12629,#9327,.T.);
#17787=EDGE_CURVE('',#13030,#12632,#9328,.T.);
#17788=EDGE_CURVE('',#13029,#12633,#9329,.T.);
#17789=EDGE_CURVE('',#13026,#12636,#9330,.T.);
#17790=EDGE_CURVE('',#13025,#12637,#9331,.T.);
#17791=EDGE_CURVE('',#13022,#12640,#9332,.T.);
#17792=EDGE_CURVE('',#13021,#12641,#9333,.T.);
#17793=EDGE_CURVE('',#12760,#12612,#9334,.T.);
#17794=EDGE_CURVE('',#12759,#12613,#9335,.T.);
#17795=EDGE_CURVE('',#12764,#12608,#9336,.T.);
#17796=EDGE_CURVE('',#12763,#12609,#9337,.T.);
#17797=EDGE_CURVE('',#12768,#12604,#9338,.T.);
#17798=EDGE_CURVE('',#12767,#12605,#9339,.T.);
#17799=EDGE_CURVE('',#12772,#12600,#9340,.T.);
#17800=EDGE_CURVE('',#12771,#12601,#9341,.T.);
#17801=EDGE_CURVE('',#12776,#12596,#9342,.T.);
#17802=EDGE_CURVE('',#12775,#12597,#9343,.T.);
#17803=EDGE_CURVE('',#12780,#12592,#9344,.T.);
#17804=EDGE_CURVE('',#12779,#12593,#9345,.T.);
#17805=EDGE_CURVE('',#12784,#12588,#9346,.T.);
#17806=EDGE_CURVE('',#12783,#12589,#9347,.T.);
#17807=EDGE_CURVE('',#12788,#12584,#9348,.T.);
#17808=EDGE_CURVE('',#12787,#12585,#9349,.T.);
#17809=EDGE_CURVE('',#12792,#12580,#9350,.T.);
#17810=EDGE_CURVE('',#12791,#12581,#9351,.T.);
#17811=EDGE_CURVE('',#12796,#12576,#9352,.T.);
#17812=EDGE_CURVE('',#12795,#12577,#9353,.T.);
#17813=EDGE_CURVE('',#12800,#12572,#9354,.T.);
#17814=EDGE_CURVE('',#12799,#12573,#9355,.T.);
#17815=EDGE_CURVE('',#12804,#12568,#9356,.T.);
#17816=EDGE_CURVE('',#12803,#12569,#9357,.T.);
#17817=EDGE_CURVE('',#12808,#12564,#9358,.T.);
#17818=EDGE_CURVE('',#12807,#12565,#9359,.T.);
#17819=EDGE_CURVE('',#12812,#12560,#9360,.T.);
#17820=EDGE_CURVE('',#12811,#12561,#9361,.T.);
#17821=EDGE_CURVE('',#12816,#12556,#9362,.T.);
#17822=EDGE_CURVE('',#12815,#12557,#9363,.T.);
#17823=EDGE_CURVE('',#12820,#12552,#9364,.T.);
#17824=EDGE_CURVE('',#12819,#12553,#9365,.T.);
#17825=EDGE_CURVE('',#12824,#12548,#9366,.T.);
#17826=EDGE_CURVE('',#12823,#12549,#9367,.T.);
#17827=EDGE_CURVE('',#12828,#12544,#9368,.T.);
#17828=EDGE_CURVE('',#12827,#12545,#9369,.T.);
#17829=EDGE_CURVE('',#12832,#12540,#9370,.T.);
#17830=EDGE_CURVE('',#12831,#12541,#9371,.T.);
#17831=EDGE_CURVE('',#12836,#12536,#9372,.T.);
#17832=EDGE_CURVE('',#12835,#12537,#9373,.T.);
#17833=EDGE_CURVE('',#12840,#12532,#9374,.T.);
#17834=EDGE_CURVE('',#12839,#12533,#9375,.T.);
#17835=EDGE_CURVE('',#12844,#12528,#9376,.T.);
#17836=EDGE_CURVE('',#12843,#12529,#9377,.T.);
#17837=EDGE_CURVE('',#12848,#12524,#9378,.T.);
#17838=EDGE_CURVE('',#12847,#12525,#9379,.T.);
#17839=EDGE_CURVE('',#12852,#12520,#9380,.T.);
#17840=EDGE_CURVE('',#12851,#12521,#9381,.T.);
#17841=EDGE_CURVE('',#12856,#12516,#9382,.T.);
#17842=EDGE_CURVE('',#12855,#12517,#9383,.T.);
#17843=EDGE_CURVE('',#12860,#12512,#9384,.T.);
#17844=EDGE_CURVE('',#12859,#12513,#9385,.T.);
#17845=EDGE_CURVE('',#12864,#12508,#9386,.T.);
#17846=EDGE_CURVE('',#12863,#12509,#9387,.T.);
#17847=EDGE_CURVE('',#12868,#12504,#9388,.T.);
#17848=EDGE_CURVE('',#12867,#12505,#9389,.T.);
#17849=EDGE_CURVE('',#12872,#12500,#9390,.T.);
#17850=EDGE_CURVE('',#12871,#12501,#9391,.T.);
#17851=EDGE_CURVE('',#12876,#12496,#9392,.T.);
#17852=EDGE_CURVE('',#12875,#12497,#9393,.T.);
#17853=EDGE_CURVE('',#12880,#12492,#9394,.T.);
#17854=EDGE_CURVE('',#12879,#12493,#9395,.T.);
#17855=EDGE_CURVE('',#12884,#12488,#9396,.T.);
#17856=EDGE_CURVE('',#12883,#12489,#9397,.T.);
#17857=EDGE_CURVE('',#12888,#12484,#9398,.T.);
#17858=EDGE_CURVE('',#12887,#12485,#9399,.T.);
#17859=EDGE_CURVE('',#12892,#12480,#9400,.T.);
#17860=EDGE_CURVE('',#12891,#12481,#9401,.T.);
#17861=EDGE_CURVE('',#12896,#12476,#9402,.T.);
#17862=EDGE_CURVE('',#12895,#12477,#9403,.T.);
#17863=EDGE_CURVE('',#12900,#12472,#9404,.T.);
#17864=EDGE_CURVE('',#12899,#12473,#9405,.T.);
#17865=EDGE_CURVE('',#12904,#12468,#9406,.T.);
#17866=EDGE_CURVE('',#12903,#12469,#9407,.T.);
#17867=EDGE_CURVE('',#12908,#12464,#9408,.T.);
#17868=EDGE_CURVE('',#12907,#12465,#9409,.T.);
#17869=EDGE_CURVE('',#12912,#12750,#9410,.T.);
#17870=EDGE_CURVE('',#12911,#12460,#9411,.T.);
#17871=EDGE_CURVE('',#12916,#12746,#9412,.T.);
#17872=EDGE_CURVE('',#12915,#12747,#9413,.T.);
#17873=EDGE_CURVE('',#12920,#12742,#9414,.T.);
#17874=EDGE_CURVE('',#12919,#12743,#9415,.T.);
#17875=EDGE_CURVE('',#12924,#12738,#9416,.T.);
#17876=EDGE_CURVE('',#12923,#12739,#9417,.T.);
#17877=EDGE_CURVE('',#12928,#12734,#9418,.T.);
#17878=EDGE_CURVE('',#12927,#12735,#9419,.T.);
#17879=EDGE_CURVE('',#12932,#12730,#9420,.T.);
#17880=EDGE_CURVE('',#12931,#12731,#9421,.T.);
#17881=EDGE_CURVE('',#12936,#12726,#9422,.T.);
#17882=EDGE_CURVE('',#12935,#12727,#9423,.T.);
#17883=EDGE_CURVE('',#12940,#12722,#9424,.T.);
#17884=EDGE_CURVE('',#12939,#12723,#9425,.T.);
#17885=EDGE_CURVE('',#12944,#12718,#9426,.T.);
#17886=EDGE_CURVE('',#12943,#12719,#9427,.T.);
#17887=EDGE_CURVE('',#12948,#12714,#9428,.T.);
#17888=EDGE_CURVE('',#12947,#12715,#9429,.T.);
#17889=EDGE_CURVE('',#12952,#12710,#9430,.T.);
#17890=EDGE_CURVE('',#12951,#12711,#9431,.T.);
#17891=EDGE_CURVE('',#12956,#12706,#9432,.T.);
#17892=EDGE_CURVE('',#12955,#12707,#9433,.T.);
#17893=EDGE_CURVE('',#12960,#12702,#9434,.T.);
#17894=EDGE_CURVE('',#12959,#12703,#9435,.T.);
#17895=EDGE_CURVE('',#12964,#12698,#9436,.T.);
#17896=EDGE_CURVE('',#12963,#12699,#9437,.T.);
#17897=EDGE_CURVE('',#12968,#12694,#9438,.T.);
#17898=EDGE_CURVE('',#12967,#12695,#9439,.T.);
#17899=EDGE_CURVE('',#12972,#12690,#9440,.T.);
#17900=EDGE_CURVE('',#12971,#12691,#9441,.T.);
#17901=EDGE_CURVE('',#12976,#12686,#9442,.T.);
#17902=EDGE_CURVE('',#12975,#12687,#9443,.T.);
#17903=EDGE_CURVE('',#12980,#12682,#9444,.T.);
#17904=EDGE_CURVE('',#12979,#12683,#9445,.T.);
#17905=EDGE_CURVE('',#12984,#12678,#9446,.T.);
#17906=EDGE_CURVE('',#12983,#12679,#9447,.T.);
#17907=EDGE_CURVE('',#12988,#12674,#9448,.T.);
#17908=EDGE_CURVE('',#12987,#12675,#9449,.T.);
#23093=ORIENTED_EDGE('',*,*,#16241,.F.);
#23094=ORIENTED_EDGE('',*,*,#16242,.F.);
#23095=ORIENTED_EDGE('',*,*,#16243,.T.);
#23096=ORIENTED_EDGE('',*,*,#16244,.T.);
#23097=ORIENTED_EDGE('',*,*,#16243,.F.);
#23098=ORIENTED_EDGE('',*,*,#16245,.F.);
#23099=ORIENTED_EDGE('',*,*,#16246,.F.);
#23100=ORIENTED_EDGE('',*,*,#16247,.F.);
#23101=ORIENTED_EDGE('',*,*,#16248,.F.);
#23102=ORIENTED_EDGE('',*,*,#16241,.T.);
#23103=ORIENTED_EDGE('',*,*,#16249,.F.);
#23104=ORIENTED_EDGE('',*,*,#16250,.F.);
#23105=ORIENTED_EDGE('',*,*,#16251,.F.);
#23106=ORIENTED_EDGE('',*,*,#16247,.T.);
#23107=ORIENTED_EDGE('',*,*,#16252,.F.);
#23108=ORIENTED_EDGE('',*,*,#16253,.F.);
#23109=ORIENTED_EDGE('',*,*,#16254,.F.);
#23110=ORIENTED_EDGE('',*,*,#16250,.T.);
#23111=ORIENTED_EDGE('',*,*,#16255,.F.);
#23112=ORIENTED_EDGE('',*,*,#16256,.F.);
#23113=ORIENTED_EDGE('',*,*,#16257,.F.);
#23114=ORIENTED_EDGE('',*,*,#16253,.T.);
#23115=ORIENTED_EDGE('',*,*,#16258,.F.);
#23116=ORIENTED_EDGE('',*,*,#16259,.F.);
#23117=ORIENTED_EDGE('',*,*,#16260,.F.);
#23118=ORIENTED_EDGE('',*,*,#16256,.T.);
#23119=ORIENTED_EDGE('',*,*,#16261,.F.);
#23120=ORIENTED_EDGE('',*,*,#16262,.F.);
#23121=ORIENTED_EDGE('',*,*,#16263,.F.);
#23122=ORIENTED_EDGE('',*,*,#16259,.T.);
#23123=ORIENTED_EDGE('',*,*,#16264,.F.);
#23124=ORIENTED_EDGE('',*,*,#16265,.F.);
#23125=ORIENTED_EDGE('',*,*,#16266,.F.);
#23126=ORIENTED_EDGE('',*,*,#16262,.T.);
#23127=ORIENTED_EDGE('',*,*,#16267,.F.);
#23128=ORIENTED_EDGE('',*,*,#16268,.F.);
#23129=ORIENTED_EDGE('',*,*,#16269,.F.);
#23130=ORIENTED_EDGE('',*,*,#16265,.T.);
#23131=ORIENTED_EDGE('',*,*,#16270,.F.);
#23132=ORIENTED_EDGE('',*,*,#16271,.F.);
#23133=ORIENTED_EDGE('',*,*,#16272,.F.);
#23134=ORIENTED_EDGE('',*,*,#16268,.T.);
#23135=ORIENTED_EDGE('',*,*,#16273,.F.);
#23136=ORIENTED_EDGE('',*,*,#16274,.F.);
#23137=ORIENTED_EDGE('',*,*,#16275,.F.);
#23138=ORIENTED_EDGE('',*,*,#16271,.T.);
#23139=ORIENTED_EDGE('',*,*,#16276,.F.);
#23140=ORIENTED_EDGE('',*,*,#16277,.F.);
#23141=ORIENTED_EDGE('',*,*,#16278,.F.);
#23142=ORIENTED_EDGE('',*,*,#16274,.T.);
#23143=ORIENTED_EDGE('',*,*,#16279,.F.);
#23144=ORIENTED_EDGE('',*,*,#16280,.F.);
#23145=ORIENTED_EDGE('',*,*,#16281,.F.);
#23146=ORIENTED_EDGE('',*,*,#16277,.T.);
#23147=ORIENTED_EDGE('',*,*,#16282,.F.);
#23148=ORIENTED_EDGE('',*,*,#16283,.F.);
#23149=ORIENTED_EDGE('',*,*,#16284,.F.);
#23150=ORIENTED_EDGE('',*,*,#16280,.T.);
#23151=ORIENTED_EDGE('',*,*,#16285,.F.);
#23152=ORIENTED_EDGE('',*,*,#16286,.F.);
#23153=ORIENTED_EDGE('',*,*,#16287,.F.);
#23154=ORIENTED_EDGE('',*,*,#16283,.T.);
#23155=ORIENTED_EDGE('',*,*,#16288,.F.);
#23156=ORIENTED_EDGE('',*,*,#16289,.F.);
#23157=ORIENTED_EDGE('',*,*,#16290,.F.);
#23158=ORIENTED_EDGE('',*,*,#16286,.T.);
#23159=ORIENTED_EDGE('',*,*,#16291,.F.);
#23160=ORIENTED_EDGE('',*,*,#16292,.F.);
#23161=ORIENTED_EDGE('',*,*,#16293,.F.);
#23162=ORIENTED_EDGE('',*,*,#16289,.T.);
#23163=ORIENTED_EDGE('',*,*,#16294,.F.);
#23164=ORIENTED_EDGE('',*,*,#16295,.F.);
#23165=ORIENTED_EDGE('',*,*,#16296,.F.);
#23166=ORIENTED_EDGE('',*,*,#16292,.T.);
#23167=ORIENTED_EDGE('',*,*,#16297,.F.);
#23168=ORIENTED_EDGE('',*,*,#16298,.F.);
#23169=ORIENTED_EDGE('',*,*,#16299,.F.);
#23170=ORIENTED_EDGE('',*,*,#16295,.T.);
#23171=ORIENTED_EDGE('',*,*,#16300,.F.);
#23172=ORIENTED_EDGE('',*,*,#16301,.F.);
#23173=ORIENTED_EDGE('',*,*,#16302,.F.);
#23174=ORIENTED_EDGE('',*,*,#16298,.T.);
#23175=ORIENTED_EDGE('',*,*,#16303,.F.);
#23176=ORIENTED_EDGE('',*,*,#16304,.F.);
#23177=ORIENTED_EDGE('',*,*,#16305,.F.);
#23178=ORIENTED_EDGE('',*,*,#16301,.T.);
#23179=ORIENTED_EDGE('',*,*,#16306,.F.);
#23180=ORIENTED_EDGE('',*,*,#16307,.F.);
#23181=ORIENTED_EDGE('',*,*,#16308,.F.);
#23182=ORIENTED_EDGE('',*,*,#16304,.T.);
#23183=ORIENTED_EDGE('',*,*,#16309,.F.);
#23184=ORIENTED_EDGE('',*,*,#16310,.F.);
#23185=ORIENTED_EDGE('',*,*,#16311,.F.);
#23186=ORIENTED_EDGE('',*,*,#16307,.T.);
#23187=ORIENTED_EDGE('',*,*,#16312,.F.);
#23188=ORIENTED_EDGE('',*,*,#16313,.F.);
#23189=ORIENTED_EDGE('',*,*,#16314,.F.);
#23190=ORIENTED_EDGE('',*,*,#16310,.T.);
#23191=ORIENTED_EDGE('',*,*,#16315,.F.);
#23192=ORIENTED_EDGE('',*,*,#16316,.F.);
#23193=ORIENTED_EDGE('',*,*,#16317,.F.);
#23194=ORIENTED_EDGE('',*,*,#16313,.T.);
#23195=ORIENTED_EDGE('',*,*,#16318,.F.);
#23196=ORIENTED_EDGE('',*,*,#16319,.F.);
#23197=ORIENTED_EDGE('',*,*,#16320,.F.);
#23198=ORIENTED_EDGE('',*,*,#16316,.T.);
#23199=ORIENTED_EDGE('',*,*,#16321,.F.);
#23200=ORIENTED_EDGE('',*,*,#16322,.F.);
#23201=ORIENTED_EDGE('',*,*,#16323,.F.);
#23202=ORIENTED_EDGE('',*,*,#16319,.T.);
#23203=ORIENTED_EDGE('',*,*,#16324,.F.);
#23204=ORIENTED_EDGE('',*,*,#16325,.F.);
#23205=ORIENTED_EDGE('',*,*,#16326,.F.);
#23206=ORIENTED_EDGE('',*,*,#16322,.T.);
#23207=ORIENTED_EDGE('',*,*,#16327,.F.);
#23208=ORIENTED_EDGE('',*,*,#16328,.F.);
#23209=ORIENTED_EDGE('',*,*,#16329,.T.);
#23210=ORIENTED_EDGE('',*,*,#16330,.F.);
#23211=ORIENTED_EDGE('',*,*,#16331,.F.);
#23212=ORIENTED_EDGE('',*,*,#16332,.F.);
#23213=ORIENTED_EDGE('',*,*,#16333,.F.);
#23214=ORIENTED_EDGE('',*,*,#16334,.F.);
#23215=ORIENTED_EDGE('',*,*,#16335,.F.);
#23216=ORIENTED_EDGE('',*,*,#16331,.T.);
#23217=ORIENTED_EDGE('',*,*,#16336,.T.);
#23218=ORIENTED_EDGE('',*,*,#16337,.F.);
#23219=ORIENTED_EDGE('',*,*,#16338,.F.);
#23220=ORIENTED_EDGE('',*,*,#16334,.T.);
#23221=ORIENTED_EDGE('',*,*,#16339,.T.);
#23222=ORIENTED_EDGE('',*,*,#16340,.F.);
#23223=ORIENTED_EDGE('',*,*,#16341,.F.);
#23224=ORIENTED_EDGE('',*,*,#16337,.T.);
#23225=ORIENTED_EDGE('',*,*,#16342,.T.);
#23226=ORIENTED_EDGE('',*,*,#16343,.F.);
#23227=ORIENTED_EDGE('',*,*,#16344,.F.);
#23228=ORIENTED_EDGE('',*,*,#16340,.T.);
#23229=ORIENTED_EDGE('',*,*,#16345,.T.);
#23230=ORIENTED_EDGE('',*,*,#16346,.F.);
#23231=ORIENTED_EDGE('',*,*,#16347,.F.);
#23232=ORIENTED_EDGE('',*,*,#16343,.T.);
#23233=ORIENTED_EDGE('',*,*,#16348,.T.);
#23234=ORIENTED_EDGE('',*,*,#16349,.F.);
#23235=ORIENTED_EDGE('',*,*,#16350,.F.);
#23236=ORIENTED_EDGE('',*,*,#16346,.T.);
#23237=ORIENTED_EDGE('',*,*,#16351,.T.);
#23238=ORIENTED_EDGE('',*,*,#16352,.F.);
#23239=ORIENTED_EDGE('',*,*,#16353,.F.);
#23240=ORIENTED_EDGE('',*,*,#16349,.T.);
#23241=ORIENTED_EDGE('',*,*,#16354,.T.);
#23242=ORIENTED_EDGE('',*,*,#16355,.F.);
#23243=ORIENTED_EDGE('',*,*,#16356,.F.);
#23244=ORIENTED_EDGE('',*,*,#16352,.T.);
#23245=ORIENTED_EDGE('',*,*,#16357,.T.);
#23246=ORIENTED_EDGE('',*,*,#16358,.F.);
#23247=ORIENTED_EDGE('',*,*,#16359,.F.);
#23248=ORIENTED_EDGE('',*,*,#16355,.T.);
#23249=ORIENTED_EDGE('',*,*,#16360,.T.);
#23250=ORIENTED_EDGE('',*,*,#16361,.F.);
#23251=ORIENTED_EDGE('',*,*,#16362,.F.);
#23252=ORIENTED_EDGE('',*,*,#16358,.T.);
#23253=ORIENTED_EDGE('',*,*,#16363,.T.);
#23254=ORIENTED_EDGE('',*,*,#16364,.F.);
#23255=ORIENTED_EDGE('',*,*,#16365,.F.);
#23256=ORIENTED_EDGE('',*,*,#16361,.T.);
#23257=ORIENTED_EDGE('',*,*,#16366,.T.);
#23258=ORIENTED_EDGE('',*,*,#16367,.F.);
#23259=ORIENTED_EDGE('',*,*,#16368,.F.);
#23260=ORIENTED_EDGE('',*,*,#16364,.T.);
#23261=ORIENTED_EDGE('',*,*,#16369,.T.);
#23262=ORIENTED_EDGE('',*,*,#16370,.F.);
#23263=ORIENTED_EDGE('',*,*,#16371,.F.);
#23264=ORIENTED_EDGE('',*,*,#16367,.T.);
#23265=ORIENTED_EDGE('',*,*,#16372,.T.);
#23266=ORIENTED_EDGE('',*,*,#16373,.F.);
#23267=ORIENTED_EDGE('',*,*,#16374,.F.);
#23268=ORIENTED_EDGE('',*,*,#16370,.T.);
#23269=ORIENTED_EDGE('',*,*,#16375,.T.);
#23270=ORIENTED_EDGE('',*,*,#16376,.F.);
#23271=ORIENTED_EDGE('',*,*,#16377,.F.);
#23272=ORIENTED_EDGE('',*,*,#16373,.T.);
#23273=ORIENTED_EDGE('',*,*,#16378,.T.);
#23274=ORIENTED_EDGE('',*,*,#16379,.F.);
#23275=ORIENTED_EDGE('',*,*,#16380,.F.);
#23276=ORIENTED_EDGE('',*,*,#16376,.T.);
#23277=ORIENTED_EDGE('',*,*,#16381,.T.);
#23278=ORIENTED_EDGE('',*,*,#16382,.F.);
#23279=ORIENTED_EDGE('',*,*,#16383,.F.);
#23280=ORIENTED_EDGE('',*,*,#16379,.T.);
#23281=ORIENTED_EDGE('',*,*,#16384,.T.);
#23282=ORIENTED_EDGE('',*,*,#16385,.F.);
#23283=ORIENTED_EDGE('',*,*,#16386,.F.);
#23284=ORIENTED_EDGE('',*,*,#16382,.T.);
#23285=ORIENTED_EDGE('',*,*,#16387,.T.);
#23286=ORIENTED_EDGE('',*,*,#16388,.F.);
#23287=ORIENTED_EDGE('',*,*,#16389,.F.);
#23288=ORIENTED_EDGE('',*,*,#16385,.T.);
#23289=ORIENTED_EDGE('',*,*,#16390,.T.);
#23290=ORIENTED_EDGE('',*,*,#16391,.F.);
#23291=ORIENTED_EDGE('',*,*,#16392,.F.);
#23292=ORIENTED_EDGE('',*,*,#16388,.T.);
#23293=ORIENTED_EDGE('',*,*,#16393,.T.);
#23294=ORIENTED_EDGE('',*,*,#16394,.F.);
#23295=ORIENTED_EDGE('',*,*,#16395,.F.);
#23296=ORIENTED_EDGE('',*,*,#16391,.T.);
#23297=ORIENTED_EDGE('',*,*,#16396,.T.);
#23298=ORIENTED_EDGE('',*,*,#16397,.F.);
#23299=ORIENTED_EDGE('',*,*,#16398,.F.);
#23300=ORIENTED_EDGE('',*,*,#16394,.T.);
#23301=ORIENTED_EDGE('',*,*,#16399,.T.);
#23302=ORIENTED_EDGE('',*,*,#16400,.F.);
#23303=ORIENTED_EDGE('',*,*,#16401,.F.);
#23304=ORIENTED_EDGE('',*,*,#16397,.T.);
#23305=ORIENTED_EDGE('',*,*,#16402,.T.);
#23306=ORIENTED_EDGE('',*,*,#16403,.F.);
#23307=ORIENTED_EDGE('',*,*,#16404,.F.);
#23308=ORIENTED_EDGE('',*,*,#16400,.T.);
#23309=ORIENTED_EDGE('',*,*,#16405,.T.);
#23310=ORIENTED_EDGE('',*,*,#16406,.F.);
#23311=ORIENTED_EDGE('',*,*,#16407,.F.);
#23312=ORIENTED_EDGE('',*,*,#16403,.T.);
#23313=ORIENTED_EDGE('',*,*,#16408,.T.);
#23314=ORIENTED_EDGE('',*,*,#16409,.F.);
#23315=ORIENTED_EDGE('',*,*,#16410,.F.);
#23316=ORIENTED_EDGE('',*,*,#16406,.T.);
#23317=ORIENTED_EDGE('',*,*,#16411,.T.);
#23318=ORIENTED_EDGE('',*,*,#16412,.F.);
#23319=ORIENTED_EDGE('',*,*,#16413,.F.);
#23320=ORIENTED_EDGE('',*,*,#16409,.T.);
#23321=ORIENTED_EDGE('',*,*,#16414,.T.);
#23322=ORIENTED_EDGE('',*,*,#16415,.F.);
#23323=ORIENTED_EDGE('',*,*,#16416,.F.);
#23324=ORIENTED_EDGE('',*,*,#16412,.T.);
#23325=ORIENTED_EDGE('',*,*,#16417,.T.);
#23326=ORIENTED_EDGE('',*,*,#16418,.F.);
#23327=ORIENTED_EDGE('',*,*,#16419,.F.);
#23328=ORIENTED_EDGE('',*,*,#16415,.T.);
#23329=ORIENTED_EDGE('',*,*,#16420,.T.);
#23330=ORIENTED_EDGE('',*,*,#16418,.T.);
#23331=ORIENTED_EDGE('',*,*,#16421,.T.);
#23332=ORIENTED_EDGE('',*,*,#16422,.F.);
#23333=ORIENTED_EDGE('',*,*,#16328,.T.);
#23334=ORIENTED_EDGE('',*,*,#16423,.F.);
#23335=ORIENTED_EDGE('',*,*,#16424,.T.);
#23336=ORIENTED_EDGE('',*,*,#16425,.T.);
#23337=ORIENTED_EDGE('',*,*,#16426,.T.);
#23338=ORIENTED_EDGE('',*,*,#16325,.T.);
#23339=ORIENTED_EDGE('',*,*,#16427,.F.);
#23340=ORIENTED_EDGE('',*,*,#16425,.F.);
#23341=ORIENTED_EDGE('',*,*,#16428,.F.);
#23342=ORIENTED_EDGE('',*,*,#16429,.T.);
#23343=ORIENTED_EDGE('',*,*,#16430,.T.);
#23344=ORIENTED_EDGE('',*,*,#16431,.T.);
#23345=ORIENTED_EDGE('',*,*,#16432,.F.);
#23346=ORIENTED_EDGE('',*,*,#16433,.T.);
#23347=ORIENTED_EDGE('',*,*,#16434,.T.);
#23348=ORIENTED_EDGE('',*,*,#16435,.T.);
#23349=ORIENTED_EDGE('',*,*,#16436,.F.);
#23350=ORIENTED_EDGE('',*,*,#16437,.T.);
#23351=ORIENTED_EDGE('',*,*,#16438,.T.);
#23352=ORIENTED_EDGE('',*,*,#16439,.T.);
#23353=ORIENTED_EDGE('',*,*,#16440,.F.);
#23354=ORIENTED_EDGE('',*,*,#16441,.T.);
#23355=ORIENTED_EDGE('',*,*,#16442,.T.);
#23356=ORIENTED_EDGE('',*,*,#16443,.T.);
#23357=ORIENTED_EDGE('',*,*,#16444,.F.);
#23358=ORIENTED_EDGE('',*,*,#16445,.T.);
#23359=ORIENTED_EDGE('',*,*,#16446,.T.);
#23360=ORIENTED_EDGE('',*,*,#16447,.T.);
#23361=ORIENTED_EDGE('',*,*,#16448,.F.);
#23362=ORIENTED_EDGE('',*,*,#16449,.T.);
#23363=ORIENTED_EDGE('',*,*,#16450,.T.);
#23364=ORIENTED_EDGE('',*,*,#16451,.T.);
#23365=ORIENTED_EDGE('',*,*,#16452,.F.);
#23366=ORIENTED_EDGE('',*,*,#16453,.T.);
#23367=ORIENTED_EDGE('',*,*,#16454,.T.);
#23368=ORIENTED_EDGE('',*,*,#16455,.T.);
#23369=ORIENTED_EDGE('',*,*,#16456,.F.);
#23370=ORIENTED_EDGE('',*,*,#16457,.T.);
#23371=ORIENTED_EDGE('',*,*,#16458,.T.);
#23372=ORIENTED_EDGE('',*,*,#16459,.T.);
#23373=ORIENTED_EDGE('',*,*,#16460,.F.);
#23374=ORIENTED_EDGE('',*,*,#16461,.T.);
#23375=ORIENTED_EDGE('',*,*,#16462,.T.);
#23376=ORIENTED_EDGE('',*,*,#16463,.T.);
#23377=ORIENTED_EDGE('',*,*,#16464,.F.);
#23378=ORIENTED_EDGE('',*,*,#16465,.T.);
#23379=ORIENTED_EDGE('',*,*,#16466,.T.);
#23380=ORIENTED_EDGE('',*,*,#16467,.T.);
#23381=ORIENTED_EDGE('',*,*,#16468,.F.);
#23382=ORIENTED_EDGE('',*,*,#16469,.T.);
#23383=ORIENTED_EDGE('',*,*,#16470,.T.);
#23384=ORIENTED_EDGE('',*,*,#16471,.T.);
#23385=ORIENTED_EDGE('',*,*,#16472,.F.);
#23386=ORIENTED_EDGE('',*,*,#16473,.T.);
#23387=ORIENTED_EDGE('',*,*,#16474,.T.);
#23388=ORIENTED_EDGE('',*,*,#16475,.T.);
#23389=ORIENTED_EDGE('',*,*,#16476,.F.);
#23390=ORIENTED_EDGE('',*,*,#16477,.T.);
#23391=ORIENTED_EDGE('',*,*,#16478,.T.);
#23392=ORIENTED_EDGE('',*,*,#16479,.T.);
#23393=ORIENTED_EDGE('',*,*,#16480,.F.);
#23394=ORIENTED_EDGE('',*,*,#16481,.T.);
#23395=ORIENTED_EDGE('',*,*,#16482,.T.);
#23396=ORIENTED_EDGE('',*,*,#16483,.T.);
#23397=ORIENTED_EDGE('',*,*,#16484,.F.);
#23398=ORIENTED_EDGE('',*,*,#16485,.T.);
#23399=ORIENTED_EDGE('',*,*,#16486,.T.);
#23400=ORIENTED_EDGE('',*,*,#16487,.T.);
#23401=ORIENTED_EDGE('',*,*,#16488,.F.);
#23402=ORIENTED_EDGE('',*,*,#16489,.F.);
#23403=ORIENTED_EDGE('',*,*,#16490,.F.);
#23404=ORIENTED_EDGE('',*,*,#16491,.F.);
#23405=ORIENTED_EDGE('',*,*,#16492,.F.);
#23406=ORIENTED_EDGE('',*,*,#16493,.F.);
#23407=ORIENTED_EDGE('',*,*,#16494,.F.);
#23408=ORIENTED_EDGE('',*,*,#16495,.F.);
#23409=ORIENTED_EDGE('',*,*,#16496,.T.);
#23410=ORIENTED_EDGE('',*,*,#16497,.T.);
#23411=ORIENTED_EDGE('',*,*,#16496,.F.);
#23412=ORIENTED_EDGE('',*,*,#16498,.F.);
#23413=ORIENTED_EDGE('',*,*,#16499,.T.);
#23414=ORIENTED_EDGE('',*,*,#16500,.T.);
#23415=ORIENTED_EDGE('',*,*,#16499,.F.);
#23416=ORIENTED_EDGE('',*,*,#16501,.F.);
#23417=ORIENTED_EDGE('',*,*,#16502,.F.);
#23418=ORIENTED_EDGE('',*,*,#16503,.F.);
#23419=ORIENTED_EDGE('',*,*,#16504,.F.);
#23420=ORIENTED_EDGE('',*,*,#16505,.F.);
#23421=ORIENTED_EDGE('',*,*,#16506,.F.);
#23422=ORIENTED_EDGE('',*,*,#16507,.F.);
#23423=ORIENTED_EDGE('',*,*,#16508,.F.);
#23424=ORIENTED_EDGE('',*,*,#16509,.F.);
#23425=ORIENTED_EDGE('',*,*,#16510,.F.);
#23426=ORIENTED_EDGE('',*,*,#16511,.F.);
#23427=ORIENTED_EDGE('',*,*,#16512,.F.);
#23428=ORIENTED_EDGE('',*,*,#16513,.F.);
#23429=ORIENTED_EDGE('',*,*,#16514,.F.);
#23430=ORIENTED_EDGE('',*,*,#16515,.F.);
#23431=ORIENTED_EDGE('',*,*,#16516,.F.);
#23432=ORIENTED_EDGE('',*,*,#16517,.F.);
#23433=ORIENTED_EDGE('',*,*,#16518,.F.);
#23434=ORIENTED_EDGE('',*,*,#16519,.F.);
#23435=ORIENTED_EDGE('',*,*,#16520,.F.);
#23436=ORIENTED_EDGE('',*,*,#16521,.F.);
#23437=ORIENTED_EDGE('',*,*,#16522,.F.);
#23438=ORIENTED_EDGE('',*,*,#16523,.F.);
#23439=ORIENTED_EDGE('',*,*,#16524,.F.);
#23440=ORIENTED_EDGE('',*,*,#16525,.F.);
#23441=ORIENTED_EDGE('',*,*,#16526,.F.);
#23442=ORIENTED_EDGE('',*,*,#16527,.F.);
#23443=ORIENTED_EDGE('',*,*,#16528,.F.);
#23444=ORIENTED_EDGE('',*,*,#16529,.F.);
#23445=ORIENTED_EDGE('',*,*,#16530,.F.);
#23446=ORIENTED_EDGE('',*,*,#16531,.F.);
#23447=ORIENTED_EDGE('',*,*,#16532,.F.);
#23448=ORIENTED_EDGE('',*,*,#16533,.F.);
#23449=ORIENTED_EDGE('',*,*,#16534,.F.);
#23450=ORIENTED_EDGE('',*,*,#16535,.F.);
#23451=ORIENTED_EDGE('',*,*,#16536,.F.);
#23452=ORIENTED_EDGE('',*,*,#16537,.F.);
#23453=ORIENTED_EDGE('',*,*,#16538,.F.);
#23454=ORIENTED_EDGE('',*,*,#16539,.F.);
#23455=ORIENTED_EDGE('',*,*,#16540,.F.);
#23456=ORIENTED_EDGE('',*,*,#16541,.F.);
#23457=ORIENTED_EDGE('',*,*,#16542,.F.);
#23458=ORIENTED_EDGE('',*,*,#16543,.F.);
#23459=ORIENTED_EDGE('',*,*,#16544,.F.);
#23460=ORIENTED_EDGE('',*,*,#16545,.F.);
#23461=ORIENTED_EDGE('',*,*,#16546,.F.);
#23462=ORIENTED_EDGE('',*,*,#16547,.F.);
#23463=ORIENTED_EDGE('',*,*,#16548,.F.);
#23464=ORIENTED_EDGE('',*,*,#16549,.F.);
#23465=ORIENTED_EDGE('',*,*,#16550,.F.);
#23466=ORIENTED_EDGE('',*,*,#16551,.F.);
#23467=ORIENTED_EDGE('',*,*,#16552,.F.);
#23468=ORIENTED_EDGE('',*,*,#16553,.F.);
#23469=ORIENTED_EDGE('',*,*,#16554,.F.);
#23470=ORIENTED_EDGE('',*,*,#16555,.F.);
#23471=ORIENTED_EDGE('',*,*,#16556,.F.);
#23472=ORIENTED_EDGE('',*,*,#16557,.F.);
#23473=ORIENTED_EDGE('',*,*,#16558,.F.);
#23474=ORIENTED_EDGE('',*,*,#16559,.F.);
#23475=ORIENTED_EDGE('',*,*,#16560,.F.);
#23476=ORIENTED_EDGE('',*,*,#16561,.F.);
#23477=ORIENTED_EDGE('',*,*,#16562,.F.);
#23478=ORIENTED_EDGE('',*,*,#16563,.F.);
#23479=ORIENTED_EDGE('',*,*,#16564,.F.);
#23480=ORIENTED_EDGE('',*,*,#16565,.F.);
#23481=ORIENTED_EDGE('',*,*,#16566,.F.);
#23482=ORIENTED_EDGE('',*,*,#16567,.F.);
#23483=ORIENTED_EDGE('',*,*,#16568,.F.);
#23484=ORIENTED_EDGE('',*,*,#16569,.F.);
#23485=ORIENTED_EDGE('',*,*,#16570,.F.);
#23486=ORIENTED_EDGE('',*,*,#16571,.F.);
#23487=ORIENTED_EDGE('',*,*,#16572,.F.);
#23488=ORIENTED_EDGE('',*,*,#16573,.F.);
#23489=ORIENTED_EDGE('',*,*,#16574,.F.);
#23490=ORIENTED_EDGE('',*,*,#16575,.F.);
#23491=ORIENTED_EDGE('',*,*,#16576,.F.);
#23492=ORIENTED_EDGE('',*,*,#16577,.F.);
#23493=ORIENTED_EDGE('',*,*,#16578,.F.);
#23494=ORIENTED_EDGE('',*,*,#16579,.F.);
#23495=ORIENTED_EDGE('',*,*,#16580,.F.);
#23496=ORIENTED_EDGE('',*,*,#16581,.F.);
#23497=ORIENTED_EDGE('',*,*,#16582,.F.);
#23498=ORIENTED_EDGE('',*,*,#16583,.F.);
#23499=ORIENTED_EDGE('',*,*,#16584,.F.);
#23500=ORIENTED_EDGE('',*,*,#16585,.F.);
#23501=ORIENTED_EDGE('',*,*,#16586,.F.);
#23502=ORIENTED_EDGE('',*,*,#16587,.F.);
#23503=ORIENTED_EDGE('',*,*,#16588,.F.);
#23504=ORIENTED_EDGE('',*,*,#16589,.F.);
#23505=ORIENTED_EDGE('',*,*,#16590,.F.);
#23506=ORIENTED_EDGE('',*,*,#16591,.F.);
#23507=ORIENTED_EDGE('',*,*,#16592,.F.);
#23508=ORIENTED_EDGE('',*,*,#16593,.F.);
#23509=ORIENTED_EDGE('',*,*,#16594,.F.);
#23510=ORIENTED_EDGE('',*,*,#16595,.F.);
#23511=ORIENTED_EDGE('',*,*,#16596,.F.);
#23512=ORIENTED_EDGE('',*,*,#16597,.F.);
#23513=ORIENTED_EDGE('',*,*,#16598,.F.);
#23514=ORIENTED_EDGE('',*,*,#16599,.F.);
#23515=ORIENTED_EDGE('',*,*,#16600,.F.);
#23516=ORIENTED_EDGE('',*,*,#16601,.F.);
#23517=ORIENTED_EDGE('',*,*,#16602,.F.);
#23518=ORIENTED_EDGE('',*,*,#16603,.F.);
#23519=ORIENTED_EDGE('',*,*,#16604,.F.);
#23520=ORIENTED_EDGE('',*,*,#16605,.F.);
#23521=ORIENTED_EDGE('',*,*,#16606,.F.);
#23522=ORIENTED_EDGE('',*,*,#16607,.F.);
#23523=ORIENTED_EDGE('',*,*,#16608,.F.);
#23524=ORIENTED_EDGE('',*,*,#16609,.F.);
#23525=ORIENTED_EDGE('',*,*,#16610,.F.);
#23526=ORIENTED_EDGE('',*,*,#16611,.F.);
#23527=ORIENTED_EDGE('',*,*,#16612,.F.);
#23528=ORIENTED_EDGE('',*,*,#16613,.F.);
#23529=ORIENTED_EDGE('',*,*,#16614,.F.);
#23530=ORIENTED_EDGE('',*,*,#16615,.F.);
#23531=ORIENTED_EDGE('',*,*,#16616,.F.);
#23532=ORIENTED_EDGE('',*,*,#16617,.F.);
#23533=ORIENTED_EDGE('',*,*,#16618,.F.);
#23534=ORIENTED_EDGE('',*,*,#16619,.F.);
#23535=ORIENTED_EDGE('',*,*,#16620,.F.);
#23536=ORIENTED_EDGE('',*,*,#16621,.F.);
#23537=ORIENTED_EDGE('',*,*,#16622,.F.);
#23538=ORIENTED_EDGE('',*,*,#16623,.F.);
#23539=ORIENTED_EDGE('',*,*,#16624,.F.);
#23540=ORIENTED_EDGE('',*,*,#16625,.F.);
#23541=ORIENTED_EDGE('',*,*,#16626,.F.);
#23542=ORIENTED_EDGE('',*,*,#16627,.F.);
#23543=ORIENTED_EDGE('',*,*,#16628,.F.);
#23544=ORIENTED_EDGE('',*,*,#16629,.F.);
#23545=ORIENTED_EDGE('',*,*,#16630,.F.);
#23546=ORIENTED_EDGE('',*,*,#16631,.F.);
#23547=ORIENTED_EDGE('',*,*,#16632,.F.);
#23548=ORIENTED_EDGE('',*,*,#16633,.F.);
#23549=ORIENTED_EDGE('',*,*,#16634,.F.);
#23550=ORIENTED_EDGE('',*,*,#16635,.F.);
#23551=ORIENTED_EDGE('',*,*,#16636,.F.);
#23552=ORIENTED_EDGE('',*,*,#16637,.F.);
#23553=ORIENTED_EDGE('',*,*,#16638,.F.);
#23554=ORIENTED_EDGE('',*,*,#16639,.F.);
#23555=ORIENTED_EDGE('',*,*,#16640,.F.);
#23556=ORIENTED_EDGE('',*,*,#16641,.F.);
#23557=ORIENTED_EDGE('',*,*,#16642,.F.);
#23558=ORIENTED_EDGE('',*,*,#16643,.F.);
#23559=ORIENTED_EDGE('',*,*,#16644,.F.);
#23560=ORIENTED_EDGE('',*,*,#16645,.F.);
#23561=ORIENTED_EDGE('',*,*,#16646,.F.);
#23562=ORIENTED_EDGE('',*,*,#16647,.F.);
#23563=ORIENTED_EDGE('',*,*,#16648,.F.);
#23564=ORIENTED_EDGE('',*,*,#16649,.F.);
#23565=ORIENTED_EDGE('',*,*,#16650,.F.);
#23566=ORIENTED_EDGE('',*,*,#16651,.F.);
#23567=ORIENTED_EDGE('',*,*,#16652,.F.);
#23568=ORIENTED_EDGE('',*,*,#16653,.F.);
#23569=ORIENTED_EDGE('',*,*,#16654,.F.);
#23570=ORIENTED_EDGE('',*,*,#16655,.F.);
#23571=ORIENTED_EDGE('',*,*,#16656,.F.);
#23572=ORIENTED_EDGE('',*,*,#16657,.F.);
#23573=ORIENTED_EDGE('',*,*,#16658,.F.);
#23574=ORIENTED_EDGE('',*,*,#16659,.F.);
#23575=ORIENTED_EDGE('',*,*,#16660,.F.);
#23576=ORIENTED_EDGE('',*,*,#16661,.F.);
#23577=ORIENTED_EDGE('',*,*,#16662,.F.);
#23578=ORIENTED_EDGE('',*,*,#16663,.F.);
#23579=ORIENTED_EDGE('',*,*,#16664,.F.);
#23580=ORIENTED_EDGE('',*,*,#16665,.F.);
#23581=ORIENTED_EDGE('',*,*,#16666,.F.);
#23582=ORIENTED_EDGE('',*,*,#16667,.F.);
#23583=ORIENTED_EDGE('',*,*,#16668,.F.);
#23584=ORIENTED_EDGE('',*,*,#16669,.F.);
#23585=ORIENTED_EDGE('',*,*,#16670,.F.);
#23586=ORIENTED_EDGE('',*,*,#16671,.F.);
#23587=ORIENTED_EDGE('',*,*,#16672,.F.);
#23588=ORIENTED_EDGE('',*,*,#16673,.F.);
#23589=ORIENTED_EDGE('',*,*,#16674,.F.);
#23590=ORIENTED_EDGE('',*,*,#16675,.F.);
#23591=ORIENTED_EDGE('',*,*,#16676,.F.);
#23592=ORIENTED_EDGE('',*,*,#16677,.F.);
#23593=ORIENTED_EDGE('',*,*,#16678,.F.);
#23594=ORIENTED_EDGE('',*,*,#16679,.F.);
#23595=ORIENTED_EDGE('',*,*,#16680,.F.);
#23596=ORIENTED_EDGE('',*,*,#16681,.F.);
#23597=ORIENTED_EDGE('',*,*,#16682,.F.);
#23598=ORIENTED_EDGE('',*,*,#16683,.F.);
#23599=ORIENTED_EDGE('',*,*,#16684,.F.);
#23600=ORIENTED_EDGE('',*,*,#16487,.F.);
#23601=ORIENTED_EDGE('',*,*,#16685,.F.);
#23602=ORIENTED_EDGE('',*,*,#16686,.F.);
#23603=ORIENTED_EDGE('',*,*,#16687,.F.);
#23604=ORIENTED_EDGE('',*,*,#16483,.F.);
#23605=ORIENTED_EDGE('',*,*,#16688,.F.);
#23606=ORIENTED_EDGE('',*,*,#16689,.F.);
#23607=ORIENTED_EDGE('',*,*,#16690,.F.);
#23608=ORIENTED_EDGE('',*,*,#16479,.F.);
#23609=ORIENTED_EDGE('',*,*,#16691,.F.);
#23610=ORIENTED_EDGE('',*,*,#16692,.F.);
#23611=ORIENTED_EDGE('',*,*,#16693,.F.);
#23612=ORIENTED_EDGE('',*,*,#16475,.F.);
#23613=ORIENTED_EDGE('',*,*,#16694,.F.);
#23614=ORIENTED_EDGE('',*,*,#16695,.F.);
#23615=ORIENTED_EDGE('',*,*,#16696,.F.);
#23616=ORIENTED_EDGE('',*,*,#16471,.F.);
#23617=ORIENTED_EDGE('',*,*,#16697,.F.);
#23618=ORIENTED_EDGE('',*,*,#16698,.F.);
#23619=ORIENTED_EDGE('',*,*,#16699,.F.);
#23620=ORIENTED_EDGE('',*,*,#16467,.F.);
#23621=ORIENTED_EDGE('',*,*,#16700,.F.);
#23622=ORIENTED_EDGE('',*,*,#16701,.F.);
#23623=ORIENTED_EDGE('',*,*,#16702,.F.);
#23624=ORIENTED_EDGE('',*,*,#16463,.F.);
#23625=ORIENTED_EDGE('',*,*,#16703,.F.);
#23626=ORIENTED_EDGE('',*,*,#16704,.F.);
#23627=ORIENTED_EDGE('',*,*,#16705,.F.);
#23628=ORIENTED_EDGE('',*,*,#16459,.F.);
#23629=ORIENTED_EDGE('',*,*,#16706,.F.);
#23630=ORIENTED_EDGE('',*,*,#16707,.F.);
#23631=ORIENTED_EDGE('',*,*,#16708,.F.);
#23632=ORIENTED_EDGE('',*,*,#16455,.F.);
#23633=ORIENTED_EDGE('',*,*,#16709,.F.);
#23634=ORIENTED_EDGE('',*,*,#16710,.F.);
#23635=ORIENTED_EDGE('',*,*,#16711,.F.);
#23636=ORIENTED_EDGE('',*,*,#16431,.F.);
#23637=ORIENTED_EDGE('',*,*,#16712,.F.);
#23638=ORIENTED_EDGE('',*,*,#16713,.F.);
#23639=ORIENTED_EDGE('',*,*,#16714,.F.);
#23640=ORIENTED_EDGE('',*,*,#16435,.F.);
#23641=ORIENTED_EDGE('',*,*,#16715,.F.);
#23642=ORIENTED_EDGE('',*,*,#16716,.F.);
#23643=ORIENTED_EDGE('',*,*,#16717,.F.);
#23644=ORIENTED_EDGE('',*,*,#16439,.F.);
#23645=ORIENTED_EDGE('',*,*,#16718,.F.);
#23646=ORIENTED_EDGE('',*,*,#16719,.F.);
#23647=ORIENTED_EDGE('',*,*,#16720,.F.);
#23648=ORIENTED_EDGE('',*,*,#16443,.F.);
#23649=ORIENTED_EDGE('',*,*,#16721,.F.);
#23650=ORIENTED_EDGE('',*,*,#16722,.F.);
#23651=ORIENTED_EDGE('',*,*,#16723,.F.);
#23652=ORIENTED_EDGE('',*,*,#16447,.F.);
#23653=ORIENTED_EDGE('',*,*,#16724,.F.);
#23654=ORIENTED_EDGE('',*,*,#16725,.F.);
#23655=ORIENTED_EDGE('',*,*,#16726,.F.);
#23656=ORIENTED_EDGE('',*,*,#16451,.F.);
#23657=ORIENTED_EDGE('',*,*,#16727,.F.);
#23658=ORIENTED_EDGE('',*,*,#16728,.F.);
#23659=ORIENTED_EDGE('',*,*,#16729,.F.);
#23660=ORIENTED_EDGE('',*,*,#16730,.F.);
#23661=ORIENTED_EDGE('',*,*,#16731,.F.);
#23662=ORIENTED_EDGE('',*,*,#16732,.F.);
#23663=ORIENTED_EDGE('',*,*,#16733,.F.);
#23664=ORIENTED_EDGE('',*,*,#16734,.F.);
#23665=ORIENTED_EDGE('',*,*,#16735,.F.);
#23666=ORIENTED_EDGE('',*,*,#16736,.F.);
#23667=ORIENTED_EDGE('',*,*,#16737,.F.);
#23668=ORIENTED_EDGE('',*,*,#16738,.F.);
#23669=ORIENTED_EDGE('',*,*,#16739,.F.);
#23670=ORIENTED_EDGE('',*,*,#16740,.F.);
#23671=ORIENTED_EDGE('',*,*,#16741,.F.);
#23672=ORIENTED_EDGE('',*,*,#16742,.F.);
#23673=ORIENTED_EDGE('',*,*,#16743,.F.);
#23674=ORIENTED_EDGE('',*,*,#16744,.F.);
#23675=ORIENTED_EDGE('',*,*,#16745,.F.);
#23676=ORIENTED_EDGE('',*,*,#16746,.F.);
#23677=ORIENTED_EDGE('',*,*,#16747,.F.);
#23678=ORIENTED_EDGE('',*,*,#16748,.F.);
#23679=ORIENTED_EDGE('',*,*,#16749,.F.);
#23680=ORIENTED_EDGE('',*,*,#16750,.F.);
#23681=ORIENTED_EDGE('',*,*,#16751,.F.);
#23682=ORIENTED_EDGE('',*,*,#16752,.F.);
#23683=ORIENTED_EDGE('',*,*,#16753,.F.);
#23684=ORIENTED_EDGE('',*,*,#16754,.F.);
#23685=ORIENTED_EDGE('',*,*,#16755,.F.);
#23686=ORIENTED_EDGE('',*,*,#16756,.F.);
#23687=ORIENTED_EDGE('',*,*,#16757,.F.);
#23688=ORIENTED_EDGE('',*,*,#16758,.F.);
#23689=ORIENTED_EDGE('',*,*,#16759,.F.);
#23690=ORIENTED_EDGE('',*,*,#16760,.F.);
#23691=ORIENTED_EDGE('',*,*,#16761,.F.);
#23692=ORIENTED_EDGE('',*,*,#16762,.F.);
#23693=ORIENTED_EDGE('',*,*,#16763,.F.);
#23694=ORIENTED_EDGE('',*,*,#16764,.F.);
#23695=ORIENTED_EDGE('',*,*,#16765,.F.);
#23696=ORIENTED_EDGE('',*,*,#16766,.F.);
#23697=ORIENTED_EDGE('',*,*,#16767,.F.);
#23698=ORIENTED_EDGE('',*,*,#16768,.F.);
#23699=ORIENTED_EDGE('',*,*,#16769,.F.);
#23700=ORIENTED_EDGE('',*,*,#16770,.F.);
#23701=ORIENTED_EDGE('',*,*,#16771,.F.);
#23702=ORIENTED_EDGE('',*,*,#16772,.F.);
#23703=ORIENTED_EDGE('',*,*,#16773,.F.);
#23704=ORIENTED_EDGE('',*,*,#16774,.F.);
#23705=ORIENTED_EDGE('',*,*,#16775,.F.);
#23706=ORIENTED_EDGE('',*,*,#16776,.F.);
#23707=ORIENTED_EDGE('',*,*,#16777,.F.);
#23708=ORIENTED_EDGE('',*,*,#16778,.F.);
#23709=ORIENTED_EDGE('',*,*,#16779,.F.);
#23710=ORIENTED_EDGE('',*,*,#16780,.F.);
#23711=ORIENTED_EDGE('',*,*,#16781,.F.);
#23712=ORIENTED_EDGE('',*,*,#16782,.F.);
#23713=ORIENTED_EDGE('',*,*,#16783,.F.);
#23714=ORIENTED_EDGE('',*,*,#16784,.F.);
#23715=ORIENTED_EDGE('',*,*,#16785,.F.);
#23716=ORIENTED_EDGE('',*,*,#16786,.F.);
#23717=ORIENTED_EDGE('',*,*,#16787,.F.);
#23718=ORIENTED_EDGE('',*,*,#16788,.F.);
#23719=ORIENTED_EDGE('',*,*,#16789,.F.);
#23720=ORIENTED_EDGE('',*,*,#16790,.F.);
#23721=ORIENTED_EDGE('',*,*,#16791,.F.);
#23722=ORIENTED_EDGE('',*,*,#16792,.F.);
#23723=ORIENTED_EDGE('',*,*,#16793,.F.);
#23724=ORIENTED_EDGE('',*,*,#16794,.F.);
#23725=ORIENTED_EDGE('',*,*,#16795,.F.);
#23726=ORIENTED_EDGE('',*,*,#16796,.F.);
#23727=ORIENTED_EDGE('',*,*,#16797,.F.);
#23728=ORIENTED_EDGE('',*,*,#16798,.F.);
#23729=ORIENTED_EDGE('',*,*,#16799,.F.);
#23730=ORIENTED_EDGE('',*,*,#16800,.F.);
#23731=ORIENTED_EDGE('',*,*,#16801,.F.);
#23732=ORIENTED_EDGE('',*,*,#16802,.F.);
#23733=ORIENTED_EDGE('',*,*,#16803,.F.);
#23734=ORIENTED_EDGE('',*,*,#16804,.F.);
#23735=ORIENTED_EDGE('',*,*,#16805,.F.);
#23736=ORIENTED_EDGE('',*,*,#16806,.F.);
#23737=ORIENTED_EDGE('',*,*,#16807,.T.);
#23738=ORIENTED_EDGE('',*,*,#16498,.T.);
#23739=ORIENTED_EDGE('',*,*,#16807,.F.);
#23740=ORIENTED_EDGE('',*,*,#16808,.F.);
#23741=ORIENTED_EDGE('',*,*,#16809,.F.);
#23742=ORIENTED_EDGE('',*,*,#16810,.T.);
#23743=ORIENTED_EDGE('',*,*,#16811,.F.);
#23744=ORIENTED_EDGE('',*,*,#16812,.F.);
#23745=ORIENTED_EDGE('',*,*,#16813,.F.);
#23746=ORIENTED_EDGE('',*,*,#16814,.T.);
#23747=ORIENTED_EDGE('',*,*,#16815,.F.);
#23748=ORIENTED_EDGE('',*,*,#16816,.F.);
#23749=ORIENTED_EDGE('',*,*,#16817,.F.);
#23750=ORIENTED_EDGE('',*,*,#16818,.T.);
#23751=ORIENTED_EDGE('',*,*,#16819,.F.);
#23752=ORIENTED_EDGE('',*,*,#16820,.F.);
#23753=ORIENTED_EDGE('',*,*,#16821,.F.);
#23754=ORIENTED_EDGE('',*,*,#16822,.T.);
#23755=ORIENTED_EDGE('',*,*,#16823,.F.);
#23756=ORIENTED_EDGE('',*,*,#16824,.F.);
#23757=ORIENTED_EDGE('',*,*,#16825,.F.);
#23758=ORIENTED_EDGE('',*,*,#16826,.T.);
#23759=ORIENTED_EDGE('',*,*,#16827,.F.);
#23760=ORIENTED_EDGE('',*,*,#16828,.F.);
#23761=ORIENTED_EDGE('',*,*,#16829,.F.);
#23762=ORIENTED_EDGE('',*,*,#16830,.T.);
#23763=ORIENTED_EDGE('',*,*,#16831,.F.);
#23764=ORIENTED_EDGE('',*,*,#16832,.F.);
#23765=ORIENTED_EDGE('',*,*,#16833,.F.);
#23766=ORIENTED_EDGE('',*,*,#16834,.T.);
#23767=ORIENTED_EDGE('',*,*,#16835,.F.);
#23768=ORIENTED_EDGE('',*,*,#16836,.F.);
#23769=ORIENTED_EDGE('',*,*,#16837,.F.);
#23770=ORIENTED_EDGE('',*,*,#16838,.T.);
#23771=ORIENTED_EDGE('',*,*,#16839,.F.);
#23772=ORIENTED_EDGE('',*,*,#16840,.F.);
#23773=ORIENTED_EDGE('',*,*,#16841,.F.);
#23774=ORIENTED_EDGE('',*,*,#16842,.T.);
#23775=ORIENTED_EDGE('',*,*,#16843,.F.);
#23776=ORIENTED_EDGE('',*,*,#16844,.F.);
#23777=ORIENTED_EDGE('',*,*,#16845,.F.);
#23778=ORIENTED_EDGE('',*,*,#16846,.T.);
#23779=ORIENTED_EDGE('',*,*,#16847,.F.);
#23780=ORIENTED_EDGE('',*,*,#16848,.F.);
#23781=ORIENTED_EDGE('',*,*,#16849,.F.);
#23782=ORIENTED_EDGE('',*,*,#16850,.T.);
#23783=ORIENTED_EDGE('',*,*,#16851,.F.);
#23784=ORIENTED_EDGE('',*,*,#16852,.F.);
#23785=ORIENTED_EDGE('',*,*,#16853,.F.);
#23786=ORIENTED_EDGE('',*,*,#16854,.T.);
#23787=ORIENTED_EDGE('',*,*,#16855,.F.);
#23788=ORIENTED_EDGE('',*,*,#16856,.F.);
#23789=ORIENTED_EDGE('',*,*,#16857,.F.);
#23790=ORIENTED_EDGE('',*,*,#16858,.T.);
#23791=ORIENTED_EDGE('',*,*,#16859,.F.);
#23792=ORIENTED_EDGE('',*,*,#16860,.F.);
#23793=ORIENTED_EDGE('',*,*,#16861,.F.);
#23794=ORIENTED_EDGE('',*,*,#16862,.T.);
#23795=ORIENTED_EDGE('',*,*,#16863,.F.);
#23796=ORIENTED_EDGE('',*,*,#16864,.F.);
#23797=ORIENTED_EDGE('',*,*,#16865,.F.);
#23798=ORIENTED_EDGE('',*,*,#16866,.T.);
#23799=ORIENTED_EDGE('',*,*,#16867,.F.);
#23800=ORIENTED_EDGE('',*,*,#16868,.F.);
#23801=ORIENTED_EDGE('',*,*,#16869,.F.);
#23802=ORIENTED_EDGE('',*,*,#16870,.T.);
#23803=ORIENTED_EDGE('',*,*,#16871,.F.);
#23804=ORIENTED_EDGE('',*,*,#16872,.F.);
#23805=ORIENTED_EDGE('',*,*,#16873,.F.);
#23806=ORIENTED_EDGE('',*,*,#16874,.T.);
#23807=ORIENTED_EDGE('',*,*,#16875,.F.);
#23808=ORIENTED_EDGE('',*,*,#16876,.F.);
#23809=ORIENTED_EDGE('',*,*,#16877,.F.);
#23810=ORIENTED_EDGE('',*,*,#16878,.T.);
#23811=ORIENTED_EDGE('',*,*,#16879,.F.);
#23812=ORIENTED_EDGE('',*,*,#16880,.F.);
#23813=ORIENTED_EDGE('',*,*,#16881,.F.);
#23814=ORIENTED_EDGE('',*,*,#16882,.T.);
#23815=ORIENTED_EDGE('',*,*,#16883,.F.);
#23816=ORIENTED_EDGE('',*,*,#16884,.F.);
#23817=ORIENTED_EDGE('',*,*,#16885,.F.);
#23818=ORIENTED_EDGE('',*,*,#16886,.T.);
#23819=ORIENTED_EDGE('',*,*,#16887,.F.);
#23820=ORIENTED_EDGE('',*,*,#16888,.F.);
#23821=ORIENTED_EDGE('',*,*,#16889,.F.);
#23822=ORIENTED_EDGE('',*,*,#16890,.T.);
#23823=ORIENTED_EDGE('',*,*,#16891,.F.);
#23824=ORIENTED_EDGE('',*,*,#16892,.F.);
#23825=ORIENTED_EDGE('',*,*,#16893,.F.);
#23826=ORIENTED_EDGE('',*,*,#16894,.T.);
#23827=ORIENTED_EDGE('',*,*,#16895,.F.);
#23828=ORIENTED_EDGE('',*,*,#16896,.F.);
#23829=ORIENTED_EDGE('',*,*,#16897,.F.);
#23830=ORIENTED_EDGE('',*,*,#16898,.T.);
#23831=ORIENTED_EDGE('',*,*,#16899,.F.);
#23832=ORIENTED_EDGE('',*,*,#16900,.F.);
#23833=ORIENTED_EDGE('',*,*,#16901,.F.);
#23834=ORIENTED_EDGE('',*,*,#16902,.T.);
#23835=ORIENTED_EDGE('',*,*,#16903,.F.);
#23836=ORIENTED_EDGE('',*,*,#16904,.F.);
#23837=ORIENTED_EDGE('',*,*,#16905,.F.);
#23838=ORIENTED_EDGE('',*,*,#16906,.T.);
#23839=ORIENTED_EDGE('',*,*,#16907,.F.);
#23840=ORIENTED_EDGE('',*,*,#16908,.F.);
#23841=ORIENTED_EDGE('',*,*,#16909,.F.);
#23842=ORIENTED_EDGE('',*,*,#16910,.T.);
#23843=ORIENTED_EDGE('',*,*,#16911,.F.);
#23844=ORIENTED_EDGE('',*,*,#16912,.F.);
#23845=ORIENTED_EDGE('',*,*,#16913,.F.);
#23846=ORIENTED_EDGE('',*,*,#16914,.T.);
#23847=ORIENTED_EDGE('',*,*,#16915,.F.);
#23848=ORIENTED_EDGE('',*,*,#16916,.F.);
#23849=ORIENTED_EDGE('',*,*,#16917,.F.);
#23850=ORIENTED_EDGE('',*,*,#16918,.T.);
#23851=ORIENTED_EDGE('',*,*,#16919,.F.);
#23852=ORIENTED_EDGE('',*,*,#16920,.F.);
#23853=ORIENTED_EDGE('',*,*,#16921,.F.);
#23854=ORIENTED_EDGE('',*,*,#16922,.T.);
#23855=ORIENTED_EDGE('',*,*,#16923,.F.);
#23856=ORIENTED_EDGE('',*,*,#16924,.F.);
#23857=ORIENTED_EDGE('',*,*,#16925,.F.);
#23858=ORIENTED_EDGE('',*,*,#16926,.T.);
#23859=ORIENTED_EDGE('',*,*,#16927,.F.);
#23860=ORIENTED_EDGE('',*,*,#16928,.F.);
#23861=ORIENTED_EDGE('',*,*,#16929,.F.);
#23862=ORIENTED_EDGE('',*,*,#16930,.T.);
#23863=ORIENTED_EDGE('',*,*,#16931,.F.);
#23864=ORIENTED_EDGE('',*,*,#16932,.F.);
#23865=ORIENTED_EDGE('',*,*,#16933,.F.);
#23866=ORIENTED_EDGE('',*,*,#16934,.T.);
#23867=ORIENTED_EDGE('',*,*,#16935,.F.);
#23868=ORIENTED_EDGE('',*,*,#16936,.F.);
#23869=ORIENTED_EDGE('',*,*,#16937,.F.);
#23870=ORIENTED_EDGE('',*,*,#16938,.T.);
#23871=ORIENTED_EDGE('',*,*,#16939,.F.);
#23872=ORIENTED_EDGE('',*,*,#16940,.F.);
#23873=ORIENTED_EDGE('',*,*,#16941,.F.);
#23874=ORIENTED_EDGE('',*,*,#16942,.T.);
#23875=ORIENTED_EDGE('',*,*,#16943,.F.);
#23876=ORIENTED_EDGE('',*,*,#16944,.F.);
#23877=ORIENTED_EDGE('',*,*,#16945,.F.);
#23878=ORIENTED_EDGE('',*,*,#16946,.T.);
#23879=ORIENTED_EDGE('',*,*,#16947,.F.);
#23880=ORIENTED_EDGE('',*,*,#16948,.F.);
#23881=ORIENTED_EDGE('',*,*,#16949,.F.);
#23882=ORIENTED_EDGE('',*,*,#16950,.T.);
#23883=ORIENTED_EDGE('',*,*,#16951,.F.);
#23884=ORIENTED_EDGE('',*,*,#16952,.F.);
#23885=ORIENTED_EDGE('',*,*,#16953,.F.);
#23886=ORIENTED_EDGE('',*,*,#16954,.T.);
#23887=ORIENTED_EDGE('',*,*,#16955,.F.);
#23888=ORIENTED_EDGE('',*,*,#16956,.F.);
#23889=ORIENTED_EDGE('',*,*,#16957,.F.);
#23890=ORIENTED_EDGE('',*,*,#16958,.T.);
#23891=ORIENTED_EDGE('',*,*,#16959,.F.);
#23892=ORIENTED_EDGE('',*,*,#16960,.F.);
#23893=ORIENTED_EDGE('',*,*,#16961,.F.);
#23894=ORIENTED_EDGE('',*,*,#16962,.T.);
#23895=ORIENTED_EDGE('',*,*,#16963,.F.);
#23896=ORIENTED_EDGE('',*,*,#16964,.F.);
#23897=ORIENTED_EDGE('',*,*,#16965,.F.);
#23898=ORIENTED_EDGE('',*,*,#16966,.T.);
#23899=ORIENTED_EDGE('',*,*,#16967,.F.);
#23900=ORIENTED_EDGE('',*,*,#16968,.F.);
#23901=ORIENTED_EDGE('',*,*,#16969,.F.);
#23902=ORIENTED_EDGE('',*,*,#16970,.T.);
#23903=ORIENTED_EDGE('',*,*,#16971,.F.);
#23904=ORIENTED_EDGE('',*,*,#16972,.F.);
#23905=ORIENTED_EDGE('',*,*,#16973,.F.);
#23906=ORIENTED_EDGE('',*,*,#16974,.T.);
#23907=ORIENTED_EDGE('',*,*,#16975,.F.);
#23908=ORIENTED_EDGE('',*,*,#16976,.F.);
#23909=ORIENTED_EDGE('',*,*,#16977,.F.);
#23910=ORIENTED_EDGE('',*,*,#16978,.T.);
#23911=ORIENTED_EDGE('',*,*,#16979,.F.);
#23912=ORIENTED_EDGE('',*,*,#16980,.F.);
#23913=ORIENTED_EDGE('',*,*,#16981,.F.);
#23914=ORIENTED_EDGE('',*,*,#16982,.T.);
#23915=ORIENTED_EDGE('',*,*,#16983,.F.);
#23916=ORIENTED_EDGE('',*,*,#16984,.F.);
#23917=ORIENTED_EDGE('',*,*,#16985,.F.);
#23918=ORIENTED_EDGE('',*,*,#16986,.T.);
#23919=ORIENTED_EDGE('',*,*,#16987,.F.);
#23920=ORIENTED_EDGE('',*,*,#16988,.F.);
#23921=ORIENTED_EDGE('',*,*,#16989,.F.);
#23922=ORIENTED_EDGE('',*,*,#16990,.T.);
#23923=ORIENTED_EDGE('',*,*,#16991,.F.);
#23924=ORIENTED_EDGE('',*,*,#16992,.F.);
#23925=ORIENTED_EDGE('',*,*,#16993,.F.);
#23926=ORIENTED_EDGE('',*,*,#16994,.T.);
#23927=ORIENTED_EDGE('',*,*,#16995,.F.);
#23928=ORIENTED_EDGE('',*,*,#16996,.F.);
#23929=ORIENTED_EDGE('',*,*,#16997,.F.);
#23930=ORIENTED_EDGE('',*,*,#16998,.T.);
#23931=ORIENTED_EDGE('',*,*,#16999,.F.);
#23932=ORIENTED_EDGE('',*,*,#17000,.F.);
#23933=ORIENTED_EDGE('',*,*,#17001,.F.);
#23934=ORIENTED_EDGE('',*,*,#17002,.T.);
#23935=ORIENTED_EDGE('',*,*,#17003,.F.);
#23936=ORIENTED_EDGE('',*,*,#17004,.F.);
#23937=ORIENTED_EDGE('',*,*,#17005,.F.);
#23938=ORIENTED_EDGE('',*,*,#17006,.T.);
#23939=ORIENTED_EDGE('',*,*,#17007,.F.);
#23940=ORIENTED_EDGE('',*,*,#17008,.F.);
#23941=ORIENTED_EDGE('',*,*,#17009,.F.);
#23942=ORIENTED_EDGE('',*,*,#17010,.T.);
#23943=ORIENTED_EDGE('',*,*,#17011,.F.);
#23944=ORIENTED_EDGE('',*,*,#17012,.F.);
#23945=ORIENTED_EDGE('',*,*,#17013,.F.);
#23946=ORIENTED_EDGE('',*,*,#17014,.T.);
#23947=ORIENTED_EDGE('',*,*,#17015,.F.);
#23948=ORIENTED_EDGE('',*,*,#17016,.F.);
#23949=ORIENTED_EDGE('',*,*,#17017,.F.);
#23950=ORIENTED_EDGE('',*,*,#17018,.T.);
#23951=ORIENTED_EDGE('',*,*,#17019,.F.);
#23952=ORIENTED_EDGE('',*,*,#17020,.F.);
#23953=ORIENTED_EDGE('',*,*,#17021,.F.);
#23954=ORIENTED_EDGE('',*,*,#17022,.T.);
#23955=ORIENTED_EDGE('',*,*,#17023,.F.);
#23956=ORIENTED_EDGE('',*,*,#17024,.F.);
#23957=ORIENTED_EDGE('',*,*,#17025,.F.);
#23958=ORIENTED_EDGE('',*,*,#17026,.T.);
#23959=ORIENTED_EDGE('',*,*,#17027,.F.);
#23960=ORIENTED_EDGE('',*,*,#17028,.F.);
#23961=ORIENTED_EDGE('',*,*,#17029,.F.);
#23962=ORIENTED_EDGE('',*,*,#17030,.T.);
#23963=ORIENTED_EDGE('',*,*,#17031,.F.);
#23964=ORIENTED_EDGE('',*,*,#17032,.F.);
#23965=ORIENTED_EDGE('',*,*,#17033,.F.);
#23966=ORIENTED_EDGE('',*,*,#17034,.T.);
#23967=ORIENTED_EDGE('',*,*,#17035,.F.);
#23968=ORIENTED_EDGE('',*,*,#17036,.F.);
#23969=ORIENTED_EDGE('',*,*,#17037,.F.);
#23970=ORIENTED_EDGE('',*,*,#17038,.T.);
#23971=ORIENTED_EDGE('',*,*,#17039,.F.);
#23972=ORIENTED_EDGE('',*,*,#17040,.F.);
#23973=ORIENTED_EDGE('',*,*,#17041,.F.);
#23974=ORIENTED_EDGE('',*,*,#17042,.T.);
#23975=ORIENTED_EDGE('',*,*,#17043,.F.);
#23976=ORIENTED_EDGE('',*,*,#17044,.F.);
#23977=ORIENTED_EDGE('',*,*,#17045,.F.);
#23978=ORIENTED_EDGE('',*,*,#17046,.T.);
#23979=ORIENTED_EDGE('',*,*,#17047,.F.);
#23980=ORIENTED_EDGE('',*,*,#16449,.F.);
#23981=ORIENTED_EDGE('',*,*,#17048,.F.);
#23982=ORIENTED_EDGE('',*,*,#17049,.T.);
#23983=ORIENTED_EDGE('',*,*,#17050,.F.);
#23984=ORIENTED_EDGE('',*,*,#16445,.F.);
#23985=ORIENTED_EDGE('',*,*,#17051,.F.);
#23986=ORIENTED_EDGE('',*,*,#17052,.T.);
#23987=ORIENTED_EDGE('',*,*,#17053,.F.);
#23988=ORIENTED_EDGE('',*,*,#16441,.F.);
#23989=ORIENTED_EDGE('',*,*,#17054,.F.);
#23990=ORIENTED_EDGE('',*,*,#17055,.T.);
#23991=ORIENTED_EDGE('',*,*,#17056,.F.);
#23992=ORIENTED_EDGE('',*,*,#16437,.F.);
#23993=ORIENTED_EDGE('',*,*,#17057,.F.);
#23994=ORIENTED_EDGE('',*,*,#17058,.T.);
#23995=ORIENTED_EDGE('',*,*,#17059,.F.);
#23996=ORIENTED_EDGE('',*,*,#16433,.F.);
#23997=ORIENTED_EDGE('',*,*,#17060,.F.);
#23998=ORIENTED_EDGE('',*,*,#17061,.T.);
#23999=ORIENTED_EDGE('',*,*,#17062,.F.);
#24000=ORIENTED_EDGE('',*,*,#16429,.F.);
#24001=ORIENTED_EDGE('',*,*,#17063,.F.);
#24002=ORIENTED_EDGE('',*,*,#17064,.T.);
#24003=ORIENTED_EDGE('',*,*,#17065,.F.);
#24004=ORIENTED_EDGE('',*,*,#16453,.F.);
#24005=ORIENTED_EDGE('',*,*,#17066,.F.);
#24006=ORIENTED_EDGE('',*,*,#17067,.T.);
#24007=ORIENTED_EDGE('',*,*,#17068,.F.);
#24008=ORIENTED_EDGE('',*,*,#16457,.F.);
#24009=ORIENTED_EDGE('',*,*,#17069,.F.);
#24010=ORIENTED_EDGE('',*,*,#17070,.T.);
#24011=ORIENTED_EDGE('',*,*,#17071,.F.);
#24012=ORIENTED_EDGE('',*,*,#16461,.F.);
#24013=ORIENTED_EDGE('',*,*,#17072,.F.);
#24014=ORIENTED_EDGE('',*,*,#17073,.T.);
#24015=ORIENTED_EDGE('',*,*,#17074,.F.);
#24016=ORIENTED_EDGE('',*,*,#16465,.F.);
#24017=ORIENTED_EDGE('',*,*,#17075,.F.);
#24018=ORIENTED_EDGE('',*,*,#17076,.T.);
#24019=ORIENTED_EDGE('',*,*,#17077,.F.);
#24020=ORIENTED_EDGE('',*,*,#16469,.F.);
#24021=ORIENTED_EDGE('',*,*,#17078,.F.);
#24022=ORIENTED_EDGE('',*,*,#17079,.T.);
#24023=ORIENTED_EDGE('',*,*,#17080,.F.);
#24024=ORIENTED_EDGE('',*,*,#16473,.F.);
#24025=ORIENTED_EDGE('',*,*,#17081,.F.);
#24026=ORIENTED_EDGE('',*,*,#17082,.T.);
#24027=ORIENTED_EDGE('',*,*,#17083,.F.);
#24028=ORIENTED_EDGE('',*,*,#16477,.F.);
#24029=ORIENTED_EDGE('',*,*,#17084,.F.);
#24030=ORIENTED_EDGE('',*,*,#17085,.T.);
#24031=ORIENTED_EDGE('',*,*,#17086,.F.);
#24032=ORIENTED_EDGE('',*,*,#16481,.F.);
#24033=ORIENTED_EDGE('',*,*,#17087,.F.);
#24034=ORIENTED_EDGE('',*,*,#17088,.T.);
#24035=ORIENTED_EDGE('',*,*,#17089,.F.);
#24036=ORIENTED_EDGE('',*,*,#16485,.F.);
#24037=ORIENTED_EDGE('',*,*,#17090,.F.);
#24038=ORIENTED_EDGE('',*,*,#17091,.T.);
#24039=ORIENTED_EDGE('',*,*,#17092,.F.);
#24040=ORIENTED_EDGE('',*,*,#17093,.F.);
#24041=ORIENTED_EDGE('',*,*,#17094,.F.);
#24042=ORIENTED_EDGE('',*,*,#17095,.T.);
#24043=ORIENTED_EDGE('',*,*,#17096,.F.);
#24044=ORIENTED_EDGE('',*,*,#17097,.F.);
#24045=ORIENTED_EDGE('',*,*,#17098,.F.);
#24046=ORIENTED_EDGE('',*,*,#17099,.T.);
#24047=ORIENTED_EDGE('',*,*,#17100,.F.);
#24048=ORIENTED_EDGE('',*,*,#17101,.F.);
#24049=ORIENTED_EDGE('',*,*,#17102,.F.);
#24050=ORIENTED_EDGE('',*,*,#17103,.T.);
#24051=ORIENTED_EDGE('',*,*,#17104,.F.);
#24052=ORIENTED_EDGE('',*,*,#17105,.F.);
#24053=ORIENTED_EDGE('',*,*,#17106,.F.);
#24054=ORIENTED_EDGE('',*,*,#17107,.T.);
#24055=ORIENTED_EDGE('',*,*,#17108,.F.);
#24056=ORIENTED_EDGE('',*,*,#17109,.F.);
#24057=ORIENTED_EDGE('',*,*,#17110,.F.);
#24058=ORIENTED_EDGE('',*,*,#17111,.T.);
#24059=ORIENTED_EDGE('',*,*,#17112,.F.);
#24060=ORIENTED_EDGE('',*,*,#17113,.F.);
#24061=ORIENTED_EDGE('',*,*,#17114,.T.);
#24062=ORIENTED_EDGE('',*,*,#17115,.F.);
#24063=ORIENTED_EDGE('',*,*,#17116,.F.);
#24064=ORIENTED_EDGE('',*,*,#17114,.F.);
#24065=ORIENTED_EDGE('',*,*,#17117,.F.);
#24066=ORIENTED_EDGE('',*,*,#17118,.T.);
#24067=ORIENTED_EDGE('',*,*,#17115,.T.);
#24068=ORIENTED_EDGE('',*,*,#17116,.T.);
#24069=ORIENTED_EDGE('',*,*,#17118,.F.);
#24070=ORIENTED_EDGE('',*,*,#17119,.F.);
#24071=ORIENTED_EDGE('',*,*,#17120,.T.);
#24072=ORIENTED_EDGE('',*,*,#17117,.T.);
#24073=ORIENTED_EDGE('',*,*,#17120,.F.);
#24074=ORIENTED_EDGE('',*,*,#17121,.F.);
#24075=ORIENTED_EDGE('',*,*,#17122,.T.);
#24076=ORIENTED_EDGE('',*,*,#17119,.T.);
#24077=ORIENTED_EDGE('',*,*,#17122,.F.);
#24078=ORIENTED_EDGE('',*,*,#16244,.F.);
#24079=ORIENTED_EDGE('',*,*,#17123,.T.);
#24080=ORIENTED_EDGE('',*,*,#17124,.T.);
#24081=ORIENTED_EDGE('',*,*,#17123,.F.);
#24082=ORIENTED_EDGE('',*,*,#17125,.F.);
#24083=ORIENTED_EDGE('',*,*,#17126,.T.);
#24084=ORIENTED_EDGE('',*,*,#17127,.F.);
#24085=ORIENTED_EDGE('',*,*,#17064,.F.);
#24086=ORIENTED_EDGE('',*,*,#17128,.F.);
#24087=ORIENTED_EDGE('',*,*,#17061,.F.);
#24088=ORIENTED_EDGE('',*,*,#17129,.F.);
#24089=ORIENTED_EDGE('',*,*,#17130,.T.);
#24090=ORIENTED_EDGE('',*,*,#17131,.F.);
#24091=ORIENTED_EDGE('',*,*,#17058,.F.);
#24092=ORIENTED_EDGE('',*,*,#17132,.F.);
#24093=ORIENTED_EDGE('',*,*,#17133,.T.);
#24094=ORIENTED_EDGE('',*,*,#17134,.F.);
#24095=ORIENTED_EDGE('',*,*,#17055,.F.);
#24096=ORIENTED_EDGE('',*,*,#17135,.F.);
#24097=ORIENTED_EDGE('',*,*,#17136,.T.);
#24098=ORIENTED_EDGE('',*,*,#17137,.F.);
#24099=ORIENTED_EDGE('',*,*,#17052,.F.);
#24100=ORIENTED_EDGE('',*,*,#17138,.F.);
#24101=ORIENTED_EDGE('',*,*,#17139,.T.);
#24102=ORIENTED_EDGE('',*,*,#17140,.F.);
#24103=ORIENTED_EDGE('',*,*,#17049,.F.);
#24104=ORIENTED_EDGE('',*,*,#17141,.F.);
#24105=ORIENTED_EDGE('',*,*,#17142,.T.);
#24106=ORIENTED_EDGE('',*,*,#17143,.F.);
#24107=ORIENTED_EDGE('',*,*,#17046,.F.);
#24108=ORIENTED_EDGE('',*,*,#17144,.F.);
#24109=ORIENTED_EDGE('',*,*,#17145,.T.);
#24110=ORIENTED_EDGE('',*,*,#17146,.F.);
#24111=ORIENTED_EDGE('',*,*,#17042,.F.);
#24112=ORIENTED_EDGE('',*,*,#17147,.F.);
#24113=ORIENTED_EDGE('',*,*,#17148,.T.);
#24114=ORIENTED_EDGE('',*,*,#17149,.F.);
#24115=ORIENTED_EDGE('',*,*,#17038,.F.);
#24116=ORIENTED_EDGE('',*,*,#17150,.F.);
#24117=ORIENTED_EDGE('',*,*,#17151,.T.);
#24118=ORIENTED_EDGE('',*,*,#17152,.F.);
#24119=ORIENTED_EDGE('',*,*,#17034,.F.);
#24120=ORIENTED_EDGE('',*,*,#17153,.F.);
#24121=ORIENTED_EDGE('',*,*,#17154,.T.);
#24122=ORIENTED_EDGE('',*,*,#17155,.F.);
#24123=ORIENTED_EDGE('',*,*,#17030,.F.);
#24124=ORIENTED_EDGE('',*,*,#17156,.F.);
#24125=ORIENTED_EDGE('',*,*,#17157,.T.);
#24126=ORIENTED_EDGE('',*,*,#17158,.F.);
#24127=ORIENTED_EDGE('',*,*,#17026,.F.);
#24128=ORIENTED_EDGE('',*,*,#17159,.F.);
#24129=ORIENTED_EDGE('',*,*,#17160,.T.);
#24130=ORIENTED_EDGE('',*,*,#17161,.F.);
#24131=ORIENTED_EDGE('',*,*,#17022,.F.);
#24132=ORIENTED_EDGE('',*,*,#17162,.F.);
#24133=ORIENTED_EDGE('',*,*,#17163,.T.);
#24134=ORIENTED_EDGE('',*,*,#17164,.F.);
#24135=ORIENTED_EDGE('',*,*,#17018,.F.);
#24136=ORIENTED_EDGE('',*,*,#17165,.F.);
#24137=ORIENTED_EDGE('',*,*,#17166,.T.);
#24138=ORIENTED_EDGE('',*,*,#17167,.F.);
#24139=ORIENTED_EDGE('',*,*,#17014,.F.);
#24140=ORIENTED_EDGE('',*,*,#17168,.F.);
#24141=ORIENTED_EDGE('',*,*,#17169,.T.);
#24142=ORIENTED_EDGE('',*,*,#17170,.F.);
#24143=ORIENTED_EDGE('',*,*,#17010,.F.);
#24144=ORIENTED_EDGE('',*,*,#17171,.F.);
#24145=ORIENTED_EDGE('',*,*,#17172,.T.);
#24146=ORIENTED_EDGE('',*,*,#17173,.F.);
#24147=ORIENTED_EDGE('',*,*,#17006,.F.);
#24148=ORIENTED_EDGE('',*,*,#17174,.F.);
#24149=ORIENTED_EDGE('',*,*,#17175,.T.);
#24150=ORIENTED_EDGE('',*,*,#17176,.F.);
#24151=ORIENTED_EDGE('',*,*,#17002,.F.);
#24152=ORIENTED_EDGE('',*,*,#17177,.F.);
#24153=ORIENTED_EDGE('',*,*,#17178,.T.);
#24154=ORIENTED_EDGE('',*,*,#17179,.F.);
#24155=ORIENTED_EDGE('',*,*,#16998,.F.);
#24156=ORIENTED_EDGE('',*,*,#17180,.F.);
#24157=ORIENTED_EDGE('',*,*,#17181,.T.);
#24158=ORIENTED_EDGE('',*,*,#17182,.F.);
#24159=ORIENTED_EDGE('',*,*,#16994,.F.);
#24160=ORIENTED_EDGE('',*,*,#17183,.F.);
#24161=ORIENTED_EDGE('',*,*,#17184,.T.);
#24162=ORIENTED_EDGE('',*,*,#17185,.F.);
#24163=ORIENTED_EDGE('',*,*,#16990,.F.);
#24164=ORIENTED_EDGE('',*,*,#17186,.F.);
#24165=ORIENTED_EDGE('',*,*,#17187,.T.);
#24166=ORIENTED_EDGE('',*,*,#17188,.F.);
#24167=ORIENTED_EDGE('',*,*,#16986,.F.);
#24168=ORIENTED_EDGE('',*,*,#17189,.F.);
#24169=ORIENTED_EDGE('',*,*,#17190,.T.);
#24170=ORIENTED_EDGE('',*,*,#17191,.F.);
#24171=ORIENTED_EDGE('',*,*,#16982,.F.);
#24172=ORIENTED_EDGE('',*,*,#17192,.F.);
#24173=ORIENTED_EDGE('',*,*,#17193,.T.);
#24174=ORIENTED_EDGE('',*,*,#17194,.F.);
#24175=ORIENTED_EDGE('',*,*,#16978,.F.);
#24176=ORIENTED_EDGE('',*,*,#17195,.F.);
#24177=ORIENTED_EDGE('',*,*,#17196,.T.);
#24178=ORIENTED_EDGE('',*,*,#17197,.F.);
#24179=ORIENTED_EDGE('',*,*,#16974,.F.);
#24180=ORIENTED_EDGE('',*,*,#17198,.F.);
#24181=ORIENTED_EDGE('',*,*,#17199,.T.);
#24182=ORIENTED_EDGE('',*,*,#17200,.F.);
#24183=ORIENTED_EDGE('',*,*,#16970,.F.);
#24184=ORIENTED_EDGE('',*,*,#17201,.F.);
#24185=ORIENTED_EDGE('',*,*,#17202,.T.);
#24186=ORIENTED_EDGE('',*,*,#17203,.F.);
#24187=ORIENTED_EDGE('',*,*,#16966,.F.);
#24188=ORIENTED_EDGE('',*,*,#17204,.F.);
#24189=ORIENTED_EDGE('',*,*,#17205,.T.);
#24190=ORIENTED_EDGE('',*,*,#17206,.F.);
#24191=ORIENTED_EDGE('',*,*,#16962,.F.);
#24192=ORIENTED_EDGE('',*,*,#17207,.F.);
#24193=ORIENTED_EDGE('',*,*,#17208,.T.);
#24194=ORIENTED_EDGE('',*,*,#17209,.F.);
#24195=ORIENTED_EDGE('',*,*,#16958,.F.);
#24196=ORIENTED_EDGE('',*,*,#17210,.F.);
#24197=ORIENTED_EDGE('',*,*,#17211,.T.);
#24198=ORIENTED_EDGE('',*,*,#17212,.F.);
#24199=ORIENTED_EDGE('',*,*,#16954,.F.);
#24200=ORIENTED_EDGE('',*,*,#17213,.F.);
#24201=ORIENTED_EDGE('',*,*,#17214,.T.);
#24202=ORIENTED_EDGE('',*,*,#17215,.F.);
#24203=ORIENTED_EDGE('',*,*,#16950,.F.);
#24204=ORIENTED_EDGE('',*,*,#17216,.F.);
#24205=ORIENTED_EDGE('',*,*,#17217,.T.);
#24206=ORIENTED_EDGE('',*,*,#17218,.F.);
#24207=ORIENTED_EDGE('',*,*,#16946,.F.);
#24208=ORIENTED_EDGE('',*,*,#17219,.F.);
#24209=ORIENTED_EDGE('',*,*,#17220,.T.);
#24210=ORIENTED_EDGE('',*,*,#17221,.F.);
#24211=ORIENTED_EDGE('',*,*,#16942,.F.);
#24212=ORIENTED_EDGE('',*,*,#17222,.F.);
#24213=ORIENTED_EDGE('',*,*,#17223,.T.);
#24214=ORIENTED_EDGE('',*,*,#17224,.F.);
#24215=ORIENTED_EDGE('',*,*,#16938,.F.);
#24216=ORIENTED_EDGE('',*,*,#17225,.F.);
#24217=ORIENTED_EDGE('',*,*,#17226,.T.);
#24218=ORIENTED_EDGE('',*,*,#17227,.F.);
#24219=ORIENTED_EDGE('',*,*,#16934,.F.);
#24220=ORIENTED_EDGE('',*,*,#17228,.F.);
#24221=ORIENTED_EDGE('',*,*,#17229,.T.);
#24222=ORIENTED_EDGE('',*,*,#17230,.F.);
#24223=ORIENTED_EDGE('',*,*,#16930,.F.);
#24224=ORIENTED_EDGE('',*,*,#17231,.F.);
#24225=ORIENTED_EDGE('',*,*,#17232,.T.);
#24226=ORIENTED_EDGE('',*,*,#17233,.F.);
#24227=ORIENTED_EDGE('',*,*,#16926,.F.);
#24228=ORIENTED_EDGE('',*,*,#17234,.F.);
#24229=ORIENTED_EDGE('',*,*,#17235,.T.);
#24230=ORIENTED_EDGE('',*,*,#17236,.F.);
#24231=ORIENTED_EDGE('',*,*,#16922,.F.);
#24232=ORIENTED_EDGE('',*,*,#17237,.F.);
#24233=ORIENTED_EDGE('',*,*,#17238,.T.);
#24234=ORIENTED_EDGE('',*,*,#17239,.F.);
#24235=ORIENTED_EDGE('',*,*,#16918,.F.);
#24236=ORIENTED_EDGE('',*,*,#17240,.F.);
#24237=ORIENTED_EDGE('',*,*,#17241,.T.);
#24238=ORIENTED_EDGE('',*,*,#17242,.F.);
#24239=ORIENTED_EDGE('',*,*,#16914,.F.);
#24240=ORIENTED_EDGE('',*,*,#17243,.F.);
#24241=ORIENTED_EDGE('',*,*,#17244,.T.);
#24242=ORIENTED_EDGE('',*,*,#17245,.F.);
#24243=ORIENTED_EDGE('',*,*,#16910,.F.);
#24244=ORIENTED_EDGE('',*,*,#17246,.F.);
#24245=ORIENTED_EDGE('',*,*,#17247,.T.);
#24246=ORIENTED_EDGE('',*,*,#17248,.F.);
#24247=ORIENTED_EDGE('',*,*,#16906,.F.);
#24248=ORIENTED_EDGE('',*,*,#17249,.F.);
#24249=ORIENTED_EDGE('',*,*,#17250,.T.);
#24250=ORIENTED_EDGE('',*,*,#17251,.F.);
#24251=ORIENTED_EDGE('',*,*,#16902,.F.);
#24252=ORIENTED_EDGE('',*,*,#17252,.F.);
#24253=ORIENTED_EDGE('',*,*,#17253,.T.);
#24254=ORIENTED_EDGE('',*,*,#17254,.F.);
#24255=ORIENTED_EDGE('',*,*,#16898,.F.);
#24256=ORIENTED_EDGE('',*,*,#17255,.F.);
#24257=ORIENTED_EDGE('',*,*,#17256,.T.);
#24258=ORIENTED_EDGE('',*,*,#17257,.F.);
#24259=ORIENTED_EDGE('',*,*,#16894,.F.);
#24260=ORIENTED_EDGE('',*,*,#17258,.F.);
#24261=ORIENTED_EDGE('',*,*,#17259,.T.);
#24262=ORIENTED_EDGE('',*,*,#17260,.F.);
#24263=ORIENTED_EDGE('',*,*,#16890,.F.);
#24264=ORIENTED_EDGE('',*,*,#17261,.F.);
#24265=ORIENTED_EDGE('',*,*,#17262,.T.);
#24266=ORIENTED_EDGE('',*,*,#17263,.F.);
#24267=ORIENTED_EDGE('',*,*,#16886,.F.);
#24268=ORIENTED_EDGE('',*,*,#17264,.F.);
#24269=ORIENTED_EDGE('',*,*,#17265,.T.);
#24270=ORIENTED_EDGE('',*,*,#17266,.F.);
#24271=ORIENTED_EDGE('',*,*,#16882,.F.);
#24272=ORIENTED_EDGE('',*,*,#17267,.F.);
#24273=ORIENTED_EDGE('',*,*,#17268,.T.);
#24274=ORIENTED_EDGE('',*,*,#17269,.F.);
#24275=ORIENTED_EDGE('',*,*,#16878,.F.);
#24276=ORIENTED_EDGE('',*,*,#17270,.F.);
#24277=ORIENTED_EDGE('',*,*,#17271,.T.);
#24278=ORIENTED_EDGE('',*,*,#17272,.F.);
#24279=ORIENTED_EDGE('',*,*,#16874,.F.);
#24280=ORIENTED_EDGE('',*,*,#17273,.F.);
#24281=ORIENTED_EDGE('',*,*,#17274,.T.);
#24282=ORIENTED_EDGE('',*,*,#17275,.F.);
#24283=ORIENTED_EDGE('',*,*,#16870,.F.);
#24284=ORIENTED_EDGE('',*,*,#17276,.F.);
#24285=ORIENTED_EDGE('',*,*,#17277,.T.);
#24286=ORIENTED_EDGE('',*,*,#17278,.F.);
#24287=ORIENTED_EDGE('',*,*,#16866,.F.);
#24288=ORIENTED_EDGE('',*,*,#17279,.F.);
#24289=ORIENTED_EDGE('',*,*,#17280,.T.);
#24290=ORIENTED_EDGE('',*,*,#17281,.F.);
#24291=ORIENTED_EDGE('',*,*,#16862,.F.);
#24292=ORIENTED_EDGE('',*,*,#17282,.F.);
#24293=ORIENTED_EDGE('',*,*,#17283,.T.);
#24294=ORIENTED_EDGE('',*,*,#17284,.F.);
#24295=ORIENTED_EDGE('',*,*,#16858,.F.);
#24296=ORIENTED_EDGE('',*,*,#17285,.F.);
#24297=ORIENTED_EDGE('',*,*,#17286,.T.);
#24298=ORIENTED_EDGE('',*,*,#17287,.F.);
#24299=ORIENTED_EDGE('',*,*,#16854,.F.);
#24300=ORIENTED_EDGE('',*,*,#17288,.F.);
#24301=ORIENTED_EDGE('',*,*,#17289,.T.);
#24302=ORIENTED_EDGE('',*,*,#17290,.F.);
#24303=ORIENTED_EDGE('',*,*,#16850,.F.);
#24304=ORIENTED_EDGE('',*,*,#17291,.F.);
#24305=ORIENTED_EDGE('',*,*,#17292,.T.);
#24306=ORIENTED_EDGE('',*,*,#17293,.F.);
#24307=ORIENTED_EDGE('',*,*,#16846,.F.);
#24308=ORIENTED_EDGE('',*,*,#17294,.F.);
#24309=ORIENTED_EDGE('',*,*,#17295,.T.);
#24310=ORIENTED_EDGE('',*,*,#17296,.F.);
#24311=ORIENTED_EDGE('',*,*,#16842,.F.);
#24312=ORIENTED_EDGE('',*,*,#17297,.F.);
#24313=ORIENTED_EDGE('',*,*,#17298,.T.);
#24314=ORIENTED_EDGE('',*,*,#17299,.F.);
#24315=ORIENTED_EDGE('',*,*,#16838,.F.);
#24316=ORIENTED_EDGE('',*,*,#17300,.F.);
#24317=ORIENTED_EDGE('',*,*,#17301,.T.);
#24318=ORIENTED_EDGE('',*,*,#17302,.F.);
#24319=ORIENTED_EDGE('',*,*,#16834,.F.);
#24320=ORIENTED_EDGE('',*,*,#17303,.F.);
#24321=ORIENTED_EDGE('',*,*,#17304,.T.);
#24322=ORIENTED_EDGE('',*,*,#17305,.F.);
#24323=ORIENTED_EDGE('',*,*,#16830,.F.);
#24324=ORIENTED_EDGE('',*,*,#17306,.F.);
#24325=ORIENTED_EDGE('',*,*,#17307,.T.);
#24326=ORIENTED_EDGE('',*,*,#17308,.F.);
#24327=ORIENTED_EDGE('',*,*,#16826,.F.);
#24328=ORIENTED_EDGE('',*,*,#17309,.F.);
#24329=ORIENTED_EDGE('',*,*,#17310,.T.);
#24330=ORIENTED_EDGE('',*,*,#17311,.F.);
#24331=ORIENTED_EDGE('',*,*,#16822,.F.);
#24332=ORIENTED_EDGE('',*,*,#17312,.F.);
#24333=ORIENTED_EDGE('',*,*,#17313,.T.);
#24334=ORIENTED_EDGE('',*,*,#17314,.F.);
#24335=ORIENTED_EDGE('',*,*,#16818,.F.);
#24336=ORIENTED_EDGE('',*,*,#17315,.F.);
#24337=ORIENTED_EDGE('',*,*,#17316,.T.);
#24338=ORIENTED_EDGE('',*,*,#17317,.F.);
#24339=ORIENTED_EDGE('',*,*,#17318,.T.);
#24340=ORIENTED_EDGE('',*,*,#17319,.F.);
#24341=ORIENTED_EDGE('',*,*,#17067,.F.);
#24342=ORIENTED_EDGE('',*,*,#17320,.F.);
#24343=ORIENTED_EDGE('',*,*,#17321,.T.);
#24344=ORIENTED_EDGE('',*,*,#17322,.F.);
#24345=ORIENTED_EDGE('',*,*,#17070,.F.);
#24346=ORIENTED_EDGE('',*,*,#17323,.F.);
#24347=ORIENTED_EDGE('',*,*,#17324,.T.);
#24348=ORIENTED_EDGE('',*,*,#17325,.F.);
#24349=ORIENTED_EDGE('',*,*,#17073,.F.);
#24350=ORIENTED_EDGE('',*,*,#17326,.F.);
#24351=ORIENTED_EDGE('',*,*,#17327,.T.);
#24352=ORIENTED_EDGE('',*,*,#17328,.F.);
#24353=ORIENTED_EDGE('',*,*,#17076,.F.);
#24354=ORIENTED_EDGE('',*,*,#17329,.F.);
#24355=ORIENTED_EDGE('',*,*,#17330,.T.);
#24356=ORIENTED_EDGE('',*,*,#17331,.F.);
#24357=ORIENTED_EDGE('',*,*,#17079,.F.);
#24358=ORIENTED_EDGE('',*,*,#17332,.F.);
#24359=ORIENTED_EDGE('',*,*,#17333,.T.);
#24360=ORIENTED_EDGE('',*,*,#17334,.F.);
#24361=ORIENTED_EDGE('',*,*,#17082,.F.);
#24362=ORIENTED_EDGE('',*,*,#17335,.F.);
#24363=ORIENTED_EDGE('',*,*,#17336,.T.);
#24364=ORIENTED_EDGE('',*,*,#17337,.F.);
#24365=ORIENTED_EDGE('',*,*,#17085,.F.);
#24366=ORIENTED_EDGE('',*,*,#17338,.F.);
#24367=ORIENTED_EDGE('',*,*,#17339,.T.);
#24368=ORIENTED_EDGE('',*,*,#17340,.F.);
#24369=ORIENTED_EDGE('',*,*,#17088,.F.);
#24370=ORIENTED_EDGE('',*,*,#17341,.F.);
#24371=ORIENTED_EDGE('',*,*,#17342,.T.);
#24372=ORIENTED_EDGE('',*,*,#17343,.F.);
#24373=ORIENTED_EDGE('',*,*,#17091,.F.);
#24374=ORIENTED_EDGE('',*,*,#17344,.F.);
#24375=ORIENTED_EDGE('',*,*,#17345,.T.);
#24376=ORIENTED_EDGE('',*,*,#17346,.F.);
#24377=ORIENTED_EDGE('',*,*,#17095,.F.);
#24378=ORIENTED_EDGE('',*,*,#17347,.F.);
#24379=ORIENTED_EDGE('',*,*,#17348,.T.);
#24380=ORIENTED_EDGE('',*,*,#17349,.F.);
#24381=ORIENTED_EDGE('',*,*,#17099,.F.);
#24382=ORIENTED_EDGE('',*,*,#17350,.F.);
#24383=ORIENTED_EDGE('',*,*,#17351,.T.);
#24384=ORIENTED_EDGE('',*,*,#17352,.F.);
#24385=ORIENTED_EDGE('',*,*,#17103,.F.);
#24386=ORIENTED_EDGE('',*,*,#17353,.F.);
#24387=ORIENTED_EDGE('',*,*,#17354,.T.);
#24388=ORIENTED_EDGE('',*,*,#17355,.F.);
#24389=ORIENTED_EDGE('',*,*,#17107,.F.);
#24390=ORIENTED_EDGE('',*,*,#17356,.F.);
#24391=ORIENTED_EDGE('',*,*,#17357,.T.);
#24392=ORIENTED_EDGE('',*,*,#17358,.F.);
#24393=ORIENTED_EDGE('',*,*,#17111,.F.);
#24394=ORIENTED_EDGE('',*,*,#17359,.F.);
#24395=ORIENTED_EDGE('',*,*,#16814,.F.);
#24396=ORIENTED_EDGE('',*,*,#17360,.F.);
#24397=ORIENTED_EDGE('',*,*,#17361,.T.);
#24398=ORIENTED_EDGE('',*,*,#17362,.F.);
#24399=ORIENTED_EDGE('',*,*,#17363,.T.);
#24400=ORIENTED_EDGE('',*,*,#17364,.F.);
#24401=ORIENTED_EDGE('',*,*,#17126,.F.);
#24402=ORIENTED_EDGE('',*,*,#17365,.F.);
#24403=ORIENTED_EDGE('',*,*,#17130,.F.);
#24404=ORIENTED_EDGE('',*,*,#17366,.F.);
#24405=ORIENTED_EDGE('',*,*,#17367,.T.);
#24406=ORIENTED_EDGE('',*,*,#17368,.F.);
#24407=ORIENTED_EDGE('',*,*,#17133,.F.);
#24408=ORIENTED_EDGE('',*,*,#17369,.F.);
#24409=ORIENTED_EDGE('',*,*,#17370,.T.);
#24410=ORIENTED_EDGE('',*,*,#17371,.F.);
#24411=ORIENTED_EDGE('',*,*,#17136,.F.);
#24412=ORIENTED_EDGE('',*,*,#17372,.F.);
#24413=ORIENTED_EDGE('',*,*,#17373,.T.);
#24414=ORIENTED_EDGE('',*,*,#17374,.F.);
#24415=ORIENTED_EDGE('',*,*,#17139,.F.);
#24416=ORIENTED_EDGE('',*,*,#17375,.F.);
#24417=ORIENTED_EDGE('',*,*,#17376,.T.);
#24418=ORIENTED_EDGE('',*,*,#17377,.F.);
#24419=ORIENTED_EDGE('',*,*,#17142,.F.);
#24420=ORIENTED_EDGE('',*,*,#17378,.F.);
#24421=ORIENTED_EDGE('',*,*,#17379,.T.);
#24422=ORIENTED_EDGE('',*,*,#17380,.F.);
#24423=ORIENTED_EDGE('',*,*,#17145,.F.);
#24424=ORIENTED_EDGE('',*,*,#17381,.F.);
#24425=ORIENTED_EDGE('',*,*,#17382,.T.);
#24426=ORIENTED_EDGE('',*,*,#17383,.F.);
#24427=ORIENTED_EDGE('',*,*,#17148,.F.);
#24428=ORIENTED_EDGE('',*,*,#17384,.F.);
#24429=ORIENTED_EDGE('',*,*,#17385,.T.);
#24430=ORIENTED_EDGE('',*,*,#17386,.F.);
#24431=ORIENTED_EDGE('',*,*,#17151,.F.);
#24432=ORIENTED_EDGE('',*,*,#17387,.F.);
#24433=ORIENTED_EDGE('',*,*,#17388,.T.);
#24434=ORIENTED_EDGE('',*,*,#17389,.F.);
#24435=ORIENTED_EDGE('',*,*,#17154,.F.);
#24436=ORIENTED_EDGE('',*,*,#17390,.F.);
#24437=ORIENTED_EDGE('',*,*,#17391,.T.);
#24438=ORIENTED_EDGE('',*,*,#17392,.F.);
#24439=ORIENTED_EDGE('',*,*,#17157,.F.);
#24440=ORIENTED_EDGE('',*,*,#17393,.F.);
#24441=ORIENTED_EDGE('',*,*,#17394,.T.);
#24442=ORIENTED_EDGE('',*,*,#17395,.F.);
#24443=ORIENTED_EDGE('',*,*,#17160,.F.);
#24444=ORIENTED_EDGE('',*,*,#17396,.F.);
#24445=ORIENTED_EDGE('',*,*,#17397,.T.);
#24446=ORIENTED_EDGE('',*,*,#17398,.F.);
#24447=ORIENTED_EDGE('',*,*,#17163,.F.);
#24448=ORIENTED_EDGE('',*,*,#17399,.F.);
#24449=ORIENTED_EDGE('',*,*,#17400,.T.);
#24450=ORIENTED_EDGE('',*,*,#17401,.F.);
#24451=ORIENTED_EDGE('',*,*,#17166,.F.);
#24452=ORIENTED_EDGE('',*,*,#17402,.F.);
#24453=ORIENTED_EDGE('',*,*,#17403,.T.);
#24454=ORIENTED_EDGE('',*,*,#17404,.F.);
#24455=ORIENTED_EDGE('',*,*,#17169,.F.);
#24456=ORIENTED_EDGE('',*,*,#17405,.F.);
#24457=ORIENTED_EDGE('',*,*,#17406,.T.);
#24458=ORIENTED_EDGE('',*,*,#17407,.F.);
#24459=ORIENTED_EDGE('',*,*,#17172,.F.);
#24460=ORIENTED_EDGE('',*,*,#17408,.F.);
#24461=ORIENTED_EDGE('',*,*,#17409,.T.);
#24462=ORIENTED_EDGE('',*,*,#17410,.F.);
#24463=ORIENTED_EDGE('',*,*,#17175,.F.);
#24464=ORIENTED_EDGE('',*,*,#17411,.F.);
#24465=ORIENTED_EDGE('',*,*,#17412,.T.);
#24466=ORIENTED_EDGE('',*,*,#17413,.F.);
#24467=ORIENTED_EDGE('',*,*,#17178,.F.);
#24468=ORIENTED_EDGE('',*,*,#17414,.F.);
#24469=ORIENTED_EDGE('',*,*,#17415,.T.);
#24470=ORIENTED_EDGE('',*,*,#17416,.F.);
#24471=ORIENTED_EDGE('',*,*,#17181,.F.);
#24472=ORIENTED_EDGE('',*,*,#17417,.F.);
#24473=ORIENTED_EDGE('',*,*,#17418,.T.);
#24474=ORIENTED_EDGE('',*,*,#17419,.F.);
#24475=ORIENTED_EDGE('',*,*,#17184,.F.);
#24476=ORIENTED_EDGE('',*,*,#17420,.F.);
#24477=ORIENTED_EDGE('',*,*,#17421,.T.);
#24478=ORIENTED_EDGE('',*,*,#17422,.F.);
#24479=ORIENTED_EDGE('',*,*,#17187,.F.);
#24480=ORIENTED_EDGE('',*,*,#17423,.F.);
#24481=ORIENTED_EDGE('',*,*,#17424,.T.);
#24482=ORIENTED_EDGE('',*,*,#17425,.F.);
#24483=ORIENTED_EDGE('',*,*,#17190,.F.);
#24484=ORIENTED_EDGE('',*,*,#17426,.F.);
#24485=ORIENTED_EDGE('',*,*,#17427,.T.);
#24486=ORIENTED_EDGE('',*,*,#17428,.F.);
#24487=ORIENTED_EDGE('',*,*,#17193,.F.);
#24488=ORIENTED_EDGE('',*,*,#17429,.F.);
#24489=ORIENTED_EDGE('',*,*,#17430,.T.);
#24490=ORIENTED_EDGE('',*,*,#17431,.F.);
#24491=ORIENTED_EDGE('',*,*,#17196,.F.);
#24492=ORIENTED_EDGE('',*,*,#17432,.F.);
#24493=ORIENTED_EDGE('',*,*,#17433,.T.);
#24494=ORIENTED_EDGE('',*,*,#17434,.F.);
#24495=ORIENTED_EDGE('',*,*,#17199,.F.);
#24496=ORIENTED_EDGE('',*,*,#17435,.F.);
#24497=ORIENTED_EDGE('',*,*,#17436,.T.);
#24498=ORIENTED_EDGE('',*,*,#17437,.F.);
#24499=ORIENTED_EDGE('',*,*,#17202,.F.);
#24500=ORIENTED_EDGE('',*,*,#17438,.F.);
#24501=ORIENTED_EDGE('',*,*,#17439,.T.);
#24502=ORIENTED_EDGE('',*,*,#17440,.F.);
#24503=ORIENTED_EDGE('',*,*,#17205,.F.);
#24504=ORIENTED_EDGE('',*,*,#17441,.F.);
#24505=ORIENTED_EDGE('',*,*,#17442,.T.);
#24506=ORIENTED_EDGE('',*,*,#17443,.F.);
#24507=ORIENTED_EDGE('',*,*,#17208,.F.);
#24508=ORIENTED_EDGE('',*,*,#17444,.F.);
#24509=ORIENTED_EDGE('',*,*,#17445,.T.);
#24510=ORIENTED_EDGE('',*,*,#17446,.F.);
#24511=ORIENTED_EDGE('',*,*,#17211,.F.);
#24512=ORIENTED_EDGE('',*,*,#17447,.F.);
#24513=ORIENTED_EDGE('',*,*,#17448,.T.);
#24514=ORIENTED_EDGE('',*,*,#17449,.F.);
#24515=ORIENTED_EDGE('',*,*,#17214,.F.);
#24516=ORIENTED_EDGE('',*,*,#17450,.F.);
#24517=ORIENTED_EDGE('',*,*,#17451,.T.);
#24518=ORIENTED_EDGE('',*,*,#17452,.F.);
#24519=ORIENTED_EDGE('',*,*,#17217,.F.);
#24520=ORIENTED_EDGE('',*,*,#17453,.F.);
#24521=ORIENTED_EDGE('',*,*,#17454,.T.);
#24522=ORIENTED_EDGE('',*,*,#17455,.F.);
#24523=ORIENTED_EDGE('',*,*,#17220,.F.);
#24524=ORIENTED_EDGE('',*,*,#17456,.F.);
#24525=ORIENTED_EDGE('',*,*,#17457,.T.);
#24526=ORIENTED_EDGE('',*,*,#17458,.F.);
#24527=ORIENTED_EDGE('',*,*,#17223,.F.);
#24528=ORIENTED_EDGE('',*,*,#17459,.F.);
#24529=ORIENTED_EDGE('',*,*,#17460,.T.);
#24530=ORIENTED_EDGE('',*,*,#17461,.F.);
#24531=ORIENTED_EDGE('',*,*,#17226,.F.);
#24532=ORIENTED_EDGE('',*,*,#17462,.F.);
#24533=ORIENTED_EDGE('',*,*,#17463,.T.);
#24534=ORIENTED_EDGE('',*,*,#17464,.F.);
#24535=ORIENTED_EDGE('',*,*,#17229,.F.);
#24536=ORIENTED_EDGE('',*,*,#17465,.F.);
#24537=ORIENTED_EDGE('',*,*,#17466,.T.);
#24538=ORIENTED_EDGE('',*,*,#17467,.F.);
#24539=ORIENTED_EDGE('',*,*,#17232,.F.);
#24540=ORIENTED_EDGE('',*,*,#17468,.F.);
#24541=ORIENTED_EDGE('',*,*,#17469,.T.);
#24542=ORIENTED_EDGE('',*,*,#17470,.F.);
#24543=ORIENTED_EDGE('',*,*,#17235,.F.);
#24544=ORIENTED_EDGE('',*,*,#17471,.F.);
#24545=ORIENTED_EDGE('',*,*,#17472,.T.);
#24546=ORIENTED_EDGE('',*,*,#17473,.F.);
#24547=ORIENTED_EDGE('',*,*,#17238,.F.);
#24548=ORIENTED_EDGE('',*,*,#17474,.F.);
#24549=ORIENTED_EDGE('',*,*,#17475,.T.);
#24550=ORIENTED_EDGE('',*,*,#17476,.F.);
#24551=ORIENTED_EDGE('',*,*,#17241,.F.);
#24552=ORIENTED_EDGE('',*,*,#17477,.F.);
#24553=ORIENTED_EDGE('',*,*,#17478,.T.);
#24554=ORIENTED_EDGE('',*,*,#17479,.F.);
#24555=ORIENTED_EDGE('',*,*,#17244,.F.);
#24556=ORIENTED_EDGE('',*,*,#17480,.F.);
#24557=ORIENTED_EDGE('',*,*,#17481,.T.);
#24558=ORIENTED_EDGE('',*,*,#17482,.F.);
#24559=ORIENTED_EDGE('',*,*,#17247,.F.);
#24560=ORIENTED_EDGE('',*,*,#17483,.F.);
#24561=ORIENTED_EDGE('',*,*,#17484,.T.);
#24562=ORIENTED_EDGE('',*,*,#17485,.F.);
#24563=ORIENTED_EDGE('',*,*,#17250,.F.);
#24564=ORIENTED_EDGE('',*,*,#17486,.F.);
#24565=ORIENTED_EDGE('',*,*,#17487,.T.);
#24566=ORIENTED_EDGE('',*,*,#17488,.F.);
#24567=ORIENTED_EDGE('',*,*,#17253,.F.);
#24568=ORIENTED_EDGE('',*,*,#17489,.F.);
#24569=ORIENTED_EDGE('',*,*,#17490,.T.);
#24570=ORIENTED_EDGE('',*,*,#17491,.F.);
#24571=ORIENTED_EDGE('',*,*,#17256,.F.);
#24572=ORIENTED_EDGE('',*,*,#17492,.F.);
#24573=ORIENTED_EDGE('',*,*,#17493,.T.);
#24574=ORIENTED_EDGE('',*,*,#17494,.F.);
#24575=ORIENTED_EDGE('',*,*,#17259,.F.);
#24576=ORIENTED_EDGE('',*,*,#17495,.F.);
#24577=ORIENTED_EDGE('',*,*,#17496,.T.);
#24578=ORIENTED_EDGE('',*,*,#17497,.F.);
#24579=ORIENTED_EDGE('',*,*,#17262,.F.);
#24580=ORIENTED_EDGE('',*,*,#17498,.F.);
#24581=ORIENTED_EDGE('',*,*,#17499,.T.);
#24582=ORIENTED_EDGE('',*,*,#17500,.F.);
#24583=ORIENTED_EDGE('',*,*,#17265,.F.);
#24584=ORIENTED_EDGE('',*,*,#17501,.F.);
#24585=ORIENTED_EDGE('',*,*,#17502,.T.);
#24586=ORIENTED_EDGE('',*,*,#17503,.F.);
#24587=ORIENTED_EDGE('',*,*,#17268,.F.);
#24588=ORIENTED_EDGE('',*,*,#17504,.F.);
#24589=ORIENTED_EDGE('',*,*,#17505,.T.);
#24590=ORIENTED_EDGE('',*,*,#17506,.F.);
#24591=ORIENTED_EDGE('',*,*,#17271,.F.);
#24592=ORIENTED_EDGE('',*,*,#17507,.F.);
#24593=ORIENTED_EDGE('',*,*,#17508,.T.);
#24594=ORIENTED_EDGE('',*,*,#17509,.F.);
#24595=ORIENTED_EDGE('',*,*,#17274,.F.);
#24596=ORIENTED_EDGE('',*,*,#17510,.F.);
#24597=ORIENTED_EDGE('',*,*,#17511,.T.);
#24598=ORIENTED_EDGE('',*,*,#17512,.F.);
#24599=ORIENTED_EDGE('',*,*,#17277,.F.);
#24600=ORIENTED_EDGE('',*,*,#17513,.F.);
#24601=ORIENTED_EDGE('',*,*,#17514,.T.);
#24602=ORIENTED_EDGE('',*,*,#17515,.F.);
#24603=ORIENTED_EDGE('',*,*,#17280,.F.);
#24604=ORIENTED_EDGE('',*,*,#17516,.F.);
#24605=ORIENTED_EDGE('',*,*,#17517,.T.);
#24606=ORIENTED_EDGE('',*,*,#17518,.F.);
#24607=ORIENTED_EDGE('',*,*,#17283,.F.);
#24608=ORIENTED_EDGE('',*,*,#17519,.F.);
#24609=ORIENTED_EDGE('',*,*,#17520,.T.);
#24610=ORIENTED_EDGE('',*,*,#17521,.F.);
#24611=ORIENTED_EDGE('',*,*,#17286,.F.);
#24612=ORIENTED_EDGE('',*,*,#17522,.F.);
#24613=ORIENTED_EDGE('',*,*,#17523,.T.);
#24614=ORIENTED_EDGE('',*,*,#17524,.F.);
#24615=ORIENTED_EDGE('',*,*,#17289,.F.);
#24616=ORIENTED_EDGE('',*,*,#17525,.F.);
#24617=ORIENTED_EDGE('',*,*,#17526,.T.);
#24618=ORIENTED_EDGE('',*,*,#17527,.F.);
#24619=ORIENTED_EDGE('',*,*,#17292,.F.);
#24620=ORIENTED_EDGE('',*,*,#17528,.F.);
#24621=ORIENTED_EDGE('',*,*,#17529,.T.);
#24622=ORIENTED_EDGE('',*,*,#17530,.F.);
#24623=ORIENTED_EDGE('',*,*,#17295,.F.);
#24624=ORIENTED_EDGE('',*,*,#17531,.F.);
#24625=ORIENTED_EDGE('',*,*,#17532,.T.);
#24626=ORIENTED_EDGE('',*,*,#17533,.F.);
#24627=ORIENTED_EDGE('',*,*,#17298,.F.);
#24628=ORIENTED_EDGE('',*,*,#17534,.F.);
#24629=ORIENTED_EDGE('',*,*,#17535,.T.);
#24630=ORIENTED_EDGE('',*,*,#17536,.F.);
#24631=ORIENTED_EDGE('',*,*,#17301,.F.);
#24632=ORIENTED_EDGE('',*,*,#17537,.F.);
#24633=ORIENTED_EDGE('',*,*,#17538,.T.);
#24634=ORIENTED_EDGE('',*,*,#17539,.F.);
#24635=ORIENTED_EDGE('',*,*,#17304,.F.);
#24636=ORIENTED_EDGE('',*,*,#17540,.F.);
#24637=ORIENTED_EDGE('',*,*,#17541,.T.);
#24638=ORIENTED_EDGE('',*,*,#17542,.F.);
#24639=ORIENTED_EDGE('',*,*,#17307,.F.);
#24640=ORIENTED_EDGE('',*,*,#17543,.F.);
#24641=ORIENTED_EDGE('',*,*,#17544,.T.);
#24642=ORIENTED_EDGE('',*,*,#17545,.F.);
#24643=ORIENTED_EDGE('',*,*,#17310,.F.);
#24644=ORIENTED_EDGE('',*,*,#17546,.F.);
#24645=ORIENTED_EDGE('',*,*,#17547,.T.);
#24646=ORIENTED_EDGE('',*,*,#17548,.F.);
#24647=ORIENTED_EDGE('',*,*,#17313,.F.);
#24648=ORIENTED_EDGE('',*,*,#17549,.F.);
#24649=ORIENTED_EDGE('',*,*,#17550,.T.);
#24650=ORIENTED_EDGE('',*,*,#17551,.F.);
#24651=ORIENTED_EDGE('',*,*,#17316,.F.);
#24652=ORIENTED_EDGE('',*,*,#17552,.F.);
#24653=ORIENTED_EDGE('',*,*,#17553,.T.);
#24654=ORIENTED_EDGE('',*,*,#17554,.F.);
#24655=ORIENTED_EDGE('',*,*,#17555,.T.);
#24656=ORIENTED_EDGE('',*,*,#17556,.F.);
#24657=ORIENTED_EDGE('',*,*,#17318,.F.);
#24658=ORIENTED_EDGE('',*,*,#17557,.F.);
#24659=ORIENTED_EDGE('',*,*,#17558,.T.);
#24660=ORIENTED_EDGE('',*,*,#17559,.F.);
#24661=ORIENTED_EDGE('',*,*,#17321,.F.);
#24662=ORIENTED_EDGE('',*,*,#17560,.F.);
#24663=ORIENTED_EDGE('',*,*,#17561,.T.);
#24664=ORIENTED_EDGE('',*,*,#17562,.F.);
#24665=ORIENTED_EDGE('',*,*,#17324,.F.);
#24666=ORIENTED_EDGE('',*,*,#17563,.F.);
#24667=ORIENTED_EDGE('',*,*,#17564,.T.);
#24668=ORIENTED_EDGE('',*,*,#17565,.F.);
#24669=ORIENTED_EDGE('',*,*,#17327,.F.);
#24670=ORIENTED_EDGE('',*,*,#17566,.F.);
#24671=ORIENTED_EDGE('',*,*,#17567,.T.);
#24672=ORIENTED_EDGE('',*,*,#17568,.F.);
#24673=ORIENTED_EDGE('',*,*,#17330,.F.);
#24674=ORIENTED_EDGE('',*,*,#17569,.F.);
#24675=ORIENTED_EDGE('',*,*,#17570,.T.);
#24676=ORIENTED_EDGE('',*,*,#17571,.F.);
#24677=ORIENTED_EDGE('',*,*,#17333,.F.);
#24678=ORIENTED_EDGE('',*,*,#17572,.F.);
#24679=ORIENTED_EDGE('',*,*,#17573,.T.);
#24680=ORIENTED_EDGE('',*,*,#17574,.F.);
#24681=ORIENTED_EDGE('',*,*,#17336,.F.);
#24682=ORIENTED_EDGE('',*,*,#17575,.F.);
#24683=ORIENTED_EDGE('',*,*,#17576,.T.);
#24684=ORIENTED_EDGE('',*,*,#17577,.F.);
#24685=ORIENTED_EDGE('',*,*,#17339,.F.);
#24686=ORIENTED_EDGE('',*,*,#17578,.F.);
#24687=ORIENTED_EDGE('',*,*,#17579,.T.);
#24688=ORIENTED_EDGE('',*,*,#17580,.F.);
#24689=ORIENTED_EDGE('',*,*,#17342,.F.);
#24690=ORIENTED_EDGE('',*,*,#17581,.F.);
#24691=ORIENTED_EDGE('',*,*,#17582,.T.);
#24692=ORIENTED_EDGE('',*,*,#17583,.F.);
#24693=ORIENTED_EDGE('',*,*,#17345,.F.);
#24694=ORIENTED_EDGE('',*,*,#17584,.F.);
#24695=ORIENTED_EDGE('',*,*,#17585,.T.);
#24696=ORIENTED_EDGE('',*,*,#17586,.F.);
#24697=ORIENTED_EDGE('',*,*,#17348,.F.);
#24698=ORIENTED_EDGE('',*,*,#17587,.F.);
#24699=ORIENTED_EDGE('',*,*,#17588,.T.);
#24700=ORIENTED_EDGE('',*,*,#17589,.F.);
#24701=ORIENTED_EDGE('',*,*,#17351,.F.);
#24702=ORIENTED_EDGE('',*,*,#17590,.F.);
#24703=ORIENTED_EDGE('',*,*,#17591,.T.);
#24704=ORIENTED_EDGE('',*,*,#17592,.F.);
#24705=ORIENTED_EDGE('',*,*,#17354,.F.);
#24706=ORIENTED_EDGE('',*,*,#17593,.F.);
#24707=ORIENTED_EDGE('',*,*,#17594,.T.);
#24708=ORIENTED_EDGE('',*,*,#17595,.F.);
#24709=ORIENTED_EDGE('',*,*,#17357,.F.);
#24710=ORIENTED_EDGE('',*,*,#17596,.F.);
#24711=ORIENTED_EDGE('',*,*,#17361,.F.);
#24712=ORIENTED_EDGE('',*,*,#17597,.F.);
#24713=ORIENTED_EDGE('',*,*,#17598,.T.);
#24714=ORIENTED_EDGE('',*,*,#17599,.F.);
#24715=ORIENTED_EDGE('',*,*,#16710,.T.);
#24716=ORIENTED_EDGE('',*,*,#17600,.F.);
#24717=ORIENTED_EDGE('',*,*,#17363,.F.);
#24718=ORIENTED_EDGE('',*,*,#17601,.F.);
#24719=ORIENTED_EDGE('',*,*,#17367,.F.);
#24720=ORIENTED_EDGE('',*,*,#17602,.F.);
#24721=ORIENTED_EDGE('',*,*,#16713,.T.);
#24722=ORIENTED_EDGE('',*,*,#17603,.F.);
#24723=ORIENTED_EDGE('',*,*,#17370,.F.);
#24724=ORIENTED_EDGE('',*,*,#17604,.F.);
#24725=ORIENTED_EDGE('',*,*,#16716,.T.);
#24726=ORIENTED_EDGE('',*,*,#17605,.F.);
#24727=ORIENTED_EDGE('',*,*,#17373,.F.);
#24728=ORIENTED_EDGE('',*,*,#17606,.F.);
#24729=ORIENTED_EDGE('',*,*,#16719,.T.);
#24730=ORIENTED_EDGE('',*,*,#17607,.F.);
#24731=ORIENTED_EDGE('',*,*,#17376,.F.);
#24732=ORIENTED_EDGE('',*,*,#17608,.F.);
#24733=ORIENTED_EDGE('',*,*,#16722,.T.);
#24734=ORIENTED_EDGE('',*,*,#17609,.F.);
#24735=ORIENTED_EDGE('',*,*,#17379,.F.);
#24736=ORIENTED_EDGE('',*,*,#17610,.F.);
#24737=ORIENTED_EDGE('',*,*,#16725,.T.);
#24738=ORIENTED_EDGE('',*,*,#17611,.F.);
#24739=ORIENTED_EDGE('',*,*,#17382,.F.);
#24740=ORIENTED_EDGE('',*,*,#17612,.F.);
#24741=ORIENTED_EDGE('',*,*,#16728,.T.);
#24742=ORIENTED_EDGE('',*,*,#17613,.F.);
#24743=ORIENTED_EDGE('',*,*,#17385,.F.);
#24744=ORIENTED_EDGE('',*,*,#17614,.F.);
#24745=ORIENTED_EDGE('',*,*,#16732,.T.);
#24746=ORIENTED_EDGE('',*,*,#17615,.F.);
#24747=ORIENTED_EDGE('',*,*,#17388,.F.);
#24748=ORIENTED_EDGE('',*,*,#17616,.F.);
#24749=ORIENTED_EDGE('',*,*,#16736,.T.);
#24750=ORIENTED_EDGE('',*,*,#17617,.F.);
#24751=ORIENTED_EDGE('',*,*,#17391,.F.);
#24752=ORIENTED_EDGE('',*,*,#17618,.F.);
#24753=ORIENTED_EDGE('',*,*,#16740,.T.);
#24754=ORIENTED_EDGE('',*,*,#17619,.F.);
#24755=ORIENTED_EDGE('',*,*,#17394,.F.);
#24756=ORIENTED_EDGE('',*,*,#17620,.F.);
#24757=ORIENTED_EDGE('',*,*,#16744,.T.);
#24758=ORIENTED_EDGE('',*,*,#17621,.F.);
#24759=ORIENTED_EDGE('',*,*,#17397,.F.);
#24760=ORIENTED_EDGE('',*,*,#17622,.F.);
#24761=ORIENTED_EDGE('',*,*,#16748,.T.);
#24762=ORIENTED_EDGE('',*,*,#17623,.F.);
#24763=ORIENTED_EDGE('',*,*,#17400,.F.);
#24764=ORIENTED_EDGE('',*,*,#17624,.F.);
#24765=ORIENTED_EDGE('',*,*,#16752,.T.);
#24766=ORIENTED_EDGE('',*,*,#17625,.F.);
#24767=ORIENTED_EDGE('',*,*,#17403,.F.);
#24768=ORIENTED_EDGE('',*,*,#17626,.F.);
#24769=ORIENTED_EDGE('',*,*,#16756,.T.);
#24770=ORIENTED_EDGE('',*,*,#17627,.F.);
#24771=ORIENTED_EDGE('',*,*,#17406,.F.);
#24772=ORIENTED_EDGE('',*,*,#17628,.F.);
#24773=ORIENTED_EDGE('',*,*,#16760,.T.);
#24774=ORIENTED_EDGE('',*,*,#17629,.F.);
#24775=ORIENTED_EDGE('',*,*,#17409,.F.);
#24776=ORIENTED_EDGE('',*,*,#17630,.F.);
#24777=ORIENTED_EDGE('',*,*,#16764,.T.);
#24778=ORIENTED_EDGE('',*,*,#17631,.F.);
#24779=ORIENTED_EDGE('',*,*,#17412,.F.);
#24780=ORIENTED_EDGE('',*,*,#17632,.F.);
#24781=ORIENTED_EDGE('',*,*,#16768,.T.);
#24782=ORIENTED_EDGE('',*,*,#17633,.F.);
#24783=ORIENTED_EDGE('',*,*,#17415,.F.);
#24784=ORIENTED_EDGE('',*,*,#17634,.F.);
#24785=ORIENTED_EDGE('',*,*,#16772,.T.);
#24786=ORIENTED_EDGE('',*,*,#17635,.F.);
#24787=ORIENTED_EDGE('',*,*,#17418,.F.);
#24788=ORIENTED_EDGE('',*,*,#17636,.F.);
#24789=ORIENTED_EDGE('',*,*,#16776,.T.);
#24790=ORIENTED_EDGE('',*,*,#17637,.F.);
#24791=ORIENTED_EDGE('',*,*,#17421,.F.);
#24792=ORIENTED_EDGE('',*,*,#17638,.F.);
#24793=ORIENTED_EDGE('',*,*,#16780,.T.);
#24794=ORIENTED_EDGE('',*,*,#17639,.F.);
#24795=ORIENTED_EDGE('',*,*,#17424,.F.);
#24796=ORIENTED_EDGE('',*,*,#17640,.F.);
#24797=ORIENTED_EDGE('',*,*,#16784,.T.);
#24798=ORIENTED_EDGE('',*,*,#17641,.F.);
#24799=ORIENTED_EDGE('',*,*,#17427,.F.);
#24800=ORIENTED_EDGE('',*,*,#17642,.F.);
#24801=ORIENTED_EDGE('',*,*,#16788,.T.);
#24802=ORIENTED_EDGE('',*,*,#17643,.F.);
#24803=ORIENTED_EDGE('',*,*,#17430,.F.);
#24804=ORIENTED_EDGE('',*,*,#17644,.F.);
#24805=ORIENTED_EDGE('',*,*,#16792,.T.);
#24806=ORIENTED_EDGE('',*,*,#17645,.F.);
#24807=ORIENTED_EDGE('',*,*,#17433,.F.);
#24808=ORIENTED_EDGE('',*,*,#17646,.F.);
#24809=ORIENTED_EDGE('',*,*,#16796,.T.);
#24810=ORIENTED_EDGE('',*,*,#17647,.F.);
#24811=ORIENTED_EDGE('',*,*,#17436,.F.);
#24812=ORIENTED_EDGE('',*,*,#17648,.F.);
#24813=ORIENTED_EDGE('',*,*,#16800,.T.);
#24814=ORIENTED_EDGE('',*,*,#17649,.F.);
#24815=ORIENTED_EDGE('',*,*,#17439,.F.);
#24816=ORIENTED_EDGE('',*,*,#17650,.F.);
#24817=ORIENTED_EDGE('',*,*,#16804,.T.);
#24818=ORIENTED_EDGE('',*,*,#17651,.F.);
#24819=ORIENTED_EDGE('',*,*,#17442,.F.);
#24820=ORIENTED_EDGE('',*,*,#17652,.F.);
#24821=ORIENTED_EDGE('',*,*,#16503,.T.);
#24822=ORIENTED_EDGE('',*,*,#17653,.F.);
#24823=ORIENTED_EDGE('',*,*,#17445,.F.);
#24824=ORIENTED_EDGE('',*,*,#17654,.F.);
#24825=ORIENTED_EDGE('',*,*,#16507,.T.);
#24826=ORIENTED_EDGE('',*,*,#17655,.F.);
#24827=ORIENTED_EDGE('',*,*,#17448,.F.);
#24828=ORIENTED_EDGE('',*,*,#17656,.F.);
#24829=ORIENTED_EDGE('',*,*,#16511,.T.);
#24830=ORIENTED_EDGE('',*,*,#17657,.F.);
#24831=ORIENTED_EDGE('',*,*,#17451,.F.);
#24832=ORIENTED_EDGE('',*,*,#17658,.F.);
#24833=ORIENTED_EDGE('',*,*,#16515,.T.);
#24834=ORIENTED_EDGE('',*,*,#17659,.F.);
#24835=ORIENTED_EDGE('',*,*,#17454,.F.);
#24836=ORIENTED_EDGE('',*,*,#17660,.F.);
#24837=ORIENTED_EDGE('',*,*,#16519,.T.);
#24838=ORIENTED_EDGE('',*,*,#17661,.F.);
#24839=ORIENTED_EDGE('',*,*,#17457,.F.);
#24840=ORIENTED_EDGE('',*,*,#17662,.F.);
#24841=ORIENTED_EDGE('',*,*,#16523,.T.);
#24842=ORIENTED_EDGE('',*,*,#17663,.F.);
#24843=ORIENTED_EDGE('',*,*,#17460,.F.);
#24844=ORIENTED_EDGE('',*,*,#17664,.F.);
#24845=ORIENTED_EDGE('',*,*,#16527,.T.);
#24846=ORIENTED_EDGE('',*,*,#17665,.F.);
#24847=ORIENTED_EDGE('',*,*,#17463,.F.);
#24848=ORIENTED_EDGE('',*,*,#17666,.F.);
#24849=ORIENTED_EDGE('',*,*,#16531,.T.);
#24850=ORIENTED_EDGE('',*,*,#17667,.F.);
#24851=ORIENTED_EDGE('',*,*,#17466,.F.);
#24852=ORIENTED_EDGE('',*,*,#17668,.F.);
#24853=ORIENTED_EDGE('',*,*,#16535,.T.);
#24854=ORIENTED_EDGE('',*,*,#17669,.F.);
#24855=ORIENTED_EDGE('',*,*,#17469,.F.);
#24856=ORIENTED_EDGE('',*,*,#17670,.F.);
#24857=ORIENTED_EDGE('',*,*,#16539,.T.);
#24858=ORIENTED_EDGE('',*,*,#17671,.F.);
#24859=ORIENTED_EDGE('',*,*,#17472,.F.);
#24860=ORIENTED_EDGE('',*,*,#17672,.F.);
#24861=ORIENTED_EDGE('',*,*,#16543,.T.);
#24862=ORIENTED_EDGE('',*,*,#17673,.F.);
#24863=ORIENTED_EDGE('',*,*,#17475,.F.);
#24864=ORIENTED_EDGE('',*,*,#17674,.F.);
#24865=ORIENTED_EDGE('',*,*,#16547,.T.);
#24866=ORIENTED_EDGE('',*,*,#17675,.F.);
#24867=ORIENTED_EDGE('',*,*,#17478,.F.);
#24868=ORIENTED_EDGE('',*,*,#17676,.F.);
#24869=ORIENTED_EDGE('',*,*,#16551,.T.);
#24870=ORIENTED_EDGE('',*,*,#17677,.F.);
#24871=ORIENTED_EDGE('',*,*,#17481,.F.);
#24872=ORIENTED_EDGE('',*,*,#17678,.F.);
#24873=ORIENTED_EDGE('',*,*,#16555,.T.);
#24874=ORIENTED_EDGE('',*,*,#17679,.F.);
#24875=ORIENTED_EDGE('',*,*,#17484,.F.);
#24876=ORIENTED_EDGE('',*,*,#17680,.F.);
#24877=ORIENTED_EDGE('',*,*,#16559,.T.);
#24878=ORIENTED_EDGE('',*,*,#17681,.F.);
#24879=ORIENTED_EDGE('',*,*,#17487,.F.);
#24880=ORIENTED_EDGE('',*,*,#17682,.F.);
#24881=ORIENTED_EDGE('',*,*,#16563,.T.);
#24882=ORIENTED_EDGE('',*,*,#17683,.F.);
#24883=ORIENTED_EDGE('',*,*,#17490,.F.);
#24884=ORIENTED_EDGE('',*,*,#17684,.F.);
#24885=ORIENTED_EDGE('',*,*,#16567,.T.);
#24886=ORIENTED_EDGE('',*,*,#17685,.F.);
#24887=ORIENTED_EDGE('',*,*,#17493,.F.);
#24888=ORIENTED_EDGE('',*,*,#17686,.F.);
#24889=ORIENTED_EDGE('',*,*,#16571,.T.);
#24890=ORIENTED_EDGE('',*,*,#17687,.F.);
#24891=ORIENTED_EDGE('',*,*,#17496,.F.);
#24892=ORIENTED_EDGE('',*,*,#17688,.F.);
#24893=ORIENTED_EDGE('',*,*,#16575,.T.);
#24894=ORIENTED_EDGE('',*,*,#17689,.F.);
#24895=ORIENTED_EDGE('',*,*,#17499,.F.);
#24896=ORIENTED_EDGE('',*,*,#17690,.F.);
#24897=ORIENTED_EDGE('',*,*,#16579,.T.);
#24898=ORIENTED_EDGE('',*,*,#17691,.F.);
#24899=ORIENTED_EDGE('',*,*,#17502,.F.);
#24900=ORIENTED_EDGE('',*,*,#17692,.F.);
#24901=ORIENTED_EDGE('',*,*,#16583,.T.);
#24902=ORIENTED_EDGE('',*,*,#17693,.F.);
#24903=ORIENTED_EDGE('',*,*,#17505,.F.);
#24904=ORIENTED_EDGE('',*,*,#17694,.F.);
#24905=ORIENTED_EDGE('',*,*,#16587,.T.);
#24906=ORIENTED_EDGE('',*,*,#17695,.F.);
#24907=ORIENTED_EDGE('',*,*,#17508,.F.);
#24908=ORIENTED_EDGE('',*,*,#17696,.F.);
#24909=ORIENTED_EDGE('',*,*,#16591,.T.);
#24910=ORIENTED_EDGE('',*,*,#17697,.F.);
#24911=ORIENTED_EDGE('',*,*,#17511,.F.);
#24912=ORIENTED_EDGE('',*,*,#17698,.F.);
#24913=ORIENTED_EDGE('',*,*,#16595,.T.);
#24914=ORIENTED_EDGE('',*,*,#17699,.F.);
#24915=ORIENTED_EDGE('',*,*,#17514,.F.);
#24916=ORIENTED_EDGE('',*,*,#17700,.F.);
#24917=ORIENTED_EDGE('',*,*,#16599,.T.);
#24918=ORIENTED_EDGE('',*,*,#17701,.F.);
#24919=ORIENTED_EDGE('',*,*,#17517,.F.);
#24920=ORIENTED_EDGE('',*,*,#17702,.F.);
#24921=ORIENTED_EDGE('',*,*,#16603,.T.);
#24922=ORIENTED_EDGE('',*,*,#17703,.F.);
#24923=ORIENTED_EDGE('',*,*,#17520,.F.);
#24924=ORIENTED_EDGE('',*,*,#17704,.F.);
#24925=ORIENTED_EDGE('',*,*,#16607,.T.);
#24926=ORIENTED_EDGE('',*,*,#17705,.F.);
#24927=ORIENTED_EDGE('',*,*,#17523,.F.);
#24928=ORIENTED_EDGE('',*,*,#17706,.F.);
#24929=ORIENTED_EDGE('',*,*,#16611,.T.);
#24930=ORIENTED_EDGE('',*,*,#17707,.F.);
#24931=ORIENTED_EDGE('',*,*,#17526,.F.);
#24932=ORIENTED_EDGE('',*,*,#17708,.F.);
#24933=ORIENTED_EDGE('',*,*,#16615,.T.);
#24934=ORIENTED_EDGE('',*,*,#17709,.F.);
#24935=ORIENTED_EDGE('',*,*,#17529,.F.);
#24936=ORIENTED_EDGE('',*,*,#17710,.F.);
#24937=ORIENTED_EDGE('',*,*,#16619,.T.);
#24938=ORIENTED_EDGE('',*,*,#17711,.F.);
#24939=ORIENTED_EDGE('',*,*,#17532,.F.);
#24940=ORIENTED_EDGE('',*,*,#17712,.F.);
#24941=ORIENTED_EDGE('',*,*,#16623,.T.);
#24942=ORIENTED_EDGE('',*,*,#17713,.F.);
#24943=ORIENTED_EDGE('',*,*,#17535,.F.);
#24944=ORIENTED_EDGE('',*,*,#17714,.F.);
#24945=ORIENTED_EDGE('',*,*,#16627,.T.);
#24946=ORIENTED_EDGE('',*,*,#17715,.F.);
#24947=ORIENTED_EDGE('',*,*,#17538,.F.);
#24948=ORIENTED_EDGE('',*,*,#17716,.F.);
#24949=ORIENTED_EDGE('',*,*,#16631,.T.);
#24950=ORIENTED_EDGE('',*,*,#17717,.F.);
#24951=ORIENTED_EDGE('',*,*,#17541,.F.);
#24952=ORIENTED_EDGE('',*,*,#17718,.F.);
#24953=ORIENTED_EDGE('',*,*,#16635,.T.);
#24954=ORIENTED_EDGE('',*,*,#17719,.F.);
#24955=ORIENTED_EDGE('',*,*,#17544,.F.);
#24956=ORIENTED_EDGE('',*,*,#17720,.F.);
#24957=ORIENTED_EDGE('',*,*,#16639,.T.);
#24958=ORIENTED_EDGE('',*,*,#17721,.F.);
#24959=ORIENTED_EDGE('',*,*,#17547,.F.);
#24960=ORIENTED_EDGE('',*,*,#17722,.F.);
#24961=ORIENTED_EDGE('',*,*,#16643,.T.);
#24962=ORIENTED_EDGE('',*,*,#17723,.F.);
#24963=ORIENTED_EDGE('',*,*,#17550,.F.);
#24964=ORIENTED_EDGE('',*,*,#17724,.F.);
#24965=ORIENTED_EDGE('',*,*,#16647,.T.);
#24966=ORIENTED_EDGE('',*,*,#17725,.F.);
#24967=ORIENTED_EDGE('',*,*,#17553,.F.);
#24968=ORIENTED_EDGE('',*,*,#17726,.F.);
#24969=ORIENTED_EDGE('',*,*,#16651,.T.);
#24970=ORIENTED_EDGE('',*,*,#17727,.F.);
#24971=ORIENTED_EDGE('',*,*,#16707,.T.);
#24972=ORIENTED_EDGE('',*,*,#17728,.F.);
#24973=ORIENTED_EDGE('',*,*,#17555,.F.);
#24974=ORIENTED_EDGE('',*,*,#17729,.F.);
#24975=ORIENTED_EDGE('',*,*,#16704,.T.);
#24976=ORIENTED_EDGE('',*,*,#17730,.F.);
#24977=ORIENTED_EDGE('',*,*,#17558,.F.);
#24978=ORIENTED_EDGE('',*,*,#17731,.F.);
#24979=ORIENTED_EDGE('',*,*,#16701,.T.);
#24980=ORIENTED_EDGE('',*,*,#17732,.F.);
#24981=ORIENTED_EDGE('',*,*,#17561,.F.);
#24982=ORIENTED_EDGE('',*,*,#17733,.F.);
#24983=ORIENTED_EDGE('',*,*,#16698,.T.);
#24984=ORIENTED_EDGE('',*,*,#17734,.F.);
#24985=ORIENTED_EDGE('',*,*,#17564,.F.);
#24986=ORIENTED_EDGE('',*,*,#17735,.F.);
#24987=ORIENTED_EDGE('',*,*,#16695,.T.);
#24988=ORIENTED_EDGE('',*,*,#17736,.F.);
#24989=ORIENTED_EDGE('',*,*,#17567,.F.);
#24990=ORIENTED_EDGE('',*,*,#17737,.F.);
#24991=ORIENTED_EDGE('',*,*,#16692,.T.);
#24992=ORIENTED_EDGE('',*,*,#17738,.F.);
#24993=ORIENTED_EDGE('',*,*,#17570,.F.);
#24994=ORIENTED_EDGE('',*,*,#17739,.F.);
#24995=ORIENTED_EDGE('',*,*,#16689,.T.);
#24996=ORIENTED_EDGE('',*,*,#17740,.F.);
#24997=ORIENTED_EDGE('',*,*,#17573,.F.);
#24998=ORIENTED_EDGE('',*,*,#17741,.F.);
#24999=ORIENTED_EDGE('',*,*,#16686,.T.);
#25000=ORIENTED_EDGE('',*,*,#17742,.F.);
#25001=ORIENTED_EDGE('',*,*,#17576,.F.);
#25002=ORIENTED_EDGE('',*,*,#17743,.F.);
#25003=ORIENTED_EDGE('',*,*,#16683,.T.);
#25004=ORIENTED_EDGE('',*,*,#17744,.F.);
#25005=ORIENTED_EDGE('',*,*,#17579,.F.);
#25006=ORIENTED_EDGE('',*,*,#17745,.F.);
#25007=ORIENTED_EDGE('',*,*,#16679,.T.);
#25008=ORIENTED_EDGE('',*,*,#17746,.F.);
#25009=ORIENTED_EDGE('',*,*,#17582,.F.);
#25010=ORIENTED_EDGE('',*,*,#17747,.F.);
#25011=ORIENTED_EDGE('',*,*,#16675,.T.);
#25012=ORIENTED_EDGE('',*,*,#17748,.F.);
#25013=ORIENTED_EDGE('',*,*,#17585,.F.);
#25014=ORIENTED_EDGE('',*,*,#17749,.F.);
#25015=ORIENTED_EDGE('',*,*,#16671,.T.);
#25016=ORIENTED_EDGE('',*,*,#17750,.F.);
#25017=ORIENTED_EDGE('',*,*,#17588,.F.);
#25018=ORIENTED_EDGE('',*,*,#17751,.F.);
#25019=ORIENTED_EDGE('',*,*,#16667,.T.);
#25020=ORIENTED_EDGE('',*,*,#17752,.F.);
#25021=ORIENTED_EDGE('',*,*,#17591,.F.);
#25022=ORIENTED_EDGE('',*,*,#17753,.F.);
#25023=ORIENTED_EDGE('',*,*,#16663,.T.);
#25024=ORIENTED_EDGE('',*,*,#17754,.F.);
#25025=ORIENTED_EDGE('',*,*,#17594,.F.);
#25026=ORIENTED_EDGE('',*,*,#17755,.F.);
#25027=ORIENTED_EDGE('',*,*,#17598,.F.);
#25028=ORIENTED_EDGE('',*,*,#17756,.F.);
#25029=ORIENTED_EDGE('',*,*,#16655,.T.);
#25030=ORIENTED_EDGE('',*,*,#16333,.T.);
#25031=ORIENTED_EDGE('',*,*,#16423,.T.);
#25032=ORIENTED_EDGE('',*,*,#16330,.T.);
#25033=ORIENTED_EDGE('',*,*,#17121,.T.);
#25034=ORIENTED_EDGE('',*,*,#17124,.F.);
#25035=ORIENTED_EDGE('',*,*,#17757,.F.);
#25036=ORIENTED_EDGE('',*,*,#16810,.F.);
#25037=ORIENTED_EDGE('',*,*,#17758,.F.);
#25038=ORIENTED_EDGE('',*,*,#17759,.T.);
#25039=ORIENTED_EDGE('',*,*,#17760,.F.);
#25040=ORIENTED_EDGE('',*,*,#17759,.F.);
#25041=ORIENTED_EDGE('',*,*,#17761,.F.);
#25042=ORIENTED_EDGE('',*,*,#17762,.T.);
#25043=ORIENTED_EDGE('',*,*,#17763,.F.);
#25044=ORIENTED_EDGE('',*,*,#17762,.F.);
#25045=ORIENTED_EDGE('',*,*,#17764,.F.);
#25046=ORIENTED_EDGE('',*,*,#16659,.T.);
#25047=ORIENTED_EDGE('',*,*,#16500,.F.);
#25048=ORIENTED_EDGE('',*,*,#16497,.F.);
#25049=ORIENTED_EDGE('',*,*,#17765,.T.);
#25050=ORIENTED_EDGE('',*,*,#17766,.T.);
#25051=ORIENTED_EDGE('',*,*,#17767,.T.);
#25052=ORIENTED_EDGE('',*,*,#17768,.T.);
#25053=ORIENTED_EDGE('',*,*,#17769,.T.);
#25054=ORIENTED_EDGE('',*,*,#17770,.T.);
#25055=ORIENTED_EDGE('',*,*,#17771,.T.);
#25056=ORIENTED_EDGE('',*,*,#16492,.T.);
#25057=ORIENTED_EDGE('',*,*,#17772,.F.);
#25058=ORIENTED_EDGE('',*,*,#17766,.F.);
#25059=ORIENTED_EDGE('',*,*,#17772,.T.);
#25060=ORIENTED_EDGE('',*,*,#16491,.T.);
#25061=ORIENTED_EDGE('',*,*,#17773,.F.);
#25062=ORIENTED_EDGE('',*,*,#17767,.F.);
#25063=ORIENTED_EDGE('',*,*,#17773,.T.);
#25064=ORIENTED_EDGE('',*,*,#16490,.T.);
#25065=ORIENTED_EDGE('',*,*,#17774,.F.);
#25066=ORIENTED_EDGE('',*,*,#17768,.F.);
#25067=ORIENTED_EDGE('',*,*,#17774,.T.);
#25068=ORIENTED_EDGE('',*,*,#16489,.T.);
#25069=ORIENTED_EDGE('',*,*,#16495,.T.);
#25070=ORIENTED_EDGE('',*,*,#17775,.F.);
#25071=ORIENTED_EDGE('',*,*,#17769,.F.);
#25072=ORIENTED_EDGE('',*,*,#17775,.T.);
#25073=ORIENTED_EDGE('',*,*,#16494,.T.);
#25074=ORIENTED_EDGE('',*,*,#17776,.F.);
#25075=ORIENTED_EDGE('',*,*,#17770,.F.);
#25076=ORIENTED_EDGE('',*,*,#17776,.T.);
#25077=ORIENTED_EDGE('',*,*,#16493,.T.);
#25078=ORIENTED_EDGE('',*,*,#17771,.F.);
#25079=ORIENTED_EDGE('',*,*,#17765,.F.);
#25080=ORIENTED_EDGE('',*,*,#17777,.F.);
#25081=ORIENTED_EDGE('',*,*,#16421,.F.);
#25082=ORIENTED_EDGE('',*,*,#16420,.F.);
#25083=ORIENTED_EDGE('',*,*,#16417,.F.);
#25084=ORIENTED_EDGE('',*,*,#16414,.F.);
#25085=ORIENTED_EDGE('',*,*,#16411,.F.);
#25086=ORIENTED_EDGE('',*,*,#16408,.F.);
#25087=ORIENTED_EDGE('',*,*,#16405,.F.);
#25088=ORIENTED_EDGE('',*,*,#16402,.F.);
#25089=ORIENTED_EDGE('',*,*,#16399,.F.);
#25090=ORIENTED_EDGE('',*,*,#16396,.F.);
#25091=ORIENTED_EDGE('',*,*,#16393,.F.);
#25092=ORIENTED_EDGE('',*,*,#16390,.F.);
#25093=ORIENTED_EDGE('',*,*,#16387,.F.);
#25094=ORIENTED_EDGE('',*,*,#16384,.F.);
#25095=ORIENTED_EDGE('',*,*,#16381,.F.);
#25096=ORIENTED_EDGE('',*,*,#16378,.F.);
#25097=ORIENTED_EDGE('',*,*,#16375,.F.);
#25098=ORIENTED_EDGE('',*,*,#16372,.F.);
#25099=ORIENTED_EDGE('',*,*,#16369,.F.);
#25100=ORIENTED_EDGE('',*,*,#16366,.F.);
#25101=ORIENTED_EDGE('',*,*,#16363,.F.);
#25102=ORIENTED_EDGE('',*,*,#16360,.F.);
#25103=ORIENTED_EDGE('',*,*,#16357,.F.);
#25104=ORIENTED_EDGE('',*,*,#16354,.F.);
#25105=ORIENTED_EDGE('',*,*,#16351,.F.);
#25106=ORIENTED_EDGE('',*,*,#16348,.F.);
#25107=ORIENTED_EDGE('',*,*,#16345,.F.);
#25108=ORIENTED_EDGE('',*,*,#16342,.F.);
#25109=ORIENTED_EDGE('',*,*,#16339,.F.);
#25110=ORIENTED_EDGE('',*,*,#16336,.F.);
#25111=ORIENTED_EDGE('',*,*,#16329,.F.);
#25112=ORIENTED_EDGE('',*,*,#16426,.F.);
#25113=ORIENTED_EDGE('',*,*,#16427,.T.);
#25114=ORIENTED_EDGE('',*,*,#16327,.T.);
#25115=ORIENTED_EDGE('',*,*,#16324,.T.);
#25116=ORIENTED_EDGE('',*,*,#16321,.T.);
#25117=ORIENTED_EDGE('',*,*,#16318,.T.);
#25118=ORIENTED_EDGE('',*,*,#16315,.T.);
#25119=ORIENTED_EDGE('',*,*,#16312,.T.);
#25120=ORIENTED_EDGE('',*,*,#16309,.T.);
#25121=ORIENTED_EDGE('',*,*,#16306,.T.);
#25122=ORIENTED_EDGE('',*,*,#16303,.T.);
#25123=ORIENTED_EDGE('',*,*,#16300,.T.);
#25124=ORIENTED_EDGE('',*,*,#16297,.T.);
#25125=ORIENTED_EDGE('',*,*,#16294,.T.);
#25126=ORIENTED_EDGE('',*,*,#16291,.T.);
#25127=ORIENTED_EDGE('',*,*,#16288,.T.);
#25128=ORIENTED_EDGE('',*,*,#16285,.T.);
#25129=ORIENTED_EDGE('',*,*,#16282,.T.);
#25130=ORIENTED_EDGE('',*,*,#16279,.T.);
#25131=ORIENTED_EDGE('',*,*,#16276,.T.);
#25132=ORIENTED_EDGE('',*,*,#16273,.T.);
#25133=ORIENTED_EDGE('',*,*,#16270,.T.);
#25134=ORIENTED_EDGE('',*,*,#16267,.T.);
#25135=ORIENTED_EDGE('',*,*,#16264,.T.);
#25136=ORIENTED_EDGE('',*,*,#16261,.T.);
#25137=ORIENTED_EDGE('',*,*,#16258,.T.);
#25138=ORIENTED_EDGE('',*,*,#16255,.T.);
#25139=ORIENTED_EDGE('',*,*,#16252,.T.);
#25140=ORIENTED_EDGE('',*,*,#16249,.T.);
#25141=ORIENTED_EDGE('',*,*,#16246,.T.);
#25142=ORIENTED_EDGE('',*,*,#17778,.F.);
#25143=ORIENTED_EDGE('',*,*,#16242,.T.);
#25144=ORIENTED_EDGE('',*,*,#16248,.T.);
#25145=ORIENTED_EDGE('',*,*,#16251,.T.);
#25146=ORIENTED_EDGE('',*,*,#16254,.T.);
#25147=ORIENTED_EDGE('',*,*,#16257,.T.);
#25148=ORIENTED_EDGE('',*,*,#16260,.T.);
#25149=ORIENTED_EDGE('',*,*,#16263,.T.);
#25150=ORIENTED_EDGE('',*,*,#16266,.T.);
#25151=ORIENTED_EDGE('',*,*,#16269,.T.);
#25152=ORIENTED_EDGE('',*,*,#16272,.T.);
#25153=ORIENTED_EDGE('',*,*,#16275,.T.);
#25154=ORIENTED_EDGE('',*,*,#16278,.T.);
#25155=ORIENTED_EDGE('',*,*,#16281,.T.);
#25156=ORIENTED_EDGE('',*,*,#16284,.T.);
#25157=ORIENTED_EDGE('',*,*,#16287,.T.);
#25158=ORIENTED_EDGE('',*,*,#16290,.T.);
#25159=ORIENTED_EDGE('',*,*,#16293,.T.);
#25160=ORIENTED_EDGE('',*,*,#16296,.T.);
#25161=ORIENTED_EDGE('',*,*,#16299,.T.);
#25162=ORIENTED_EDGE('',*,*,#16302,.T.);
#25163=ORIENTED_EDGE('',*,*,#16305,.T.);
#25164=ORIENTED_EDGE('',*,*,#16308,.T.);
#25165=ORIENTED_EDGE('',*,*,#16311,.T.);
#25166=ORIENTED_EDGE('',*,*,#16314,.T.);
#25167=ORIENTED_EDGE('',*,*,#16317,.T.);
#25168=ORIENTED_EDGE('',*,*,#16320,.T.);
#25169=ORIENTED_EDGE('',*,*,#16323,.T.);
#25170=ORIENTED_EDGE('',*,*,#16326,.T.);
#25171=ORIENTED_EDGE('',*,*,#16428,.T.);
#25172=ORIENTED_EDGE('',*,*,#16424,.F.);
#25173=ORIENTED_EDGE('',*,*,#16332,.T.);
#25174=ORIENTED_EDGE('',*,*,#16335,.T.);
#25175=ORIENTED_EDGE('',*,*,#16338,.T.);
#25176=ORIENTED_EDGE('',*,*,#16341,.T.);
#25177=ORIENTED_EDGE('',*,*,#16344,.T.);
#25178=ORIENTED_EDGE('',*,*,#16347,.T.);
#25179=ORIENTED_EDGE('',*,*,#16350,.T.);
#25180=ORIENTED_EDGE('',*,*,#16353,.T.);
#25181=ORIENTED_EDGE('',*,*,#16356,.T.);
#25182=ORIENTED_EDGE('',*,*,#16359,.T.);
#25183=ORIENTED_EDGE('',*,*,#16362,.T.);
#25184=ORIENTED_EDGE('',*,*,#16365,.T.);
#25185=ORIENTED_EDGE('',*,*,#16368,.T.);
#25186=ORIENTED_EDGE('',*,*,#16371,.T.);
#25187=ORIENTED_EDGE('',*,*,#16374,.T.);
#25188=ORIENTED_EDGE('',*,*,#16377,.T.);
#25189=ORIENTED_EDGE('',*,*,#16380,.T.);
#25190=ORIENTED_EDGE('',*,*,#16383,.T.);
#25191=ORIENTED_EDGE('',*,*,#16386,.T.);
#25192=ORIENTED_EDGE('',*,*,#16389,.T.);
#25193=ORIENTED_EDGE('',*,*,#16392,.T.);
#25194=ORIENTED_EDGE('',*,*,#16395,.T.);
#25195=ORIENTED_EDGE('',*,*,#16398,.T.);
#25196=ORIENTED_EDGE('',*,*,#16401,.T.);
#25197=ORIENTED_EDGE('',*,*,#16404,.T.);
#25198=ORIENTED_EDGE('',*,*,#16407,.T.);
#25199=ORIENTED_EDGE('',*,*,#16410,.T.);
#25200=ORIENTED_EDGE('',*,*,#16413,.T.);
#25201=ORIENTED_EDGE('',*,*,#16416,.T.);
#25202=ORIENTED_EDGE('',*,*,#16419,.T.);
#25203=ORIENTED_EDGE('',*,*,#16422,.T.);
#25204=ORIENTED_EDGE('',*,*,#17777,.T.);
#25205=ORIENTED_EDGE('',*,*,#16245,.T.);
#25206=ORIENTED_EDGE('',*,*,#17778,.T.);
#25207=ORIENTED_EDGE('',*,*,#16809,.T.);
#25208=ORIENTED_EDGE('',*,*,#17779,.T.);
#25209=ORIENTED_EDGE('',*,*,#16660,.T.);
#25210=ORIENTED_EDGE('',*,*,#17764,.T.);
#25211=ORIENTED_EDGE('',*,*,#17761,.T.);
#25212=ORIENTED_EDGE('',*,*,#17758,.T.);
#25213=ORIENTED_EDGE('',*,*,#16808,.T.);
#25214=ORIENTED_EDGE('',*,*,#17113,.T.);
#25215=ORIENTED_EDGE('',*,*,#17780,.T.);
#25216=ORIENTED_EDGE('',*,*,#16661,.T.);
#25217=ORIENTED_EDGE('',*,*,#17779,.F.);
#25218=ORIENTED_EDGE('',*,*,#17112,.T.);
#25219=ORIENTED_EDGE('',*,*,#17358,.T.);
#25220=ORIENTED_EDGE('',*,*,#17595,.T.);
#25221=ORIENTED_EDGE('',*,*,#17754,.T.);
#25222=ORIENTED_EDGE('',*,*,#16662,.T.);
#25223=ORIENTED_EDGE('',*,*,#17780,.F.);
#25224=ORIENTED_EDGE('',*,*,#16813,.T.);
#25225=ORIENTED_EDGE('',*,*,#17781,.T.);
#25226=ORIENTED_EDGE('',*,*,#16656,.T.);
#25227=ORIENTED_EDGE('',*,*,#17756,.T.);
#25228=ORIENTED_EDGE('',*,*,#17597,.T.);
#25229=ORIENTED_EDGE('',*,*,#17360,.T.);
#25230=ORIENTED_EDGE('',*,*,#16812,.T.);
#25231=ORIENTED_EDGE('',*,*,#17782,.T.);
#25232=ORIENTED_EDGE('',*,*,#16657,.T.);
#25233=ORIENTED_EDGE('',*,*,#17781,.F.);
#25234=ORIENTED_EDGE('',*,*,#16811,.T.);
#25235=ORIENTED_EDGE('',*,*,#17757,.T.);
#25236=ORIENTED_EDGE('',*,*,#17760,.T.);
#25237=ORIENTED_EDGE('',*,*,#17763,.T.);
#25238=ORIENTED_EDGE('',*,*,#16658,.T.);
#25239=ORIENTED_EDGE('',*,*,#17782,.F.);
#25240=ORIENTED_EDGE('',*,*,#17110,.T.);
#25241=ORIENTED_EDGE('',*,*,#17783,.T.);
#25242=ORIENTED_EDGE('',*,*,#16664,.T.);
#25243=ORIENTED_EDGE('',*,*,#17753,.T.);
#25244=ORIENTED_EDGE('',*,*,#17593,.T.);
#25245=ORIENTED_EDGE('',*,*,#17356,.T.);
#25246=ORIENTED_EDGE('',*,*,#17109,.T.);
#25247=ORIENTED_EDGE('',*,*,#17784,.T.);
#25248=ORIENTED_EDGE('',*,*,#16665,.T.);
#25249=ORIENTED_EDGE('',*,*,#17783,.F.);
#25250=ORIENTED_EDGE('',*,*,#17108,.T.);
#25251=ORIENTED_EDGE('',*,*,#17355,.T.);
#25252=ORIENTED_EDGE('',*,*,#17592,.T.);
#25253=ORIENTED_EDGE('',*,*,#17752,.T.);
#25254=ORIENTED_EDGE('',*,*,#16666,.T.);
#25255=ORIENTED_EDGE('',*,*,#17784,.F.);
#25256=ORIENTED_EDGE('',*,*,#17106,.T.);
#25257=ORIENTED_EDGE('',*,*,#17785,.T.);
#25258=ORIENTED_EDGE('',*,*,#16668,.T.);
#25259=ORIENTED_EDGE('',*,*,#17751,.T.);
#25260=ORIENTED_EDGE('',*,*,#17590,.T.);
#25261=ORIENTED_EDGE('',*,*,#17353,.T.);
#25262=ORIENTED_EDGE('',*,*,#17105,.T.);
#25263=ORIENTED_EDGE('',*,*,#17786,.T.);
#25264=ORIENTED_EDGE('',*,*,#16669,.T.);
#25265=ORIENTED_EDGE('',*,*,#17785,.F.);
#25266=ORIENTED_EDGE('',*,*,#17104,.T.);
#25267=ORIENTED_EDGE('',*,*,#17352,.T.);
#25268=ORIENTED_EDGE('',*,*,#17589,.T.);
#25269=ORIENTED_EDGE('',*,*,#17750,.T.);
#25270=ORIENTED_EDGE('',*,*,#16670,.T.);
#25271=ORIENTED_EDGE('',*,*,#17786,.F.);
#25272=ORIENTED_EDGE('',*,*,#17102,.T.);
#25273=ORIENTED_EDGE('',*,*,#17787,.T.);
#25274=ORIENTED_EDGE('',*,*,#16672,.T.);
#25275=ORIENTED_EDGE('',*,*,#17749,.T.);
#25276=ORIENTED_EDGE('',*,*,#17587,.T.);
#25277=ORIENTED_EDGE('',*,*,#17350,.T.);
#25278=ORIENTED_EDGE('',*,*,#17101,.T.);
#25279=ORIENTED_EDGE('',*,*,#17788,.T.);
#25280=ORIENTED_EDGE('',*,*,#16673,.T.);
#25281=ORIENTED_EDGE('',*,*,#17787,.F.);
#25282=ORIENTED_EDGE('',*,*,#17100,.T.);
#25283=ORIENTED_EDGE('',*,*,#17349,.T.);
#25284=ORIENTED_EDGE('',*,*,#17586,.T.);
#25285=ORIENTED_EDGE('',*,*,#17748,.T.);
#25286=ORIENTED_EDGE('',*,*,#16674,.T.);
#25287=ORIENTED_EDGE('',*,*,#17788,.F.);
#25288=ORIENTED_EDGE('',*,*,#17098,.T.);
#25289=ORIENTED_EDGE('',*,*,#17789,.T.);
#25290=ORIENTED_EDGE('',*,*,#16676,.T.);
#25291=ORIENTED_EDGE('',*,*,#17747,.T.);
#25292=ORIENTED_EDGE('',*,*,#17584,.T.);
#25293=ORIENTED_EDGE('',*,*,#17347,.T.);
#25294=ORIENTED_EDGE('',*,*,#17097,.T.);
#25295=ORIENTED_EDGE('',*,*,#17790,.T.);
#25296=ORIENTED_EDGE('',*,*,#16677,.T.);
#25297=ORIENTED_EDGE('',*,*,#17789,.F.);
#25298=ORIENTED_EDGE('',*,*,#17096,.T.);
#25299=ORIENTED_EDGE('',*,*,#17346,.T.);
#25300=ORIENTED_EDGE('',*,*,#17583,.T.);
#25301=ORIENTED_EDGE('',*,*,#17746,.T.);
#25302=ORIENTED_EDGE('',*,*,#16678,.T.);
#25303=ORIENTED_EDGE('',*,*,#17790,.F.);
#25304=ORIENTED_EDGE('',*,*,#17094,.T.);
#25305=ORIENTED_EDGE('',*,*,#17791,.T.);
#25306=ORIENTED_EDGE('',*,*,#16680,.T.);
#25307=ORIENTED_EDGE('',*,*,#17745,.T.);
#25308=ORIENTED_EDGE('',*,*,#17581,.T.);
#25309=ORIENTED_EDGE('',*,*,#17344,.T.);
#25310=ORIENTED_EDGE('',*,*,#17093,.T.);
#25311=ORIENTED_EDGE('',*,*,#17792,.T.);
#25312=ORIENTED_EDGE('',*,*,#16681,.T.);
#25313=ORIENTED_EDGE('',*,*,#17791,.F.);
#25314=ORIENTED_EDGE('',*,*,#17092,.T.);
#25315=ORIENTED_EDGE('',*,*,#17343,.T.);
#25316=ORIENTED_EDGE('',*,*,#17580,.T.);
#25317=ORIENTED_EDGE('',*,*,#17744,.T.);
#25318=ORIENTED_EDGE('',*,*,#16682,.T.);
#25319=ORIENTED_EDGE('',*,*,#17792,.F.);
#25320=ORIENTED_EDGE('',*,*,#17090,.T.);
#25321=ORIENTED_EDGE('',*,*,#16488,.T.);
#25322=ORIENTED_EDGE('',*,*,#16684,.T.);
#25323=ORIENTED_EDGE('',*,*,#17743,.T.);
#25324=ORIENTED_EDGE('',*,*,#17578,.T.);
#25325=ORIENTED_EDGE('',*,*,#17341,.T.);
#25326=ORIENTED_EDGE('',*,*,#17089,.T.);
#25327=ORIENTED_EDGE('',*,*,#17340,.T.);
#25328=ORIENTED_EDGE('',*,*,#17577,.T.);
#25329=ORIENTED_EDGE('',*,*,#17742,.T.);
#25330=ORIENTED_EDGE('',*,*,#16685,.T.);
#25331=ORIENTED_EDGE('',*,*,#16486,.F.);
#25332=ORIENTED_EDGE('',*,*,#17087,.T.);
#25333=ORIENTED_EDGE('',*,*,#16484,.T.);
#25334=ORIENTED_EDGE('',*,*,#16687,.T.);
#25335=ORIENTED_EDGE('',*,*,#17741,.T.);
#25336=ORIENTED_EDGE('',*,*,#17575,.T.);
#25337=ORIENTED_EDGE('',*,*,#17338,.T.);
#25338=ORIENTED_EDGE('',*,*,#17086,.T.);
#25339=ORIENTED_EDGE('',*,*,#17337,.T.);
#25340=ORIENTED_EDGE('',*,*,#17574,.T.);
#25341=ORIENTED_EDGE('',*,*,#17740,.T.);
#25342=ORIENTED_EDGE('',*,*,#16688,.T.);
#25343=ORIENTED_EDGE('',*,*,#16482,.F.);
#25344=ORIENTED_EDGE('',*,*,#17084,.T.);
#25345=ORIENTED_EDGE('',*,*,#16480,.T.);
#25346=ORIENTED_EDGE('',*,*,#16690,.T.);
#25347=ORIENTED_EDGE('',*,*,#17739,.T.);
#25348=ORIENTED_EDGE('',*,*,#17572,.T.);
#25349=ORIENTED_EDGE('',*,*,#17335,.T.);
#25350=ORIENTED_EDGE('',*,*,#17083,.T.);
#25351=ORIENTED_EDGE('',*,*,#17334,.T.);
#25352=ORIENTED_EDGE('',*,*,#17571,.T.);
#25353=ORIENTED_EDGE('',*,*,#17738,.T.);
#25354=ORIENTED_EDGE('',*,*,#16691,.T.);
#25355=ORIENTED_EDGE('',*,*,#16478,.F.);
#25356=ORIENTED_EDGE('',*,*,#17081,.T.);
#25357=ORIENTED_EDGE('',*,*,#16476,.T.);
#25358=ORIENTED_EDGE('',*,*,#16693,.T.);
#25359=ORIENTED_EDGE('',*,*,#17737,.T.);
#25360=ORIENTED_EDGE('',*,*,#17569,.T.);
#25361=ORIENTED_EDGE('',*,*,#17332,.T.);
#25362=ORIENTED_EDGE('',*,*,#17080,.T.);
#25363=ORIENTED_EDGE('',*,*,#17331,.T.);
#25364=ORIENTED_EDGE('',*,*,#17568,.T.);
#25365=ORIENTED_EDGE('',*,*,#17736,.T.);
#25366=ORIENTED_EDGE('',*,*,#16694,.T.);
#25367=ORIENTED_EDGE('',*,*,#16474,.F.);
#25368=ORIENTED_EDGE('',*,*,#17078,.T.);
#25369=ORIENTED_EDGE('',*,*,#16472,.T.);
#25370=ORIENTED_EDGE('',*,*,#16696,.T.);
#25371=ORIENTED_EDGE('',*,*,#17735,.T.);
#25372=ORIENTED_EDGE('',*,*,#17566,.T.);
#25373=ORIENTED_EDGE('',*,*,#17329,.T.);
#25374=ORIENTED_EDGE('',*,*,#17077,.T.);
#25375=ORIENTED_EDGE('',*,*,#17328,.T.);
#25376=ORIENTED_EDGE('',*,*,#17565,.T.);
#25377=ORIENTED_EDGE('',*,*,#17734,.T.);
#25378=ORIENTED_EDGE('',*,*,#16697,.T.);
#25379=ORIENTED_EDGE('',*,*,#16470,.F.);
#25380=ORIENTED_EDGE('',*,*,#17075,.T.);
#25381=ORIENTED_EDGE('',*,*,#16468,.T.);
#25382=ORIENTED_EDGE('',*,*,#16699,.T.);
#25383=ORIENTED_EDGE('',*,*,#17733,.T.);
#25384=ORIENTED_EDGE('',*,*,#17563,.T.);
#25385=ORIENTED_EDGE('',*,*,#17326,.T.);
#25386=ORIENTED_EDGE('',*,*,#17074,.T.);
#25387=ORIENTED_EDGE('',*,*,#17325,.T.);
#25388=ORIENTED_EDGE('',*,*,#17562,.T.);
#25389=ORIENTED_EDGE('',*,*,#17732,.T.);
#25390=ORIENTED_EDGE('',*,*,#16700,.T.);
#25391=ORIENTED_EDGE('',*,*,#16466,.F.);
#25392=ORIENTED_EDGE('',*,*,#17072,.T.);
#25393=ORIENTED_EDGE('',*,*,#16464,.T.);
#25394=ORIENTED_EDGE('',*,*,#16702,.T.);
#25395=ORIENTED_EDGE('',*,*,#17731,.T.);
#25396=ORIENTED_EDGE('',*,*,#17560,.T.);
#25397=ORIENTED_EDGE('',*,*,#17323,.T.);
#25398=ORIENTED_EDGE('',*,*,#17071,.T.);
#25399=ORIENTED_EDGE('',*,*,#17322,.T.);
#25400=ORIENTED_EDGE('',*,*,#17559,.T.);
#25401=ORIENTED_EDGE('',*,*,#17730,.T.);
#25402=ORIENTED_EDGE('',*,*,#16703,.T.);
#25403=ORIENTED_EDGE('',*,*,#16462,.F.);
#25404=ORIENTED_EDGE('',*,*,#17069,.T.);
#25405=ORIENTED_EDGE('',*,*,#16460,.T.);
#25406=ORIENTED_EDGE('',*,*,#16705,.T.);
#25407=ORIENTED_EDGE('',*,*,#17729,.T.);
#25408=ORIENTED_EDGE('',*,*,#17557,.T.);
#25409=ORIENTED_EDGE('',*,*,#17320,.T.);
#25410=ORIENTED_EDGE('',*,*,#17068,.T.);
#25411=ORIENTED_EDGE('',*,*,#17319,.T.);
#25412=ORIENTED_EDGE('',*,*,#17556,.T.);
#25413=ORIENTED_EDGE('',*,*,#17728,.T.);
#25414=ORIENTED_EDGE('',*,*,#16706,.T.);
#25415=ORIENTED_EDGE('',*,*,#16458,.F.);
#25416=ORIENTED_EDGE('',*,*,#17066,.T.);
#25417=ORIENTED_EDGE('',*,*,#16456,.T.);
#25418=ORIENTED_EDGE('',*,*,#16708,.T.);
#25419=ORIENTED_EDGE('',*,*,#17727,.T.);
#25420=ORIENTED_EDGE('',*,*,#17554,.T.);
#25421=ORIENTED_EDGE('',*,*,#17317,.T.);
#25422=ORIENTED_EDGE('',*,*,#17065,.T.);
#25423=ORIENTED_EDGE('',*,*,#17127,.T.);
#25424=ORIENTED_EDGE('',*,*,#17364,.T.);
#25425=ORIENTED_EDGE('',*,*,#17600,.T.);
#25426=ORIENTED_EDGE('',*,*,#16709,.T.);
#25427=ORIENTED_EDGE('',*,*,#16454,.F.);
#25428=ORIENTED_EDGE('',*,*,#16817,.T.);
#25429=ORIENTED_EDGE('',*,*,#17793,.T.);
#25430=ORIENTED_EDGE('',*,*,#16652,.T.);
#25431=ORIENTED_EDGE('',*,*,#17726,.T.);
#25432=ORIENTED_EDGE('',*,*,#17552,.T.);
#25433=ORIENTED_EDGE('',*,*,#17315,.T.);
#25434=ORIENTED_EDGE('',*,*,#16816,.T.);
#25435=ORIENTED_EDGE('',*,*,#17794,.T.);
#25436=ORIENTED_EDGE('',*,*,#16653,.T.);
#25437=ORIENTED_EDGE('',*,*,#17793,.F.);
#25438=ORIENTED_EDGE('',*,*,#16815,.T.);
#25439=ORIENTED_EDGE('',*,*,#17359,.T.);
#25440=ORIENTED_EDGE('',*,*,#17596,.T.);
#25441=ORIENTED_EDGE('',*,*,#17755,.T.);
#25442=ORIENTED_EDGE('',*,*,#16654,.T.);
#25443=ORIENTED_EDGE('',*,*,#17794,.F.);
#25444=ORIENTED_EDGE('',*,*,#16821,.T.);
#25445=ORIENTED_EDGE('',*,*,#17795,.T.);
#25446=ORIENTED_EDGE('',*,*,#16648,.T.);
#25447=ORIENTED_EDGE('',*,*,#17724,.T.);
#25448=ORIENTED_EDGE('',*,*,#17549,.T.);
#25449=ORIENTED_EDGE('',*,*,#17312,.T.);
#25450=ORIENTED_EDGE('',*,*,#16820,.T.);
#25451=ORIENTED_EDGE('',*,*,#17796,.T.);
#25452=ORIENTED_EDGE('',*,*,#16649,.T.);
#25453=ORIENTED_EDGE('',*,*,#17795,.F.);
#25454=ORIENTED_EDGE('',*,*,#16819,.T.);
#25455=ORIENTED_EDGE('',*,*,#17314,.T.);
#25456=ORIENTED_EDGE('',*,*,#17551,.T.);
#25457=ORIENTED_EDGE('',*,*,#17725,.T.);
#25458=ORIENTED_EDGE('',*,*,#16650,.T.);
#25459=ORIENTED_EDGE('',*,*,#17796,.F.);
#25460=ORIENTED_EDGE('',*,*,#16825,.T.);
#25461=ORIENTED_EDGE('',*,*,#17797,.T.);
#25462=ORIENTED_EDGE('',*,*,#16644,.T.);
#25463=ORIENTED_EDGE('',*,*,#17722,.T.);
#25464=ORIENTED_EDGE('',*,*,#17546,.T.);
#25465=ORIENTED_EDGE('',*,*,#17309,.T.);
#25466=ORIENTED_EDGE('',*,*,#16824,.T.);
#25467=ORIENTED_EDGE('',*,*,#17798,.T.);
#25468=ORIENTED_EDGE('',*,*,#16645,.T.);
#25469=ORIENTED_EDGE('',*,*,#17797,.F.);
#25470=ORIENTED_EDGE('',*,*,#16823,.T.);
#25471=ORIENTED_EDGE('',*,*,#17311,.T.);
#25472=ORIENTED_EDGE('',*,*,#17548,.T.);
#25473=ORIENTED_EDGE('',*,*,#17723,.T.);
#25474=ORIENTED_EDGE('',*,*,#16646,.T.);
#25475=ORIENTED_EDGE('',*,*,#17798,.F.);
#25476=ORIENTED_EDGE('',*,*,#16829,.T.);
#25477=ORIENTED_EDGE('',*,*,#17799,.T.);
#25478=ORIENTED_EDGE('',*,*,#16640,.T.);
#25479=ORIENTED_EDGE('',*,*,#17720,.T.);
#25480=ORIENTED_EDGE('',*,*,#17543,.T.);
#25481=ORIENTED_EDGE('',*,*,#17306,.T.);
#25482=ORIENTED_EDGE('',*,*,#16828,.T.);
#25483=ORIENTED_EDGE('',*,*,#17800,.T.);
#25484=ORIENTED_EDGE('',*,*,#16641,.T.);
#25485=ORIENTED_EDGE('',*,*,#17799,.F.);
#25486=ORIENTED_EDGE('',*,*,#16827,.T.);
#25487=ORIENTED_EDGE('',*,*,#17308,.T.);
#25488=ORIENTED_EDGE('',*,*,#17545,.T.);
#25489=ORIENTED_EDGE('',*,*,#17721,.T.);
#25490=ORIENTED_EDGE('',*,*,#16642,.T.);
#25491=ORIENTED_EDGE('',*,*,#17800,.F.);
#25492=ORIENTED_EDGE('',*,*,#16833,.T.);
#25493=ORIENTED_EDGE('',*,*,#17801,.T.);
#25494=ORIENTED_EDGE('',*,*,#16636,.T.);
#25495=ORIENTED_EDGE('',*,*,#17718,.T.);
#25496=ORIENTED_EDGE('',*,*,#17540,.T.);
#25497=ORIENTED_EDGE('',*,*,#17303,.T.);
#25498=ORIENTED_EDGE('',*,*,#16832,.T.);
#25499=ORIENTED_EDGE('',*,*,#17802,.T.);
#25500=ORIENTED_EDGE('',*,*,#16637,.T.);
#25501=ORIENTED_EDGE('',*,*,#17801,.F.);
#25502=ORIENTED_EDGE('',*,*,#16831,.T.);
#25503=ORIENTED_EDGE('',*,*,#17305,.T.);
#25504=ORIENTED_EDGE('',*,*,#17542,.T.);
#25505=ORIENTED_EDGE('',*,*,#17719,.T.);
#25506=ORIENTED_EDGE('',*,*,#16638,.T.);
#25507=ORIENTED_EDGE('',*,*,#17802,.F.);
#25508=ORIENTED_EDGE('',*,*,#16837,.T.);
#25509=ORIENTED_EDGE('',*,*,#17803,.T.);
#25510=ORIENTED_EDGE('',*,*,#16632,.T.);
#25511=ORIENTED_EDGE('',*,*,#17716,.T.);
#25512=ORIENTED_EDGE('',*,*,#17537,.T.);
#25513=ORIENTED_EDGE('',*,*,#17300,.T.);
#25514=ORIENTED_EDGE('',*,*,#16836,.T.);
#25515=ORIENTED_EDGE('',*,*,#17804,.T.);
#25516=ORIENTED_EDGE('',*,*,#16633,.T.);
#25517=ORIENTED_EDGE('',*,*,#17803,.F.);
#25518=ORIENTED_EDGE('',*,*,#16835,.T.);
#25519=ORIENTED_EDGE('',*,*,#17302,.T.);
#25520=ORIENTED_EDGE('',*,*,#17539,.T.);
#25521=ORIENTED_EDGE('',*,*,#17717,.T.);
#25522=ORIENTED_EDGE('',*,*,#16634,.T.);
#25523=ORIENTED_EDGE('',*,*,#17804,.F.);
#25524=ORIENTED_EDGE('',*,*,#16841,.T.);
#25525=ORIENTED_EDGE('',*,*,#17805,.T.);
#25526=ORIENTED_EDGE('',*,*,#16628,.T.);
#25527=ORIENTED_EDGE('',*,*,#17714,.T.);
#25528=ORIENTED_EDGE('',*,*,#17534,.T.);
#25529=ORIENTED_EDGE('',*,*,#17297,.T.);
#25530=ORIENTED_EDGE('',*,*,#16840,.T.);
#25531=ORIENTED_EDGE('',*,*,#17806,.T.);
#25532=ORIENTED_EDGE('',*,*,#16629,.T.);
#25533=ORIENTED_EDGE('',*,*,#17805,.F.);
#25534=ORIENTED_EDGE('',*,*,#16839,.T.);
#25535=ORIENTED_EDGE('',*,*,#17299,.T.);
#25536=ORIENTED_EDGE('',*,*,#17536,.T.);
#25537=ORIENTED_EDGE('',*,*,#17715,.T.);
#25538=ORIENTED_EDGE('',*,*,#16630,.T.);
#25539=ORIENTED_EDGE('',*,*,#17806,.F.);
#25540=ORIENTED_EDGE('',*,*,#16845,.T.);
#25541=ORIENTED_EDGE('',*,*,#17807,.T.);
#25542=ORIENTED_EDGE('',*,*,#16624,.T.);
#25543=ORIENTED_EDGE('',*,*,#17712,.T.);
#25544=ORIENTED_EDGE('',*,*,#17531,.T.);
#25545=ORIENTED_EDGE('',*,*,#17294,.T.);
#25546=ORIENTED_EDGE('',*,*,#16844,.T.);
#25547=ORIENTED_EDGE('',*,*,#17808,.T.);
#25548=ORIENTED_EDGE('',*,*,#16625,.T.);
#25549=ORIENTED_EDGE('',*,*,#17807,.F.);
#25550=ORIENTED_EDGE('',*,*,#16843,.T.);
#25551=ORIENTED_EDGE('',*,*,#17296,.T.);
#25552=ORIENTED_EDGE('',*,*,#17533,.T.);
#25553=ORIENTED_EDGE('',*,*,#17713,.T.);
#25554=ORIENTED_EDGE('',*,*,#16626,.T.);
#25555=ORIENTED_EDGE('',*,*,#17808,.F.);
#25556=ORIENTED_EDGE('',*,*,#16849,.T.);
#25557=ORIENTED_EDGE('',*,*,#17809,.T.);
#25558=ORIENTED_EDGE('',*,*,#16620,.T.);
#25559=ORIENTED_EDGE('',*,*,#17710,.T.);
#25560=ORIENTED_EDGE('',*,*,#17528,.T.);
#25561=ORIENTED_EDGE('',*,*,#17291,.T.);
#25562=ORIENTED_EDGE('',*,*,#16848,.T.);
#25563=ORIENTED_EDGE('',*,*,#17810,.T.);
#25564=ORIENTED_EDGE('',*,*,#16621,.T.);
#25565=ORIENTED_EDGE('',*,*,#17809,.F.);
#25566=ORIENTED_EDGE('',*,*,#16847,.T.);
#25567=ORIENTED_EDGE('',*,*,#17293,.T.);
#25568=ORIENTED_EDGE('',*,*,#17530,.T.);
#25569=ORIENTED_EDGE('',*,*,#17711,.T.);
#25570=ORIENTED_EDGE('',*,*,#16622,.T.);
#25571=ORIENTED_EDGE('',*,*,#17810,.F.);
#25572=ORIENTED_EDGE('',*,*,#16853,.T.);
#25573=ORIENTED_EDGE('',*,*,#17811,.T.);
#25574=ORIENTED_EDGE('',*,*,#16616,.T.);
#25575=ORIENTED_EDGE('',*,*,#17708,.T.);
#25576=ORIENTED_EDGE('',*,*,#17525,.T.);
#25577=ORIENTED_EDGE('',*,*,#17288,.T.);
#25578=ORIENTED_EDGE('',*,*,#16852,.T.);
#25579=ORIENTED_EDGE('',*,*,#17812,.T.);
#25580=ORIENTED_EDGE('',*,*,#16617,.T.);
#25581=ORIENTED_EDGE('',*,*,#17811,.F.);
#25582=ORIENTED_EDGE('',*,*,#16851,.T.);
#25583=ORIENTED_EDGE('',*,*,#17290,.T.);
#25584=ORIENTED_EDGE('',*,*,#17527,.T.);
#25585=ORIENTED_EDGE('',*,*,#17709,.T.);
#25586=ORIENTED_EDGE('',*,*,#16618,.T.);
#25587=ORIENTED_EDGE('',*,*,#17812,.F.);
#25588=ORIENTED_EDGE('',*,*,#16857,.T.);
#25589=ORIENTED_EDGE('',*,*,#17813,.T.);
#25590=ORIENTED_EDGE('',*,*,#16612,.T.);
#25591=ORIENTED_EDGE('',*,*,#17706,.T.);
#25592=ORIENTED_EDGE('',*,*,#17522,.T.);
#25593=ORIENTED_EDGE('',*,*,#17285,.T.);
#25594=ORIENTED_EDGE('',*,*,#16856,.T.);
#25595=ORIENTED_EDGE('',*,*,#17814,.T.);
#25596=ORIENTED_EDGE('',*,*,#16613,.T.);
#25597=ORIENTED_EDGE('',*,*,#17813,.F.);
#25598=ORIENTED_EDGE('',*,*,#16855,.T.);
#25599=ORIENTED_EDGE('',*,*,#17287,.T.);
#25600=ORIENTED_EDGE('',*,*,#17524,.T.);
#25601=ORIENTED_EDGE('',*,*,#17707,.T.);
#25602=ORIENTED_EDGE('',*,*,#16614,.T.);
#25603=ORIENTED_EDGE('',*,*,#17814,.F.);
#25604=ORIENTED_EDGE('',*,*,#16861,.T.);
#25605=ORIENTED_EDGE('',*,*,#17815,.T.);
#25606=ORIENTED_EDGE('',*,*,#16608,.T.);
#25607=ORIENTED_EDGE('',*,*,#17704,.T.);
#25608=ORIENTED_EDGE('',*,*,#17519,.T.);
#25609=ORIENTED_EDGE('',*,*,#17282,.T.);
#25610=ORIENTED_EDGE('',*,*,#16860,.T.);
#25611=ORIENTED_EDGE('',*,*,#17816,.T.);
#25612=ORIENTED_EDGE('',*,*,#16609,.T.);
#25613=ORIENTED_EDGE('',*,*,#17815,.F.);
#25614=ORIENTED_EDGE('',*,*,#16859,.T.);
#25615=ORIENTED_EDGE('',*,*,#17284,.T.);
#25616=ORIENTED_EDGE('',*,*,#17521,.T.);
#25617=ORIENTED_EDGE('',*,*,#17705,.T.);
#25618=ORIENTED_EDGE('',*,*,#16610,.T.);
#25619=ORIENTED_EDGE('',*,*,#17816,.F.);
#25620=ORIENTED_EDGE('',*,*,#16865,.T.);
#25621=ORIENTED_EDGE('',*,*,#17817,.T.);
#25622=ORIENTED_EDGE('',*,*,#16604,.T.);
#25623=ORIENTED_EDGE('',*,*,#17702,.T.);
#25624=ORIENTED_EDGE('',*,*,#17516,.T.);
#25625=ORIENTED_EDGE('',*,*,#17279,.T.);
#25626=ORIENTED_EDGE('',*,*,#16864,.T.);
#25627=ORIENTED_EDGE('',*,*,#17818,.T.);
#25628=ORIENTED_EDGE('',*,*,#16605,.T.);
#25629=ORIENTED_EDGE('',*,*,#17817,.F.);
#25630=ORIENTED_EDGE('',*,*,#16863,.T.);
#25631=ORIENTED_EDGE('',*,*,#17281,.T.);
#25632=ORIENTED_EDGE('',*,*,#17518,.T.);
#25633=ORIENTED_EDGE('',*,*,#17703,.T.);
#25634=ORIENTED_EDGE('',*,*,#16606,.T.);
#25635=ORIENTED_EDGE('',*,*,#17818,.F.);
#25636=ORIENTED_EDGE('',*,*,#16869,.T.);
#25637=ORIENTED_EDGE('',*,*,#17819,.T.);
#25638=ORIENTED_EDGE('',*,*,#16600,.T.);
#25639=ORIENTED_EDGE('',*,*,#17700,.T.);
#25640=ORIENTED_EDGE('',*,*,#17513,.T.);
#25641=ORIENTED_EDGE('',*,*,#17276,.T.);
#25642=ORIENTED_EDGE('',*,*,#16868,.T.);
#25643=ORIENTED_EDGE('',*,*,#17820,.T.);
#25644=ORIENTED_EDGE('',*,*,#16601,.T.);
#25645=ORIENTED_EDGE('',*,*,#17819,.F.);
#25646=ORIENTED_EDGE('',*,*,#16867,.T.);
#25647=ORIENTED_EDGE('',*,*,#17278,.T.);
#25648=ORIENTED_EDGE('',*,*,#17515,.T.);
#25649=ORIENTED_EDGE('',*,*,#17701,.T.);
#25650=ORIENTED_EDGE('',*,*,#16602,.T.);
#25651=ORIENTED_EDGE('',*,*,#17820,.F.);
#25652=ORIENTED_EDGE('',*,*,#16873,.T.);
#25653=ORIENTED_EDGE('',*,*,#17821,.T.);
#25654=ORIENTED_EDGE('',*,*,#16596,.T.);
#25655=ORIENTED_EDGE('',*,*,#17698,.T.);
#25656=ORIENTED_EDGE('',*,*,#17510,.T.);
#25657=ORIENTED_EDGE('',*,*,#17273,.T.);
#25658=ORIENTED_EDGE('',*,*,#16872,.T.);
#25659=ORIENTED_EDGE('',*,*,#17822,.T.);
#25660=ORIENTED_EDGE('',*,*,#16597,.T.);
#25661=ORIENTED_EDGE('',*,*,#17821,.F.);
#25662=ORIENTED_EDGE('',*,*,#16871,.T.);
#25663=ORIENTED_EDGE('',*,*,#17275,.T.);
#25664=ORIENTED_EDGE('',*,*,#17512,.T.);
#25665=ORIENTED_EDGE('',*,*,#17699,.T.);
#25666=ORIENTED_EDGE('',*,*,#16598,.T.);
#25667=ORIENTED_EDGE('',*,*,#17822,.F.);
#25668=ORIENTED_EDGE('',*,*,#16877,.T.);
#25669=ORIENTED_EDGE('',*,*,#17823,.T.);
#25670=ORIENTED_EDGE('',*,*,#16592,.T.);
#25671=ORIENTED_EDGE('',*,*,#17696,.T.);
#25672=ORIENTED_EDGE('',*,*,#17507,.T.);
#25673=ORIENTED_EDGE('',*,*,#17270,.T.);
#25674=ORIENTED_EDGE('',*,*,#16876,.T.);
#25675=ORIENTED_EDGE('',*,*,#17824,.T.);
#25676=ORIENTED_EDGE('',*,*,#16593,.T.);
#25677=ORIENTED_EDGE('',*,*,#17823,.F.);
#25678=ORIENTED_EDGE('',*,*,#16875,.T.);
#25679=ORIENTED_EDGE('',*,*,#17272,.T.);
#25680=ORIENTED_EDGE('',*,*,#17509,.T.);
#25681=ORIENTED_EDGE('',*,*,#17697,.T.);
#25682=ORIENTED_EDGE('',*,*,#16594,.T.);
#25683=ORIENTED_EDGE('',*,*,#17824,.F.);
#25684=ORIENTED_EDGE('',*,*,#16881,.T.);
#25685=ORIENTED_EDGE('',*,*,#17825,.T.);
#25686=ORIENTED_EDGE('',*,*,#16588,.T.);
#25687=ORIENTED_EDGE('',*,*,#17694,.T.);
#25688=ORIENTED_EDGE('',*,*,#17504,.T.);
#25689=ORIENTED_EDGE('',*,*,#17267,.T.);
#25690=ORIENTED_EDGE('',*,*,#16880,.T.);
#25691=ORIENTED_EDGE('',*,*,#17826,.T.);
#25692=ORIENTED_EDGE('',*,*,#16589,.T.);
#25693=ORIENTED_EDGE('',*,*,#17825,.F.);
#25694=ORIENTED_EDGE('',*,*,#16879,.T.);
#25695=ORIENTED_EDGE('',*,*,#17269,.T.);
#25696=ORIENTED_EDGE('',*,*,#17506,.T.);
#25697=ORIENTED_EDGE('',*,*,#17695,.T.);
#25698=ORIENTED_EDGE('',*,*,#16590,.T.);
#25699=ORIENTED_EDGE('',*,*,#17826,.F.);
#25700=ORIENTED_EDGE('',*,*,#16885,.T.);
#25701=ORIENTED_EDGE('',*,*,#17827,.T.);
#25702=ORIENTED_EDGE('',*,*,#16584,.T.);
#25703=ORIENTED_EDGE('',*,*,#17692,.T.);
#25704=ORIENTED_EDGE('',*,*,#17501,.T.);
#25705=ORIENTED_EDGE('',*,*,#17264,.T.);
#25706=ORIENTED_EDGE('',*,*,#16884,.T.);
#25707=ORIENTED_EDGE('',*,*,#17828,.T.);
#25708=ORIENTED_EDGE('',*,*,#16585,.T.);
#25709=ORIENTED_EDGE('',*,*,#17827,.F.);
#25710=ORIENTED_EDGE('',*,*,#16883,.T.);
#25711=ORIENTED_EDGE('',*,*,#17266,.T.);
#25712=ORIENTED_EDGE('',*,*,#17503,.T.);
#25713=ORIENTED_EDGE('',*,*,#17693,.T.);
#25714=ORIENTED_EDGE('',*,*,#16586,.T.);
#25715=ORIENTED_EDGE('',*,*,#17828,.F.);
#25716=ORIENTED_EDGE('',*,*,#16889,.T.);
#25717=ORIENTED_EDGE('',*,*,#17829,.T.);
#25718=ORIENTED_EDGE('',*,*,#16580,.T.);
#25719=ORIENTED_EDGE('',*,*,#17690,.T.);
#25720=ORIENTED_EDGE('',*,*,#17498,.T.);
#25721=ORIENTED_EDGE('',*,*,#17261,.T.);
#25722=ORIENTED_EDGE('',*,*,#16888,.T.);
#25723=ORIENTED_EDGE('',*,*,#17830,.T.);
#25724=ORIENTED_EDGE('',*,*,#16581,.T.);
#25725=ORIENTED_EDGE('',*,*,#17829,.F.);
#25726=ORIENTED_EDGE('',*,*,#16887,.T.);
#25727=ORIENTED_EDGE('',*,*,#17263,.T.);
#25728=ORIENTED_EDGE('',*,*,#17500,.T.);
#25729=ORIENTED_EDGE('',*,*,#17691,.T.);
#25730=ORIENTED_EDGE('',*,*,#16582,.T.);
#25731=ORIENTED_EDGE('',*,*,#17830,.F.);
#25732=ORIENTED_EDGE('',*,*,#16893,.T.);
#25733=ORIENTED_EDGE('',*,*,#17831,.T.);
#25734=ORIENTED_EDGE('',*,*,#16576,.T.);
#25735=ORIENTED_EDGE('',*,*,#17688,.T.);
#25736=ORIENTED_EDGE('',*,*,#17495,.T.);
#25737=ORIENTED_EDGE('',*,*,#17258,.T.);
#25738=ORIENTED_EDGE('',*,*,#16892,.T.);
#25739=ORIENTED_EDGE('',*,*,#17832,.T.);
#25740=ORIENTED_EDGE('',*,*,#16577,.T.);
#25741=ORIENTED_EDGE('',*,*,#17831,.F.);
#25742=ORIENTED_EDGE('',*,*,#16891,.T.);
#25743=ORIENTED_EDGE('',*,*,#17260,.T.);
#25744=ORIENTED_EDGE('',*,*,#17497,.T.);
#25745=ORIENTED_EDGE('',*,*,#17689,.T.);
#25746=ORIENTED_EDGE('',*,*,#16578,.T.);
#25747=ORIENTED_EDGE('',*,*,#17832,.F.);
#25748=ORIENTED_EDGE('',*,*,#16897,.T.);
#25749=ORIENTED_EDGE('',*,*,#17833,.T.);
#25750=ORIENTED_EDGE('',*,*,#16572,.T.);
#25751=ORIENTED_EDGE('',*,*,#17686,.T.);
#25752=ORIENTED_EDGE('',*,*,#17492,.T.);
#25753=ORIENTED_EDGE('',*,*,#17255,.T.);
#25754=ORIENTED_EDGE('',*,*,#16896,.T.);
#25755=ORIENTED_EDGE('',*,*,#17834,.T.);
#25756=ORIENTED_EDGE('',*,*,#16573,.T.);
#25757=ORIENTED_EDGE('',*,*,#17833,.F.);
#25758=ORIENTED_EDGE('',*,*,#16895,.T.);
#25759=ORIENTED_EDGE('',*,*,#17257,.T.);
#25760=ORIENTED_EDGE('',*,*,#17494,.T.);
#25761=ORIENTED_EDGE('',*,*,#17687,.T.);
#25762=ORIENTED_EDGE('',*,*,#16574,.T.);
#25763=ORIENTED_EDGE('',*,*,#17834,.F.);
#25764=ORIENTED_EDGE('',*,*,#16901,.T.);
#25765=ORIENTED_EDGE('',*,*,#17835,.T.);
#25766=ORIENTED_EDGE('',*,*,#16568,.T.);
#25767=ORIENTED_EDGE('',*,*,#17684,.T.);
#25768=ORIENTED_EDGE('',*,*,#17489,.T.);
#25769=ORIENTED_EDGE('',*,*,#17252,.T.);
#25770=ORIENTED_EDGE('',*,*,#16900,.T.);
#25771=ORIENTED_EDGE('',*,*,#17836,.T.);
#25772=ORIENTED_EDGE('',*,*,#16569,.T.);
#25773=ORIENTED_EDGE('',*,*,#17835,.F.);
#25774=ORIENTED_EDGE('',*,*,#16899,.T.);
#25775=ORIENTED_EDGE('',*,*,#17254,.T.);
#25776=ORIENTED_EDGE('',*,*,#17491,.T.);
#25777=ORIENTED_EDGE('',*,*,#17685,.T.);
#25778=ORIENTED_EDGE('',*,*,#16570,.T.);
#25779=ORIENTED_EDGE('',*,*,#17836,.F.);
#25780=ORIENTED_EDGE('',*,*,#16905,.T.);
#25781=ORIENTED_EDGE('',*,*,#17837,.T.);
#25782=ORIENTED_EDGE('',*,*,#16564,.T.);
#25783=ORIENTED_EDGE('',*,*,#17682,.T.);
#25784=ORIENTED_EDGE('',*,*,#17486,.T.);
#25785=ORIENTED_EDGE('',*,*,#17249,.T.);
#25786=ORIENTED_EDGE('',*,*,#16904,.T.);
#25787=ORIENTED_EDGE('',*,*,#17838,.T.);
#25788=ORIENTED_EDGE('',*,*,#16565,.T.);
#25789=ORIENTED_EDGE('',*,*,#17837,.F.);
#25790=ORIENTED_EDGE('',*,*,#16903,.T.);
#25791=ORIENTED_EDGE('',*,*,#17251,.T.);
#25792=ORIENTED_EDGE('',*,*,#17488,.T.);
#25793=ORIENTED_EDGE('',*,*,#17683,.T.);
#25794=ORIENTED_EDGE('',*,*,#16566,.T.);
#25795=ORIENTED_EDGE('',*,*,#17838,.F.);
#25796=ORIENTED_EDGE('',*,*,#16909,.T.);
#25797=ORIENTED_EDGE('',*,*,#17839,.T.);
#25798=ORIENTED_EDGE('',*,*,#16560,.T.);
#25799=ORIENTED_EDGE('',*,*,#17680,.T.);
#25800=ORIENTED_EDGE('',*,*,#17483,.T.);
#25801=ORIENTED_EDGE('',*,*,#17246,.T.);
#25802=ORIENTED_EDGE('',*,*,#16908,.T.);
#25803=ORIENTED_EDGE('',*,*,#17840,.T.);
#25804=ORIENTED_EDGE('',*,*,#16561,.T.);
#25805=ORIENTED_EDGE('',*,*,#17839,.F.);
#25806=ORIENTED_EDGE('',*,*,#16907,.T.);
#25807=ORIENTED_EDGE('',*,*,#17248,.T.);
#25808=ORIENTED_EDGE('',*,*,#17485,.T.);
#25809=ORIENTED_EDGE('',*,*,#17681,.T.);
#25810=ORIENTED_EDGE('',*,*,#16562,.T.);
#25811=ORIENTED_EDGE('',*,*,#17840,.F.);
#25812=ORIENTED_EDGE('',*,*,#16913,.T.);
#25813=ORIENTED_EDGE('',*,*,#17841,.T.);
#25814=ORIENTED_EDGE('',*,*,#16556,.T.);
#25815=ORIENTED_EDGE('',*,*,#17678,.T.);
#25816=ORIENTED_EDGE('',*,*,#17480,.T.);
#25817=ORIENTED_EDGE('',*,*,#17243,.T.);
#25818=ORIENTED_EDGE('',*,*,#16912,.T.);
#25819=ORIENTED_EDGE('',*,*,#17842,.T.);
#25820=ORIENTED_EDGE('',*,*,#16557,.T.);
#25821=ORIENTED_EDGE('',*,*,#17841,.F.);
#25822=ORIENTED_EDGE('',*,*,#16911,.T.);
#25823=ORIENTED_EDGE('',*,*,#17245,.T.);
#25824=ORIENTED_EDGE('',*,*,#17482,.T.);
#25825=ORIENTED_EDGE('',*,*,#17679,.T.);
#25826=ORIENTED_EDGE('',*,*,#16558,.T.);
#25827=ORIENTED_EDGE('',*,*,#17842,.F.);
#25828=ORIENTED_EDGE('',*,*,#16917,.T.);
#25829=ORIENTED_EDGE('',*,*,#17843,.T.);
#25830=ORIENTED_EDGE('',*,*,#16552,.T.);
#25831=ORIENTED_EDGE('',*,*,#17676,.T.);
#25832=ORIENTED_EDGE('',*,*,#17477,.T.);
#25833=ORIENTED_EDGE('',*,*,#17240,.T.);
#25834=ORIENTED_EDGE('',*,*,#16916,.T.);
#25835=ORIENTED_EDGE('',*,*,#17844,.T.);
#25836=ORIENTED_EDGE('',*,*,#16553,.T.);
#25837=ORIENTED_EDGE('',*,*,#17843,.F.);
#25838=ORIENTED_EDGE('',*,*,#16915,.T.);
#25839=ORIENTED_EDGE('',*,*,#17242,.T.);
#25840=ORIENTED_EDGE('',*,*,#17479,.T.);
#25841=ORIENTED_EDGE('',*,*,#17677,.T.);
#25842=ORIENTED_EDGE('',*,*,#16554,.T.);
#25843=ORIENTED_EDGE('',*,*,#17844,.F.);
#25844=ORIENTED_EDGE('',*,*,#16921,.T.);
#25845=ORIENTED_EDGE('',*,*,#17845,.T.);
#25846=ORIENTED_EDGE('',*,*,#16548,.T.);
#25847=ORIENTED_EDGE('',*,*,#17674,.T.);
#25848=ORIENTED_EDGE('',*,*,#17474,.T.);
#25849=ORIENTED_EDGE('',*,*,#17237,.T.);
#25850=ORIENTED_EDGE('',*,*,#16920,.T.);
#25851=ORIENTED_EDGE('',*,*,#17846,.T.);
#25852=ORIENTED_EDGE('',*,*,#16549,.T.);
#25853=ORIENTED_EDGE('',*,*,#17845,.F.);
#25854=ORIENTED_EDGE('',*,*,#16919,.T.);
#25855=ORIENTED_EDGE('',*,*,#17239,.T.);
#25856=ORIENTED_EDGE('',*,*,#17476,.T.);
#25857=ORIENTED_EDGE('',*,*,#17675,.T.);
#25858=ORIENTED_EDGE('',*,*,#16550,.T.);
#25859=ORIENTED_EDGE('',*,*,#17846,.F.);
#25860=ORIENTED_EDGE('',*,*,#16925,.T.);
#25861=ORIENTED_EDGE('',*,*,#17847,.T.);
#25862=ORIENTED_EDGE('',*,*,#16544,.T.);
#25863=ORIENTED_EDGE('',*,*,#17672,.T.);
#25864=ORIENTED_EDGE('',*,*,#17471,.T.);
#25865=ORIENTED_EDGE('',*,*,#17234,.T.);
#25866=ORIENTED_EDGE('',*,*,#16924,.T.);
#25867=ORIENTED_EDGE('',*,*,#17848,.T.);
#25868=ORIENTED_EDGE('',*,*,#16545,.T.);
#25869=ORIENTED_EDGE('',*,*,#17847,.F.);
#25870=ORIENTED_EDGE('',*,*,#16923,.T.);
#25871=ORIENTED_EDGE('',*,*,#17236,.T.);
#25872=ORIENTED_EDGE('',*,*,#17473,.T.);
#25873=ORIENTED_EDGE('',*,*,#17673,.T.);
#25874=ORIENTED_EDGE('',*,*,#16546,.T.);
#25875=ORIENTED_EDGE('',*,*,#17848,.F.);
#25876=ORIENTED_EDGE('',*,*,#16929,.T.);
#25877=ORIENTED_EDGE('',*,*,#17849,.T.);
#25878=ORIENTED_EDGE('',*,*,#16540,.T.);
#25879=ORIENTED_EDGE('',*,*,#17670,.T.);
#25880=ORIENTED_EDGE('',*,*,#17468,.T.);
#25881=ORIENTED_EDGE('',*,*,#17231,.T.);
#25882=ORIENTED_EDGE('',*,*,#16928,.T.);
#25883=ORIENTED_EDGE('',*,*,#17850,.T.);
#25884=ORIENTED_EDGE('',*,*,#16541,.T.);
#25885=ORIENTED_EDGE('',*,*,#17849,.F.);
#25886=ORIENTED_EDGE('',*,*,#16927,.T.);
#25887=ORIENTED_EDGE('',*,*,#17233,.T.);
#25888=ORIENTED_EDGE('',*,*,#17470,.T.);
#25889=ORIENTED_EDGE('',*,*,#17671,.T.);
#25890=ORIENTED_EDGE('',*,*,#16542,.T.);
#25891=ORIENTED_EDGE('',*,*,#17850,.F.);
#25892=ORIENTED_EDGE('',*,*,#16933,.T.);
#25893=ORIENTED_EDGE('',*,*,#17851,.T.);
#25894=ORIENTED_EDGE('',*,*,#16536,.T.);
#25895=ORIENTED_EDGE('',*,*,#17668,.T.);
#25896=ORIENTED_EDGE('',*,*,#17465,.T.);
#25897=ORIENTED_EDGE('',*,*,#17228,.T.);
#25898=ORIENTED_EDGE('',*,*,#16932,.T.);
#25899=ORIENTED_EDGE('',*,*,#17852,.T.);
#25900=ORIENTED_EDGE('',*,*,#16537,.T.);
#25901=ORIENTED_EDGE('',*,*,#17851,.F.);
#25902=ORIENTED_EDGE('',*,*,#16931,.T.);
#25903=ORIENTED_EDGE('',*,*,#17230,.T.);
#25904=ORIENTED_EDGE('',*,*,#17467,.T.);
#25905=ORIENTED_EDGE('',*,*,#17669,.T.);
#25906=ORIENTED_EDGE('',*,*,#16538,.T.);
#25907=ORIENTED_EDGE('',*,*,#17852,.F.);
#25908=ORIENTED_EDGE('',*,*,#16937,.T.);
#25909=ORIENTED_EDGE('',*,*,#17853,.T.);
#25910=ORIENTED_EDGE('',*,*,#16532,.T.);
#25911=ORIENTED_EDGE('',*,*,#17666,.T.);
#25912=ORIENTED_EDGE('',*,*,#17462,.T.);
#25913=ORIENTED_EDGE('',*,*,#17225,.T.);
#25914=ORIENTED_EDGE('',*,*,#16936,.T.);
#25915=ORIENTED_EDGE('',*,*,#17854,.T.);
#25916=ORIENTED_EDGE('',*,*,#16533,.T.);
#25917=ORIENTED_EDGE('',*,*,#17853,.F.);
#25918=ORIENTED_EDGE('',*,*,#16935,.T.);
#25919=ORIENTED_EDGE('',*,*,#17227,.T.);
#25920=ORIENTED_EDGE('',*,*,#17464,.T.);
#25921=ORIENTED_EDGE('',*,*,#17667,.T.);
#25922=ORIENTED_EDGE('',*,*,#16534,.T.);
#25923=ORIENTED_EDGE('',*,*,#17854,.F.);
#25924=ORIENTED_EDGE('',*,*,#16941,.T.);
#25925=ORIENTED_EDGE('',*,*,#17855,.T.);
#25926=ORIENTED_EDGE('',*,*,#16528,.T.);
#25927=ORIENTED_EDGE('',*,*,#17664,.T.);
#25928=ORIENTED_EDGE('',*,*,#17459,.T.);
#25929=ORIENTED_EDGE('',*,*,#17222,.T.);
#25930=ORIENTED_EDGE('',*,*,#16940,.T.);
#25931=ORIENTED_EDGE('',*,*,#17856,.T.);
#25932=ORIENTED_EDGE('',*,*,#16529,.T.);
#25933=ORIENTED_EDGE('',*,*,#17855,.F.);
#25934=ORIENTED_EDGE('',*,*,#16939,.T.);
#25935=ORIENTED_EDGE('',*,*,#17224,.T.);
#25936=ORIENTED_EDGE('',*,*,#17461,.T.);
#25937=ORIENTED_EDGE('',*,*,#17665,.T.);
#25938=ORIENTED_EDGE('',*,*,#16530,.T.);
#25939=ORIENTED_EDGE('',*,*,#17856,.F.);
#25940=ORIENTED_EDGE('',*,*,#16945,.T.);
#25941=ORIENTED_EDGE('',*,*,#17857,.T.);
#25942=ORIENTED_EDGE('',*,*,#16524,.T.);
#25943=ORIENTED_EDGE('',*,*,#17662,.T.);
#25944=ORIENTED_EDGE('',*,*,#17456,.T.);
#25945=ORIENTED_EDGE('',*,*,#17219,.T.);
#25946=ORIENTED_EDGE('',*,*,#16944,.T.);
#25947=ORIENTED_EDGE('',*,*,#17858,.T.);
#25948=ORIENTED_EDGE('',*,*,#16525,.T.);
#25949=ORIENTED_EDGE('',*,*,#17857,.F.);
#25950=ORIENTED_EDGE('',*,*,#16943,.T.);
#25951=ORIENTED_EDGE('',*,*,#17221,.T.);
#25952=ORIENTED_EDGE('',*,*,#17458,.T.);
#25953=ORIENTED_EDGE('',*,*,#17663,.T.);
#25954=ORIENTED_EDGE('',*,*,#16526,.T.);
#25955=ORIENTED_EDGE('',*,*,#17858,.F.);
#25956=ORIENTED_EDGE('',*,*,#16949,.T.);
#25957=ORIENTED_EDGE('',*,*,#17859,.T.);
#25958=ORIENTED_EDGE('',*,*,#16520,.T.);
#25959=ORIENTED_EDGE('',*,*,#17660,.T.);
#25960=ORIENTED_EDGE('',*,*,#17453,.T.);
#25961=ORIENTED_EDGE('',*,*,#17216,.T.);
#25962=ORIENTED_EDGE('',*,*,#16948,.T.);
#25963=ORIENTED_EDGE('',*,*,#17860,.T.);
#25964=ORIENTED_EDGE('',*,*,#16521,.T.);
#25965=ORIENTED_EDGE('',*,*,#17859,.F.);
#25966=ORIENTED_EDGE('',*,*,#16947,.T.);
#25967=ORIENTED_EDGE('',*,*,#17218,.T.);
#25968=ORIENTED_EDGE('',*,*,#17455,.T.);
#25969=ORIENTED_EDGE('',*,*,#17661,.T.);
#25970=ORIENTED_EDGE('',*,*,#16522,.T.);
#25971=ORIENTED_EDGE('',*,*,#17860,.F.);
#25972=ORIENTED_EDGE('',*,*,#16953,.T.);
#25973=ORIENTED_EDGE('',*,*,#17861,.T.);
#25974=ORIENTED_EDGE('',*,*,#16516,.T.);
#25975=ORIENTED_EDGE('',*,*,#17658,.T.);
#25976=ORIENTED_EDGE('',*,*,#17450,.T.);
#25977=ORIENTED_EDGE('',*,*,#17213,.T.);
#25978=ORIENTED_EDGE('',*,*,#16952,.T.);
#25979=ORIENTED_EDGE('',*,*,#17862,.T.);
#25980=ORIENTED_EDGE('',*,*,#16517,.T.);
#25981=ORIENTED_EDGE('',*,*,#17861,.F.);
#25982=ORIENTED_EDGE('',*,*,#16951,.T.);
#25983=ORIENTED_EDGE('',*,*,#17215,.T.);
#25984=ORIENTED_EDGE('',*,*,#17452,.T.);
#25985=ORIENTED_EDGE('',*,*,#17659,.T.);
#25986=ORIENTED_EDGE('',*,*,#16518,.T.);
#25987=ORIENTED_EDGE('',*,*,#17862,.F.);
#25988=ORIENTED_EDGE('',*,*,#16957,.T.);
#25989=ORIENTED_EDGE('',*,*,#17863,.T.);
#25990=ORIENTED_EDGE('',*,*,#16512,.T.);
#25991=ORIENTED_EDGE('',*,*,#17656,.T.);
#25992=ORIENTED_EDGE('',*,*,#17447,.T.);
#25993=ORIENTED_EDGE('',*,*,#17210,.T.);
#25994=ORIENTED_EDGE('',*,*,#16956,.T.);
#25995=ORIENTED_EDGE('',*,*,#17864,.T.);
#25996=ORIENTED_EDGE('',*,*,#16513,.T.);
#25997=ORIENTED_EDGE('',*,*,#17863,.F.);
#25998=ORIENTED_EDGE('',*,*,#16955,.T.);
#25999=ORIENTED_EDGE('',*,*,#17212,.T.);
#26000=ORIENTED_EDGE('',*,*,#17449,.T.);
#26001=ORIENTED_EDGE('',*,*,#17657,.T.);
#26002=ORIENTED_EDGE('',*,*,#16514,.T.);
#26003=ORIENTED_EDGE('',*,*,#17864,.F.);
#26004=ORIENTED_EDGE('',*,*,#16961,.T.);
#26005=ORIENTED_EDGE('',*,*,#17865,.T.);
#26006=ORIENTED_EDGE('',*,*,#16508,.T.);
#26007=ORIENTED_EDGE('',*,*,#17654,.T.);
#26008=ORIENTED_EDGE('',*,*,#17444,.T.);
#26009=ORIENTED_EDGE('',*,*,#17207,.T.);
#26010=ORIENTED_EDGE('',*,*,#16960,.T.);
#26011=ORIENTED_EDGE('',*,*,#17866,.T.);
#26012=ORIENTED_EDGE('',*,*,#16509,.T.);
#26013=ORIENTED_EDGE('',*,*,#17865,.F.);
#26014=ORIENTED_EDGE('',*,*,#16959,.T.);
#26015=ORIENTED_EDGE('',*,*,#17209,.T.);
#26016=ORIENTED_EDGE('',*,*,#17446,.T.);
#26017=ORIENTED_EDGE('',*,*,#17655,.T.);
#26018=ORIENTED_EDGE('',*,*,#16510,.T.);
#26019=ORIENTED_EDGE('',*,*,#17866,.F.);
#26020=ORIENTED_EDGE('',*,*,#16965,.T.);
#26021=ORIENTED_EDGE('',*,*,#17867,.T.);
#26022=ORIENTED_EDGE('',*,*,#16504,.T.);
#26023=ORIENTED_EDGE('',*,*,#17652,.T.);
#26024=ORIENTED_EDGE('',*,*,#17441,.T.);
#26025=ORIENTED_EDGE('',*,*,#17204,.T.);
#26026=ORIENTED_EDGE('',*,*,#16964,.T.);
#26027=ORIENTED_EDGE('',*,*,#17868,.T.);
#26028=ORIENTED_EDGE('',*,*,#16505,.T.);
#26029=ORIENTED_EDGE('',*,*,#17867,.F.);
#26030=ORIENTED_EDGE('',*,*,#16963,.T.);
#26031=ORIENTED_EDGE('',*,*,#17206,.T.);
#26032=ORIENTED_EDGE('',*,*,#17443,.T.);
#26033=ORIENTED_EDGE('',*,*,#17653,.T.);
#26034=ORIENTED_EDGE('',*,*,#16506,.T.);
#26035=ORIENTED_EDGE('',*,*,#17868,.F.);
#26036=ORIENTED_EDGE('',*,*,#16969,.T.);
#26037=ORIENTED_EDGE('',*,*,#17869,.T.);
#26038=ORIENTED_EDGE('',*,*,#16805,.T.);
#26039=ORIENTED_EDGE('',*,*,#17650,.T.);
#26040=ORIENTED_EDGE('',*,*,#17438,.T.);
#26041=ORIENTED_EDGE('',*,*,#17201,.T.);
#26042=ORIENTED_EDGE('',*,*,#16968,.T.);
#26043=ORIENTED_EDGE('',*,*,#17870,.T.);
#26044=ORIENTED_EDGE('',*,*,#16501,.T.);
#26045=ORIENTED_EDGE('',*,*,#16806,.T.);
#26046=ORIENTED_EDGE('',*,*,#17869,.F.);
#26047=ORIENTED_EDGE('',*,*,#16967,.T.);
#26048=ORIENTED_EDGE('',*,*,#17203,.T.);
#26049=ORIENTED_EDGE('',*,*,#17440,.T.);
#26050=ORIENTED_EDGE('',*,*,#17651,.T.);
#26051=ORIENTED_EDGE('',*,*,#16502,.T.);
#26052=ORIENTED_EDGE('',*,*,#17870,.F.);
#26053=ORIENTED_EDGE('',*,*,#16973,.T.);
#26054=ORIENTED_EDGE('',*,*,#17871,.T.);
#26055=ORIENTED_EDGE('',*,*,#16801,.T.);
#26056=ORIENTED_EDGE('',*,*,#17648,.T.);
#26057=ORIENTED_EDGE('',*,*,#17435,.T.);
#26058=ORIENTED_EDGE('',*,*,#17198,.T.);
#26059=ORIENTED_EDGE('',*,*,#16972,.T.);
#26060=ORIENTED_EDGE('',*,*,#17872,.T.);
#26061=ORIENTED_EDGE('',*,*,#16802,.T.);
#26062=ORIENTED_EDGE('',*,*,#17871,.F.);
#26063=ORIENTED_EDGE('',*,*,#16971,.T.);
#26064=ORIENTED_EDGE('',*,*,#17200,.T.);
#26065=ORIENTED_EDGE('',*,*,#17437,.T.);
#26066=ORIENTED_EDGE('',*,*,#17649,.T.);
#26067=ORIENTED_EDGE('',*,*,#16803,.T.);
#26068=ORIENTED_EDGE('',*,*,#17872,.F.);
#26069=ORIENTED_EDGE('',*,*,#16977,.T.);
#26070=ORIENTED_EDGE('',*,*,#17873,.T.);
#26071=ORIENTED_EDGE('',*,*,#16797,.T.);
#26072=ORIENTED_EDGE('',*,*,#17646,.T.);
#26073=ORIENTED_EDGE('',*,*,#17432,.T.);
#26074=ORIENTED_EDGE('',*,*,#17195,.T.);
#26075=ORIENTED_EDGE('',*,*,#16976,.T.);
#26076=ORIENTED_EDGE('',*,*,#17874,.T.);
#26077=ORIENTED_EDGE('',*,*,#16798,.T.);
#26078=ORIENTED_EDGE('',*,*,#17873,.F.);
#26079=ORIENTED_EDGE('',*,*,#16975,.T.);
#26080=ORIENTED_EDGE('',*,*,#17197,.T.);
#26081=ORIENTED_EDGE('',*,*,#17434,.T.);
#26082=ORIENTED_EDGE('',*,*,#17647,.T.);
#26083=ORIENTED_EDGE('',*,*,#16799,.T.);
#26084=ORIENTED_EDGE('',*,*,#17874,.F.);
#26085=ORIENTED_EDGE('',*,*,#16981,.T.);
#26086=ORIENTED_EDGE('',*,*,#17875,.T.);
#26087=ORIENTED_EDGE('',*,*,#16793,.T.);
#26088=ORIENTED_EDGE('',*,*,#17644,.T.);
#26089=ORIENTED_EDGE('',*,*,#17429,.T.);
#26090=ORIENTED_EDGE('',*,*,#17192,.T.);
#26091=ORIENTED_EDGE('',*,*,#16980,.T.);
#26092=ORIENTED_EDGE('',*,*,#17876,.T.);
#26093=ORIENTED_EDGE('',*,*,#16794,.T.);
#26094=ORIENTED_EDGE('',*,*,#17875,.F.);
#26095=ORIENTED_EDGE('',*,*,#16979,.T.);
#26096=ORIENTED_EDGE('',*,*,#17194,.T.);
#26097=ORIENTED_EDGE('',*,*,#17431,.T.);
#26098=ORIENTED_EDGE('',*,*,#17645,.T.);
#26099=ORIENTED_EDGE('',*,*,#16795,.T.);
#26100=ORIENTED_EDGE('',*,*,#17876,.F.);
#26101=ORIENTED_EDGE('',*,*,#16985,.T.);
#26102=ORIENTED_EDGE('',*,*,#17877,.T.);
#26103=ORIENTED_EDGE('',*,*,#16789,.T.);
#26104=ORIENTED_EDGE('',*,*,#17642,.T.);
#26105=ORIENTED_EDGE('',*,*,#17426,.T.);
#26106=ORIENTED_EDGE('',*,*,#17189,.T.);
#26107=ORIENTED_EDGE('',*,*,#16984,.T.);
#26108=ORIENTED_EDGE('',*,*,#17878,.T.);
#26109=ORIENTED_EDGE('',*,*,#16790,.T.);
#26110=ORIENTED_EDGE('',*,*,#17877,.F.);
#26111=ORIENTED_EDGE('',*,*,#16983,.T.);
#26112=ORIENTED_EDGE('',*,*,#17191,.T.);
#26113=ORIENTED_EDGE('',*,*,#17428,.T.);
#26114=ORIENTED_EDGE('',*,*,#17643,.T.);
#26115=ORIENTED_EDGE('',*,*,#16791,.T.);
#26116=ORIENTED_EDGE('',*,*,#17878,.F.);
#26117=ORIENTED_EDGE('',*,*,#16989,.T.);
#26118=ORIENTED_EDGE('',*,*,#17879,.T.);
#26119=ORIENTED_EDGE('',*,*,#16785,.T.);
#26120=ORIENTED_EDGE('',*,*,#17640,.T.);
#26121=ORIENTED_EDGE('',*,*,#17423,.T.);
#26122=ORIENTED_EDGE('',*,*,#17186,.T.);
#26123=ORIENTED_EDGE('',*,*,#16988,.T.);
#26124=ORIENTED_EDGE('',*,*,#17880,.T.);
#26125=ORIENTED_EDGE('',*,*,#16786,.T.);
#26126=ORIENTED_EDGE('',*,*,#17879,.F.);
#26127=ORIENTED_EDGE('',*,*,#16987,.T.);
#26128=ORIENTED_EDGE('',*,*,#17188,.T.);
#26129=ORIENTED_EDGE('',*,*,#17425,.T.);
#26130=ORIENTED_EDGE('',*,*,#17641,.T.);
#26131=ORIENTED_EDGE('',*,*,#16787,.T.);
#26132=ORIENTED_EDGE('',*,*,#17880,.F.);
#26133=ORIENTED_EDGE('',*,*,#16993,.T.);
#26134=ORIENTED_EDGE('',*,*,#17881,.T.);
#26135=ORIENTED_EDGE('',*,*,#16781,.T.);
#26136=ORIENTED_EDGE('',*,*,#17638,.T.);
#26137=ORIENTED_EDGE('',*,*,#17420,.T.);
#26138=ORIENTED_EDGE('',*,*,#17183,.T.);
#26139=ORIENTED_EDGE('',*,*,#16992,.T.);
#26140=ORIENTED_EDGE('',*,*,#17882,.T.);
#26141=ORIENTED_EDGE('',*,*,#16782,.T.);
#26142=ORIENTED_EDGE('',*,*,#17881,.F.);
#26143=ORIENTED_EDGE('',*,*,#16991,.T.);
#26144=ORIENTED_EDGE('',*,*,#17185,.T.);
#26145=ORIENTED_EDGE('',*,*,#17422,.T.);
#26146=ORIENTED_EDGE('',*,*,#17639,.T.);
#26147=ORIENTED_EDGE('',*,*,#16783,.T.);
#26148=ORIENTED_EDGE('',*,*,#17882,.F.);
#26149=ORIENTED_EDGE('',*,*,#16997,.T.);
#26150=ORIENTED_EDGE('',*,*,#17883,.T.);
#26151=ORIENTED_EDGE('',*,*,#16777,.T.);
#26152=ORIENTED_EDGE('',*,*,#17636,.T.);
#26153=ORIENTED_EDGE('',*,*,#17417,.T.);
#26154=ORIENTED_EDGE('',*,*,#17180,.T.);
#26155=ORIENTED_EDGE('',*,*,#16996,.T.);
#26156=ORIENTED_EDGE('',*,*,#17884,.T.);
#26157=ORIENTED_EDGE('',*,*,#16778,.T.);
#26158=ORIENTED_EDGE('',*,*,#17883,.F.);
#26159=ORIENTED_EDGE('',*,*,#16995,.T.);
#26160=ORIENTED_EDGE('',*,*,#17182,.T.);
#26161=ORIENTED_EDGE('',*,*,#17419,.T.);
#26162=ORIENTED_EDGE('',*,*,#17637,.T.);
#26163=ORIENTED_EDGE('',*,*,#16779,.T.);
#26164=ORIENTED_EDGE('',*,*,#17884,.F.);
#26165=ORIENTED_EDGE('',*,*,#17001,.T.);
#26166=ORIENTED_EDGE('',*,*,#17885,.T.);
#26167=ORIENTED_EDGE('',*,*,#16773,.T.);
#26168=ORIENTED_EDGE('',*,*,#17634,.T.);
#26169=ORIENTED_EDGE('',*,*,#17414,.T.);
#26170=ORIENTED_EDGE('',*,*,#17177,.T.);
#26171=ORIENTED_EDGE('',*,*,#17000,.T.);
#26172=ORIENTED_EDGE('',*,*,#17886,.T.);
#26173=ORIENTED_EDGE('',*,*,#16774,.T.);
#26174=ORIENTED_EDGE('',*,*,#17885,.F.);
#26175=ORIENTED_EDGE('',*,*,#16999,.T.);
#26176=ORIENTED_EDGE('',*,*,#17179,.T.);
#26177=ORIENTED_EDGE('',*,*,#17416,.T.);
#26178=ORIENTED_EDGE('',*,*,#17635,.T.);
#26179=ORIENTED_EDGE('',*,*,#16775,.T.);
#26180=ORIENTED_EDGE('',*,*,#17886,.F.);
#26181=ORIENTED_EDGE('',*,*,#17005,.T.);
#26182=ORIENTED_EDGE('',*,*,#17887,.T.);
#26183=ORIENTED_EDGE('',*,*,#16769,.T.);
#26184=ORIENTED_EDGE('',*,*,#17632,.T.);
#26185=ORIENTED_EDGE('',*,*,#17411,.T.);
#26186=ORIENTED_EDGE('',*,*,#17174,.T.);
#26187=ORIENTED_EDGE('',*,*,#17004,.T.);
#26188=ORIENTED_EDGE('',*,*,#17888,.T.);
#26189=ORIENTED_EDGE('',*,*,#16770,.T.);
#26190=ORIENTED_EDGE('',*,*,#17887,.F.);
#26191=ORIENTED_EDGE('',*,*,#17003,.T.);
#26192=ORIENTED_EDGE('',*,*,#17176,.T.);
#26193=ORIENTED_EDGE('',*,*,#17413,.T.);
#26194=ORIENTED_EDGE('',*,*,#17633,.T.);
#26195=ORIENTED_EDGE('',*,*,#16771,.T.);
#26196=ORIENTED_EDGE('',*,*,#17888,.F.);
#26197=ORIENTED_EDGE('',*,*,#17009,.T.);
#26198=ORIENTED_EDGE('',*,*,#17889,.T.);
#26199=ORIENTED_EDGE('',*,*,#16765,.T.);
#26200=ORIENTED_EDGE('',*,*,#17630,.T.);
#26201=ORIENTED_EDGE('',*,*,#17408,.T.);
#26202=ORIENTED_EDGE('',*,*,#17171,.T.);
#26203=ORIENTED_EDGE('',*,*,#17008,.T.);
#26204=ORIENTED_EDGE('',*,*,#17890,.T.);
#26205=ORIENTED_EDGE('',*,*,#16766,.T.);
#26206=ORIENTED_EDGE('',*,*,#17889,.F.);
#26207=ORIENTED_EDGE('',*,*,#17007,.T.);
#26208=ORIENTED_EDGE('',*,*,#17173,.T.);
#26209=ORIENTED_EDGE('',*,*,#17410,.T.);
#26210=ORIENTED_EDGE('',*,*,#17631,.T.);
#26211=ORIENTED_EDGE('',*,*,#16767,.T.);
#26212=ORIENTED_EDGE('',*,*,#17890,.F.);
#26213=ORIENTED_EDGE('',*,*,#17013,.T.);
#26214=ORIENTED_EDGE('',*,*,#17891,.T.);
#26215=ORIENTED_EDGE('',*,*,#16761,.T.);
#26216=ORIENTED_EDGE('',*,*,#17628,.T.);
#26217=ORIENTED_EDGE('',*,*,#17405,.T.);
#26218=ORIENTED_EDGE('',*,*,#17168,.T.);
#26219=ORIENTED_EDGE('',*,*,#17012,.T.);
#26220=ORIENTED_EDGE('',*,*,#17892,.T.);
#26221=ORIENTED_EDGE('',*,*,#16762,.T.);
#26222=ORIENTED_EDGE('',*,*,#17891,.F.);
#26223=ORIENTED_EDGE('',*,*,#17011,.T.);
#26224=ORIENTED_EDGE('',*,*,#17170,.T.);
#26225=ORIENTED_EDGE('',*,*,#17407,.T.);
#26226=ORIENTED_EDGE('',*,*,#17629,.T.);
#26227=ORIENTED_EDGE('',*,*,#16763,.T.);
#26228=ORIENTED_EDGE('',*,*,#17892,.F.);
#26229=ORIENTED_EDGE('',*,*,#17017,.T.);
#26230=ORIENTED_EDGE('',*,*,#17893,.T.);
#26231=ORIENTED_EDGE('',*,*,#16757,.T.);
#26232=ORIENTED_EDGE('',*,*,#17626,.T.);
#26233=ORIENTED_EDGE('',*,*,#17402,.T.);
#26234=ORIENTED_EDGE('',*,*,#17165,.T.);
#26235=ORIENTED_EDGE('',*,*,#17016,.T.);
#26236=ORIENTED_EDGE('',*,*,#17894,.T.);
#26237=ORIENTED_EDGE('',*,*,#16758,.T.);
#26238=ORIENTED_EDGE('',*,*,#17893,.F.);
#26239=ORIENTED_EDGE('',*,*,#17015,.T.);
#26240=ORIENTED_EDGE('',*,*,#17167,.T.);
#26241=ORIENTED_EDGE('',*,*,#17404,.T.);
#26242=ORIENTED_EDGE('',*,*,#17627,.T.);
#26243=ORIENTED_EDGE('',*,*,#16759,.T.);
#26244=ORIENTED_EDGE('',*,*,#17894,.F.);
#26245=ORIENTED_EDGE('',*,*,#17021,.T.);
#26246=ORIENTED_EDGE('',*,*,#17895,.T.);
#26247=ORIENTED_EDGE('',*,*,#16753,.T.);
#26248=ORIENTED_EDGE('',*,*,#17624,.T.);
#26249=ORIENTED_EDGE('',*,*,#17399,.T.);
#26250=ORIENTED_EDGE('',*,*,#17162,.T.);
#26251=ORIENTED_EDGE('',*,*,#17020,.T.);
#26252=ORIENTED_EDGE('',*,*,#17896,.T.);
#26253=ORIENTED_EDGE('',*,*,#16754,.T.);
#26254=ORIENTED_EDGE('',*,*,#17895,.F.);
#26255=ORIENTED_EDGE('',*,*,#17019,.T.);
#26256=ORIENTED_EDGE('',*,*,#17164,.T.);
#26257=ORIENTED_EDGE('',*,*,#17401,.T.);
#26258=ORIENTED_EDGE('',*,*,#17625,.T.);
#26259=ORIENTED_EDGE('',*,*,#16755,.T.);
#26260=ORIENTED_EDGE('',*,*,#17896,.F.);
#26261=ORIENTED_EDGE('',*,*,#17025,.T.);
#26262=ORIENTED_EDGE('',*,*,#17897,.T.);
#26263=ORIENTED_EDGE('',*,*,#16749,.T.);
#26264=ORIENTED_EDGE('',*,*,#17622,.T.);
#26265=ORIENTED_EDGE('',*,*,#17396,.T.);
#26266=ORIENTED_EDGE('',*,*,#17159,.T.);
#26267=ORIENTED_EDGE('',*,*,#17024,.T.);
#26268=ORIENTED_EDGE('',*,*,#17898,.T.);
#26269=ORIENTED_EDGE('',*,*,#16750,.T.);
#26270=ORIENTED_EDGE('',*,*,#17897,.F.);
#26271=ORIENTED_EDGE('',*,*,#17023,.T.);
#26272=ORIENTED_EDGE('',*,*,#17161,.T.);
#26273=ORIENTED_EDGE('',*,*,#17398,.T.);
#26274=ORIENTED_EDGE('',*,*,#17623,.T.);
#26275=ORIENTED_EDGE('',*,*,#16751,.T.);
#26276=ORIENTED_EDGE('',*,*,#17898,.F.);
#26277=ORIENTED_EDGE('',*,*,#17029,.T.);
#26278=ORIENTED_EDGE('',*,*,#17899,.T.);
#26279=ORIENTED_EDGE('',*,*,#16745,.T.);
#26280=ORIENTED_EDGE('',*,*,#17620,.T.);
#26281=ORIENTED_EDGE('',*,*,#17393,.T.);
#26282=ORIENTED_EDGE('',*,*,#17156,.T.);
#26283=ORIENTED_EDGE('',*,*,#17028,.T.);
#26284=ORIENTED_EDGE('',*,*,#17900,.T.);
#26285=ORIENTED_EDGE('',*,*,#16746,.T.);
#26286=ORIENTED_EDGE('',*,*,#17899,.F.);
#26287=ORIENTED_EDGE('',*,*,#17027,.T.);
#26288=ORIENTED_EDGE('',*,*,#17158,.T.);
#26289=ORIENTED_EDGE('',*,*,#17395,.T.);
#26290=ORIENTED_EDGE('',*,*,#17621,.T.);
#26291=ORIENTED_EDGE('',*,*,#16747,.T.);
#26292=ORIENTED_EDGE('',*,*,#17900,.F.);
#26293=ORIENTED_EDGE('',*,*,#17033,.T.);
#26294=ORIENTED_EDGE('',*,*,#17901,.T.);
#26295=ORIENTED_EDGE('',*,*,#16741,.T.);
#26296=ORIENTED_EDGE('',*,*,#17618,.T.);
#26297=ORIENTED_EDGE('',*,*,#17390,.T.);
#26298=ORIENTED_EDGE('',*,*,#17153,.T.);
#26299=ORIENTED_EDGE('',*,*,#17032,.T.);
#26300=ORIENTED_EDGE('',*,*,#17902,.T.);
#26301=ORIENTED_EDGE('',*,*,#16742,.T.);
#26302=ORIENTED_EDGE('',*,*,#17901,.F.);
#26303=ORIENTED_EDGE('',*,*,#17031,.T.);
#26304=ORIENTED_EDGE('',*,*,#17155,.T.);
#26305=ORIENTED_EDGE('',*,*,#17392,.T.);
#26306=ORIENTED_EDGE('',*,*,#17619,.T.);
#26307=ORIENTED_EDGE('',*,*,#16743,.T.);
#26308=ORIENTED_EDGE('',*,*,#17902,.F.);
#26309=ORIENTED_EDGE('',*,*,#17037,.T.);
#26310=ORIENTED_EDGE('',*,*,#17903,.T.);
#26311=ORIENTED_EDGE('',*,*,#16737,.T.);
#26312=ORIENTED_EDGE('',*,*,#17616,.T.);
#26313=ORIENTED_EDGE('',*,*,#17387,.T.);
#26314=ORIENTED_EDGE('',*,*,#17150,.T.);
#26315=ORIENTED_EDGE('',*,*,#17036,.T.);
#26316=ORIENTED_EDGE('',*,*,#17904,.T.);
#26317=ORIENTED_EDGE('',*,*,#16738,.T.);
#26318=ORIENTED_EDGE('',*,*,#17903,.F.);
#26319=ORIENTED_EDGE('',*,*,#17035,.T.);
#26320=ORIENTED_EDGE('',*,*,#17152,.T.);
#26321=ORIENTED_EDGE('',*,*,#17389,.T.);
#26322=ORIENTED_EDGE('',*,*,#17617,.T.);
#26323=ORIENTED_EDGE('',*,*,#16739,.T.);
#26324=ORIENTED_EDGE('',*,*,#17904,.F.);
#26325=ORIENTED_EDGE('',*,*,#17041,.T.);
#26326=ORIENTED_EDGE('',*,*,#17905,.T.);
#26327=ORIENTED_EDGE('',*,*,#16733,.T.);
#26328=ORIENTED_EDGE('',*,*,#17614,.T.);
#26329=ORIENTED_EDGE('',*,*,#17384,.T.);
#26330=ORIENTED_EDGE('',*,*,#17147,.T.);
#26331=ORIENTED_EDGE('',*,*,#17040,.T.);
#26332=ORIENTED_EDGE('',*,*,#17906,.T.);
#26333=ORIENTED_EDGE('',*,*,#16734,.T.);
#26334=ORIENTED_EDGE('',*,*,#17905,.F.);
#26335=ORIENTED_EDGE('',*,*,#17039,.T.);
#26336=ORIENTED_EDGE('',*,*,#17149,.T.);
#26337=ORIENTED_EDGE('',*,*,#17386,.T.);
#26338=ORIENTED_EDGE('',*,*,#17615,.T.);
#26339=ORIENTED_EDGE('',*,*,#16735,.T.);
#26340=ORIENTED_EDGE('',*,*,#17906,.F.);
#26341=ORIENTED_EDGE('',*,*,#17045,.T.);
#26342=ORIENTED_EDGE('',*,*,#17907,.T.);
#26343=ORIENTED_EDGE('',*,*,#16729,.T.);
#26344=ORIENTED_EDGE('',*,*,#17612,.T.);
#26345=ORIENTED_EDGE('',*,*,#17381,.T.);
#26346=ORIENTED_EDGE('',*,*,#17144,.T.);
#26347=ORIENTED_EDGE('',*,*,#17044,.T.);
#26348=ORIENTED_EDGE('',*,*,#17908,.T.);
#26349=ORIENTED_EDGE('',*,*,#16730,.T.);
#26350=ORIENTED_EDGE('',*,*,#17907,.F.);
#26351=ORIENTED_EDGE('',*,*,#17043,.T.);
#26352=ORIENTED_EDGE('',*,*,#17146,.T.);
#26353=ORIENTED_EDGE('',*,*,#17383,.T.);
#26354=ORIENTED_EDGE('',*,*,#17613,.T.);
#26355=ORIENTED_EDGE('',*,*,#16731,.T.);
#26356=ORIENTED_EDGE('',*,*,#17908,.F.);
#26357=ORIENTED_EDGE('',*,*,#17048,.T.);
#26358=ORIENTED_EDGE('',*,*,#16452,.T.);
#26359=ORIENTED_EDGE('',*,*,#16726,.T.);
#26360=ORIENTED_EDGE('',*,*,#17610,.T.);
#26361=ORIENTED_EDGE('',*,*,#17378,.T.);
#26362=ORIENTED_EDGE('',*,*,#17141,.T.);
#26363=ORIENTED_EDGE('',*,*,#17047,.T.);
#26364=ORIENTED_EDGE('',*,*,#17143,.T.);
#26365=ORIENTED_EDGE('',*,*,#17380,.T.);
#26366=ORIENTED_EDGE('',*,*,#17611,.T.);
#26367=ORIENTED_EDGE('',*,*,#16727,.T.);
#26368=ORIENTED_EDGE('',*,*,#16450,.F.);
#26369=ORIENTED_EDGE('',*,*,#17051,.T.);
#26370=ORIENTED_EDGE('',*,*,#16448,.T.);
#26371=ORIENTED_EDGE('',*,*,#16723,.T.);
#26372=ORIENTED_EDGE('',*,*,#17608,.T.);
#26373=ORIENTED_EDGE('',*,*,#17375,.T.);
#26374=ORIENTED_EDGE('',*,*,#17138,.T.);
#26375=ORIENTED_EDGE('',*,*,#17050,.T.);
#26376=ORIENTED_EDGE('',*,*,#17140,.T.);
#26377=ORIENTED_EDGE('',*,*,#17377,.T.);
#26378=ORIENTED_EDGE('',*,*,#17609,.T.);
#26379=ORIENTED_EDGE('',*,*,#16724,.T.);
#26380=ORIENTED_EDGE('',*,*,#16446,.F.);
#26381=ORIENTED_EDGE('',*,*,#17054,.T.);
#26382=ORIENTED_EDGE('',*,*,#16444,.T.);
#26383=ORIENTED_EDGE('',*,*,#16720,.T.);
#26384=ORIENTED_EDGE('',*,*,#17606,.T.);
#26385=ORIENTED_EDGE('',*,*,#17372,.T.);
#26386=ORIENTED_EDGE('',*,*,#17135,.T.);
#26387=ORIENTED_EDGE('',*,*,#17053,.T.);
#26388=ORIENTED_EDGE('',*,*,#17137,.T.);
#26389=ORIENTED_EDGE('',*,*,#17374,.T.);
#26390=ORIENTED_EDGE('',*,*,#17607,.T.);
#26391=ORIENTED_EDGE('',*,*,#16721,.T.);
#26392=ORIENTED_EDGE('',*,*,#16442,.F.);
#26393=ORIENTED_EDGE('',*,*,#17057,.T.);
#26394=ORIENTED_EDGE('',*,*,#16440,.T.);
#26395=ORIENTED_EDGE('',*,*,#16717,.T.);
#26396=ORIENTED_EDGE('',*,*,#17604,.T.);
#26397=ORIENTED_EDGE('',*,*,#17369,.T.);
#26398=ORIENTED_EDGE('',*,*,#17132,.T.);
#26399=ORIENTED_EDGE('',*,*,#17056,.T.);
#26400=ORIENTED_EDGE('',*,*,#17134,.T.);
#26401=ORIENTED_EDGE('',*,*,#17371,.T.);
#26402=ORIENTED_EDGE('',*,*,#17605,.T.);
#26403=ORIENTED_EDGE('',*,*,#16718,.T.);
#26404=ORIENTED_EDGE('',*,*,#16438,.F.);
#26405=ORIENTED_EDGE('',*,*,#17060,.T.);
#26406=ORIENTED_EDGE('',*,*,#16436,.T.);
#26407=ORIENTED_EDGE('',*,*,#16714,.T.);
#26408=ORIENTED_EDGE('',*,*,#17602,.T.);
#26409=ORIENTED_EDGE('',*,*,#17366,.T.);
#26410=ORIENTED_EDGE('',*,*,#17129,.T.);
#26411=ORIENTED_EDGE('',*,*,#17059,.T.);
#26412=ORIENTED_EDGE('',*,*,#17131,.T.);
#26413=ORIENTED_EDGE('',*,*,#17368,.T.);
#26414=ORIENTED_EDGE('',*,*,#17603,.T.);
#26415=ORIENTED_EDGE('',*,*,#16715,.T.);
#26416=ORIENTED_EDGE('',*,*,#16434,.F.);
#26417=ORIENTED_EDGE('',*,*,#17063,.T.);
#26418=ORIENTED_EDGE('',*,*,#16432,.T.);
#26419=ORIENTED_EDGE('',*,*,#16711,.T.);
#26420=ORIENTED_EDGE('',*,*,#17599,.T.);
#26421=ORIENTED_EDGE('',*,*,#17362,.T.);
#26422=ORIENTED_EDGE('',*,*,#17125,.T.);
#26423=ORIENTED_EDGE('',*,*,#17062,.T.);
#26424=ORIENTED_EDGE('',*,*,#17128,.T.);
#26425=ORIENTED_EDGE('',*,*,#17365,.T.);
#26426=ORIENTED_EDGE('',*,*,#17601,.T.);
#26427=ORIENTED_EDGE('',*,*,#16712,.T.);
#26428=ORIENTED_EDGE('',*,*,#16430,.F.);
#29954=PLANE('',#34712);
#29955=PLANE('',#34713);
#29956=PLANE('',#34723);
#29957=PLANE('',#34724);
#29958=PLANE('',#34725);
#29959=PLANE('',#34726);
#29960=PLANE('',#34727);
#29961=PLANE('',#34728);
#29962=PLANE('',#34729);
#29963=PLANE('',#34730);
#29964=PLANE('',#34732);
#29965=PLANE('',#34734);
#29966=PLANE('',#34735);
#29967=PLANE('',#34737);
#29968=PLANE('',#34738);
#29969=PLANE('',#34740);
#29970=PLANE('',#34741);
#29971=PLANE('',#34743);
#29972=PLANE('',#34744);
#29973=PLANE('',#34746);
#29974=PLANE('',#34747);
#29975=PLANE('',#34749);
#29976=PLANE('',#34750);
#29977=PLANE('',#34752);
#29978=PLANE('',#34753);
#29979=PLANE('',#34754);
#29980=PLANE('',#34755);
#29981=PLANE('',#34756);
#29982=PLANE('',#34757);
#29983=PLANE('',#34758);
#29984=PLANE('',#34759);
#29985=PLANE('',#34760);
#29986=PLANE('',#34761);
#29987=PLANE('',#34762);
#29988=PLANE('',#34763);
#29989=PLANE('',#34764);
#29990=PLANE('',#34765);
#29991=PLANE('',#34766);
#29992=PLANE('',#34767);
#29993=PLANE('',#34768);
#29994=PLANE('',#34769);
#29995=PLANE('',#34770);
#29996=PLANE('',#34771);
#29997=PLANE('',#34773);
#29998=PLANE('',#34774);
#29999=PLANE('',#34776);
#30000=PLANE('',#34777);
#30001=PLANE('',#34779);
#30002=PLANE('',#34780);
#30003=PLANE('',#34782);
#30004=PLANE('',#34783);
#30005=PLANE('',#34785);
#30006=PLANE('',#34786);
#30007=PLANE('',#34788);
#30008=PLANE('',#34789);
#30009=PLANE('',#34791);
#30010=PLANE('',#34792);
#30011=PLANE('',#34794);
#30012=PLANE('',#34795);
#30013=PLANE('',#34797);
#30014=PLANE('',#34798);
#30015=PLANE('',#34800);
#30016=PLANE('',#34801);
#30017=PLANE('',#34803);
#30018=PLANE('',#34804);
#30019=PLANE('',#34806);
#30020=PLANE('',#34807);
#30021=PLANE('',#34809);
#30022=PLANE('',#34810);
#30023=PLANE('',#34812);
#30024=PLANE('',#34813);
#30025=PLANE('',#34815);
#30026=PLANE('',#34816);
#30027=PLANE('',#34818);
#30028=PLANE('',#34819);
#30029=PLANE('',#34821);
#30030=PLANE('',#34822);
#30031=PLANE('',#34824);
#30032=PLANE('',#34825);
#30033=PLANE('',#34827);
#30034=PLANE('',#34828);
#30035=PLANE('',#34830);
#30036=PLANE('',#34831);
#30037=PLANE('',#34833);
#30038=PLANE('',#34834);
#30039=PLANE('',#34836);
#30040=PLANE('',#34837);
#30041=PLANE('',#34839);
#30042=PLANE('',#34840);
#30043=PLANE('',#34842);
#30044=PLANE('',#34843);
#30045=PLANE('',#34845);
#30046=PLANE('',#34846);
#30047=PLANE('',#34848);
#30048=PLANE('',#34849);
#30049=PLANE('',#34851);
#30050=PLANE('',#34852);
#30051=PLANE('',#34854);
#30052=PLANE('',#34855);
#30053=PLANE('',#34857);
#30054=PLANE('',#34858);
#30055=PLANE('',#34860);
#30056=PLANE('',#34861);
#30057=PLANE('',#34863);
#30058=PLANE('',#34864);
#30059=PLANE('',#34866);
#30060=PLANE('',#34867);
#30061=PLANE('',#34869);
#30062=PLANE('',#34870);
#30063=PLANE('',#34872);
#30064=PLANE('',#34873);
#30065=PLANE('',#34875);
#30066=PLANE('',#34876);
#30067=PLANE('',#34878);
#30068=PLANE('',#34879);
#30069=PLANE('',#34881);
#30070=PLANE('',#34882);
#30071=PLANE('',#34884);
#30072=PLANE('',#34885);
#30073=PLANE('',#34887);
#30074=PLANE('',#34888);
#30075=PLANE('',#34890);
#30076=PLANE('',#34891);
#30077=PLANE('',#34893);
#30078=PLANE('',#34894);
#30079=PLANE('',#34896);
#30080=PLANE('',#34897);
#30081=PLANE('',#34899);
#30082=PLANE('',#34900);
#30083=PLANE('',#34902);
#30084=PLANE('',#34903);
#30085=PLANE('',#34905);
#30086=PLANE('',#34906);
#30087=PLANE('',#34908);
#30088=PLANE('',#34909);
#30089=PLANE('',#34911);
#30090=PLANE('',#34912);
#30091=PLANE('',#34914);
#30092=PLANE('',#34915);
#30093=PLANE('',#34917);
#30094=PLANE('',#34918);
#30095=PLANE('',#34920);
#30096=PLANE('',#34921);
#30097=PLANE('',#34923);
#30098=PLANE('',#34924);
#30099=PLANE('',#34926);
#30100=PLANE('',#34927);
#30101=PLANE('',#34929);
#30102=PLANE('',#34930);
#30103=PLANE('',#34932);
#30104=PLANE('',#34933);
#30105=PLANE('',#34935);
#30106=PLANE('',#34936);
#30107=PLANE('',#34938);
#30108=PLANE('',#34939);
#30109=PLANE('',#34941);
#30110=PLANE('',#34942);
#30111=PLANE('',#34944);
#30112=PLANE('',#34945);
#30113=PLANE('',#34946);
#30114=PLANE('',#34947);
#30115=PLANE('',#34948);
#30116=PLANE('',#34949);
#30117=PLANE('',#34950);
#30118=PLANE('',#34951);
#30119=PLANE('',#34952);
#30120=PLANE('',#34953);
#30121=PLANE('',#34954);
#30122=PLANE('',#34955);
#30123=PLANE('',#34956);
#30895=ADVANCED_FACE('',(#5735),#4692,.T.);
#30896=ADVANCED_FACE('',(#5736),#4693,.T.);
#30897=ADVANCED_FACE('',(#5737),#4694,.T.);
#30898=ADVANCED_FACE('',(#5738),#4695,.T.);
#30899=ADVANCED_FACE('',(#5739),#4696,.T.);
#30900=ADVANCED_FACE('',(#5740),#4697,.T.);
#30901=ADVANCED_FACE('',(#5741),#4698,.T.);
#30902=ADVANCED_FACE('',(#5742),#4699,.T.);
#30903=ADVANCED_FACE('',(#5743),#4700,.T.);
#30904=ADVANCED_FACE('',(#5744),#4701,.T.);
#30905=ADVANCED_FACE('',(#5745),#4702,.T.);
#30906=ADVANCED_FACE('',(#5746),#4703,.T.);
#30907=ADVANCED_FACE('',(#5747),#4704,.T.);
#30908=ADVANCED_FACE('',(#5748),#4705,.T.);
#30909=ADVANCED_FACE('',(#5749),#4706,.T.);
#30910=ADVANCED_FACE('',(#5750),#4707,.T.);
#30911=ADVANCED_FACE('',(#5751),#4708,.T.);
#30912=ADVANCED_FACE('',(#5752),#4709,.T.);
#30913=ADVANCED_FACE('',(#5753),#4710,.T.);
#30914=ADVANCED_FACE('',(#5754),#4711,.T.);
#30915=ADVANCED_FACE('',(#5755),#4712,.T.);
#30916=ADVANCED_FACE('',(#5756),#4713,.T.);
#30917=ADVANCED_FACE('',(#5757),#4714,.T.);
#30918=ADVANCED_FACE('',(#5758),#4715,.T.);
#30919=ADVANCED_FACE('',(#5759),#4716,.T.);
#30920=ADVANCED_FACE('',(#5760),#4717,.T.);
#30921=ADVANCED_FACE('',(#5761),#4718,.T.);
#30922=ADVANCED_FACE('',(#5762),#4719,.T.);
#30923=ADVANCED_FACE('',(#5763),#2962,.T.);
#30924=ADVANCED_FACE('',(#5764),#4720,.T.);
#30925=ADVANCED_FACE('',(#5765),#4721,.T.);
#30926=ADVANCED_FACE('',(#5766),#4722,.T.);
#30927=ADVANCED_FACE('',(#5767),#4723,.T.);
#30928=ADVANCED_FACE('',(#5768),#4724,.T.);
#30929=ADVANCED_FACE('',(#5769),#4725,.T.);
#30930=ADVANCED_FACE('',(#5770),#4726,.T.);
#30931=ADVANCED_FACE('',(#5771),#4727,.T.);
#30932=ADVANCED_FACE('',(#5772),#4728,.T.);
#30933=ADVANCED_FACE('',(#5773),#4729,.T.);
#30934=ADVANCED_FACE('',(#5774),#4730,.T.);
#30935=ADVANCED_FACE('',(#5775),#4731,.T.);
#30936=ADVANCED_FACE('',(#5776),#4732,.T.);
#30937=ADVANCED_FACE('',(#5777),#4733,.T.);
#30938=ADVANCED_FACE('',(#5778),#4734,.T.);
#30939=ADVANCED_FACE('',(#5779),#4735,.T.);
#30940=ADVANCED_FACE('',(#5780),#4736,.T.);
#30941=ADVANCED_FACE('',(#5781),#4737,.T.);
#30942=ADVANCED_FACE('',(#5782),#4738,.T.);
#30943=ADVANCED_FACE('',(#5783),#4739,.T.);
#30944=ADVANCED_FACE('',(#5784),#4740,.T.);
#30945=ADVANCED_FACE('',(#5785),#4741,.T.);
#30946=ADVANCED_FACE('',(#5786),#4742,.T.);
#30947=ADVANCED_FACE('',(#5787),#4743,.T.);
#30948=ADVANCED_FACE('',(#5788),#4744,.T.);
#30949=ADVANCED_FACE('',(#5789),#4745,.T.);
#30950=ADVANCED_FACE('',(#5790),#4746,.T.);
#30951=ADVANCED_FACE('',(#5791),#4747,.T.);
#30952=ADVANCED_FACE('',(#5792),#4748,.T.);
#30953=ADVANCED_FACE('',(#5793),#4749,.T.);
#30954=ADVANCED_FACE('',(#5794),#4750,.T.);
#30955=ADVANCED_FACE('',(#5795),#2963,.T.);
#30956=ADVANCED_FACE('',(#5796),#4751,.T.);
#30957=ADVANCED_FACE('',(#5797),#4752,.F.);
#30958=ADVANCED_FACE('',(#5798),#4753,.F.);
#30959=ADVANCED_FACE('',(#5799),#4754,.F.);
#30960=ADVANCED_FACE('',(#5800),#4755,.F.);
#30961=ADVANCED_FACE('',(#5801),#4756,.F.);
#30962=ADVANCED_FACE('',(#5802),#4757,.F.);
#30963=ADVANCED_FACE('',(#5803),#4758,.F.);
#30964=ADVANCED_FACE('',(#5804),#4759,.F.);
#30965=ADVANCED_FACE('',(#5805),#4760,.F.);
#30966=ADVANCED_FACE('',(#5806),#4761,.F.);
#30967=ADVANCED_FACE('',(#5807),#4762,.F.);
#30968=ADVANCED_FACE('',(#5808),#4763,.F.);
#30969=ADVANCED_FACE('',(#5809),#4764,.F.);
#30970=ADVANCED_FACE('',(#5810),#4765,.F.);
#30971=ADVANCED_FACE('',(#5811),#4766,.F.);
#30972=ADVANCED_FACE('',(#5812),#2964,.F.);
#30973=ADVANCED_FACE('',(#5813),#213,.T.);
#30974=ADVANCED_FACE('',(#5814),#2965,.T.);
#30975=ADVANCED_FACE('',(#5815),#2966,.T.);
#30976=ADVANCED_FACE('',(#5816),#214,.F.);
#30977=ADVANCED_FACE('',(#5817),#4767,.T.);
#30978=ADVANCED_FACE('',(#5818),#215,.T.);
#30979=ADVANCED_FACE('',(#5819),#216,.F.);
#30980=ADVANCED_FACE('',(#5820),#217,.T.);
#30981=ADVANCED_FACE('',(#5821),#218,.T.);
#30982=ADVANCED_FACE('',(#5822),#219,.T.);
#30983=ADVANCED_FACE('',(#5823),#220,.T.);
#30984=ADVANCED_FACE('',(#5824),#221,.T.);
#30985=ADVANCED_FACE('',(#5825),#222,.T.);
#30986=ADVANCED_FACE('',(#5826),#223,.T.);
#30987=ADVANCED_FACE('',(#5827),#224,.T.);
#30988=ADVANCED_FACE('',(#5828),#225,.T.);
#30989=ADVANCED_FACE('',(#5829),#226,.T.);
#30990=ADVANCED_FACE('',(#5830),#227,.T.);
#30991=ADVANCED_FACE('',(#5831),#228,.T.);
#30992=ADVANCED_FACE('',(#5832),#229,.T.);
#30993=ADVANCED_FACE('',(#5833),#230,.T.);
#30994=ADVANCED_FACE('',(#5834),#231,.T.);
#30995=ADVANCED_FACE('',(#5835),#232,.T.);
#30996=ADVANCED_FACE('',(#5836),#233,.T.);
#30997=ADVANCED_FACE('',(#5837),#234,.T.);
#30998=ADVANCED_FACE('',(#5838),#235,.T.);
#30999=ADVANCED_FACE('',(#5839),#236,.T.);
#31000=ADVANCED_FACE('',(#5840),#237,.T.);
#31001=ADVANCED_FACE('',(#5841),#238,.T.);
#31002=ADVANCED_FACE('',(#5842),#239,.T.);
#31003=ADVANCED_FACE('',(#5843),#240,.T.);
#31004=ADVANCED_FACE('',(#5844),#241,.T.);
#31005=ADVANCED_FACE('',(#5845),#242,.T.);
#31006=ADVANCED_FACE('',(#5846),#243,.T.);
#31007=ADVANCED_FACE('',(#5847),#244,.T.);
#31008=ADVANCED_FACE('',(#5848),#245,.T.);
#31009=ADVANCED_FACE('',(#5849),#246,.T.);
#31010=ADVANCED_FACE('',(#5850),#247,.T.);
#31011=ADVANCED_FACE('',(#5851),#248,.T.);
#31012=ADVANCED_FACE('',(#5852),#249,.T.);
#31013=ADVANCED_FACE('',(#5853),#250,.T.);
#31014=ADVANCED_FACE('',(#5854),#251,.T.);
#31015=ADVANCED_FACE('',(#5855),#252,.T.);
#31016=ADVANCED_FACE('',(#5856),#253,.T.);
#31017=ADVANCED_FACE('',(#5857),#254,.T.);
#31018=ADVANCED_FACE('',(#5858),#255,.T.);
#31019=ADVANCED_FACE('',(#5859),#256,.T.);
#31020=ADVANCED_FACE('',(#5860),#257,.T.);
#31021=ADVANCED_FACE('',(#5861),#258,.T.);
#31022=ADVANCED_FACE('',(#5862),#259,.T.);
#31023=ADVANCED_FACE('',(#5863),#260,.T.);
#31024=ADVANCED_FACE('',(#5864),#261,.T.);
#31025=ADVANCED_FACE('',(#5865),#262,.T.);
#31026=ADVANCED_FACE('',(#5866),#263,.T.);
#31027=ADVANCED_FACE('',(#5867),#264,.T.);
#31028=ADVANCED_FACE('',(#5868),#265,.T.);
#31029=ADVANCED_FACE('',(#5869),#266,.T.);
#31030=ADVANCED_FACE('',(#5870),#267,.T.);
#31031=ADVANCED_FACE('',(#5871),#268,.T.);
#31032=ADVANCED_FACE('',(#5872),#269,.T.);
#31033=ADVANCED_FACE('',(#5873),#270,.T.);
#31034=ADVANCED_FACE('',(#5874),#271,.T.);
#31035=ADVANCED_FACE('',(#5875),#272,.T.);
#31036=ADVANCED_FACE('',(#5876),#273,.T.);
#31037=ADVANCED_FACE('',(#5877),#274,.T.);
#31038=ADVANCED_FACE('',(#5878),#275,.T.);
#31039=ADVANCED_FACE('',(#5879),#276,.T.);
#31040=ADVANCED_FACE('',(#5880),#277,.T.);
#31041=ADVANCED_FACE('',(#5881),#278,.T.);
#31042=ADVANCED_FACE('',(#5882),#279,.T.);
#31043=ADVANCED_FACE('',(#5883),#280,.T.);
#31044=ADVANCED_FACE('',(#5884),#281,.T.);
#31045=ADVANCED_FACE('',(#5885),#282,.T.);
#31046=ADVANCED_FACE('',(#5886),#283,.T.);
#31047=ADVANCED_FACE('',(#5887),#284,.T.);
#31048=ADVANCED_FACE('',(#5888),#285,.T.);
#31049=ADVANCED_FACE('',(#5889),#286,.T.);
#31050=ADVANCED_FACE('',(#5890),#287,.T.);
#31051=ADVANCED_FACE('',(#5891),#288,.T.);
#31052=ADVANCED_FACE('',(#5892),#289,.T.);
#31053=ADVANCED_FACE('',(#5893),#290,.T.);
#31054=ADVANCED_FACE('',(#5894),#291,.T.);
#31055=ADVANCED_FACE('',(#5895),#292,.T.);
#31056=ADVANCED_FACE('',(#5896),#293,.T.);
#31057=ADVANCED_FACE('',(#5897),#294,.T.);
#31058=ADVANCED_FACE('',(#5898),#295,.T.);
#31059=ADVANCED_FACE('',(#5899),#4768,.T.);
#31060=ADVANCED_FACE('',(#5900),#4769,.T.);
#31061=ADVANCED_FACE('',(#5901),#4770,.T.);
#31062=ADVANCED_FACE('',(#5902),#4771,.T.);
#31063=ADVANCED_FACE('',(#5903),#4772,.T.);
#31064=ADVANCED_FACE('',(#5904),#4773,.T.);
#31065=ADVANCED_FACE('',(#5905),#4774,.T.);
#31066=ADVANCED_FACE('',(#5906),#4775,.T.);
#31067=ADVANCED_FACE('',(#5907),#4776,.T.);
#31068=ADVANCED_FACE('',(#5908),#4777,.T.);
#31069=ADVANCED_FACE('',(#5909),#4778,.T.);
#31070=ADVANCED_FACE('',(#5910),#4779,.T.);
#31071=ADVANCED_FACE('',(#5911),#4780,.T.);
#31072=ADVANCED_FACE('',(#5912),#4781,.T.);
#31073=ADVANCED_FACE('',(#5913),#4782,.T.);
#31074=ADVANCED_FACE('',(#5914),#4783,.T.);
#31075=ADVANCED_FACE('',(#5915),#4784,.T.);
#31076=ADVANCED_FACE('',(#5916),#4785,.T.);
#31077=ADVANCED_FACE('',(#5917),#4786,.T.);
#31078=ADVANCED_FACE('',(#5918),#4787,.T.);
#31079=ADVANCED_FACE('',(#5919),#4788,.T.);
#31080=ADVANCED_FACE('',(#5920),#4789,.T.);
#31081=ADVANCED_FACE('',(#5921),#4790,.T.);
#31082=ADVANCED_FACE('',(#5922),#4791,.T.);
#31083=ADVANCED_FACE('',(#5923),#4792,.T.);
#31084=ADVANCED_FACE('',(#5924),#4793,.T.);
#31085=ADVANCED_FACE('',(#5925),#4794,.T.);
#31086=ADVANCED_FACE('',(#5926),#4795,.T.);
#31087=ADVANCED_FACE('',(#5927),#4796,.T.);
#31088=ADVANCED_FACE('',(#5928),#4797,.T.);
#31089=ADVANCED_FACE('',(#5929),#4798,.T.);
#31090=ADVANCED_FACE('',(#5930),#4799,.T.);
#31091=ADVANCED_FACE('',(#5931),#4800,.T.);
#31092=ADVANCED_FACE('',(#5932),#4801,.T.);
#31093=ADVANCED_FACE('',(#5933),#4802,.T.);
#31094=ADVANCED_FACE('',(#5934),#4803,.T.);
#31095=ADVANCED_FACE('',(#5935),#4804,.T.);
#31096=ADVANCED_FACE('',(#5936),#4805,.T.);
#31097=ADVANCED_FACE('',(#5937),#4806,.T.);
#31098=ADVANCED_FACE('',(#5938),#4807,.T.);
#31099=ADVANCED_FACE('',(#5939),#4808,.T.);
#31100=ADVANCED_FACE('',(#5940),#4809,.T.);
#31101=ADVANCED_FACE('',(#5941),#4810,.T.);
#31102=ADVANCED_FACE('',(#5942),#4811,.T.);
#31103=ADVANCED_FACE('',(#5943),#4812,.T.);
#31104=ADVANCED_FACE('',(#5944),#4813,.T.);
#31105=ADVANCED_FACE('',(#5945),#4814,.T.);
#31106=ADVANCED_FACE('',(#5946),#4815,.T.);
#31107=ADVANCED_FACE('',(#5947),#4816,.T.);
#31108=ADVANCED_FACE('',(#5948),#4817,.T.);
#31109=ADVANCED_FACE('',(#5949),#4818,.T.);
#31110=ADVANCED_FACE('',(#5950),#4819,.T.);
#31111=ADVANCED_FACE('',(#5951),#4820,.T.);
#31112=ADVANCED_FACE('',(#5952),#4821,.T.);
#31113=ADVANCED_FACE('',(#5953),#4822,.T.);
#31114=ADVANCED_FACE('',(#5954),#4823,.T.);
#31115=ADVANCED_FACE('',(#5955),#4824,.T.);
#31116=ADVANCED_FACE('',(#5956),#4825,.T.);
#31117=ADVANCED_FACE('',(#5957),#4826,.T.);
#31118=ADVANCED_FACE('',(#5958),#4827,.T.);
#31119=ADVANCED_FACE('',(#5959),#4828,.T.);
#31120=ADVANCED_FACE('',(#5960),#4829,.T.);
#31121=ADVANCED_FACE('',(#5961),#4830,.T.);
#31122=ADVANCED_FACE('',(#5962),#4831,.T.);
#31123=ADVANCED_FACE('',(#5963),#4832,.T.);
#31124=ADVANCED_FACE('',(#5964),#4833,.T.);
#31125=ADVANCED_FACE('',(#5965),#4834,.T.);
#31126=ADVANCED_FACE('',(#5966),#4835,.T.);
#31127=ADVANCED_FACE('',(#5967),#4836,.T.);
#31128=ADVANCED_FACE('',(#5968),#4837,.T.);
#31129=ADVANCED_FACE('',(#5969),#4838,.T.);
#31130=ADVANCED_FACE('',(#5970),#4839,.T.);
#31131=ADVANCED_FACE('',(#5971),#4840,.T.);
#31132=ADVANCED_FACE('',(#5972),#4841,.T.);
#31133=ADVANCED_FACE('',(#5973),#4842,.T.);
#31134=ADVANCED_FACE('',(#5974),#4843,.T.);
#31135=ADVANCED_FACE('',(#5975),#4844,.T.);
#31136=ADVANCED_FACE('',(#5976),#4845,.T.);
#31137=ADVANCED_FACE('',(#5977),#4846,.T.);
#31138=ADVANCED_FACE('',(#5978),#296,.T.);
#31139=ADVANCED_FACE('',(#5979),#297,.T.);
#31140=ADVANCED_FACE('',(#5980),#298,.T.);
#31141=ADVANCED_FACE('',(#5981),#299,.T.);
#31142=ADVANCED_FACE('',(#5982),#300,.T.);
#31143=ADVANCED_FACE('',(#5983),#301,.T.);
#31144=ADVANCED_FACE('',(#5984),#302,.T.);
#31145=ADVANCED_FACE('',(#5985),#303,.T.);
#31146=ADVANCED_FACE('',(#5986),#304,.T.);
#31147=ADVANCED_FACE('',(#5987),#305,.T.);
#31148=ADVANCED_FACE('',(#5988),#306,.T.);
#31149=ADVANCED_FACE('',(#5989),#307,.T.);
#31150=ADVANCED_FACE('',(#5990),#308,.T.);
#31151=ADVANCED_FACE('',(#5991),#309,.T.);
#31152=ADVANCED_FACE('',(#5992),#310,.T.);
#31153=ADVANCED_FACE('',(#5993),#311,.T.);
#31154=ADVANCED_FACE('',(#5994),#312,.T.);
#31155=ADVANCED_FACE('',(#5995),#313,.T.);
#31156=ADVANCED_FACE('',(#5996),#314,.T.);
#31157=ADVANCED_FACE('',(#5997),#315,.T.);
#31158=ADVANCED_FACE('',(#5998),#316,.T.);
#31159=ADVANCED_FACE('',(#5999),#317,.T.);
#31160=ADVANCED_FACE('',(#6000),#318,.T.);
#31161=ADVANCED_FACE('',(#6001),#319,.T.);
#31162=ADVANCED_FACE('',(#6002),#320,.T.);
#31163=ADVANCED_FACE('',(#6003),#321,.T.);
#31164=ADVANCED_FACE('',(#6004),#322,.T.);
#31165=ADVANCED_FACE('',(#6005),#323,.T.);
#31166=ADVANCED_FACE('',(#6006),#324,.T.);
#31167=ADVANCED_FACE('',(#6007),#325,.T.);
#31168=ADVANCED_FACE('',(#6008),#326,.T.);
#31169=ADVANCED_FACE('',(#6009),#327,.T.);
#31170=ADVANCED_FACE('',(#6010),#328,.T.);
#31171=ADVANCED_FACE('',(#6011),#329,.T.);
#31172=ADVANCED_FACE('',(#6012),#330,.T.);
#31173=ADVANCED_FACE('',(#6013),#331,.T.);
#31174=ADVANCED_FACE('',(#6014),#332,.T.);
#31175=ADVANCED_FACE('',(#6015),#333,.T.);
#31176=ADVANCED_FACE('',(#6016),#334,.T.);
#31177=ADVANCED_FACE('',(#6017),#335,.T.);
#31178=ADVANCED_FACE('',(#6018),#336,.T.);
#31179=ADVANCED_FACE('',(#6019),#337,.T.);
#31180=ADVANCED_FACE('',(#6020),#338,.T.);
#31181=ADVANCED_FACE('',(#6021),#339,.T.);
#31182=ADVANCED_FACE('',(#6022),#340,.T.);
#31183=ADVANCED_FACE('',(#6023),#341,.T.);
#31184=ADVANCED_FACE('',(#6024),#342,.T.);
#31185=ADVANCED_FACE('',(#6025),#343,.T.);
#31186=ADVANCED_FACE('',(#6026),#344,.T.);
#31187=ADVANCED_FACE('',(#6027),#345,.T.);
#31188=ADVANCED_FACE('',(#6028),#346,.T.);
#31189=ADVANCED_FACE('',(#6029),#347,.T.);
#31190=ADVANCED_FACE('',(#6030),#348,.T.);
#31191=ADVANCED_FACE('',(#6031),#349,.T.);
#31192=ADVANCED_FACE('',(#6032),#350,.T.);
#31193=ADVANCED_FACE('',(#6033),#351,.T.);
#31194=ADVANCED_FACE('',(#6034),#352,.T.);
#31195=ADVANCED_FACE('',(#6035),#353,.T.);
#31196=ADVANCED_FACE('',(#6036),#354,.T.);
#31197=ADVANCED_FACE('',(#6037),#355,.T.);
#31198=ADVANCED_FACE('',(#6038),#356,.T.);
#31199=ADVANCED_FACE('',(#6039),#357,.T.);
#31200=ADVANCED_FACE('',(#6040),#358,.T.);
#31201=ADVANCED_FACE('',(#6041),#359,.T.);
#31202=ADVANCED_FACE('',(#6042),#360,.T.);
#31203=ADVANCED_FACE('',(#6043),#361,.T.);
#31204=ADVANCED_FACE('',(#6044),#362,.T.);
#31205=ADVANCED_FACE('',(#6045),#363,.T.);
#31206=ADVANCED_FACE('',(#6046),#364,.T.);
#31207=ADVANCED_FACE('',(#6047),#365,.T.);
#31208=ADVANCED_FACE('',(#6048),#366,.T.);
#31209=ADVANCED_FACE('',(#6049),#367,.T.);
#31210=ADVANCED_FACE('',(#6050),#368,.T.);
#31211=ADVANCED_FACE('',(#6051),#369,.T.);
#31212=ADVANCED_FACE('',(#6052),#370,.T.);
#31213=ADVANCED_FACE('',(#6053),#371,.T.);
#31214=ADVANCED_FACE('',(#6054),#372,.T.);
#31215=ADVANCED_FACE('',(#6055),#373,.T.);
#31216=ADVANCED_FACE('',(#6056),#374,.T.);
#31217=ADVANCED_FACE('',(#6057),#29954,.T.);
#31218=ADVANCED_FACE('',(#6058,#3396),#29955,.T.);
#31219=ADVANCED_FACE('',(#6059),#375,.T.);
#31220=ADVANCED_FACE('',(#6060),#4847,.T.);
#31221=ADVANCED_FACE('',(#6061),#376,.T.);
#31222=ADVANCED_FACE('',(#6062,#3397),#29956,.T.);
#31223=ADVANCED_FACE('',(#6063),#29957,.T.);
#31224=ADVANCED_FACE('',(#6064),#29958,.F.);
#31225=ADVANCED_FACE('',(#6065),#29959,.F.);
#31226=ADVANCED_FACE('',(#6066),#29960,.F.);
#31227=ADVANCED_FACE('',(#6067),#29961,.F.);
#31228=ADVANCED_FACE('',(#6068),#29962,.F.);
#31229=ADVANCED_FACE('',(#6069),#29963,.F.);
#31230=ADVANCED_FACE('',(#6070),#45,.T.);
#31231=ADVANCED_FACE('',(#6071),#46,.T.);
#31232=ADVANCED_FACE('',(#6072),#2967,.T.);
#31233=ADVANCED_FACE('',(#6073),#29964,.F.);
#31234=ADVANCED_FACE('',(#6074),#4848,.F.);
#31235=ADVANCED_FACE('',(#6075),#29965,.F.);
#31236=ADVANCED_FACE('',(#6076),#29966,.F.);
#31237=ADVANCED_FACE('',(#6077),#4849,.F.);
#31238=ADVANCED_FACE('',(#6078),#29967,.F.);
#31239=ADVANCED_FACE('',(#6079),#29968,.F.);
#31240=ADVANCED_FACE('',(#6080),#4850,.F.);
#31241=ADVANCED_FACE('',(#6081),#29969,.F.);
#31242=ADVANCED_FACE('',(#6082),#29970,.F.);
#31243=ADVANCED_FACE('',(#6083),#4851,.F.);
#31244=ADVANCED_FACE('',(#6084),#29971,.F.);
#31245=ADVANCED_FACE('',(#6085),#29972,.F.);
#31246=ADVANCED_FACE('',(#6086),#4852,.F.);
#31247=ADVANCED_FACE('',(#6087),#29973,.F.);
#31248=ADVANCED_FACE('',(#6088),#29974,.F.);
#31249=ADVANCED_FACE('',(#6089),#4853,.F.);
#31250=ADVANCED_FACE('',(#6090),#29975,.F.);
#31251=ADVANCED_FACE('',(#6091),#29976,.F.);
#31252=ADVANCED_FACE('',(#6092),#4854,.F.);
#31253=ADVANCED_FACE('',(#6093),#29977,.F.);
#31254=ADVANCED_FACE('',(#6094),#29978,.F.);
#31255=ADVANCED_FACE('',(#6095),#29979,.F.);
#31256=ADVANCED_FACE('',(#6096),#29980,.F.);
#31257=ADVANCED_FACE('',(#6097),#29981,.F.);
#31258=ADVANCED_FACE('',(#6098),#29982,.F.);
#31259=ADVANCED_FACE('',(#6099),#29983,.F.);
#31260=ADVANCED_FACE('',(#6100),#29984,.F.);
#31261=ADVANCED_FACE('',(#6101),#29985,.F.);
#31262=ADVANCED_FACE('',(#6102),#29986,.F.);
#31263=ADVANCED_FACE('',(#6103),#29987,.F.);
#31264=ADVANCED_FACE('',(#6104),#29988,.F.);
#31265=ADVANCED_FACE('',(#6105),#29989,.F.);
#31266=ADVANCED_FACE('',(#6106),#29990,.F.);
#31267=ADVANCED_FACE('',(#6107),#29991,.F.);
#31268=ADVANCED_FACE('',(#6108),#29992,.F.);
#31269=ADVANCED_FACE('',(#6109),#29993,.F.);
#31270=ADVANCED_FACE('',(#6110),#29994,.F.);
#31271=ADVANCED_FACE('',(#6111),#29995,.F.);
#31272=ADVANCED_FACE('',(#6112),#29996,.F.);
#31273=ADVANCED_FACE('',(#6113),#4855,.F.);
#31274=ADVANCED_FACE('',(#6114),#29997,.F.);
#31275=ADVANCED_FACE('',(#6115),#29998,.F.);
#31276=ADVANCED_FACE('',(#6116),#4856,.F.);
#31277=ADVANCED_FACE('',(#6117),#29999,.F.);
#31278=ADVANCED_FACE('',(#6118),#30000,.F.);
#31279=ADVANCED_FACE('',(#6119),#4857,.F.);
#31280=ADVANCED_FACE('',(#6120),#30001,.F.);
#31281=ADVANCED_FACE('',(#6121),#30002,.F.);
#31282=ADVANCED_FACE('',(#6122),#4858,.F.);
#31283=ADVANCED_FACE('',(#6123),#30003,.F.);
#31284=ADVANCED_FACE('',(#6124),#30004,.F.);
#31285=ADVANCED_FACE('',(#6125),#4859,.F.);
#31286=ADVANCED_FACE('',(#6126),#30005,.F.);
#31287=ADVANCED_FACE('',(#6127),#30006,.F.);
#31288=ADVANCED_FACE('',(#6128),#4860,.F.);
#31289=ADVANCED_FACE('',(#6129),#30007,.F.);
#31290=ADVANCED_FACE('',(#6130),#30008,.F.);
#31291=ADVANCED_FACE('',(#6131),#4861,.F.);
#31292=ADVANCED_FACE('',(#6132),#30009,.F.);
#31293=ADVANCED_FACE('',(#6133),#30010,.F.);
#31294=ADVANCED_FACE('',(#6134),#4862,.F.);
#31295=ADVANCED_FACE('',(#6135),#30011,.F.);
#31296=ADVANCED_FACE('',(#6136),#30012,.F.);
#31297=ADVANCED_FACE('',(#6137),#4863,.F.);
#31298=ADVANCED_FACE('',(#6138),#30013,.F.);
#31299=ADVANCED_FACE('',(#6139),#30014,.F.);
#31300=ADVANCED_FACE('',(#6140),#4864,.F.);
#31301=ADVANCED_FACE('',(#6141),#30015,.F.);
#31302=ADVANCED_FACE('',(#6142),#30016,.F.);
#31303=ADVANCED_FACE('',(#6143),#4865,.F.);
#31304=ADVANCED_FACE('',(#6144),#30017,.F.);
#31305=ADVANCED_FACE('',(#6145),#30018,.F.);
#31306=ADVANCED_FACE('',(#6146),#4866,.F.);
#31307=ADVANCED_FACE('',(#6147),#30019,.F.);
#31308=ADVANCED_FACE('',(#6148),#30020,.F.);
#31309=ADVANCED_FACE('',(#6149),#4867,.F.);
#31310=ADVANCED_FACE('',(#6150),#30021,.F.);
#31311=ADVANCED_FACE('',(#6151),#30022,.F.);
#31312=ADVANCED_FACE('',(#6152),#4868,.F.);
#31313=ADVANCED_FACE('',(#6153),#30023,.F.);
#31314=ADVANCED_FACE('',(#6154),#30024,.F.);
#31315=ADVANCED_FACE('',(#6155),#4869,.F.);
#31316=ADVANCED_FACE('',(#6156),#30025,.F.);
#31317=ADVANCED_FACE('',(#6157),#30026,.F.);
#31318=ADVANCED_FACE('',(#6158),#4870,.F.);
#31319=ADVANCED_FACE('',(#6159),#30027,.F.);
#31320=ADVANCED_FACE('',(#6160),#30028,.F.);
#31321=ADVANCED_FACE('',(#6161),#4871,.F.);
#31322=ADVANCED_FACE('',(#6162),#30029,.F.);
#31323=ADVANCED_FACE('',(#6163),#30030,.F.);
#31324=ADVANCED_FACE('',(#6164),#4872,.F.);
#31325=ADVANCED_FACE('',(#6165),#30031,.F.);
#31326=ADVANCED_FACE('',(#6166),#30032,.F.);
#31327=ADVANCED_FACE('',(#6167),#4873,.F.);
#31328=ADVANCED_FACE('',(#6168),#30033,.F.);
#31329=ADVANCED_FACE('',(#6169),#30034,.F.);
#31330=ADVANCED_FACE('',(#6170),#4874,.F.);
#31331=ADVANCED_FACE('',(#6171),#30035,.F.);
#31332=ADVANCED_FACE('',(#6172),#30036,.F.);
#31333=ADVANCED_FACE('',(#6173),#4875,.F.);
#31334=ADVANCED_FACE('',(#6174),#30037,.F.);
#31335=ADVANCED_FACE('',(#6175),#30038,.F.);
#31336=ADVANCED_FACE('',(#6176),#4876,.F.);
#31337=ADVANCED_FACE('',(#6177),#30039,.F.);
#31338=ADVANCED_FACE('',(#6178),#30040,.F.);
#31339=ADVANCED_FACE('',(#6179),#4877,.F.);
#31340=ADVANCED_FACE('',(#6180),#30041,.F.);
#31341=ADVANCED_FACE('',(#6181),#30042,.F.);
#31342=ADVANCED_FACE('',(#6182),#4878,.F.);
#31343=ADVANCED_FACE('',(#6183),#30043,.F.);
#31344=ADVANCED_FACE('',(#6184),#30044,.F.);
#31345=ADVANCED_FACE('',(#6185),#4879,.F.);
#31346=ADVANCED_FACE('',(#6186),#30045,.F.);
#31347=ADVANCED_FACE('',(#6187),#30046,.F.);
#31348=ADVANCED_FACE('',(#6188),#4880,.F.);
#31349=ADVANCED_FACE('',(#6189),#30047,.F.);
#31350=ADVANCED_FACE('',(#6190),#30048,.F.);
#31351=ADVANCED_FACE('',(#6191),#4881,.F.);
#31352=ADVANCED_FACE('',(#6192),#30049,.F.);
#31353=ADVANCED_FACE('',(#6193),#30050,.F.);
#31354=ADVANCED_FACE('',(#6194),#4882,.F.);
#31355=ADVANCED_FACE('',(#6195),#30051,.F.);
#31356=ADVANCED_FACE('',(#6196),#30052,.F.);
#31357=ADVANCED_FACE('',(#6197),#4883,.F.);
#31358=ADVANCED_FACE('',(#6198),#30053,.F.);
#31359=ADVANCED_FACE('',(#6199),#30054,.F.);
#31360=ADVANCED_FACE('',(#6200),#4884,.F.);
#31361=ADVANCED_FACE('',(#6201),#30055,.F.);
#31362=ADVANCED_FACE('',(#6202),#30056,.F.);
#31363=ADVANCED_FACE('',(#6203),#4885,.F.);
#31364=ADVANCED_FACE('',(#6204),#30057,.F.);
#31365=ADVANCED_FACE('',(#6205),#30058,.F.);
#31366=ADVANCED_FACE('',(#6206),#4886,.F.);
#31367=ADVANCED_FACE('',(#6207),#30059,.F.);
#31368=ADVANCED_FACE('',(#6208),#30060,.F.);
#31369=ADVANCED_FACE('',(#6209),#4887,.F.);
#31370=ADVANCED_FACE('',(#6210),#30061,.F.);
#31371=ADVANCED_FACE('',(#6211),#30062,.F.);
#31372=ADVANCED_FACE('',(#6212),#4888,.F.);
#31373=ADVANCED_FACE('',(#6213),#30063,.F.);
#31374=ADVANCED_FACE('',(#6214),#30064,.F.);
#31375=ADVANCED_FACE('',(#6215),#4889,.F.);
#31376=ADVANCED_FACE('',(#6216),#30065,.F.);
#31377=ADVANCED_FACE('',(#6217),#30066,.F.);
#31378=ADVANCED_FACE('',(#6218),#4890,.F.);
#31379=ADVANCED_FACE('',(#6219),#30067,.F.);
#31380=ADVANCED_FACE('',(#6220),#30068,.F.);
#31381=ADVANCED_FACE('',(#6221),#4891,.F.);
#31382=ADVANCED_FACE('',(#6222),#30069,.F.);
#31383=ADVANCED_FACE('',(#6223),#30070,.F.);
#31384=ADVANCED_FACE('',(#6224),#4892,.F.);
#31385=ADVANCED_FACE('',(#6225),#30071,.F.);
#31386=ADVANCED_FACE('',(#6226),#30072,.F.);
#31387=ADVANCED_FACE('',(#6227),#4893,.F.);
#31388=ADVANCED_FACE('',(#6228),#30073,.F.);
#31389=ADVANCED_FACE('',(#6229),#30074,.F.);
#31390=ADVANCED_FACE('',(#6230),#4894,.F.);
#31391=ADVANCED_FACE('',(#6231),#30075,.F.);
#31392=ADVANCED_FACE('',(#6232),#30076,.F.);
#31393=ADVANCED_FACE('',(#6233),#4895,.F.);
#31394=ADVANCED_FACE('',(#6234),#30077,.F.);
#31395=ADVANCED_FACE('',(#6235),#30078,.F.);
#31396=ADVANCED_FACE('',(#6236),#4896,.F.);
#31397=ADVANCED_FACE('',(#6237),#30079,.F.);
#31398=ADVANCED_FACE('',(#6238),#30080,.F.);
#31399=ADVANCED_FACE('',(#6239),#4897,.F.);
#31400=ADVANCED_FACE('',(#6240),#30081,.F.);
#31401=ADVANCED_FACE('',(#6241),#30082,.F.);
#31402=ADVANCED_FACE('',(#6242),#4898,.F.);
#31403=ADVANCED_FACE('',(#6243),#30083,.F.);
#31404=ADVANCED_FACE('',(#6244),#30084,.F.);
#31405=ADVANCED_FACE('',(#6245),#4899,.F.);
#31406=ADVANCED_FACE('',(#6246),#30085,.F.);
#31407=ADVANCED_FACE('',(#6247),#30086,.F.);
#31408=ADVANCED_FACE('',(#6248),#4900,.F.);
#31409=ADVANCED_FACE('',(#6249),#30087,.F.);
#31410=ADVANCED_FACE('',(#6250),#30088,.F.);
#31411=ADVANCED_FACE('',(#6251),#4901,.F.);
#31412=ADVANCED_FACE('',(#6252),#30089,.F.);
#31413=ADVANCED_FACE('',(#6253),#30090,.F.);
#31414=ADVANCED_FACE('',(#6254),#4902,.F.);
#31415=ADVANCED_FACE('',(#6255),#30091,.F.);
#31416=ADVANCED_FACE('',(#6256),#30092,.F.);
#31417=ADVANCED_FACE('',(#6257),#4903,.F.);
#31418=ADVANCED_FACE('',(#6258),#30093,.F.);
#31419=ADVANCED_FACE('',(#6259),#30094,.F.);
#31420=ADVANCED_FACE('',(#6260),#4904,.F.);
#31421=ADVANCED_FACE('',(#6261),#30095,.F.);
#31422=ADVANCED_FACE('',(#6262),#30096,.F.);
#31423=ADVANCED_FACE('',(#6263),#4905,.F.);
#31424=ADVANCED_FACE('',(#6264),#30097,.F.);
#31425=ADVANCED_FACE('',(#6265),#30098,.F.);
#31426=ADVANCED_FACE('',(#6266),#4906,.F.);
#31427=ADVANCED_FACE('',(#6267),#30099,.F.);
#31428=ADVANCED_FACE('',(#6268),#30100,.F.);
#31429=ADVANCED_FACE('',(#6269),#4907,.F.);
#31430=ADVANCED_FACE('',(#6270),#30101,.F.);
#31431=ADVANCED_FACE('',(#6271),#30102,.F.);
#31432=ADVANCED_FACE('',(#6272),#4908,.F.);
#31433=ADVANCED_FACE('',(#6273),#30103,.F.);
#31434=ADVANCED_FACE('',(#6274),#30104,.F.);
#31435=ADVANCED_FACE('',(#6275),#4909,.F.);
#31436=ADVANCED_FACE('',(#6276),#30105,.F.);
#31437=ADVANCED_FACE('',(#6277),#30106,.F.);
#31438=ADVANCED_FACE('',(#6278),#4910,.F.);
#31439=ADVANCED_FACE('',(#6279),#30107,.F.);
#31440=ADVANCED_FACE('',(#6280),#30108,.F.);
#31441=ADVANCED_FACE('',(#6281),#4911,.F.);
#31442=ADVANCED_FACE('',(#6282),#30109,.F.);
#31443=ADVANCED_FACE('',(#6283),#30110,.F.);
#31444=ADVANCED_FACE('',(#6284),#4912,.F.);
#31445=ADVANCED_FACE('',(#6285),#30111,.F.);
#31446=ADVANCED_FACE('',(#6286),#30112,.F.);
#31447=ADVANCED_FACE('',(#6287),#30113,.F.);
#31448=ADVANCED_FACE('',(#6288),#30114,.F.);
#31449=ADVANCED_FACE('',(#6289),#30115,.F.);
#31450=ADVANCED_FACE('',(#6290),#30116,.F.);
#31451=ADVANCED_FACE('',(#6291),#30117,.F.);
#31452=ADVANCED_FACE('',(#6292),#30118,.F.);
#31453=ADVANCED_FACE('',(#6293),#30119,.F.);
#31454=ADVANCED_FACE('',(#6294),#30120,.F.);
#31455=ADVANCED_FACE('',(#6295),#30121,.F.);
#31456=ADVANCED_FACE('',(#6296),#30122,.F.);
#31457=ADVANCED_FACE('',(#6297),#30123,.F.);
#32027=CLOSED_SHELL('',(#30895,#30896,#30897,#30898,#30899,#30900,#30901,
#30902,#30903,#30904,#30905,#30906,#30907,#30908,#30909,#30910,#30911,#30912,
#30913,#30914,#30915,#30916,#30917,#30918,#30919,#30920,#30921,#30922,#30923,
#30924,#30925,#30926,#30927,#30928,#30929,#30930,#30931,#30932,#30933,#30934,
#30935,#30936,#30937,#30938,#30939,#30940,#30941,#30942,#30943,#30944,#30945,
#30946,#30947,#30948,#30949,#30950,#30951,#30952,#30953,#30954,#30955,#30956,
#30957,#30958,#30959,#30960,#30961,#30962,#30963,#30964,#30965,#30966,#30967,
#30968,#30969,#30970,#30971,#30972,#30973,#30974,#30975,#30976,#30977,#30978,
#30979,#30980,#30981,#30982,#30983,#30984,#30985,#30986,#30987,#30988,#30989,
#30990,#30991,#30992,#30993,#30994,#30995,#30996,#30997,#30998,#30999,#31000,
#31001,#31002,#31003,#31004,#31005,#31006,#31007,#31008,#31009,#31010,#31011,
#31012,#31013,#31014,#31015,#31016,#31017,#31018,#31019,#31020,#31021,#31022,
#31023,#31024,#31025,#31026,#31027,#31028,#31029,#31030,#31031,#31032,#31033,
#31034,#31035,#31036,#31037,#31038,#31039,#31040,#31041,#31042,#31043,#31044,
#31045,#31046,#31047,#31048,#31049,#31050,#31051,#31052,#31053,#31054,#31055,
#31056,#31057,#31058,#31059,#31060,#31061,#31062,#31063,#31064,#31065,#31066,
#31067,#31068,#31069,#31070,#31071,#31072,#31073,#31074,#31075,#31076,#31077,
#31078,#31079,#31080,#31081,#31082,#31083,#31084,#31085,#31086,#31087,#31088,
#31089,#31090,#31091,#31092,#31093,#31094,#31095,#31096,#31097,#31098,#31099,
#31100,#31101,#31102,#31103,#31104,#31105,#31106,#31107,#31108,#31109,#31110,
#31111,#31112,#31113,#31114,#31115,#31116,#31117,#31118,#31119,#31120,#31121,
#31122,#31123,#31124,#31125,#31126,#31127,#31128,#31129,#31130,#31131,#31132,
#31133,#31134,#31135,#31136,#31137,#31138,#31139,#31140,#31141,#31142,#31143,
#31144,#31145,#31146,#31147,#31148,#31149,#31150,#31151,#31152,#31153,#31154,
#31155,#31156,#31157,#31158,#31159,#31160,#31161,#31162,#31163,#31164,#31165,
#31166,#31167,#31168,#31169,#31170,#31171,#31172,#31173,#31174,#31175,#31176,
#31177,#31178,#31179,#31180,#31181,#31182,#31183,#31184,#31185,#31186,#31187,
#31188,#31189,#31190,#31191,#31192,#31193,#31194,#31195,#31196,#31197,#31198,
#31199,#31200,#31201,#31202,#31203,#31204,#31205,#31206,#31207,#31208,#31209,
#31210,#31211,#31212,#31213,#31214,#31215,#31216,#31217,#31218,#31219,#31220,
#31221,#31222,#31223,#31224,#31225,#31226,#31227,#31228,#31229,#31230,#31231,
#31232,#31233,#31234,#31235,#31236,#31237,#31238,#31239,#31240,#31241,#31242,
#31243,#31244,#31245,#31246,#31247,#31248,#31249,#31250,#31251,#31252,#31253,
#31254,#31255,#31256,#31257,#31258,#31259,#31260,#31261,#31262,#31263,#31264,
#31265,#31266,#31267,#31268,#31269,#31270,#31271,#31272,#31273,#31274,#31275,
#31276,#31277,#31278,#31279,#31280,#31281,#31282,#31283,#31284,#31285,#31286,
#31287,#31288,#31289,#31290,#31291,#31292,#31293,#31294,#31295,#31296,#31297,
#31298,#31299,#31300,#31301,#31302,#31303,#31304,#31305,#31306,#31307,#31308,
#31309,#31310,#31311,#31312,#31313,#31314,#31315,#31316,#31317,#31318,#31319,
#31320,#31321,#31322,#31323,#31324,#31325,#31326,#31327,#31328,#31329,#31330,
#31331,#31332,#31333,#31334,#31335,#31336,#31337,#31338,#31339,#31340,#31341,
#31342,#31343,#31344,#31345,#31346,#31347,#31348,#31349,#31350,#31351,#31352,
#31353,#31354,#31355,#31356,#31357,#31358,#31359,#31360,#31361,#31362,#31363,
#31364,#31365,#31366,#31367,#31368,#31369,#31370,#31371,#31372,#31373,#31374,
#31375,#31376,#31377,#31378,#31379,#31380,#31381,#31382,#31383,#31384,#31385,
#31386,#31387,#31388,#31389,#31390,#31391,#31392,#31393,#31394,#31395,#31396,
#31397,#31398,#31399,#31400,#31401,#31402,#31403,#31404,#31405,#31406,#31407,
#31408,#31409,#31410,#31411,#31412,#31413,#31414,#31415,#31416,#31417,#31418,
#31419,#31420,#31421,#31422,#31423,#31424,#31425,#31426,#31427,#31428,#31429,
#31430,#31431,#31432,#31433,#31434,#31435,#31436,#31437,#31438,#31439,#31440,
#31441,#31442,#31443,#31444,#31445,#31446,#31447,#31448,#31449,#31450,#31451,
#31452,#31453,#31454,#31455,#31456,#31457));
#33577=AXIS2_PLACEMENT_3D('',#55931,#39715,#39716);
#33578=AXIS2_PLACEMENT_3D('',#55932,#39717,#39718);
#33579=AXIS2_PLACEMENT_3D('',#55975,#39721,#39722);
#33580=AXIS2_PLACEMENT_3D('',#55977,#39723,#39724);
#33581=AXIS2_PLACEMENT_3D('',#56012,#39725,#39726);
#33582=AXIS2_PLACEMENT_3D('',#56088,#39728,#39729);
#33583=AXIS2_PLACEMENT_3D('',#56166,#39731,#39732);
#33584=AXIS2_PLACEMENT_3D('',#56242,#39734,#39735);
#33585=AXIS2_PLACEMENT_3D('',#56318,#39737,#39738);
#33586=AXIS2_PLACEMENT_3D('',#56394,#39740,#39741);
#33587=AXIS2_PLACEMENT_3D('',#56470,#39743,#39744);
#33588=AXIS2_PLACEMENT_3D('',#56548,#39746,#39747);
#33589=AXIS2_PLACEMENT_3D('',#56626,#39749,#39750);
#33590=AXIS2_PLACEMENT_3D('',#56702,#39752,#39753);
#33591=AXIS2_PLACEMENT_3D('',#56778,#39755,#39756);
#33592=AXIS2_PLACEMENT_3D('',#56854,#39758,#39759);
#33593=AXIS2_PLACEMENT_3D('',#56930,#39761,#39762);
#33594=AXIS2_PLACEMENT_3D('',#57008,#39764,#39765);
#33595=AXIS2_PLACEMENT_3D('',#57084,#39767,#39768);
#33596=AXIS2_PLACEMENT_3D('',#57162,#39770,#39771);
#33597=AXIS2_PLACEMENT_3D('',#57238,#39773,#39774);
#33598=AXIS2_PLACEMENT_3D('',#57314,#39776,#39777);
#33599=AXIS2_PLACEMENT_3D('',#57390,#39779,#39780);
#33600=AXIS2_PLACEMENT_3D('',#57466,#39782,#39783);
#33601=AXIS2_PLACEMENT_3D('',#57544,#39785,#39786);
#33602=AXIS2_PLACEMENT_3D('',#57622,#39788,#39789);
#33603=AXIS2_PLACEMENT_3D('',#57698,#39791,#39792);
#33604=AXIS2_PLACEMENT_3D('',#57774,#39794,#39795);
#33605=AXIS2_PLACEMENT_3D('',#57850,#39797,#39798);
#33606=AXIS2_PLACEMENT_3D('',#57926,#39800,#39801);
#33607=AXIS2_PLACEMENT_3D('',#58004,#39803,#39804);
#33608=AXIS2_PLACEMENT_3D('',#58080,#39806,#39807);
#33609=AXIS2_PLACEMENT_3D('',#58105,#39809,#39810);
#33610=AXIS2_PLACEMENT_3D('',#58106,#39811,#39812);
#33611=AXIS2_PLACEMENT_3D('',#58118,#39814,#39815);
#33612=AXIS2_PLACEMENT_3D('',#58119,#39816,#39817);
#33613=AXIS2_PLACEMENT_3D('',#58195,#39819,#39820);
#33614=AXIS2_PLACEMENT_3D('',#58271,#39822,#39823);
#33615=AXIS2_PLACEMENT_3D('',#58349,#39825,#39826);
#33616=AXIS2_PLACEMENT_3D('',#58425,#39828,#39829);
#33617=AXIS2_PLACEMENT_3D('',#58503,#39831,#39832);
#33618=AXIS2_PLACEMENT_3D('',#58579,#39834,#39835);
#33619=AXIS2_PLACEMENT_3D('',#58655,#39837,#39838);
#33620=AXIS2_PLACEMENT_3D('',#58731,#39840,#39841);
#33621=AXIS2_PLACEMENT_3D('',#58807,#39843,#39844);
#33622=AXIS2_PLACEMENT_3D('',#58885,#39846,#39847);
#33623=AXIS2_PLACEMENT_3D('',#58961,#39849,#39850);
#33624=AXIS2_PLACEMENT_3D('',#59039,#39852,#39853);
#33625=AXIS2_PLACEMENT_3D('',#59115,#39855,#39856);
#33626=AXIS2_PLACEMENT_3D('',#59191,#39858,#39859);
#33627=AXIS2_PLACEMENT_3D('',#59267,#39861,#39862);
#33628=AXIS2_PLACEMENT_3D('',#59343,#39864,#39865);
#33629=AXIS2_PLACEMENT_3D('',#59419,#39867,#39868);
#33630=AXIS2_PLACEMENT_3D('',#59497,#39870,#39871);
#33631=AXIS2_PLACEMENT_3D('',#59573,#39873,#39874);
#33632=AXIS2_PLACEMENT_3D('',#59651,#39876,#39877);
#33633=AXIS2_PLACEMENT_3D('',#59727,#39879,#39880);
#33634=AXIS2_PLACEMENT_3D('',#59803,#39882,#39883);
#33635=AXIS2_PLACEMENT_3D('',#59879,#39885,#39886);
#33636=AXIS2_PLACEMENT_3D('',#59955,#39888,#39889);
#33637=AXIS2_PLACEMENT_3D('',#60033,#39891,#39892);
#33638=AXIS2_PLACEMENT_3D('',#60109,#39894,#39895);
#33639=AXIS2_PLACEMENT_3D('',#60187,#39897,#39898);
#33640=AXIS2_PLACEMENT_3D('',#60263,#39900,#39901);
#33641=AXIS2_PLACEMENT_3D('',#60339,#39903,#39904);
#33642=AXIS2_PLACEMENT_3D('',#60349,#39905,#39906);
#33643=AXIS2_PLACEMENT_3D('',#60350,#39907,#39908);
#33644=AXIS2_PLACEMENT_3D('',#60351,#39909,#39910);
#33645=AXIS2_PLACEMENT_3D('',#60366,#39911,#39912);
#33646=AXIS2_PLACEMENT_3D('',#60389,#39913,#39914);
#33647=AXIS2_PLACEMENT_3D('',#60456,#39915,#39916);
#33648=AXIS2_PLACEMENT_3D('',#60459,#39917,#39918);
#33649=AXIS2_PLACEMENT_3D('',#60463,#39920,#39921);
#33650=AXIS2_PLACEMENT_3D('',#60465,#39923,#39924);
#33651=AXIS2_PLACEMENT_3D('',#60468,#39925,#39926);
#33652=AXIS2_PLACEMENT_3D('',#60472,#39928,#39929);
#33653=AXIS2_PLACEMENT_3D('',#60474,#39931,#39932);
#33654=AXIS2_PLACEMENT_3D('',#60477,#39933,#39934);
#33655=AXIS2_PLACEMENT_3D('',#60481,#39936,#39937);
#33656=AXIS2_PLACEMENT_3D('',#60483,#39939,#39940);
#33657=AXIS2_PLACEMENT_3D('',#60486,#39941,#39942);
#33658=AXIS2_PLACEMENT_3D('',#60490,#39944,#39945);
#33659=AXIS2_PLACEMENT_3D('',#60492,#39947,#39948);
#33660=AXIS2_PLACEMENT_3D('',#60495,#39949,#39950);
#33661=AXIS2_PLACEMENT_3D('',#60499,#39952,#39953);
#33662=AXIS2_PLACEMENT_3D('',#60501,#39955,#39956);
#33663=AXIS2_PLACEMENT_3D('',#60504,#39957,#39958);
#33664=AXIS2_PLACEMENT_3D('',#60508,#39960,#39961);
#33665=AXIS2_PLACEMENT_3D('',#60510,#39963,#39964);
#33666=AXIS2_PLACEMENT_3D('',#60513,#39965,#39966);
#33667=AXIS2_PLACEMENT_3D('',#60517,#39968,#39969);
#33668=AXIS2_PLACEMENT_3D('',#60519,#39971,#39972);
#33669=AXIS2_PLACEMENT_3D('',#60522,#39973,#39974);
#33670=AXIS2_PLACEMENT_3D('',#60526,#39976,#39977);
#33671=AXIS2_PLACEMENT_3D('',#60528,#39979,#39980);
#33672=AXIS2_PLACEMENT_3D('',#60531,#39981,#39982);
#33673=AXIS2_PLACEMENT_3D('',#60535,#39984,#39985);
#33674=AXIS2_PLACEMENT_3D('',#60537,#39987,#39988);
#33675=AXIS2_PLACEMENT_3D('',#60540,#39989,#39990);
#33676=AXIS2_PLACEMENT_3D('',#60544,#39992,#39993);
#33677=AXIS2_PLACEMENT_3D('',#60546,#39995,#39996);
#33678=AXIS2_PLACEMENT_3D('',#60549,#39997,#39998);
#33679=AXIS2_PLACEMENT_3D('',#60553,#40000,#40001);
#33680=AXIS2_PLACEMENT_3D('',#60555,#40003,#40004);
#33681=AXIS2_PLACEMENT_3D('',#60558,#40005,#40006);
#33682=AXIS2_PLACEMENT_3D('',#60562,#40008,#40009);
#33683=AXIS2_PLACEMENT_3D('',#60564,#40011,#40012);
#33684=AXIS2_PLACEMENT_3D('',#60567,#40013,#40014);
#33685=AXIS2_PLACEMENT_3D('',#60571,#40016,#40017);
#33686=AXIS2_PLACEMENT_3D('',#60573,#40019,#40020);
#33687=AXIS2_PLACEMENT_3D('',#60576,#40021,#40022);
#33688=AXIS2_PLACEMENT_3D('',#60580,#40024,#40025);
#33689=AXIS2_PLACEMENT_3D('',#60582,#40027,#40028);
#33690=AXIS2_PLACEMENT_3D('',#60585,#40029,#40030);
#33691=AXIS2_PLACEMENT_3D('',#60589,#40032,#40033);
#33692=AXIS2_PLACEMENT_3D('',#60591,#40035,#40036);
#33693=AXIS2_PLACEMENT_3D('',#60622,#40038,#40039);
#33694=AXIS2_PLACEMENT_3D('',#60623,#40040,#40041);
#33695=AXIS2_PLACEMENT_3D('',#60625,#40042,#40043);
#33696=AXIS2_PLACEMENT_3D('',#60627,#40044,#40045);
#33697=AXIS2_PLACEMENT_3D('',#60628,#40046,#40047);
#33698=AXIS2_PLACEMENT_3D('',#60629,#40048,#40049);
#33699=AXIS2_PLACEMENT_3D('',#60645,#40050,#40051);
#33700=AXIS2_PLACEMENT_3D('',#60651,#40052,#40053);
#33701=AXIS2_PLACEMENT_3D('',#60657,#40054,#40055);
#33702=AXIS2_PLACEMENT_3D('',#60663,#40056,#40057);
#33703=AXIS2_PLACEMENT_3D('',#60669,#40058,#40059);
#33704=AXIS2_PLACEMENT_3D('',#60675,#40060,#40061);
#33705=AXIS2_PLACEMENT_3D('',#60681,#40062,#40063);
#33706=AXIS2_PLACEMENT_3D('',#60687,#40064,#40065);
#33707=AXIS2_PLACEMENT_3D('',#60693,#40066,#40067);
#33708=AXIS2_PLACEMENT_3D('',#60699,#40068,#40069);
#33709=AXIS2_PLACEMENT_3D('',#60705,#40070,#40071);
#33710=AXIS2_PLACEMENT_3D('',#60711,#40072,#40073);
#33711=AXIS2_PLACEMENT_3D('',#60717,#40074,#40075);
#33712=AXIS2_PLACEMENT_3D('',#60723,#40076,#40077);
#33713=AXIS2_PLACEMENT_3D('',#60729,#40078,#40079);
#33714=AXIS2_PLACEMENT_3D('',#60735,#40080,#40081);
#33715=AXIS2_PLACEMENT_3D('',#60741,#40082,#40083);
#33716=AXIS2_PLACEMENT_3D('',#60747,#40084,#40085);
#33717=AXIS2_PLACEMENT_3D('',#60753,#40086,#40087);
#33718=AXIS2_PLACEMENT_3D('',#60759,#40088,#40089);
#33719=AXIS2_PLACEMENT_3D('',#60765,#40090,#40091);
#33720=AXIS2_PLACEMENT_3D('',#60771,#40092,#40093);
#33721=AXIS2_PLACEMENT_3D('',#60777,#40094,#40095);
#33722=AXIS2_PLACEMENT_3D('',#60783,#40096,#40097);
#33723=AXIS2_PLACEMENT_3D('',#60789,#40098,#40099);
#33724=AXIS2_PLACEMENT_3D('',#60795,#40100,#40101);
#33725=AXIS2_PLACEMENT_3D('',#60801,#40102,#40103);
#33726=AXIS2_PLACEMENT_3D('',#60807,#40104,#40105);
#33727=AXIS2_PLACEMENT_3D('',#60813,#40106,#40107);
#33728=AXIS2_PLACEMENT_3D('',#60819,#40108,#40109);
#33729=AXIS2_PLACEMENT_3D('',#60825,#40110,#40111);
#33730=AXIS2_PLACEMENT_3D('',#60831,#40112,#40113);
#33731=AXIS2_PLACEMENT_3D('',#60837,#40114,#40115);
#33732=AXIS2_PLACEMENT_3D('',#60843,#40116,#40117);
#33733=AXIS2_PLACEMENT_3D('',#60849,#40118,#40119);
#33734=AXIS2_PLACEMENT_3D('',#60855,#40120,#40121);
#33735=AXIS2_PLACEMENT_3D('',#60861,#40122,#40123);
#33736=AXIS2_PLACEMENT_3D('',#60867,#40124,#40125);
#33737=AXIS2_PLACEMENT_3D('',#60873,#40126,#40127);
#33738=AXIS2_PLACEMENT_3D('',#60879,#40128,#40129);
#33739=AXIS2_PLACEMENT_3D('',#60885,#40130,#40131);
#33740=AXIS2_PLACEMENT_3D('',#60891,#40132,#40133);
#33741=AXIS2_PLACEMENT_3D('',#60897,#40134,#40135);
#33742=AXIS2_PLACEMENT_3D('',#60903,#40136,#40137);
#33743=AXIS2_PLACEMENT_3D('',#60909,#40138,#40139);
#33744=AXIS2_PLACEMENT_3D('',#60915,#40140,#40141);
#33745=AXIS2_PLACEMENT_3D('',#60921,#40142,#40143);
#33746=AXIS2_PLACEMENT_3D('',#60927,#40144,#40145);
#33747=AXIS2_PLACEMENT_3D('',#60933,#40146,#40147);
#33748=AXIS2_PLACEMENT_3D('',#60939,#40148,#40149);
#33749=AXIS2_PLACEMENT_3D('',#60945,#40150,#40151);
#33750=AXIS2_PLACEMENT_3D('',#60951,#40152,#40153);
#33751=AXIS2_PLACEMENT_3D('',#60957,#40154,#40155);
#33752=AXIS2_PLACEMENT_3D('',#60963,#40156,#40157);
#33753=AXIS2_PLACEMENT_3D('',#60969,#40158,#40159);
#33754=AXIS2_PLACEMENT_3D('',#60975,#40160,#40161);
#33755=AXIS2_PLACEMENT_3D('',#60981,#40162,#40163);
#33756=AXIS2_PLACEMENT_3D('',#60987,#40164,#40165);
#33757=AXIS2_PLACEMENT_3D('',#60993,#40166,#40167);
#33758=AXIS2_PLACEMENT_3D('',#60999,#40168,#40169);
#33759=AXIS2_PLACEMENT_3D('',#61005,#40170,#40171);
#33760=AXIS2_PLACEMENT_3D('',#61011,#40172,#40173);
#33761=AXIS2_PLACEMENT_3D('',#61017,#40174,#40175);
#33762=AXIS2_PLACEMENT_3D('',#61023,#40176,#40177);
#33763=AXIS2_PLACEMENT_3D('',#61029,#40178,#40179);
#33764=AXIS2_PLACEMENT_3D('',#61035,#40180,#40181);
#33765=AXIS2_PLACEMENT_3D('',#61041,#40182,#40183);
#33766=AXIS2_PLACEMENT_3D('',#61047,#40184,#40185);
#33767=AXIS2_PLACEMENT_3D('',#61053,#40186,#40187);
#33768=AXIS2_PLACEMENT_3D('',#61059,#40188,#40189);
#33769=AXIS2_PLACEMENT_3D('',#61065,#40190,#40191);
#33770=AXIS2_PLACEMENT_3D('',#61071,#40192,#40193);
#33771=AXIS2_PLACEMENT_3D('',#61077,#40194,#40195);
#33772=AXIS2_PLACEMENT_3D('',#61083,#40196,#40197);
#33773=AXIS2_PLACEMENT_3D('',#61089,#40198,#40199);
#33774=AXIS2_PLACEMENT_3D('',#61095,#40200,#40201);
#33775=AXIS2_PLACEMENT_3D('',#61101,#40202,#40203);
#33776=AXIS2_PLACEMENT_3D('',#61107,#40204,#40205);
#33777=AXIS2_PLACEMENT_3D('',#61113,#40206,#40207);
#33778=AXIS2_PLACEMENT_3D('',#61119,#40208,#40209);
#33779=AXIS2_PLACEMENT_3D('',#61125,#40210,#40211);
#33780=AXIS2_PLACEMENT_3D('',#61131,#40212,#40213);
#33781=AXIS2_PLACEMENT_3D('',#61137,#40214,#40215);
#33782=AXIS2_PLACEMENT_3D('',#61143,#40216,#40217);
#33783=AXIS2_PLACEMENT_3D('',#61149,#40218,#40219);
#33784=AXIS2_PLACEMENT_3D('',#61155,#40220,#40221);
#33785=AXIS2_PLACEMENT_3D('',#61161,#40222,#40223);
#33786=AXIS2_PLACEMENT_3D('',#61167,#40224,#40225);
#33787=AXIS2_PLACEMENT_3D('',#61173,#40226,#40227);
#33788=AXIS2_PLACEMENT_3D('',#61179,#40228,#40229);
#33789=AXIS2_PLACEMENT_3D('',#61185,#40230,#40231);
#33790=AXIS2_PLACEMENT_3D('',#61194,#40232,#40233);
#33791=AXIS2_PLACEMENT_3D('',#61203,#40234,#40235);
#33792=AXIS2_PLACEMENT_3D('',#61212,#40236,#40237);
#33793=AXIS2_PLACEMENT_3D('',#61221,#40238,#40239);
#33794=AXIS2_PLACEMENT_3D('',#61230,#40240,#40241);
#33795=AXIS2_PLACEMENT_3D('',#61239,#40242,#40243);
#33796=AXIS2_PLACEMENT_3D('',#61248,#40244,#40245);
#33797=AXIS2_PLACEMENT_3D('',#61257,#40246,#40247);
#33798=AXIS2_PLACEMENT_3D('',#61266,#40248,#40249);
#33799=AXIS2_PLACEMENT_3D('',#61275,#40250,#40251);
#33800=AXIS2_PLACEMENT_3D('',#61284,#40252,#40253);
#33801=AXIS2_PLACEMENT_3D('',#61293,#40254,#40255);
#33802=AXIS2_PLACEMENT_3D('',#61302,#40256,#40257);
#33803=AXIS2_PLACEMENT_3D('',#61311,#40258,#40259);
#33804=AXIS2_PLACEMENT_3D('',#61320,#40260,#40261);
#33805=AXIS2_PLACEMENT_3D('',#61326,#40262,#40263);
#33806=AXIS2_PLACEMENT_3D('',#61332,#40264,#40265);
#33807=AXIS2_PLACEMENT_3D('',#61338,#40266,#40267);
#33808=AXIS2_PLACEMENT_3D('',#61344,#40268,#40269);
#33809=AXIS2_PLACEMENT_3D('',#61350,#40270,#40271);
#33810=AXIS2_PLACEMENT_3D('',#61356,#40272,#40273);
#33811=AXIS2_PLACEMENT_3D('',#61362,#40274,#40275);
#33812=AXIS2_PLACEMENT_3D('',#61368,#40276,#40277);
#33813=AXIS2_PLACEMENT_3D('',#61374,#40278,#40279);
#33814=AXIS2_PLACEMENT_3D('',#61380,#40280,#40281);
#33815=AXIS2_PLACEMENT_3D('',#61386,#40282,#40283);
#33816=AXIS2_PLACEMENT_3D('',#61392,#40284,#40285);
#33817=AXIS2_PLACEMENT_3D('',#61398,#40286,#40287);
#33818=AXIS2_PLACEMENT_3D('',#61404,#40288,#40289);
#33819=AXIS2_PLACEMENT_3D('',#61410,#40290,#40291);
#33820=AXIS2_PLACEMENT_3D('',#61416,#40292,#40293);
#33821=AXIS2_PLACEMENT_3D('',#61422,#40294,#40295);
#33822=AXIS2_PLACEMENT_3D('',#61428,#40296,#40297);
#33823=AXIS2_PLACEMENT_3D('',#61434,#40298,#40299);
#33824=AXIS2_PLACEMENT_3D('',#61440,#40300,#40301);
#33825=AXIS2_PLACEMENT_3D('',#61446,#40302,#40303);
#33826=AXIS2_PLACEMENT_3D('',#61452,#40304,#40305);
#33827=AXIS2_PLACEMENT_3D('',#61458,#40306,#40307);
#33828=AXIS2_PLACEMENT_3D('',#61464,#40308,#40309);
#33829=AXIS2_PLACEMENT_3D('',#61470,#40310,#40311);
#33830=AXIS2_PLACEMENT_3D('',#61476,#40312,#40313);
#33831=AXIS2_PLACEMENT_3D('',#61482,#40314,#40315);
#33832=AXIS2_PLACEMENT_3D('',#61488,#40316,#40317);
#33833=AXIS2_PLACEMENT_3D('',#61494,#40318,#40319);
#33834=AXIS2_PLACEMENT_3D('',#61500,#40320,#40321);
#33835=AXIS2_PLACEMENT_3D('',#61506,#40322,#40323);
#33836=AXIS2_PLACEMENT_3D('',#61512,#40324,#40325);
#33837=AXIS2_PLACEMENT_3D('',#61518,#40326,#40327);
#33838=AXIS2_PLACEMENT_3D('',#61524,#40328,#40329);
#33839=AXIS2_PLACEMENT_3D('',#61530,#40330,#40331);
#33840=AXIS2_PLACEMENT_3D('',#61536,#40332,#40333);
#33841=AXIS2_PLACEMENT_3D('',#61542,#40334,#40335);
#33842=AXIS2_PLACEMENT_3D('',#61548,#40336,#40337);
#33843=AXIS2_PLACEMENT_3D('',#61562,#40339,#40340);
#33844=AXIS2_PLACEMENT_3D('',#61578,#40341,#40342);
#33845=AXIS2_PLACEMENT_3D('',#61584,#40343,#40344);
#33846=AXIS2_PLACEMENT_3D('',#61590,#40345,#40346);
#33847=AXIS2_PLACEMENT_3D('',#61596,#40347,#40348);
#33848=AXIS2_PLACEMENT_3D('',#61602,#40349,#40350);
#33849=AXIS2_PLACEMENT_3D('',#61608,#40351,#40352);
#33850=AXIS2_PLACEMENT_3D('',#61614,#40353,#40354);
#33851=AXIS2_PLACEMENT_3D('',#61620,#40355,#40356);
#33852=AXIS2_PLACEMENT_3D('',#61626,#40357,#40358);
#33853=AXIS2_PLACEMENT_3D('',#61632,#40359,#40360);
#33854=AXIS2_PLACEMENT_3D('',#61638,#40361,#40362);
#33855=AXIS2_PLACEMENT_3D('',#61644,#40363,#40364);
#33856=AXIS2_PLACEMENT_3D('',#61650,#40365,#40366);
#33857=AXIS2_PLACEMENT_3D('',#61656,#40367,#40368);
#33858=AXIS2_PLACEMENT_3D('',#61662,#40369,#40370);
#33859=AXIS2_PLACEMENT_3D('',#61668,#40371,#40372);
#33860=AXIS2_PLACEMENT_3D('',#61674,#40373,#40374);
#33861=AXIS2_PLACEMENT_3D('',#61680,#40375,#40376);
#33862=AXIS2_PLACEMENT_3D('',#61686,#40377,#40378);
#33863=AXIS2_PLACEMENT_3D('',#61692,#40379,#40380);
#33864=AXIS2_PLACEMENT_3D('',#61698,#40381,#40382);
#33865=AXIS2_PLACEMENT_3D('',#61704,#40383,#40384);
#33866=AXIS2_PLACEMENT_3D('',#61710,#40385,#40386);
#33867=AXIS2_PLACEMENT_3D('',#61716,#40387,#40388);
#33868=AXIS2_PLACEMENT_3D('',#61722,#40389,#40390);
#33869=AXIS2_PLACEMENT_3D('',#61728,#40391,#40392);
#33870=AXIS2_PLACEMENT_3D('',#61734,#40393,#40394);
#33871=AXIS2_PLACEMENT_3D('',#61740,#40395,#40396);
#33872=AXIS2_PLACEMENT_3D('',#61746,#40397,#40398);
#33873=AXIS2_PLACEMENT_3D('',#61752,#40399,#40400);
#33874=AXIS2_PLACEMENT_3D('',#61758,#40401,#40402);
#33875=AXIS2_PLACEMENT_3D('',#61764,#40403,#40404);
#33876=AXIS2_PLACEMENT_3D('',#61770,#40405,#40406);
#33877=AXIS2_PLACEMENT_3D('',#61776,#40407,#40408);
#33878=AXIS2_PLACEMENT_3D('',#61782,#40409,#40410);
#33879=AXIS2_PLACEMENT_3D('',#61788,#40411,#40412);
#33880=AXIS2_PLACEMENT_3D('',#61794,#40413,#40414);
#33881=AXIS2_PLACEMENT_3D('',#61800,#40415,#40416);
#33882=AXIS2_PLACEMENT_3D('',#61806,#40417,#40418);
#33883=AXIS2_PLACEMENT_3D('',#61812,#40419,#40420);
#33884=AXIS2_PLACEMENT_3D('',#61818,#40421,#40422);
#33885=AXIS2_PLACEMENT_3D('',#61824,#40423,#40424);
#33886=AXIS2_PLACEMENT_3D('',#61830,#40425,#40426);
#33887=AXIS2_PLACEMENT_3D('',#61836,#40427,#40428);
#33888=AXIS2_PLACEMENT_3D('',#61842,#40429,#40430);
#33889=AXIS2_PLACEMENT_3D('',#61848,#40431,#40432);
#33890=AXIS2_PLACEMENT_3D('',#61854,#40433,#40434);
#33891=AXIS2_PLACEMENT_3D('',#61860,#40435,#40436);
#33892=AXIS2_PLACEMENT_3D('',#61866,#40437,#40438);
#33893=AXIS2_PLACEMENT_3D('',#61872,#40439,#40440);
#33894=AXIS2_PLACEMENT_3D('',#61878,#40441,#40442);
#33895=AXIS2_PLACEMENT_3D('',#61884,#40443,#40444);
#33896=AXIS2_PLACEMENT_3D('',#61890,#40445,#40446);
#33897=AXIS2_PLACEMENT_3D('',#61896,#40447,#40448);
#33898=AXIS2_PLACEMENT_3D('',#61902,#40449,#40450);
#33899=AXIS2_PLACEMENT_3D('',#61908,#40451,#40452);
#33900=AXIS2_PLACEMENT_3D('',#61914,#40453,#40454);
#33901=AXIS2_PLACEMENT_3D('',#61920,#40455,#40456);
#33902=AXIS2_PLACEMENT_3D('',#61926,#40457,#40458);
#33903=AXIS2_PLACEMENT_3D('',#61932,#40459,#40460);
#33904=AXIS2_PLACEMENT_3D('',#61938,#40461,#40462);
#33905=AXIS2_PLACEMENT_3D('',#61944,#40463,#40464);
#33906=AXIS2_PLACEMENT_3D('',#61950,#40465,#40466);
#33907=AXIS2_PLACEMENT_3D('',#61956,#40467,#40468);
#33908=AXIS2_PLACEMENT_3D('',#61962,#40469,#40470);
#33909=AXIS2_PLACEMENT_3D('',#61968,#40471,#40472);
#33910=AXIS2_PLACEMENT_3D('',#61974,#40473,#40474);
#33911=AXIS2_PLACEMENT_3D('',#61980,#40475,#40476);
#33912=AXIS2_PLACEMENT_3D('',#61986,#40477,#40478);
#33913=AXIS2_PLACEMENT_3D('',#61992,#40479,#40480);
#33914=AXIS2_PLACEMENT_3D('',#61998,#40481,#40482);
#33915=AXIS2_PLACEMENT_3D('',#62004,#40483,#40484);
#33916=AXIS2_PLACEMENT_3D('',#62010,#40485,#40486);
#33917=AXIS2_PLACEMENT_3D('',#62016,#40487,#40488);
#33918=AXIS2_PLACEMENT_3D('',#62022,#40489,#40490);
#33919=AXIS2_PLACEMENT_3D('',#62028,#40491,#40492);
#33920=AXIS2_PLACEMENT_3D('',#62034,#40493,#40494);
#33921=AXIS2_PLACEMENT_3D('',#62040,#40495,#40496);
#33922=AXIS2_PLACEMENT_3D('',#62046,#40497,#40498);
#33923=AXIS2_PLACEMENT_3D('',#62052,#40499,#40500);
#33924=AXIS2_PLACEMENT_3D('',#62058,#40501,#40502);
#33925=AXIS2_PLACEMENT_3D('',#62064,#40503,#40504);
#33926=AXIS2_PLACEMENT_3D('',#62070,#40505,#40506);
#33927=AXIS2_PLACEMENT_3D('',#62076,#40507,#40508);
#33928=AXIS2_PLACEMENT_3D('',#62082,#40509,#40510);
#33929=AXIS2_PLACEMENT_3D('',#62088,#40511,#40512);
#33930=AXIS2_PLACEMENT_3D('',#62094,#40513,#40514);
#33931=AXIS2_PLACEMENT_3D('',#62100,#40515,#40516);
#33932=AXIS2_PLACEMENT_3D('',#62106,#40517,#40518);
#33933=AXIS2_PLACEMENT_3D('',#62112,#40519,#40520);
#33934=AXIS2_PLACEMENT_3D('',#62118,#40521,#40522);
#33935=AXIS2_PLACEMENT_3D('',#62124,#40523,#40524);
#33936=AXIS2_PLACEMENT_3D('',#62130,#40525,#40526);
#33937=AXIS2_PLACEMENT_3D('',#62136,#40527,#40528);
#33938=AXIS2_PLACEMENT_3D('',#62142,#40529,#40530);
#33939=AXIS2_PLACEMENT_3D('',#62148,#40531,#40532);
#33940=AXIS2_PLACEMENT_3D('',#62154,#40533,#40534);
#33941=AXIS2_PLACEMENT_3D('',#62160,#40535,#40536);
#33942=AXIS2_PLACEMENT_3D('',#62166,#40537,#40538);
#33943=AXIS2_PLACEMENT_3D('',#62172,#40539,#40540);
#33944=AXIS2_PLACEMENT_3D('',#62178,#40541,#40542);
#33945=AXIS2_PLACEMENT_3D('',#62184,#40543,#40544);
#33946=AXIS2_PLACEMENT_3D('',#62190,#40545,#40546);
#33947=AXIS2_PLACEMENT_3D('',#62196,#40547,#40548);
#33948=AXIS2_PLACEMENT_3D('',#62202,#40549,#40550);
#33949=AXIS2_PLACEMENT_3D('',#62208,#40551,#40552);
#33950=AXIS2_PLACEMENT_3D('',#62214,#40553,#40554);
#33951=AXIS2_PLACEMENT_3D('',#62220,#40555,#40556);
#33952=AXIS2_PLACEMENT_3D('',#62226,#40557,#40558);
#33953=AXIS2_PLACEMENT_3D('',#62232,#40559,#40560);
#33954=AXIS2_PLACEMENT_3D('',#62238,#40561,#40562);
#33955=AXIS2_PLACEMENT_3D('',#62244,#40563,#40564);
#33956=AXIS2_PLACEMENT_3D('',#62250,#40565,#40566);
#33957=AXIS2_PLACEMENT_3D('',#62256,#40567,#40568);
#33958=AXIS2_PLACEMENT_3D('',#62262,#40569,#40570);
#33959=AXIS2_PLACEMENT_3D('',#62268,#40571,#40572);
#33960=AXIS2_PLACEMENT_3D('',#62274,#40573,#40574);
#33961=AXIS2_PLACEMENT_3D('',#62280,#40575,#40576);
#33962=AXIS2_PLACEMENT_3D('',#62286,#40577,#40578);
#33963=AXIS2_PLACEMENT_3D('',#62295,#40579,#40580);
#33964=AXIS2_PLACEMENT_3D('',#62304,#40581,#40582);
#33965=AXIS2_PLACEMENT_3D('',#62313,#40583,#40584);
#33966=AXIS2_PLACEMENT_3D('',#62322,#40585,#40586);
#33967=AXIS2_PLACEMENT_3D('',#62331,#40587,#40588);
#33968=AXIS2_PLACEMENT_3D('',#62340,#40589,#40590);
#33969=AXIS2_PLACEMENT_3D('',#62349,#40591,#40592);
#33970=AXIS2_PLACEMENT_3D('',#62358,#40593,#40594);
#33971=AXIS2_PLACEMENT_3D('',#62367,#40595,#40596);
#33972=AXIS2_PLACEMENT_3D('',#62376,#40597,#40598);
#33973=AXIS2_PLACEMENT_3D('',#62385,#40599,#40600);
#33974=AXIS2_PLACEMENT_3D('',#62394,#40601,#40602);
#33975=AXIS2_PLACEMENT_3D('',#62403,#40603,#40604);
#33976=AXIS2_PLACEMENT_3D('',#62412,#40605,#40606);
#33977=AXIS2_PLACEMENT_3D('',#62421,#40607,#40608);
#33978=AXIS2_PLACEMENT_3D('',#62427,#40609,#40610);
#33979=AXIS2_PLACEMENT_3D('',#62433,#40611,#40612);
#33980=AXIS2_PLACEMENT_3D('',#62439,#40613,#40614);
#33981=AXIS2_PLACEMENT_3D('',#62445,#40615,#40616);
#33982=AXIS2_PLACEMENT_3D('',#62451,#40617,#40618);
#33983=AXIS2_PLACEMENT_3D('',#62457,#40619,#40620);
#33984=AXIS2_PLACEMENT_3D('',#62463,#40621,#40622);
#33985=AXIS2_PLACEMENT_3D('',#62469,#40623,#40624);
#33986=AXIS2_PLACEMENT_3D('',#62475,#40625,#40626);
#33987=AXIS2_PLACEMENT_3D('',#62481,#40627,#40628);
#33988=AXIS2_PLACEMENT_3D('',#62497,#40630,#40631);
#33989=AXIS2_PLACEMENT_3D('',#62498,#40632,#40633);
#33990=AXIS2_PLACEMENT_3D('',#62499,#40634,#40635);
#33991=AXIS2_PLACEMENT_3D('',#62501,#40636,#40637);
#33992=AXIS2_PLACEMENT_3D('',#62502,#40638,#40639);
#33993=AXIS2_PLACEMENT_3D('',#62503,#40640,#40641);
#33994=AXIS2_PLACEMENT_3D('',#62505,#40642,#40643);
#33995=AXIS2_PLACEMENT_3D('',#62507,#40645,#40646);
#33996=AXIS2_PLACEMENT_3D('',#62509,#40647,#40648);
#33997=AXIS2_PLACEMENT_3D('',#62510,#40649,#40650);
#33998=AXIS2_PLACEMENT_3D('',#62511,#40651,#40652);
#33999=AXIS2_PLACEMENT_3D('',#62513,#40653,#40654);
#34000=AXIS2_PLACEMENT_3D('',#62514,#40655,#40656);
#34001=AXIS2_PLACEMENT_3D('',#62515,#40657,#40658);
#34002=AXIS2_PLACEMENT_3D('',#62517,#40659,#40660);
#34003=AXIS2_PLACEMENT_3D('',#62519,#40661,#40662);
#34004=AXIS2_PLACEMENT_3D('',#62520,#40663,#40664);
#34005=AXIS2_PLACEMENT_3D('',#62521,#40665,#40666);
#34006=AXIS2_PLACEMENT_3D('',#62523,#40667,#40668);
#34007=AXIS2_PLACEMENT_3D('',#62525,#40669,#40670);
#34008=AXIS2_PLACEMENT_3D('',#62526,#40671,#40672);
#34009=AXIS2_PLACEMENT_3D('',#62527,#40673,#40674);
#34010=AXIS2_PLACEMENT_3D('',#62529,#40675,#40676);
#34011=AXIS2_PLACEMENT_3D('',#62531,#40677,#40678);
#34012=AXIS2_PLACEMENT_3D('',#62532,#40679,#40680);
#34013=AXIS2_PLACEMENT_3D('',#62533,#40681,#40682);
#34014=AXIS2_PLACEMENT_3D('',#62535,#40683,#40684);
#34015=AXIS2_PLACEMENT_3D('',#62537,#40685,#40686);
#34016=AXIS2_PLACEMENT_3D('',#62538,#40687,#40688);
#34017=AXIS2_PLACEMENT_3D('',#62539,#40689,#40690);
#34018=AXIS2_PLACEMENT_3D('',#62541,#40691,#40692);
#34019=AXIS2_PLACEMENT_3D('',#62543,#40693,#40694);
#34020=AXIS2_PLACEMENT_3D('',#62544,#40695,#40696);
#34021=AXIS2_PLACEMENT_3D('',#62545,#40697,#40698);
#34022=AXIS2_PLACEMENT_3D('',#62547,#40699,#40700);
#34023=AXIS2_PLACEMENT_3D('',#62549,#40701,#40702);
#34024=AXIS2_PLACEMENT_3D('',#62550,#40703,#40704);
#34025=AXIS2_PLACEMENT_3D('',#62551,#40705,#40706);
#34026=AXIS2_PLACEMENT_3D('',#62553,#40707,#40708);
#34027=AXIS2_PLACEMENT_3D('',#62555,#40709,#40710);
#34028=AXIS2_PLACEMENT_3D('',#62556,#40711,#40712);
#34029=AXIS2_PLACEMENT_3D('',#62557,#40713,#40714);
#34030=AXIS2_PLACEMENT_3D('',#62559,#40715,#40716);
#34031=AXIS2_PLACEMENT_3D('',#62561,#40717,#40718);
#34032=AXIS2_PLACEMENT_3D('',#62562,#40719,#40720);
#34033=AXIS2_PLACEMENT_3D('',#62563,#40721,#40722);
#34034=AXIS2_PLACEMENT_3D('',#62565,#40723,#40724);
#34035=AXIS2_PLACEMENT_3D('',#62567,#40725,#40726);
#34036=AXIS2_PLACEMENT_3D('',#62568,#40727,#40728);
#34037=AXIS2_PLACEMENT_3D('',#62569,#40729,#40730);
#34038=AXIS2_PLACEMENT_3D('',#62571,#40731,#40732);
#34039=AXIS2_PLACEMENT_3D('',#62573,#40733,#40734);
#34040=AXIS2_PLACEMENT_3D('',#62574,#40735,#40736);
#34041=AXIS2_PLACEMENT_3D('',#62575,#40737,#40738);
#34042=AXIS2_PLACEMENT_3D('',#62577,#40739,#40740);
#34043=AXIS2_PLACEMENT_3D('',#62579,#40741,#40742);
#34044=AXIS2_PLACEMENT_3D('',#62580,#40743,#40744);
#34045=AXIS2_PLACEMENT_3D('',#62581,#40745,#40746);
#34046=AXIS2_PLACEMENT_3D('',#62583,#40747,#40748);
#34047=AXIS2_PLACEMENT_3D('',#62585,#40749,#40750);
#34048=AXIS2_PLACEMENT_3D('',#62586,#40751,#40752);
#34049=AXIS2_PLACEMENT_3D('',#62587,#40753,#40754);
#34050=AXIS2_PLACEMENT_3D('',#62589,#40755,#40756);
#34051=AXIS2_PLACEMENT_3D('',#62591,#40757,#40758);
#34052=AXIS2_PLACEMENT_3D('',#62592,#40759,#40760);
#34053=AXIS2_PLACEMENT_3D('',#62593,#40761,#40762);
#34054=AXIS2_PLACEMENT_3D('',#62595,#40763,#40764);
#34055=AXIS2_PLACEMENT_3D('',#62597,#40765,#40766);
#34056=AXIS2_PLACEMENT_3D('',#62598,#40767,#40768);
#34057=AXIS2_PLACEMENT_3D('',#62599,#40769,#40770);
#34058=AXIS2_PLACEMENT_3D('',#62601,#40771,#40772);
#34059=AXIS2_PLACEMENT_3D('',#62603,#40773,#40774);
#34060=AXIS2_PLACEMENT_3D('',#62604,#40775,#40776);
#34061=AXIS2_PLACEMENT_3D('',#62605,#40777,#40778);
#34062=AXIS2_PLACEMENT_3D('',#62607,#40779,#40780);
#34063=AXIS2_PLACEMENT_3D('',#62609,#40781,#40782);
#34064=AXIS2_PLACEMENT_3D('',#62610,#40783,#40784);
#34065=AXIS2_PLACEMENT_3D('',#62611,#40785,#40786);
#34066=AXIS2_PLACEMENT_3D('',#62613,#40787,#40788);
#34067=AXIS2_PLACEMENT_3D('',#62615,#40789,#40790);
#34068=AXIS2_PLACEMENT_3D('',#62616,#40791,#40792);
#34069=AXIS2_PLACEMENT_3D('',#62617,#40793,#40794);
#34070=AXIS2_PLACEMENT_3D('',#62619,#40795,#40796);
#34071=AXIS2_PLACEMENT_3D('',#62621,#40797,#40798);
#34072=AXIS2_PLACEMENT_3D('',#62622,#40799,#40800);
#34073=AXIS2_PLACEMENT_3D('',#62623,#40801,#40802);
#34074=AXIS2_PLACEMENT_3D('',#62625,#40803,#40804);
#34075=AXIS2_PLACEMENT_3D('',#62627,#40805,#40806);
#34076=AXIS2_PLACEMENT_3D('',#62628,#40807,#40808);
#34077=AXIS2_PLACEMENT_3D('',#62629,#40809,#40810);
#34078=AXIS2_PLACEMENT_3D('',#62631,#40811,#40812);
#34079=AXIS2_PLACEMENT_3D('',#62633,#40813,#40814);
#34080=AXIS2_PLACEMENT_3D('',#62634,#40815,#40816);
#34081=AXIS2_PLACEMENT_3D('',#62635,#40817,#40818);
#34082=AXIS2_PLACEMENT_3D('',#62637,#40819,#40820);
#34083=AXIS2_PLACEMENT_3D('',#62639,#40821,#40822);
#34084=AXIS2_PLACEMENT_3D('',#62640,#40823,#40824);
#34085=AXIS2_PLACEMENT_3D('',#62641,#40825,#40826);
#34086=AXIS2_PLACEMENT_3D('',#62643,#40827,#40828);
#34087=AXIS2_PLACEMENT_3D('',#62645,#40829,#40830);
#34088=AXIS2_PLACEMENT_3D('',#62646,#40831,#40832);
#34089=AXIS2_PLACEMENT_3D('',#62647,#40833,#40834);
#34090=AXIS2_PLACEMENT_3D('',#62649,#40835,#40836);
#34091=AXIS2_PLACEMENT_3D('',#62651,#40837,#40838);
#34092=AXIS2_PLACEMENT_3D('',#62652,#40839,#40840);
#34093=AXIS2_PLACEMENT_3D('',#62653,#40841,#40842);
#34094=AXIS2_PLACEMENT_3D('',#62655,#40843,#40844);
#34095=AXIS2_PLACEMENT_3D('',#62657,#40845,#40846);
#34096=AXIS2_PLACEMENT_3D('',#62658,#40847,#40848);
#34097=AXIS2_PLACEMENT_3D('',#62659,#40849,#40850);
#34098=AXIS2_PLACEMENT_3D('',#62661,#40851,#40852);
#34099=AXIS2_PLACEMENT_3D('',#62663,#40853,#40854);
#34100=AXIS2_PLACEMENT_3D('',#62664,#40855,#40856);
#34101=AXIS2_PLACEMENT_3D('',#62665,#40857,#40858);
#34102=AXIS2_PLACEMENT_3D('',#62667,#40859,#40860);
#34103=AXIS2_PLACEMENT_3D('',#62669,#40861,#40862);
#34104=AXIS2_PLACEMENT_3D('',#62670,#40863,#40864);
#34105=AXIS2_PLACEMENT_3D('',#62671,#40865,#40866);
#34106=AXIS2_PLACEMENT_3D('',#62673,#40867,#40868);
#34107=AXIS2_PLACEMENT_3D('',#62675,#40869,#40870);
#34108=AXIS2_PLACEMENT_3D('',#62676,#40871,#40872);
#34109=AXIS2_PLACEMENT_3D('',#62677,#40873,#40874);
#34110=AXIS2_PLACEMENT_3D('',#62679,#40875,#40876);
#34111=AXIS2_PLACEMENT_3D('',#62681,#40877,#40878);
#34112=AXIS2_PLACEMENT_3D('',#62682,#40879,#40880);
#34113=AXIS2_PLACEMENT_3D('',#62683,#40881,#40882);
#34114=AXIS2_PLACEMENT_3D('',#62685,#40883,#40884);
#34115=AXIS2_PLACEMENT_3D('',#62687,#40885,#40886);
#34116=AXIS2_PLACEMENT_3D('',#62688,#40887,#40888);
#34117=AXIS2_PLACEMENT_3D('',#62689,#40889,#40890);
#34118=AXIS2_PLACEMENT_3D('',#62691,#40891,#40892);
#34119=AXIS2_PLACEMENT_3D('',#62693,#40893,#40894);
#34120=AXIS2_PLACEMENT_3D('',#62694,#40895,#40896);
#34121=AXIS2_PLACEMENT_3D('',#62695,#40897,#40898);
#34122=AXIS2_PLACEMENT_3D('',#62697,#40899,#40900);
#34123=AXIS2_PLACEMENT_3D('',#62699,#40901,#40902);
#34124=AXIS2_PLACEMENT_3D('',#62700,#40903,#40904);
#34125=AXIS2_PLACEMENT_3D('',#62701,#40905,#40906);
#34126=AXIS2_PLACEMENT_3D('',#62703,#40907,#40908);
#34127=AXIS2_PLACEMENT_3D('',#62705,#40909,#40910);
#34128=AXIS2_PLACEMENT_3D('',#62706,#40911,#40912);
#34129=AXIS2_PLACEMENT_3D('',#62707,#40913,#40914);
#34130=AXIS2_PLACEMENT_3D('',#62709,#40915,#40916);
#34131=AXIS2_PLACEMENT_3D('',#62711,#40917,#40918);
#34132=AXIS2_PLACEMENT_3D('',#62712,#40919,#40920);
#34133=AXIS2_PLACEMENT_3D('',#62713,#40921,#40922);
#34134=AXIS2_PLACEMENT_3D('',#62715,#40923,#40924);
#34135=AXIS2_PLACEMENT_3D('',#62717,#40925,#40926);
#34136=AXIS2_PLACEMENT_3D('',#62718,#40927,#40928);
#34137=AXIS2_PLACEMENT_3D('',#62719,#40929,#40930);
#34138=AXIS2_PLACEMENT_3D('',#62721,#40931,#40932);
#34139=AXIS2_PLACEMENT_3D('',#62723,#40933,#40934);
#34140=AXIS2_PLACEMENT_3D('',#62724,#40935,#40936);
#34141=AXIS2_PLACEMENT_3D('',#62725,#40937,#40938);
#34142=AXIS2_PLACEMENT_3D('',#62727,#40939,#40940);
#34143=AXIS2_PLACEMENT_3D('',#62729,#40941,#40942);
#34144=AXIS2_PLACEMENT_3D('',#62730,#40943,#40944);
#34145=AXIS2_PLACEMENT_3D('',#62731,#40945,#40946);
#34146=AXIS2_PLACEMENT_3D('',#62733,#40947,#40948);
#34147=AXIS2_PLACEMENT_3D('',#62735,#40949,#40950);
#34148=AXIS2_PLACEMENT_3D('',#62736,#40951,#40952);
#34149=AXIS2_PLACEMENT_3D('',#62737,#40953,#40954);
#34150=AXIS2_PLACEMENT_3D('',#62739,#40955,#40956);
#34151=AXIS2_PLACEMENT_3D('',#62741,#40957,#40958);
#34152=AXIS2_PLACEMENT_3D('',#62742,#40959,#40960);
#34153=AXIS2_PLACEMENT_3D('',#62743,#40961,#40962);
#34154=AXIS2_PLACEMENT_3D('',#62745,#40963,#40964);
#34155=AXIS2_PLACEMENT_3D('',#62747,#40965,#40966);
#34156=AXIS2_PLACEMENT_3D('',#62748,#40967,#40968);
#34157=AXIS2_PLACEMENT_3D('',#62749,#40969,#40970);
#34158=AXIS2_PLACEMENT_3D('',#62751,#40971,#40972);
#34159=AXIS2_PLACEMENT_3D('',#62753,#40973,#40974);
#34160=AXIS2_PLACEMENT_3D('',#62754,#40975,#40976);
#34161=AXIS2_PLACEMENT_3D('',#62755,#40977,#40978);
#34162=AXIS2_PLACEMENT_3D('',#62757,#40979,#40980);
#34163=AXIS2_PLACEMENT_3D('',#62759,#40981,#40982);
#34164=AXIS2_PLACEMENT_3D('',#62760,#40983,#40984);
#34165=AXIS2_PLACEMENT_3D('',#62761,#40985,#40986);
#34166=AXIS2_PLACEMENT_3D('',#62763,#40987,#40988);
#34167=AXIS2_PLACEMENT_3D('',#62765,#40989,#40990);
#34168=AXIS2_PLACEMENT_3D('',#62766,#40991,#40992);
#34169=AXIS2_PLACEMENT_3D('',#62767,#40993,#40994);
#34170=AXIS2_PLACEMENT_3D('',#62769,#40995,#40996);
#34171=AXIS2_PLACEMENT_3D('',#62771,#40997,#40998);
#34172=AXIS2_PLACEMENT_3D('',#62772,#40999,#41000);
#34173=AXIS2_PLACEMENT_3D('',#62773,#41001,#41002);
#34174=AXIS2_PLACEMENT_3D('',#62775,#41003,#41004);
#34175=AXIS2_PLACEMENT_3D('',#62777,#41005,#41006);
#34176=AXIS2_PLACEMENT_3D('',#62778,#41007,#41008);
#34177=AXIS2_PLACEMENT_3D('',#62779,#41009,#41010);
#34178=AXIS2_PLACEMENT_3D('',#62781,#41011,#41012);
#34179=AXIS2_PLACEMENT_3D('',#62783,#41013,#41014);
#34180=AXIS2_PLACEMENT_3D('',#62784,#41015,#41016);
#34181=AXIS2_PLACEMENT_3D('',#62785,#41017,#41018);
#34182=AXIS2_PLACEMENT_3D('',#62787,#41019,#41020);
#34183=AXIS2_PLACEMENT_3D('',#62789,#41021,#41022);
#34184=AXIS2_PLACEMENT_3D('',#62790,#41023,#41024);
#34185=AXIS2_PLACEMENT_3D('',#62791,#41025,#41026);
#34186=AXIS2_PLACEMENT_3D('',#62793,#41027,#41028);
#34187=AXIS2_PLACEMENT_3D('',#62795,#41029,#41030);
#34188=AXIS2_PLACEMENT_3D('',#62796,#41031,#41032);
#34189=AXIS2_PLACEMENT_3D('',#62797,#41033,#41034);
#34190=AXIS2_PLACEMENT_3D('',#62799,#41035,#41036);
#34191=AXIS2_PLACEMENT_3D('',#62801,#41037,#41038);
#34192=AXIS2_PLACEMENT_3D('',#62802,#41039,#41040);
#34193=AXIS2_PLACEMENT_3D('',#62803,#41041,#41042);
#34194=AXIS2_PLACEMENT_3D('',#62805,#41043,#41044);
#34195=AXIS2_PLACEMENT_3D('',#62807,#41045,#41046);
#34196=AXIS2_PLACEMENT_3D('',#62808,#41047,#41048);
#34197=AXIS2_PLACEMENT_3D('',#62809,#41049,#41050);
#34198=AXIS2_PLACEMENT_3D('',#62811,#41051,#41052);
#34199=AXIS2_PLACEMENT_3D('',#62813,#41053,#41054);
#34200=AXIS2_PLACEMENT_3D('',#62814,#41055,#41056);
#34201=AXIS2_PLACEMENT_3D('',#62815,#41057,#41058);
#34202=AXIS2_PLACEMENT_3D('',#62817,#41059,#41060);
#34203=AXIS2_PLACEMENT_3D('',#62819,#41061,#41062);
#34204=AXIS2_PLACEMENT_3D('',#62820,#41063,#41064);
#34205=AXIS2_PLACEMENT_3D('',#62821,#41065,#41066);
#34206=AXIS2_PLACEMENT_3D('',#62823,#41067,#41068);
#34207=AXIS2_PLACEMENT_3D('',#62825,#41069,#41070);
#34208=AXIS2_PLACEMENT_3D('',#62826,#41071,#41072);
#34209=AXIS2_PLACEMENT_3D('',#62827,#41073,#41074);
#34210=AXIS2_PLACEMENT_3D('',#62829,#41075,#41076);
#34211=AXIS2_PLACEMENT_3D('',#62831,#41077,#41078);
#34212=AXIS2_PLACEMENT_3D('',#62832,#41079,#41080);
#34213=AXIS2_PLACEMENT_3D('',#62833,#41081,#41082);
#34214=AXIS2_PLACEMENT_3D('',#62835,#41083,#41084);
#34215=AXIS2_PLACEMENT_3D('',#62837,#41085,#41086);
#34216=AXIS2_PLACEMENT_3D('',#62838,#41087,#41088);
#34217=AXIS2_PLACEMENT_3D('',#62839,#41089,#41090);
#34218=AXIS2_PLACEMENT_3D('',#62841,#41091,#41092);
#34219=AXIS2_PLACEMENT_3D('',#62843,#41093,#41094);
#34220=AXIS2_PLACEMENT_3D('',#62844,#41095,#41096);
#34221=AXIS2_PLACEMENT_3D('',#62845,#41097,#41098);
#34222=AXIS2_PLACEMENT_3D('',#62847,#41099,#41100);
#34223=AXIS2_PLACEMENT_3D('',#62849,#41101,#41102);
#34224=AXIS2_PLACEMENT_3D('',#62850,#41103,#41104);
#34225=AXIS2_PLACEMENT_3D('',#62851,#41105,#41106);
#34226=AXIS2_PLACEMENT_3D('',#62853,#41107,#41108);
#34227=AXIS2_PLACEMENT_3D('',#62855,#41109,#41110);
#34228=AXIS2_PLACEMENT_3D('',#62856,#41111,#41112);
#34229=AXIS2_PLACEMENT_3D('',#62857,#41113,#41114);
#34230=AXIS2_PLACEMENT_3D('',#62859,#41115,#41116);
#34231=AXIS2_PLACEMENT_3D('',#62861,#41117,#41118);
#34232=AXIS2_PLACEMENT_3D('',#62862,#41119,#41120);
#34233=AXIS2_PLACEMENT_3D('',#62863,#41121,#41122);
#34234=AXIS2_PLACEMENT_3D('',#62865,#41123,#41124);
#34235=AXIS2_PLACEMENT_3D('',#62867,#41125,#41126);
#34236=AXIS2_PLACEMENT_3D('',#62868,#41127,#41128);
#34237=AXIS2_PLACEMENT_3D('',#62869,#41129,#41130);
#34238=AXIS2_PLACEMENT_3D('',#62871,#41131,#41132);
#34239=AXIS2_PLACEMENT_3D('',#62873,#41133,#41134);
#34240=AXIS2_PLACEMENT_3D('',#62874,#41135,#41136);
#34241=AXIS2_PLACEMENT_3D('',#62875,#41137,#41138);
#34242=AXIS2_PLACEMENT_3D('',#62877,#41139,#41140);
#34243=AXIS2_PLACEMENT_3D('',#62879,#41141,#41142);
#34244=AXIS2_PLACEMENT_3D('',#62880,#41143,#41144);
#34245=AXIS2_PLACEMENT_3D('',#62881,#41145,#41146);
#34246=AXIS2_PLACEMENT_3D('',#62883,#41147,#41148);
#34247=AXIS2_PLACEMENT_3D('',#62885,#41149,#41150);
#34248=AXIS2_PLACEMENT_3D('',#62886,#41151,#41152);
#34249=AXIS2_PLACEMENT_3D('',#62887,#41153,#41154);
#34250=AXIS2_PLACEMENT_3D('',#62889,#41155,#41156);
#34251=AXIS2_PLACEMENT_3D('',#62891,#41157,#41158);
#34252=AXIS2_PLACEMENT_3D('',#62892,#41159,#41160);
#34253=AXIS2_PLACEMENT_3D('',#62893,#41161,#41162);
#34254=AXIS2_PLACEMENT_3D('',#62895,#41163,#41164);
#34255=AXIS2_PLACEMENT_3D('',#62897,#41165,#41166);
#34256=AXIS2_PLACEMENT_3D('',#62898,#41167,#41168);
#34257=AXIS2_PLACEMENT_3D('',#62899,#41169,#41170);
#34258=AXIS2_PLACEMENT_3D('',#62901,#41171,#41172);
#34259=AXIS2_PLACEMENT_3D('',#62903,#41173,#41174);
#34260=AXIS2_PLACEMENT_3D('',#62904,#41175,#41176);
#34261=AXIS2_PLACEMENT_3D('',#62905,#41177,#41178);
#34262=AXIS2_PLACEMENT_3D('',#62907,#41179,#41180);
#34263=AXIS2_PLACEMENT_3D('',#62909,#41181,#41182);
#34264=AXIS2_PLACEMENT_3D('',#62910,#41183,#41184);
#34265=AXIS2_PLACEMENT_3D('',#62911,#41185,#41186);
#34266=AXIS2_PLACEMENT_3D('',#62913,#41187,#41188);
#34267=AXIS2_PLACEMENT_3D('',#62915,#41189,#41190);
#34268=AXIS2_PLACEMENT_3D('',#62916,#41191,#41192);
#34269=AXIS2_PLACEMENT_3D('',#62917,#41193,#41194);
#34270=AXIS2_PLACEMENT_3D('',#62919,#41195,#41196);
#34271=AXIS2_PLACEMENT_3D('',#62921,#41197,#41198);
#34272=AXIS2_PLACEMENT_3D('',#62922,#41199,#41200);
#34273=AXIS2_PLACEMENT_3D('',#62923,#41201,#41202);
#34274=AXIS2_PLACEMENT_3D('',#62925,#41203,#41204);
#34275=AXIS2_PLACEMENT_3D('',#62927,#41205,#41206);
#34276=AXIS2_PLACEMENT_3D('',#62928,#41207,#41208);
#34277=AXIS2_PLACEMENT_3D('',#62929,#41209,#41210);
#34278=AXIS2_PLACEMENT_3D('',#62931,#41211,#41212);
#34279=AXIS2_PLACEMENT_3D('',#62933,#41213,#41214);
#34280=AXIS2_PLACEMENT_3D('',#62934,#41215,#41216);
#34281=AXIS2_PLACEMENT_3D('',#62935,#41217,#41218);
#34282=AXIS2_PLACEMENT_3D('',#62937,#41219,#41220);
#34283=AXIS2_PLACEMENT_3D('',#62939,#41221,#41222);
#34284=AXIS2_PLACEMENT_3D('',#62940,#41223,#41224);
#34285=AXIS2_PLACEMENT_3D('',#62941,#41225,#41226);
#34286=AXIS2_PLACEMENT_3D('',#62943,#41227,#41228);
#34287=AXIS2_PLACEMENT_3D('',#62945,#41229,#41230);
#34288=AXIS2_PLACEMENT_3D('',#62946,#41231,#41232);
#34289=AXIS2_PLACEMENT_3D('',#62947,#41233,#41234);
#34290=AXIS2_PLACEMENT_3D('',#62949,#41235,#41236);
#34291=AXIS2_PLACEMENT_3D('',#62951,#41237,#41238);
#34292=AXIS2_PLACEMENT_3D('',#62952,#41239,#41240);
#34293=AXIS2_PLACEMENT_3D('',#62953,#41241,#41242);
#34294=AXIS2_PLACEMENT_3D('',#62955,#41243,#41244);
#34295=AXIS2_PLACEMENT_3D('',#62957,#41245,#41246);
#34296=AXIS2_PLACEMENT_3D('',#62958,#41247,#41248);
#34297=AXIS2_PLACEMENT_3D('',#62959,#41249,#41250);
#34298=AXIS2_PLACEMENT_3D('',#62961,#41251,#41252);
#34299=AXIS2_PLACEMENT_3D('',#62963,#41253,#41254);
#34300=AXIS2_PLACEMENT_3D('',#62964,#41255,#41256);
#34301=AXIS2_PLACEMENT_3D('',#62965,#41257,#41258);
#34302=AXIS2_PLACEMENT_3D('',#62967,#41259,#41260);
#34303=AXIS2_PLACEMENT_3D('',#62969,#41261,#41262);
#34304=AXIS2_PLACEMENT_3D('',#62970,#41263,#41264);
#34305=AXIS2_PLACEMENT_3D('',#62971,#41265,#41266);
#34306=AXIS2_PLACEMENT_3D('',#62973,#41267,#41268);
#34307=AXIS2_PLACEMENT_3D('',#62975,#41269,#41270);
#34308=AXIS2_PLACEMENT_3D('',#62976,#41271,#41272);
#34309=AXIS2_PLACEMENT_3D('',#62977,#41273,#41274);
#34310=AXIS2_PLACEMENT_3D('',#62979,#41275,#41276);
#34311=AXIS2_PLACEMENT_3D('',#62981,#41277,#41278);
#34312=AXIS2_PLACEMENT_3D('',#62982,#41279,#41280);
#34313=AXIS2_PLACEMENT_3D('',#62983,#41281,#41282);
#34314=AXIS2_PLACEMENT_3D('',#62985,#41283,#41284);
#34315=AXIS2_PLACEMENT_3D('',#62987,#41285,#41286);
#34316=AXIS2_PLACEMENT_3D('',#62988,#41287,#41288);
#34317=AXIS2_PLACEMENT_3D('',#62989,#41289,#41290);
#34318=AXIS2_PLACEMENT_3D('',#62993,#41292,#41293);
#34319=AXIS2_PLACEMENT_3D('',#62995,#41295,#41296);
#34320=AXIS2_PLACEMENT_3D('',#63000,#41299,#41300);
#34321=AXIS2_PLACEMENT_3D('',#63001,#41301,#41302);
#34322=AXIS2_PLACEMENT_3D('',#63006,#41305,#41306);
#34323=AXIS2_PLACEMENT_3D('',#63007,#41307,#41308);
#34324=AXIS2_PLACEMENT_3D('',#63012,#41311,#41312);
#34325=AXIS2_PLACEMENT_3D('',#63013,#41313,#41314);
#34326=AXIS2_PLACEMENT_3D('',#63018,#41317,#41318);
#34327=AXIS2_PLACEMENT_3D('',#63019,#41319,#41320);
#34328=AXIS2_PLACEMENT_3D('',#63024,#41323,#41324);
#34329=AXIS2_PLACEMENT_3D('',#63025,#41325,#41326);
#34330=AXIS2_PLACEMENT_3D('',#63030,#41329,#41330);
#34331=AXIS2_PLACEMENT_3D('',#63031,#41331,#41332);
#34332=AXIS2_PLACEMENT_3D('',#63036,#41335,#41336);
#34333=AXIS2_PLACEMENT_3D('',#63037,#41337,#41338);
#34334=AXIS2_PLACEMENT_3D('',#63042,#41341,#41342);
#34335=AXIS2_PLACEMENT_3D('',#63043,#41343,#41344);
#34336=AXIS2_PLACEMENT_3D('',#63048,#41347,#41348);
#34337=AXIS2_PLACEMENT_3D('',#63049,#41349,#41350);
#34338=AXIS2_PLACEMENT_3D('',#63054,#41353,#41354);
#34339=AXIS2_PLACEMENT_3D('',#63055,#41355,#41356);
#34340=AXIS2_PLACEMENT_3D('',#63060,#41359,#41360);
#34341=AXIS2_PLACEMENT_3D('',#63061,#41361,#41362);
#34342=AXIS2_PLACEMENT_3D('',#63066,#41365,#41366);
#34343=AXIS2_PLACEMENT_3D('',#63067,#41367,#41368);
#34344=AXIS2_PLACEMENT_3D('',#63072,#41371,#41372);
#34345=AXIS2_PLACEMENT_3D('',#63073,#41373,#41374);
#34346=AXIS2_PLACEMENT_3D('',#63078,#41377,#41378);
#34347=AXIS2_PLACEMENT_3D('',#63079,#41379,#41380);
#34348=AXIS2_PLACEMENT_3D('',#63084,#41383,#41384);
#34349=AXIS2_PLACEMENT_3D('',#63085,#41385,#41386);
#34350=AXIS2_PLACEMENT_3D('',#63090,#41389,#41390);
#34351=AXIS2_PLACEMENT_3D('',#63091,#41391,#41392);
#34352=AXIS2_PLACEMENT_3D('',#63096,#41395,#41396);
#34353=AXIS2_PLACEMENT_3D('',#63097,#41397,#41398);
#34354=AXIS2_PLACEMENT_3D('',#63102,#41401,#41402);
#34355=AXIS2_PLACEMENT_3D('',#63103,#41403,#41404);
#34356=AXIS2_PLACEMENT_3D('',#63108,#41407,#41408);
#34357=AXIS2_PLACEMENT_3D('',#63109,#41409,#41410);
#34358=AXIS2_PLACEMENT_3D('',#63114,#41413,#41414);
#34359=AXIS2_PLACEMENT_3D('',#63115,#41415,#41416);
#34360=AXIS2_PLACEMENT_3D('',#63120,#41419,#41420);
#34361=AXIS2_PLACEMENT_3D('',#63121,#41421,#41422);
#34362=AXIS2_PLACEMENT_3D('',#63126,#41425,#41426);
#34363=AXIS2_PLACEMENT_3D('',#63127,#41427,#41428);
#34364=AXIS2_PLACEMENT_3D('',#63132,#41431,#41432);
#34365=AXIS2_PLACEMENT_3D('',#63133,#41433,#41434);
#34366=AXIS2_PLACEMENT_3D('',#63138,#41437,#41438);
#34367=AXIS2_PLACEMENT_3D('',#63139,#41439,#41440);
#34368=AXIS2_PLACEMENT_3D('',#63144,#41443,#41444);
#34369=AXIS2_PLACEMENT_3D('',#63145,#41445,#41446);
#34370=AXIS2_PLACEMENT_3D('',#63150,#41449,#41450);
#34371=AXIS2_PLACEMENT_3D('',#63151,#41451,#41452);
#34372=AXIS2_PLACEMENT_3D('',#63156,#41455,#41456);
#34373=AXIS2_PLACEMENT_3D('',#63157,#41457,#41458);
#34374=AXIS2_PLACEMENT_3D('',#63162,#41461,#41462);
#34375=AXIS2_PLACEMENT_3D('',#63163,#41463,#41464);
#34376=AXIS2_PLACEMENT_3D('',#63168,#41467,#41468);
#34377=AXIS2_PLACEMENT_3D('',#63169,#41469,#41470);
#34378=AXIS2_PLACEMENT_3D('',#63174,#41473,#41474);
#34379=AXIS2_PLACEMENT_3D('',#63175,#41475,#41476);
#34380=AXIS2_PLACEMENT_3D('',#63180,#41479,#41480);
#34381=AXIS2_PLACEMENT_3D('',#63181,#41481,#41482);
#34382=AXIS2_PLACEMENT_3D('',#63186,#41485,#41486);
#34383=AXIS2_PLACEMENT_3D('',#63187,#41487,#41488);
#34384=AXIS2_PLACEMENT_3D('',#63192,#41491,#41492);
#34385=AXIS2_PLACEMENT_3D('',#63193,#41493,#41494);
#34386=AXIS2_PLACEMENT_3D('',#63198,#41497,#41498);
#34387=AXIS2_PLACEMENT_3D('',#63199,#41499,#41500);
#34388=AXIS2_PLACEMENT_3D('',#63204,#41503,#41504);
#34389=AXIS2_PLACEMENT_3D('',#63205,#41505,#41506);
#34390=AXIS2_PLACEMENT_3D('',#63210,#41509,#41510);
#34391=AXIS2_PLACEMENT_3D('',#63211,#41511,#41512);
#34392=AXIS2_PLACEMENT_3D('',#63216,#41515,#41516);
#34393=AXIS2_PLACEMENT_3D('',#63217,#41517,#41518);
#34394=AXIS2_PLACEMENT_3D('',#63222,#41521,#41522);
#34395=AXIS2_PLACEMENT_3D('',#63223,#41523,#41524);
#34396=AXIS2_PLACEMENT_3D('',#63228,#41527,#41528);
#34397=AXIS2_PLACEMENT_3D('',#63229,#41529,#41530);
#34398=AXIS2_PLACEMENT_3D('',#63234,#41533,#41534);
#34399=AXIS2_PLACEMENT_3D('',#63235,#41535,#41536);
#34400=AXIS2_PLACEMENT_3D('',#63240,#41539,#41540);
#34401=AXIS2_PLACEMENT_3D('',#63241,#41541,#41542);
#34402=AXIS2_PLACEMENT_3D('',#63246,#41545,#41546);
#34403=AXIS2_PLACEMENT_3D('',#63247,#41547,#41548);
#34404=AXIS2_PLACEMENT_3D('',#63252,#41551,#41552);
#34405=AXIS2_PLACEMENT_3D('',#63253,#41553,#41554);
#34406=AXIS2_PLACEMENT_3D('',#63258,#41557,#41558);
#34407=AXIS2_PLACEMENT_3D('',#63259,#41559,#41560);
#34408=AXIS2_PLACEMENT_3D('',#63264,#41563,#41564);
#34409=AXIS2_PLACEMENT_3D('',#63265,#41565,#41566);
#34410=AXIS2_PLACEMENT_3D('',#63270,#41569,#41570);
#34411=AXIS2_PLACEMENT_3D('',#63271,#41571,#41572);
#34412=AXIS2_PLACEMENT_3D('',#63276,#41575,#41576);
#34413=AXIS2_PLACEMENT_3D('',#63277,#41577,#41578);
#34414=AXIS2_PLACEMENT_3D('',#63282,#41581,#41582);
#34415=AXIS2_PLACEMENT_3D('',#63283,#41583,#41584);
#34416=AXIS2_PLACEMENT_3D('',#63288,#41587,#41588);
#34417=AXIS2_PLACEMENT_3D('',#63289,#41589,#41590);
#34418=AXIS2_PLACEMENT_3D('',#63294,#41593,#41594);
#34419=AXIS2_PLACEMENT_3D('',#63295,#41595,#41596);
#34420=AXIS2_PLACEMENT_3D('',#63300,#41599,#41600);
#34421=AXIS2_PLACEMENT_3D('',#63301,#41601,#41602);
#34422=AXIS2_PLACEMENT_3D('',#63306,#41605,#41606);
#34423=AXIS2_PLACEMENT_3D('',#63307,#41607,#41608);
#34424=AXIS2_PLACEMENT_3D('',#63312,#41611,#41612);
#34425=AXIS2_PLACEMENT_3D('',#63313,#41613,#41614);
#34426=AXIS2_PLACEMENT_3D('',#63318,#41617,#41618);
#34427=AXIS2_PLACEMENT_3D('',#63319,#41619,#41620);
#34428=AXIS2_PLACEMENT_3D('',#63324,#41623,#41624);
#34429=AXIS2_PLACEMENT_3D('',#63325,#41625,#41626);
#34430=AXIS2_PLACEMENT_3D('',#63330,#41629,#41630);
#34431=AXIS2_PLACEMENT_3D('',#63331,#41631,#41632);
#34432=AXIS2_PLACEMENT_3D('',#63336,#41635,#41636);
#34433=AXIS2_PLACEMENT_3D('',#63337,#41637,#41638);
#34434=AXIS2_PLACEMENT_3D('',#63342,#41641,#41642);
#34435=AXIS2_PLACEMENT_3D('',#63343,#41643,#41644);
#34436=AXIS2_PLACEMENT_3D('',#63348,#41647,#41648);
#34437=AXIS2_PLACEMENT_3D('',#63349,#41649,#41650);
#34438=AXIS2_PLACEMENT_3D('',#63354,#41653,#41654);
#34439=AXIS2_PLACEMENT_3D('',#63355,#41655,#41656);
#34440=AXIS2_PLACEMENT_3D('',#63360,#41659,#41660);
#34441=AXIS2_PLACEMENT_3D('',#63361,#41661,#41662);
#34442=AXIS2_PLACEMENT_3D('',#63366,#41665,#41666);
#34443=AXIS2_PLACEMENT_3D('',#63367,#41667,#41668);
#34444=AXIS2_PLACEMENT_3D('',#63372,#41671,#41672);
#34445=AXIS2_PLACEMENT_3D('',#63373,#41673,#41674);
#34446=AXIS2_PLACEMENT_3D('',#63377,#41676,#41677);
#34447=AXIS2_PLACEMENT_3D('',#63379,#41679,#41680);
#34448=AXIS2_PLACEMENT_3D('',#63383,#41682,#41683);
#34449=AXIS2_PLACEMENT_3D('',#63385,#41685,#41686);
#34450=AXIS2_PLACEMENT_3D('',#63389,#41688,#41689);
#34451=AXIS2_PLACEMENT_3D('',#63391,#41691,#41692);
#34452=AXIS2_PLACEMENT_3D('',#63395,#41694,#41695);
#34453=AXIS2_PLACEMENT_3D('',#63397,#41697,#41698);
#34454=AXIS2_PLACEMENT_3D('',#63401,#41700,#41701);
#34455=AXIS2_PLACEMENT_3D('',#63403,#41703,#41704);
#34456=AXIS2_PLACEMENT_3D('',#63407,#41706,#41707);
#34457=AXIS2_PLACEMENT_3D('',#63409,#41709,#41710);
#34458=AXIS2_PLACEMENT_3D('',#63413,#41712,#41713);
#34459=AXIS2_PLACEMENT_3D('',#63415,#41715,#41716);
#34460=AXIS2_PLACEMENT_3D('',#63419,#41718,#41719);
#34461=AXIS2_PLACEMENT_3D('',#63421,#41721,#41722);
#34462=AXIS2_PLACEMENT_3D('',#63425,#41724,#41725);
#34463=AXIS2_PLACEMENT_3D('',#63427,#41727,#41728);
#34464=AXIS2_PLACEMENT_3D('',#63431,#41730,#41731);
#34465=AXIS2_PLACEMENT_3D('',#63433,#41733,#41734);
#34466=AXIS2_PLACEMENT_3D('',#63437,#41736,#41737);
#34467=AXIS2_PLACEMENT_3D('',#63439,#41739,#41740);
#34468=AXIS2_PLACEMENT_3D('',#63443,#41742,#41743);
#34469=AXIS2_PLACEMENT_3D('',#63445,#41745,#41746);
#34470=AXIS2_PLACEMENT_3D('',#63449,#41748,#41749);
#34471=AXIS2_PLACEMENT_3D('',#63451,#41751,#41752);
#34472=AXIS2_PLACEMENT_3D('',#63455,#41754,#41755);
#34473=AXIS2_PLACEMENT_3D('',#63457,#41757,#41758);
#34474=AXIS2_PLACEMENT_3D('',#63462,#41761,#41762);
#34475=AXIS2_PLACEMENT_3D('',#63463,#41763,#41764);
#34476=AXIS2_PLACEMENT_3D('',#63464,#41765,#41766);
#34477=AXIS2_PLACEMENT_3D('',#63465,#41767,#41768);
#34478=AXIS2_PLACEMENT_3D('',#63466,#41769,#41770);
#34479=AXIS2_PLACEMENT_3D('',#63467,#41771,#41772);
#34480=AXIS2_PLACEMENT_3D('',#63468,#41773,#41774);
#34481=AXIS2_PLACEMENT_3D('',#63469,#41775,#41776);
#34482=AXIS2_PLACEMENT_3D('',#63470,#41777,#41778);
#34483=AXIS2_PLACEMENT_3D('',#63471,#41779,#41780);
#34484=AXIS2_PLACEMENT_3D('',#63472,#41781,#41782);
#34485=AXIS2_PLACEMENT_3D('',#63473,#41783,#41784);
#34486=AXIS2_PLACEMENT_3D('',#63474,#41785,#41786);
#34487=AXIS2_PLACEMENT_3D('',#63475,#41787,#41788);
#34488=AXIS2_PLACEMENT_3D('',#63476,#41789,#41790);
#34489=AXIS2_PLACEMENT_3D('',#63477,#41791,#41792);
#34490=AXIS2_PLACEMENT_3D('',#63478,#41793,#41794);
#34491=AXIS2_PLACEMENT_3D('',#63479,#41795,#41796);
#34492=AXIS2_PLACEMENT_3D('',#63480,#41797,#41798);
#34493=AXIS2_PLACEMENT_3D('',#63481,#41799,#41800);
#34494=AXIS2_PLACEMENT_3D('',#63482,#41801,#41802);
#34495=AXIS2_PLACEMENT_3D('',#63483,#41803,#41804);
#34496=AXIS2_PLACEMENT_3D('',#63484,#41805,#41806);
#34497=AXIS2_PLACEMENT_3D('',#63485,#41807,#41808);
#34498=AXIS2_PLACEMENT_3D('',#63486,#41809,#41810);
#34499=AXIS2_PLACEMENT_3D('',#63487,#41811,#41812);
#34500=AXIS2_PLACEMENT_3D('',#63488,#41813,#41814);
#34501=AXIS2_PLACEMENT_3D('',#63489,#41815,#41816);
#34502=AXIS2_PLACEMENT_3D('',#63490,#41817,#41818);
#34503=AXIS2_PLACEMENT_3D('',#63491,#41819,#41820);
#34504=AXIS2_PLACEMENT_3D('',#63492,#41821,#41822);
#34505=AXIS2_PLACEMENT_3D('',#63493,#41823,#41824);
#34506=AXIS2_PLACEMENT_3D('',#63494,#41825,#41826);
#34507=AXIS2_PLACEMENT_3D('',#63495,#41827,#41828);
#34508=AXIS2_PLACEMENT_3D('',#63496,#41829,#41830);
#34509=AXIS2_PLACEMENT_3D('',#63497,#41831,#41832);
#34510=AXIS2_PLACEMENT_3D('',#63498,#41833,#41834);
#34511=AXIS2_PLACEMENT_3D('',#63499,#41835,#41836);
#34512=AXIS2_PLACEMENT_3D('',#63500,#41837,#41838);
#34513=AXIS2_PLACEMENT_3D('',#63501,#41839,#41840);
#34514=AXIS2_PLACEMENT_3D('',#63502,#41841,#41842);
#34515=AXIS2_PLACEMENT_3D('',#63503,#41843,#41844);
#34516=AXIS2_PLACEMENT_3D('',#63504,#41845,#41846);
#34517=AXIS2_PLACEMENT_3D('',#63505,#41847,#41848);
#34518=AXIS2_PLACEMENT_3D('',#63506,#41849,#41850);
#34519=AXIS2_PLACEMENT_3D('',#63507,#41851,#41852);
#34520=AXIS2_PLACEMENT_3D('',#63508,#41853,#41854);
#34521=AXIS2_PLACEMENT_3D('',#63509,#41855,#41856);
#34522=AXIS2_PLACEMENT_3D('',#63510,#41857,#41858);
#34523=AXIS2_PLACEMENT_3D('',#63511,#41859,#41860);
#34524=AXIS2_PLACEMENT_3D('',#63512,#41861,#41862);
#34525=AXIS2_PLACEMENT_3D('',#63513,#41863,#41864);
#34526=AXIS2_PLACEMENT_3D('',#63514,#41865,#41866);
#34527=AXIS2_PLACEMENT_3D('',#63515,#41867,#41868);
#34528=AXIS2_PLACEMENT_3D('',#63516,#41869,#41870);
#34529=AXIS2_PLACEMENT_3D('',#63517,#41871,#41872);
#34530=AXIS2_PLACEMENT_3D('',#63518,#41873,#41874);
#34531=AXIS2_PLACEMENT_3D('',#63519,#41875,#41876);
#34532=AXIS2_PLACEMENT_3D('',#63520,#41877,#41878);
#34533=AXIS2_PLACEMENT_3D('',#63521,#41879,#41880);
#34534=AXIS2_PLACEMENT_3D('',#63522,#41881,#41882);
#34535=AXIS2_PLACEMENT_3D('',#63523,#41883,#41884);
#34536=AXIS2_PLACEMENT_3D('',#63524,#41885,#41886);
#34537=AXIS2_PLACEMENT_3D('',#63525,#41887,#41888);
#34538=AXIS2_PLACEMENT_3D('',#63526,#41889,#41890);
#34539=AXIS2_PLACEMENT_3D('',#63527,#41891,#41892);
#34540=AXIS2_PLACEMENT_3D('',#63528,#41893,#41894);
#34541=AXIS2_PLACEMENT_3D('',#63529,#41895,#41896);
#34542=AXIS2_PLACEMENT_3D('',#63530,#41897,#41898);
#34543=AXIS2_PLACEMENT_3D('',#63531,#41899,#41900);
#34544=AXIS2_PLACEMENT_3D('',#63532,#41901,#41902);
#34545=AXIS2_PLACEMENT_3D('',#63533,#41903,#41904);
#34546=AXIS2_PLACEMENT_3D('',#63534,#41905,#41906);
#34547=AXIS2_PLACEMENT_3D('',#63535,#41907,#41908);
#34548=AXIS2_PLACEMENT_3D('',#63536,#41909,#41910);
#34549=AXIS2_PLACEMENT_3D('',#63537,#41911,#41912);
#34550=AXIS2_PLACEMENT_3D('',#63538,#41913,#41914);
#34551=AXIS2_PLACEMENT_3D('',#63539,#41915,#41916);
#34552=AXIS2_PLACEMENT_3D('',#63540,#41917,#41918);
#34553=AXIS2_PLACEMENT_3D('',#63541,#41919,#41920);
#34554=AXIS2_PLACEMENT_3D('',#63542,#41921,#41922);
#34555=AXIS2_PLACEMENT_3D('',#63543,#41923,#41924);
#34556=AXIS2_PLACEMENT_3D('',#63544,#41925,#41926);
#34557=AXIS2_PLACEMENT_3D('',#63545,#41927,#41928);
#34558=AXIS2_PLACEMENT_3D('',#63546,#41929,#41930);
#34559=AXIS2_PLACEMENT_3D('',#63547,#41931,#41932);
#34560=AXIS2_PLACEMENT_3D('',#63548,#41933,#41934);
#34561=AXIS2_PLACEMENT_3D('',#63549,#41935,#41936);
#34562=AXIS2_PLACEMENT_3D('',#63550,#41937,#41938);
#34563=AXIS2_PLACEMENT_3D('',#63551,#41939,#41940);
#34564=AXIS2_PLACEMENT_3D('',#63552,#41941,#41942);
#34565=AXIS2_PLACEMENT_3D('',#63553,#41943,#41944);
#34566=AXIS2_PLACEMENT_3D('',#63554,#41945,#41946);
#34567=AXIS2_PLACEMENT_3D('',#63555,#41947,#41948);
#34568=AXIS2_PLACEMENT_3D('',#63556,#41949,#41950);
#34569=AXIS2_PLACEMENT_3D('',#63557,#41951,#41952);
#34570=AXIS2_PLACEMENT_3D('',#63558,#41953,#41954);
#34571=AXIS2_PLACEMENT_3D('',#63559,#41955,#41956);
#34572=AXIS2_PLACEMENT_3D('',#63560,#41957,#41958);
#34573=AXIS2_PLACEMENT_3D('',#63561,#41959,#41960);
#34574=AXIS2_PLACEMENT_3D('',#63562,#41961,#41962);
#34575=AXIS2_PLACEMENT_3D('',#63563,#41963,#41964);
#34576=AXIS2_PLACEMENT_3D('',#63564,#41965,#41966);
#34577=AXIS2_PLACEMENT_3D('',#63565,#41967,#41968);
#34578=AXIS2_PLACEMENT_3D('',#63566,#41969,#41970);
#34579=AXIS2_PLACEMENT_3D('',#63567,#41971,#41972);
#34580=AXIS2_PLACEMENT_3D('',#63568,#41973,#41974);
#34581=AXIS2_PLACEMENT_3D('',#63569,#41975,#41976);
#34582=AXIS2_PLACEMENT_3D('',#63570,#41977,#41978);
#34583=AXIS2_PLACEMENT_3D('',#63571,#41979,#41980);
#34584=AXIS2_PLACEMENT_3D('',#63572,#41981,#41982);
#34585=AXIS2_PLACEMENT_3D('',#63573,#41983,#41984);
#34586=AXIS2_PLACEMENT_3D('',#63574,#41985,#41986);
#34587=AXIS2_PLACEMENT_3D('',#63575,#41987,#41988);
#34588=AXIS2_PLACEMENT_3D('',#63576,#41989,#41990);
#34589=AXIS2_PLACEMENT_3D('',#63577,#41991,#41992);
#34590=AXIS2_PLACEMENT_3D('',#63578,#41993,#41994);
#34591=AXIS2_PLACEMENT_3D('',#63579,#41995,#41996);
#34592=AXIS2_PLACEMENT_3D('',#63580,#41997,#41998);
#34593=AXIS2_PLACEMENT_3D('',#63581,#41999,#42000);
#34594=AXIS2_PLACEMENT_3D('',#63582,#42001,#42002);
#34595=AXIS2_PLACEMENT_3D('',#63583,#42003,#42004);
#34596=AXIS2_PLACEMENT_3D('',#63584,#42005,#42006);
#34597=AXIS2_PLACEMENT_3D('',#63585,#42007,#42008);
#34598=AXIS2_PLACEMENT_3D('',#63586,#42009,#42010);
#34599=AXIS2_PLACEMENT_3D('',#63587,#42011,#42012);
#34600=AXIS2_PLACEMENT_3D('',#63588,#42013,#42014);
#34601=AXIS2_PLACEMENT_3D('',#63589,#42015,#42016);
#34602=AXIS2_PLACEMENT_3D('',#63590,#42017,#42018);
#34603=AXIS2_PLACEMENT_3D('',#63591,#42019,#42020);
#34604=AXIS2_PLACEMENT_3D('',#63592,#42021,#42022);
#34605=AXIS2_PLACEMENT_3D('',#63593,#42023,#42024);
#34606=AXIS2_PLACEMENT_3D('',#63594,#42025,#42026);
#34607=AXIS2_PLACEMENT_3D('',#63595,#42027,#42028);
#34608=AXIS2_PLACEMENT_3D('',#63596,#42029,#42030);
#34609=AXIS2_PLACEMENT_3D('',#63597,#42031,#42032);
#34610=AXIS2_PLACEMENT_3D('',#63598,#42033,#42034);
#34611=AXIS2_PLACEMENT_3D('',#63599,#42035,#42036);
#34612=AXIS2_PLACEMENT_3D('',#63600,#42037,#42038);
#34613=AXIS2_PLACEMENT_3D('',#63601,#42039,#42040);
#34614=AXIS2_PLACEMENT_3D('',#63602,#42041,#42042);
#34615=AXIS2_PLACEMENT_3D('',#63603,#42043,#42044);
#34616=AXIS2_PLACEMENT_3D('',#63604,#42045,#42046);
#34617=AXIS2_PLACEMENT_3D('',#63605,#42047,#42048);
#34618=AXIS2_PLACEMENT_3D('',#63606,#42049,#42050);
#34619=AXIS2_PLACEMENT_3D('',#63607,#42051,#42052);
#34620=AXIS2_PLACEMENT_3D('',#63608,#42053,#42054);
#34621=AXIS2_PLACEMENT_3D('',#63609,#42055,#42056);
#34622=AXIS2_PLACEMENT_3D('',#63610,#42057,#42058);
#34623=AXIS2_PLACEMENT_3D('',#63611,#42059,#42060);
#34624=AXIS2_PLACEMENT_3D('',#63612,#42061,#42062);
#34625=AXIS2_PLACEMENT_3D('',#63613,#42063,#42064);
#34626=AXIS2_PLACEMENT_3D('',#63614,#42065,#42066);
#34627=AXIS2_PLACEMENT_3D('',#63615,#42067,#42068);
#34628=AXIS2_PLACEMENT_3D('',#63616,#42069,#42070);
#34629=AXIS2_PLACEMENT_3D('',#63617,#42071,#42072);
#34630=AXIS2_PLACEMENT_3D('',#63618,#42073,#42074);
#34631=AXIS2_PLACEMENT_3D('',#63619,#42075,#42076);
#34632=AXIS2_PLACEMENT_3D('',#63620,#42077,#42078);
#34633=AXIS2_PLACEMENT_3D('',#63621,#42079,#42080);
#34634=AXIS2_PLACEMENT_3D('',#63622,#42081,#42082);
#34635=AXIS2_PLACEMENT_3D('',#63623,#42083,#42084);
#34636=AXIS2_PLACEMENT_3D('',#63624,#42085,#42086);
#34637=AXIS2_PLACEMENT_3D('',#63625,#42087,#42088);
#34638=AXIS2_PLACEMENT_3D('',#63626,#42089,#42090);
#34639=AXIS2_PLACEMENT_3D('',#63627,#42091,#42092);
#34640=AXIS2_PLACEMENT_3D('',#63628,#42093,#42094);
#34641=AXIS2_PLACEMENT_3D('',#63629,#42095,#42096);
#34642=AXIS2_PLACEMENT_3D('',#63630,#42097,#42098);
#34643=AXIS2_PLACEMENT_3D('',#63631,#42099,#42100);
#34644=AXIS2_PLACEMENT_3D('',#63632,#42101,#42102);
#34645=AXIS2_PLACEMENT_3D('',#63633,#42103,#42104);
#34646=AXIS2_PLACEMENT_3D('',#63634,#42105,#42106);
#34647=AXIS2_PLACEMENT_3D('',#63635,#42107,#42108);
#34648=AXIS2_PLACEMENT_3D('',#63636,#42109,#42110);
#34649=AXIS2_PLACEMENT_3D('',#63637,#42111,#42112);
#34650=AXIS2_PLACEMENT_3D('',#63638,#42113,#42114);
#34651=AXIS2_PLACEMENT_3D('',#63639,#42115,#42116);
#34652=AXIS2_PLACEMENT_3D('',#63640,#42117,#42118);
#34653=AXIS2_PLACEMENT_3D('',#63641,#42119,#42120);
#34654=AXIS2_PLACEMENT_3D('',#63642,#42121,#42122);
#34655=AXIS2_PLACEMENT_3D('',#63643,#42123,#42124);
#34656=AXIS2_PLACEMENT_3D('',#63644,#42125,#42126);
#34657=AXIS2_PLACEMENT_3D('',#63645,#42127,#42128);
#34658=AXIS2_PLACEMENT_3D('',#63646,#42129,#42130);
#34659=AXIS2_PLACEMENT_3D('',#63647,#42131,#42132);
#34660=AXIS2_PLACEMENT_3D('',#63648,#42133,#42134);
#34661=AXIS2_PLACEMENT_3D('',#63649,#42135,#42136);
#34662=AXIS2_PLACEMENT_3D('',#63650,#42137,#42138);
#34663=AXIS2_PLACEMENT_3D('',#63651,#42139,#42140);
#34664=AXIS2_PLACEMENT_3D('',#63652,#42141,#42142);
#34665=AXIS2_PLACEMENT_3D('',#63653,#42143,#42144);
#34666=AXIS2_PLACEMENT_3D('',#63654,#42145,#42146);
#34667=AXIS2_PLACEMENT_3D('',#63655,#42147,#42148);
#34668=AXIS2_PLACEMENT_3D('',#63656,#42149,#42150);
#34669=AXIS2_PLACEMENT_3D('',#63657,#42151,#42152);
#34670=AXIS2_PLACEMENT_3D('',#63658,#42153,#42154);
#34671=AXIS2_PLACEMENT_3D('',#63659,#42155,#42156);
#34672=AXIS2_PLACEMENT_3D('',#63660,#42157,#42158);
#34673=AXIS2_PLACEMENT_3D('',#63661,#42159,#42160);
#34674=AXIS2_PLACEMENT_3D('',#63662,#42161,#42162);
#34675=AXIS2_PLACEMENT_3D('',#63663,#42163,#42164);
#34676=AXIS2_PLACEMENT_3D('',#63664,#42165,#42166);
#34677=AXIS2_PLACEMENT_3D('',#63665,#42167,#42168);
#34678=AXIS2_PLACEMENT_3D('',#63666,#42169,#42170);
#34679=AXIS2_PLACEMENT_3D('',#63667,#42171,#42172);
#34680=AXIS2_PLACEMENT_3D('',#63668,#42173,#42174);
#34681=AXIS2_PLACEMENT_3D('',#63669,#42175,#42176);
#34682=AXIS2_PLACEMENT_3D('',#63670,#42177,#42178);
#34683=AXIS2_PLACEMENT_3D('',#63671,#42179,#42180);
#34684=AXIS2_PLACEMENT_3D('',#63672,#42181,#42182);
#34685=AXIS2_PLACEMENT_3D('',#63673,#42183,#42184);
#34686=AXIS2_PLACEMENT_3D('',#63674,#42185,#42186);
#34687=AXIS2_PLACEMENT_3D('',#63675,#42187,#42188);
#34688=AXIS2_PLACEMENT_3D('',#63676,#42189,#42190);
#34689=AXIS2_PLACEMENT_3D('',#63677,#42191,#42192);
#34690=AXIS2_PLACEMENT_3D('',#63678,#42193,#42194);
#34691=AXIS2_PLACEMENT_3D('',#63679,#42195,#42196);
#34692=AXIS2_PLACEMENT_3D('',#63680,#42197,#42198);
#34693=AXIS2_PLACEMENT_3D('',#63681,#42199,#42200);
#34694=AXIS2_PLACEMENT_3D('',#63682,#42201,#42202);
#34695=AXIS2_PLACEMENT_3D('',#63683,#42203,#42204);
#34696=AXIS2_PLACEMENT_3D('',#63684,#42205,#42206);
#34697=AXIS2_PLACEMENT_3D('',#63685,#42207,#42208);
#34698=AXIS2_PLACEMENT_3D('',#63686,#42209,#42210);
#34699=AXIS2_PLACEMENT_3D('',#63687,#42211,#42212);
#34700=AXIS2_PLACEMENT_3D('',#63688,#42213,#42214);
#34701=AXIS2_PLACEMENT_3D('',#63689,#42215,#42216);
#34702=AXIS2_PLACEMENT_3D('',#63690,#42217,#42218);
#34703=AXIS2_PLACEMENT_3D('',#63691,#42219,#42220);
#34704=AXIS2_PLACEMENT_3D('',#63692,#42221,#42222);
#34705=AXIS2_PLACEMENT_3D('',#63693,#42223,#42224);
#34706=AXIS2_PLACEMENT_3D('',#63694,#42225,#42226);
#34707=AXIS2_PLACEMENT_3D('',#63695,#42227,#42228);
#34708=AXIS2_PLACEMENT_3D('',#63696,#42229,#42230);
#34709=AXIS2_PLACEMENT_3D('',#63697,#42231,#42232);
#34710=AXIS2_PLACEMENT_3D('',#63698,#42233,#42234);
#34711=AXIS2_PLACEMENT_3D('',#63699,#42235,#42236);
#34712=AXIS2_PLACEMENT_3D('',#63700,#42237,#42238);
#34713=AXIS2_PLACEMENT_3D('',#63701,#42239,#42240);
#34714=AXIS2_PLACEMENT_3D('',#63702,#42241,#42242);
#34715=AXIS2_PLACEMENT_3D('',#63704,#42243,#42244);
#34716=AXIS2_PLACEMENT_3D('',#63706,#42245,#42246);
#34717=AXIS2_PLACEMENT_3D('',#63707,#42247,#42248);
#34718=AXIS2_PLACEMENT_3D('',#63708,#42249,#42250);
#34719=AXIS2_PLACEMENT_3D('',#63713,#42253,#42254);
#34720=AXIS2_PLACEMENT_3D('',#63714,#42255,#42256);
#34721=AXIS2_PLACEMENT_3D('',#63715,#42257,#42258);
#34722=AXIS2_PLACEMENT_3D('',#63716,#42259,#42260);
#34723=AXIS2_PLACEMENT_3D('',#63717,#42261,#42262);
#34724=AXIS2_PLACEMENT_3D('',#63718,#42263,#42264);
#34725=AXIS2_PLACEMENT_3D('',#63731,#42271,#42272);
#34726=AXIS2_PLACEMENT_3D('',#63734,#42275,#42276);
#34727=AXIS2_PLACEMENT_3D('',#63736,#42278,#42279);
#34728=AXIS2_PLACEMENT_3D('',#63738,#42281,#42282);
#34729=AXIS2_PLACEMENT_3D('',#63740,#42284,#42285);
#34730=AXIS2_PLACEMENT_3D('',#63742,#42287,#42288);
#34731=AXIS2_PLACEMENT_3D('',#65264,#42290,#42291);
#34732=AXIS2_PLACEMENT_3D('',#65265,#42292,#42293);
#34733=AXIS2_PLACEMENT_3D('',#65267,#42295,#42296);
#34734=AXIS2_PLACEMENT_3D('',#65269,#42298,#42299);
#34735=AXIS2_PLACEMENT_3D('',#65270,#42300,#42301);
#34736=AXIS2_PLACEMENT_3D('',#65272,#42303,#42304);
#34737=AXIS2_PLACEMENT_3D('',#65274,#42306,#42307);
#34738=AXIS2_PLACEMENT_3D('',#65275,#42308,#42309);
#34739=AXIS2_PLACEMENT_3D('',#65277,#42311,#42312);
#34740=AXIS2_PLACEMENT_3D('',#65279,#42314,#42315);
#34741=AXIS2_PLACEMENT_3D('',#65280,#42316,#42317);
#34742=AXIS2_PLACEMENT_3D('',#65282,#42319,#42320);
#34743=AXIS2_PLACEMENT_3D('',#65284,#42322,#42323);
#34744=AXIS2_PLACEMENT_3D('',#65285,#42324,#42325);
#34745=AXIS2_PLACEMENT_3D('',#65287,#42327,#42328);
#34746=AXIS2_PLACEMENT_3D('',#65289,#42330,#42331);
#34747=AXIS2_PLACEMENT_3D('',#65290,#42332,#42333);
#34748=AXIS2_PLACEMENT_3D('',#65292,#42335,#42336);
#34749=AXIS2_PLACEMENT_3D('',#65294,#42338,#42339);
#34750=AXIS2_PLACEMENT_3D('',#65295,#42340,#42341);
#34751=AXIS2_PLACEMENT_3D('',#65297,#42343,#42344);
#34752=AXIS2_PLACEMENT_3D('',#65299,#42346,#42347);
#34753=AXIS2_PLACEMENT_3D('',#65300,#42348,#42349);
#34754=AXIS2_PLACEMENT_3D('',#65301,#42350,#42351);
#34755=AXIS2_PLACEMENT_3D('',#65302,#42352,#42353);
#34756=AXIS2_PLACEMENT_3D('',#65303,#42354,#42355);
#34757=AXIS2_PLACEMENT_3D('',#65304,#42356,#42357);
#34758=AXIS2_PLACEMENT_3D('',#65305,#42358,#42359);
#34759=AXIS2_PLACEMENT_3D('',#65306,#42360,#42361);
#34760=AXIS2_PLACEMENT_3D('',#65307,#42362,#42363);
#34761=AXIS2_PLACEMENT_3D('',#65308,#42364,#42365);
#34762=AXIS2_PLACEMENT_3D('',#65309,#42366,#42367);
#34763=AXIS2_PLACEMENT_3D('',#65310,#42368,#42369);
#34764=AXIS2_PLACEMENT_3D('',#65311,#42370,#42371);
#34765=AXIS2_PLACEMENT_3D('',#65312,#42372,#42373);
#34766=AXIS2_PLACEMENT_3D('',#65313,#42374,#42375);
#34767=AXIS2_PLACEMENT_3D('',#65314,#42376,#42377);
#34768=AXIS2_PLACEMENT_3D('',#65315,#42378,#42379);
#34769=AXIS2_PLACEMENT_3D('',#65316,#42380,#42381);
#34770=AXIS2_PLACEMENT_3D('',#65317,#42382,#42383);
#34771=AXIS2_PLACEMENT_3D('',#65318,#42384,#42385);
#34772=AXIS2_PLACEMENT_3D('',#65320,#42387,#42388);
#34773=AXIS2_PLACEMENT_3D('',#65322,#42390,#42391);
#34774=AXIS2_PLACEMENT_3D('',#65323,#42392,#42393);
#34775=AXIS2_PLACEMENT_3D('',#65325,#42395,#42396);
#34776=AXIS2_PLACEMENT_3D('',#65327,#42398,#42399);
#34777=AXIS2_PLACEMENT_3D('',#65328,#42400,#42401);
#34778=AXIS2_PLACEMENT_3D('',#65330,#42403,#42404);
#34779=AXIS2_PLACEMENT_3D('',#65332,#42406,#42407);
#34780=AXIS2_PLACEMENT_3D('',#65333,#42408,#42409);
#34781=AXIS2_PLACEMENT_3D('',#65335,#42411,#42412);
#34782=AXIS2_PLACEMENT_3D('',#65337,#42414,#42415);
#34783=AXIS2_PLACEMENT_3D('',#65338,#42416,#42417);
#34784=AXIS2_PLACEMENT_3D('',#65340,#42419,#42420);
#34785=AXIS2_PLACEMENT_3D('',#65342,#42422,#42423);
#34786=AXIS2_PLACEMENT_3D('',#65343,#42424,#42425);
#34787=AXIS2_PLACEMENT_3D('',#65345,#42427,#42428);
#34788=AXIS2_PLACEMENT_3D('',#65347,#42430,#42431);
#34789=AXIS2_PLACEMENT_3D('',#65348,#42432,#42433);
#34790=AXIS2_PLACEMENT_3D('',#65350,#42435,#42436);
#34791=AXIS2_PLACEMENT_3D('',#65352,#42438,#42439);
#34792=AXIS2_PLACEMENT_3D('',#65353,#42440,#42441);
#34793=AXIS2_PLACEMENT_3D('',#65355,#42443,#42444);
#34794=AXIS2_PLACEMENT_3D('',#65357,#42446,#42447);
#34795=AXIS2_PLACEMENT_3D('',#65358,#42448,#42449);
#34796=AXIS2_PLACEMENT_3D('',#65360,#42451,#42452);
#34797=AXIS2_PLACEMENT_3D('',#65362,#42454,#42455);
#34798=AXIS2_PLACEMENT_3D('',#65363,#42456,#42457);
#34799=AXIS2_PLACEMENT_3D('',#65365,#42459,#42460);
#34800=AXIS2_PLACEMENT_3D('',#65367,#42462,#42463);
#34801=AXIS2_PLACEMENT_3D('',#65368,#42464,#42465);
#34802=AXIS2_PLACEMENT_3D('',#65370,#42467,#42468);
#34803=AXIS2_PLACEMENT_3D('',#65372,#42470,#42471);
#34804=AXIS2_PLACEMENT_3D('',#65373,#42472,#42473);
#34805=AXIS2_PLACEMENT_3D('',#65375,#42475,#42476);
#34806=AXIS2_PLACEMENT_3D('',#65377,#42478,#42479);
#34807=AXIS2_PLACEMENT_3D('',#65378,#42480,#42481);
#34808=AXIS2_PLACEMENT_3D('',#65380,#42483,#42484);
#34809=AXIS2_PLACEMENT_3D('',#65382,#42486,#42487);
#34810=AXIS2_PLACEMENT_3D('',#65383,#42488,#42489);
#34811=AXIS2_PLACEMENT_3D('',#65385,#42491,#42492);
#34812=AXIS2_PLACEMENT_3D('',#65387,#42494,#42495);
#34813=AXIS2_PLACEMENT_3D('',#65388,#42496,#42497);
#34814=AXIS2_PLACEMENT_3D('',#65390,#42499,#42500);
#34815=AXIS2_PLACEMENT_3D('',#65392,#42502,#42503);
#34816=AXIS2_PLACEMENT_3D('',#65393,#42504,#42505);
#34817=AXIS2_PLACEMENT_3D('',#65395,#42507,#42508);
#34818=AXIS2_PLACEMENT_3D('',#65397,#42510,#42511);
#34819=AXIS2_PLACEMENT_3D('',#65398,#42512,#42513);
#34820=AXIS2_PLACEMENT_3D('',#65400,#42515,#42516);
#34821=AXIS2_PLACEMENT_3D('',#65402,#42518,#42519);
#34822=AXIS2_PLACEMENT_3D('',#65403,#42520,#42521);
#34823=AXIS2_PLACEMENT_3D('',#65405,#42523,#42524);
#34824=AXIS2_PLACEMENT_3D('',#65407,#42526,#42527);
#34825=AXIS2_PLACEMENT_3D('',#65408,#42528,#42529);
#34826=AXIS2_PLACEMENT_3D('',#65410,#42531,#42532);
#34827=AXIS2_PLACEMENT_3D('',#65412,#42534,#42535);
#34828=AXIS2_PLACEMENT_3D('',#65413,#42536,#42537);
#34829=AXIS2_PLACEMENT_3D('',#65415,#42539,#42540);
#34830=AXIS2_PLACEMENT_3D('',#65417,#42542,#42543);
#34831=AXIS2_PLACEMENT_3D('',#65418,#42544,#42545);
#34832=AXIS2_PLACEMENT_3D('',#65420,#42547,#42548);
#34833=AXIS2_PLACEMENT_3D('',#65422,#42550,#42551);
#34834=AXIS2_PLACEMENT_3D('',#65423,#42552,#42553);
#34835=AXIS2_PLACEMENT_3D('',#65425,#42555,#42556);
#34836=AXIS2_PLACEMENT_3D('',#65427,#42558,#42559);
#34837=AXIS2_PLACEMENT_3D('',#65428,#42560,#42561);
#34838=AXIS2_PLACEMENT_3D('',#65430,#42563,#42564);
#34839=AXIS2_PLACEMENT_3D('',#65432,#42566,#42567);
#34840=AXIS2_PLACEMENT_3D('',#65433,#42568,#42569);
#34841=AXIS2_PLACEMENT_3D('',#65435,#42571,#42572);
#34842=AXIS2_PLACEMENT_3D('',#65437,#42574,#42575);
#34843=AXIS2_PLACEMENT_3D('',#65438,#42576,#42577);
#34844=AXIS2_PLACEMENT_3D('',#65440,#42579,#42580);
#34845=AXIS2_PLACEMENT_3D('',#65442,#42582,#42583);
#34846=AXIS2_PLACEMENT_3D('',#65443,#42584,#42585);
#34847=AXIS2_PLACEMENT_3D('',#65445,#42587,#42588);
#34848=AXIS2_PLACEMENT_3D('',#65447,#42590,#42591);
#34849=AXIS2_PLACEMENT_3D('',#65448,#42592,#42593);
#34850=AXIS2_PLACEMENT_3D('',#65450,#42595,#42596);
#34851=AXIS2_PLACEMENT_3D('',#65452,#42598,#42599);
#34852=AXIS2_PLACEMENT_3D('',#65453,#42600,#42601);
#34853=AXIS2_PLACEMENT_3D('',#65455,#42603,#42604);
#34854=AXIS2_PLACEMENT_3D('',#65457,#42606,#42607);
#34855=AXIS2_PLACEMENT_3D('',#65458,#42608,#42609);
#34856=AXIS2_PLACEMENT_3D('',#65460,#42611,#42612);
#34857=AXIS2_PLACEMENT_3D('',#65462,#42614,#42615);
#34858=AXIS2_PLACEMENT_3D('',#65463,#42616,#42617);
#34859=AXIS2_PLACEMENT_3D('',#65465,#42619,#42620);
#34860=AXIS2_PLACEMENT_3D('',#65467,#42622,#42623);
#34861=AXIS2_PLACEMENT_3D('',#65468,#42624,#42625);
#34862=AXIS2_PLACEMENT_3D('',#65470,#42627,#42628);
#34863=AXIS2_PLACEMENT_3D('',#65472,#42630,#42631);
#34864=AXIS2_PLACEMENT_3D('',#65473,#42632,#42633);
#34865=AXIS2_PLACEMENT_3D('',#65475,#42635,#42636);
#34866=AXIS2_PLACEMENT_3D('',#65477,#42638,#42639);
#34867=AXIS2_PLACEMENT_3D('',#65478,#42640,#42641);
#34868=AXIS2_PLACEMENT_3D('',#65480,#42643,#42644);
#34869=AXIS2_PLACEMENT_3D('',#65482,#42646,#42647);
#34870=AXIS2_PLACEMENT_3D('',#65483,#42648,#42649);
#34871=AXIS2_PLACEMENT_3D('',#65485,#42651,#42652);
#34872=AXIS2_PLACEMENT_3D('',#65487,#42654,#42655);
#34873=AXIS2_PLACEMENT_3D('',#65488,#42656,#42657);
#34874=AXIS2_PLACEMENT_3D('',#65490,#42659,#42660);
#34875=AXIS2_PLACEMENT_3D('',#65492,#42662,#42663);
#34876=AXIS2_PLACEMENT_3D('',#65493,#42664,#42665);
#34877=AXIS2_PLACEMENT_3D('',#65495,#42667,#42668);
#34878=AXIS2_PLACEMENT_3D('',#65497,#42670,#42671);
#34879=AXIS2_PLACEMENT_3D('',#65498,#42672,#42673);
#34880=AXIS2_PLACEMENT_3D('',#65500,#42675,#42676);
#34881=AXIS2_PLACEMENT_3D('',#65502,#42678,#42679);
#34882=AXIS2_PLACEMENT_3D('',#65503,#42680,#42681);
#34883=AXIS2_PLACEMENT_3D('',#65505,#42683,#42684);
#34884=AXIS2_PLACEMENT_3D('',#65507,#42686,#42687);
#34885=AXIS2_PLACEMENT_3D('',#65508,#42688,#42689);
#34886=AXIS2_PLACEMENT_3D('',#65510,#42691,#42692);
#34887=AXIS2_PLACEMENT_3D('',#65512,#42694,#42695);
#34888=AXIS2_PLACEMENT_3D('',#65513,#42696,#42697);
#34889=AXIS2_PLACEMENT_3D('',#65515,#42699,#42700);
#34890=AXIS2_PLACEMENT_3D('',#65517,#42702,#42703);
#34891=AXIS2_PLACEMENT_3D('',#65518,#42704,#42705);
#34892=AXIS2_PLACEMENT_3D('',#65520,#42707,#42708);
#34893=AXIS2_PLACEMENT_3D('',#65522,#42710,#42711);
#34894=AXIS2_PLACEMENT_3D('',#65523,#42712,#42713);
#34895=AXIS2_PLACEMENT_3D('',#65525,#42715,#42716);
#34896=AXIS2_PLACEMENT_3D('',#65527,#42718,#42719);
#34897=AXIS2_PLACEMENT_3D('',#65528,#42720,#42721);
#34898=AXIS2_PLACEMENT_3D('',#65530,#42723,#42724);
#34899=AXIS2_PLACEMENT_3D('',#65532,#42726,#42727);
#34900=AXIS2_PLACEMENT_3D('',#65533,#42728,#42729);
#34901=AXIS2_PLACEMENT_3D('',#65535,#42731,#42732);
#34902=AXIS2_PLACEMENT_3D('',#65537,#42734,#42735);
#34903=AXIS2_PLACEMENT_3D('',#65538,#42736,#42737);
#34904=AXIS2_PLACEMENT_3D('',#65540,#42739,#42740);
#34905=AXIS2_PLACEMENT_3D('',#65542,#42742,#42743);
#34906=AXIS2_PLACEMENT_3D('',#65543,#42744,#42745);
#34907=AXIS2_PLACEMENT_3D('',#65545,#42747,#42748);
#34908=AXIS2_PLACEMENT_3D('',#65547,#42750,#42751);
#34909=AXIS2_PLACEMENT_3D('',#65548,#42752,#42753);
#34910=AXIS2_PLACEMENT_3D('',#65550,#42755,#42756);
#34911=AXIS2_PLACEMENT_3D('',#65552,#42758,#42759);
#34912=AXIS2_PLACEMENT_3D('',#65553,#42760,#42761);
#34913=AXIS2_PLACEMENT_3D('',#65555,#42763,#42764);
#34914=AXIS2_PLACEMENT_3D('',#65557,#42766,#42767);
#34915=AXIS2_PLACEMENT_3D('',#65558,#42768,#42769);
#34916=AXIS2_PLACEMENT_3D('',#65560,#42771,#42772);
#34917=AXIS2_PLACEMENT_3D('',#65562,#42774,#42775);
#34918=AXIS2_PLACEMENT_3D('',#65563,#42776,#42777);
#34919=AXIS2_PLACEMENT_3D('',#65565,#42779,#42780);
#34920=AXIS2_PLACEMENT_3D('',#65567,#42782,#42783);
#34921=AXIS2_PLACEMENT_3D('',#65568,#42784,#42785);
#34922=AXIS2_PLACEMENT_3D('',#65570,#42787,#42788);
#34923=AXIS2_PLACEMENT_3D('',#65572,#42790,#42791);
#34924=AXIS2_PLACEMENT_3D('',#65573,#42792,#42793);
#34925=AXIS2_PLACEMENT_3D('',#65575,#42795,#42796);
#34926=AXIS2_PLACEMENT_3D('',#65577,#42798,#42799);
#34927=AXIS2_PLACEMENT_3D('',#65578,#42800,#42801);
#34928=AXIS2_PLACEMENT_3D('',#65580,#42803,#42804);
#34929=AXIS2_PLACEMENT_3D('',#65582,#42806,#42807);
#34930=AXIS2_PLACEMENT_3D('',#65583,#42808,#42809);
#34931=AXIS2_PLACEMENT_3D('',#65585,#42811,#42812);
#34932=AXIS2_PLACEMENT_3D('',#65587,#42814,#42815);
#34933=AXIS2_PLACEMENT_3D('',#65588,#42816,#42817);
#34934=AXIS2_PLACEMENT_3D('',#65590,#42819,#42820);
#34935=AXIS2_PLACEMENT_3D('',#65592,#42822,#42823);
#34936=AXIS2_PLACEMENT_3D('',#65593,#42824,#42825);
#34937=AXIS2_PLACEMENT_3D('',#65595,#42827,#42828);
#34938=AXIS2_PLACEMENT_3D('',#65597,#42830,#42831);
#34939=AXIS2_PLACEMENT_3D('',#65598,#42832,#42833);
#34940=AXIS2_PLACEMENT_3D('',#65600,#42835,#42836);
#34941=AXIS2_PLACEMENT_3D('',#65602,#42838,#42839);
#34942=AXIS2_PLACEMENT_3D('',#65603,#42840,#42841);
#34943=AXIS2_PLACEMENT_3D('',#65605,#42843,#42844);
#34944=AXIS2_PLACEMENT_3D('',#65607,#42846,#42847);
#34945=AXIS2_PLACEMENT_3D('',#65608,#42848,#42849);
#34946=AXIS2_PLACEMENT_3D('',#65609,#42850,#42851);
#34947=AXIS2_PLACEMENT_3D('',#65610,#42852,#42853);
#34948=AXIS2_PLACEMENT_3D('',#65611,#42854,#42855);
#34949=AXIS2_PLACEMENT_3D('',#65612,#42856,#42857);
#34950=AXIS2_PLACEMENT_3D('',#65613,#42858,#42859);
#34951=AXIS2_PLACEMENT_3D('',#65614,#42860,#42861);
#34952=AXIS2_PLACEMENT_3D('',#65615,#42862,#42863);
#34953=AXIS2_PLACEMENT_3D('',#65616,#42864,#42865);
#34954=AXIS2_PLACEMENT_3D('',#65617,#42866,#42867);
#34955=AXIS2_PLACEMENT_3D('',#65618,#42868,#42869);
#34956=AXIS2_PLACEMENT_3D('',#65619,#42870,#42871);
#39715=DIRECTION('axis',(0.,0.,1.));
#39716=DIRECTION('refdir',(1.,0.,0.));
#39717=DIRECTION('center_axis',(5.15167520928809E-67,-1.18789542670764E-48,
-1.));
#39718=DIRECTION('ref_axis',(-4.33680868994202E-19,1.,-1.18789542670764E-48));
#39719=DIRECTION('',(-5.15167520928809E-67,1.18789542670764E-48,1.));
#39720=DIRECTION('',(-5.15167520928809E-67,1.18789542670764E-48,1.));
#39721=DIRECTION('center_axis',(5.15167520928809E-67,-1.18789542670764E-48,
-1.));
#39722=DIRECTION('ref_axis',(-4.33680868994202E-19,1.,-1.18789542670764E-48));
#39723=DIRECTION('center_axis',(-4.70261923768679E-35,1.08435016942139E-16,
-1.));
#39724=DIRECTION('ref_axis',(-4.33680868994202E-19,1.,1.08435016942139E-16));
#39725=DIRECTION('center_axis',(5.15167520928809E-67,-1.18789542670764E-48,
-1.));
#39726=DIRECTION('ref_axis',(-4.33680868994202E-19,1.,-1.18789542670764E-48));
#39727=DIRECTION('',(-5.15167520928809E-67,1.18789542670764E-48,1.));
#39728=DIRECTION('center_axis',(5.15167520928809E-67,-1.18789542670764E-48,
-1.));
#39729=DIRECTION('ref_axis',(-4.33680868994202E-19,1.,-1.18789542670764E-48));
#39730=DIRECTION('',(-5.15167520928809E-67,1.18789542670764E-48,1.));
#39731=DIRECTION('center_axis',(5.15167520928809E-67,-1.18789542670764E-48,
-1.));
#39732=DIRECTION('ref_axis',(-4.33680868994202E-19,1.,-1.18789542670764E-48));
#39733=DIRECTION('',(-5.15167520928809E-67,1.18789542670764E-48,1.));
#39734=DIRECTION('center_axis',(5.15167520928809E-67,-1.18789542670764E-48,
-1.));
#39735=DIRECTION('ref_axis',(-4.33680868994202E-19,1.,-1.18789542670764E-48));
#39736=DIRECTION('',(-5.15167520928809E-67,1.18789542670764E-48,1.));
#39737=DIRECTION('center_axis',(5.15167520928809E-67,-1.18789542670764E-48,
-1.));
#39738=DIRECTION('ref_axis',(-4.33680868994202E-19,1.,-1.18789542670764E-48));
#39739=DIRECTION('',(-5.15167520928809E-67,1.18789542670764E-48,1.));
#39740=DIRECTION('center_axis',(5.15167520928809E-67,-1.18789542670764E-48,
-1.));
#39741=DIRECTION('ref_axis',(-4.33680868994202E-19,1.,-1.18789542670764E-48));
#39742=DIRECTION('',(-5.15167520928809E-67,1.18789542670764E-48,1.));
#39743=DIRECTION('center_axis',(5.15167520928809E-67,-1.18789542670764E-48,
-1.));
#39744=DIRECTION('ref_axis',(-4.33680868994202E-19,1.,-1.18789542670764E-48));
#39745=DIRECTION('',(-5.15167520928809E-67,1.18789542670764E-48,1.));
#39746=DIRECTION('center_axis',(5.15167520928809E-67,-1.18789542670764E-48,
-1.));
#39747=DIRECTION('ref_axis',(-4.33680868994202E-19,1.,-1.18789542670764E-48));
#39748=DIRECTION('',(-5.15167520928809E-67,1.18789542670764E-48,1.));
#39749=DIRECTION('center_axis',(5.15167520928809E-67,-1.18789542670764E-48,
-1.));
#39750=DIRECTION('ref_axis',(-4.33680868994202E-19,1.,-1.18789542670764E-48));
#39751=DIRECTION('',(-5.15167520928809E-67,1.18789542670764E-48,1.));
#39752=DIRECTION('center_axis',(5.15167520928809E-67,-1.18789542670764E-48,
-1.));
#39753=DIRECTION('ref_axis',(-4.33680868994202E-19,1.,-1.18789542670764E-48));
#39754=DIRECTION('',(-5.15167520928809E-67,1.18789542670764E-48,1.));
#39755=DIRECTION('center_axis',(5.15167520928809E-67,-1.18789542670764E-48,
-1.));
#39756=DIRECTION('ref_axis',(-4.33680868994202E-19,1.,-1.18789542670764E-48));
#39757=DIRECTION('',(-5.15167520928809E-67,1.18789542670764E-48,1.));
#39758=DIRECTION('center_axis',(5.15167520928809E-67,-1.18789542670764E-48,
-1.));
#39759=DIRECTION('ref_axis',(-4.33680868994202E-19,1.,-1.18789542670764E-48));
#39760=DIRECTION('',(-5.15167520928809E-67,1.18789542670764E-48,1.));
#39761=DIRECTION('center_axis',(5.15167520928809E-67,-1.18789542670764E-48,
-1.));
#39762=DIRECTION('ref_axis',(-4.33680868994202E-19,1.,-1.18789542670764E-48));
#39763=DIRECTION('',(-5.15167520928809E-67,1.18789542670764E-48,1.));
#39764=DIRECTION('center_axis',(5.15167520928809E-67,-1.18789542670764E-48,
-1.));
#39765=DIRECTION('ref_axis',(-4.33680868994202E-19,1.,-1.18789542670764E-48));
#39766=DIRECTION('',(-5.15167520928809E-67,1.18789542670764E-48,1.));
#39767=DIRECTION('center_axis',(5.15167520928809E-67,-1.18789542670764E-48,
-1.));
#39768=DIRECTION('ref_axis',(-4.33680868994202E-19,1.,-1.18789542670764E-48));
#39769=DIRECTION('',(-5.15167520928809E-67,1.18789542670764E-48,1.));
#39770=DIRECTION('center_axis',(5.15167520928809E-67,-1.18789542670764E-48,
-1.));
#39771=DIRECTION('ref_axis',(-4.33680868994202E-19,1.,-1.18789542670764E-48));
#39772=DIRECTION('',(-5.15167520928809E-67,1.18789542670764E-48,1.));
#39773=DIRECTION('center_axis',(5.15167520928809E-67,-1.18789542670764E-48,
-1.));
#39774=DIRECTION('ref_axis',(-4.33680868994202E-19,1.,-1.18789542670764E-48));
#39775=DIRECTION('',(-5.15167520928809E-67,1.18789542670764E-48,1.));
#39776=DIRECTION('center_axis',(5.15167520928809E-67,-1.18789542670764E-48,
-1.));
#39777=DIRECTION('ref_axis',(-4.33680868994202E-19,1.,-1.18789542670764E-48));
#39778=DIRECTION('',(-5.15167520928809E-67,1.18789542670764E-48,1.));
#39779=DIRECTION('center_axis',(5.15167520928809E-67,-1.18789542670764E-48,
-1.));
#39780=DIRECTION('ref_axis',(-4.33680868994202E-19,1.,-1.18789542670764E-48));
#39781=DIRECTION('',(-5.15167520928809E-67,1.18789542670764E-48,1.));
#39782=DIRECTION('center_axis',(5.15167520928809E-67,-1.18789542670764E-48,
-1.));
#39783=DIRECTION('ref_axis',(-4.33680868994202E-19,1.,-1.18789542670764E-48));
#39784=DIRECTION('',(-5.15167520928809E-67,1.18789542670764E-48,1.));
#39785=DIRECTION('center_axis',(5.15167520928809E-67,-1.18789542670764E-48,
-1.));
#39786=DIRECTION('ref_axis',(-4.33680868994202E-19,1.,-1.18789542670764E-48));
#39787=DIRECTION('',(-5.15167520928809E-67,1.18789542670764E-48,1.));
#39788=DIRECTION('center_axis',(5.15167520928809E-67,-1.18789542670764E-48,
-1.));
#39789=DIRECTION('ref_axis',(-4.33680868994202E-19,1.,-1.18789542670764E-48));
#39790=DIRECTION('',(-5.15167520928809E-67,1.18789542670764E-48,1.));
#39791=DIRECTION('center_axis',(5.15167520928809E-67,-1.18789542670764E-48,
-1.));
#39792=DIRECTION('ref_axis',(-4.33680868994202E-19,1.,-1.18789542670764E-48));
#39793=DIRECTION('',(-5.15167520928809E-67,1.18789542670764E-48,1.));
#39794=DIRECTION('center_axis',(5.15167520928809E-67,-1.18789542670764E-48,
-1.));
#39795=DIRECTION('ref_axis',(-4.33680868994202E-19,1.,-1.18789542670764E-48));
#39796=DIRECTION('',(-5.15167520928809E-67,1.18789542670764E-48,1.));
#39797=DIRECTION('center_axis',(5.15167520928809E-67,-1.18789542670764E-48,
-1.));
#39798=DIRECTION('ref_axis',(-4.33680868994202E-19,1.,-1.18789542670764E-48));
#39799=DIRECTION('',(-5.15167520928809E-67,1.18789542670764E-48,1.));
#39800=DIRECTION('center_axis',(5.15167520928809E-67,-1.18789542670764E-48,
-1.));
#39801=DIRECTION('ref_axis',(-4.33680868994202E-19,1.,-1.18789542670764E-48));
#39802=DIRECTION('',(-5.15167520928809E-67,1.18789542670764E-48,1.));
#39803=DIRECTION('center_axis',(5.15167520928809E-67,-1.18789542670764E-48,
-1.));
#39804=DIRECTION('ref_axis',(-4.33680868994202E-19,1.,-1.18789542670764E-48));
#39805=DIRECTION('',(-5.15167520928809E-67,1.18789542670764E-48,1.));
#39806=DIRECTION('center_axis',(-5.15167520928809E-67,1.18789542670764E-48,
1.));
#39807=DIRECTION('ref_axis',(4.33680868994202E-19,-1.,1.18789542670764E-48));
#39808=DIRECTION('',(8.69022643068855E-17,-0.707106781186544,-0.707106781186551));
#39809=DIRECTION('center_axis',(5.15167520928809E-67,-1.18789542670764E-48,
-1.));
#39810=DIRECTION('ref_axis',(-4.33680868994202E-19,1.,-1.18789542670764E-48));
#39811=DIRECTION('center_axis',(0.,0.,1.));
#39812=DIRECTION('ref_axis',(5.30947313395831E-16,1.,0.));
#39813=DIRECTION('',(0.,0.,-1.));
#39814=DIRECTION('center_axis',(5.15167520928809E-67,-1.18789542670764E-48,
-1.));
#39815=DIRECTION('ref_axis',(-4.33680868994202E-19,1.,-1.18789542670764E-48));
#39816=DIRECTION('center_axis',(0.,0.,1.));
#39817=DIRECTION('ref_axis',(5.30947313395831E-16,1.,0.));
#39818=DIRECTION('',(0.,0.,-1.));
#39819=DIRECTION('center_axis',(0.,0.,1.));
#39820=DIRECTION('ref_axis',(5.30947313395831E-16,1.,0.));
#39821=DIRECTION('',(0.,0.,-1.));
#39822=DIRECTION('center_axis',(0.,0.,1.));
#39823=DIRECTION('ref_axis',(5.30947313395831E-16,1.,0.));
#39824=DIRECTION('',(0.,0.,-1.));
#39825=DIRECTION('center_axis',(0.,0.,1.));
#39826=DIRECTION('ref_axis',(5.30947313395831E-16,1.,0.));
#39827=DIRECTION('',(0.,0.,-1.));
#39828=DIRECTION('center_axis',(0.,0.,1.));
#39829=DIRECTION('ref_axis',(5.30947313395831E-16,1.,0.));
#39830=DIRECTION('',(0.,0.,-1.));
#39831=DIRECTION('center_axis',(0.,0.,1.));
#39832=DIRECTION('ref_axis',(5.30947313395831E-16,1.,0.));
#39833=DIRECTION('',(0.,0.,-1.));
#39834=DIRECTION('center_axis',(0.,0.,1.));
#39835=DIRECTION('ref_axis',(5.30947313395831E-16,1.,0.));
#39836=DIRECTION('',(0.,0.,-1.));
#39837=DIRECTION('center_axis',(0.,0.,1.));
#39838=DIRECTION('ref_axis',(5.30947313395831E-16,1.,0.));
#39839=DIRECTION('',(0.,0.,-1.));
#39840=DIRECTION('center_axis',(0.,0.,1.));
#39841=DIRECTION('ref_axis',(5.30947313395831E-16,1.,0.));
#39842=DIRECTION('',(0.,0.,-1.));
#39843=DIRECTION('center_axis',(0.,0.,1.));
#39844=DIRECTION('ref_axis',(5.30947313395831E-16,1.,0.));
#39845=DIRECTION('',(0.,0.,-1.));
#39846=DIRECTION('center_axis',(0.,0.,1.));
#39847=DIRECTION('ref_axis',(5.30947313395831E-16,1.,0.));
#39848=DIRECTION('',(0.,0.,-1.));
#39849=DIRECTION('center_axis',(0.,0.,1.));
#39850=DIRECTION('ref_axis',(5.30947313395831E-16,1.,0.));
#39851=DIRECTION('',(0.,0.,-1.));
#39852=DIRECTION('center_axis',(0.,0.,1.));
#39853=DIRECTION('ref_axis',(5.30947313395831E-16,1.,0.));
#39854=DIRECTION('',(0.,0.,-1.));
#39855=DIRECTION('center_axis',(0.,0.,1.));
#39856=DIRECTION('ref_axis',(5.30947313395831E-16,1.,0.));
#39857=DIRECTION('',(0.,0.,-1.));
#39858=DIRECTION('center_axis',(0.,0.,1.));
#39859=DIRECTION('ref_axis',(5.30947313395831E-16,1.,0.));
#39860=DIRECTION('',(0.,0.,-1.));
#39861=DIRECTION('center_axis',(0.,0.,1.));
#39862=DIRECTION('ref_axis',(5.30947313395831E-16,1.,0.));
#39863=DIRECTION('',(0.,0.,-1.));
#39864=DIRECTION('center_axis',(0.,0.,1.));
#39865=DIRECTION('ref_axis',(5.30947313395831E-16,1.,0.));
#39866=DIRECTION('',(0.,0.,-1.));
#39867=DIRECTION('center_axis',(0.,0.,1.));
#39868=DIRECTION('ref_axis',(5.30947313395831E-16,1.,0.));
#39869=DIRECTION('',(0.,0.,-1.));
#39870=DIRECTION('center_axis',(0.,0.,1.));
#39871=DIRECTION('ref_axis',(5.30947313395831E-16,1.,0.));
#39872=DIRECTION('',(0.,0.,-1.));
#39873=DIRECTION('center_axis',(0.,0.,1.));
#39874=DIRECTION('ref_axis',(5.30947313395831E-16,1.,0.));
#39875=DIRECTION('',(0.,0.,-1.));
#39876=DIRECTION('center_axis',(0.,0.,1.));
#39877=DIRECTION('ref_axis',(5.30947313395831E-16,1.,0.));
#39878=DIRECTION('',(0.,0.,-1.));
#39879=DIRECTION('center_axis',(0.,0.,1.));
#39880=DIRECTION('ref_axis',(5.30947313395831E-16,1.,0.));
#39881=DIRECTION('',(0.,0.,-1.));
#39882=DIRECTION('center_axis',(0.,0.,1.));
#39883=DIRECTION('ref_axis',(5.30947313395831E-16,1.,0.));
#39884=DIRECTION('',(0.,0.,-1.));
#39885=DIRECTION('center_axis',(0.,0.,1.));
#39886=DIRECTION('ref_axis',(5.30947313395831E-16,1.,0.));
#39887=DIRECTION('',(0.,0.,-1.));
#39888=DIRECTION('center_axis',(0.,0.,1.));
#39889=DIRECTION('ref_axis',(5.30947313395831E-16,1.,0.));
#39890=DIRECTION('',(0.,0.,-1.));
#39891=DIRECTION('center_axis',(0.,0.,1.));
#39892=DIRECTION('ref_axis',(5.30947313395831E-16,1.,0.));
#39893=DIRECTION('',(0.,0.,-1.));
#39894=DIRECTION('center_axis',(0.,0.,1.));
#39895=DIRECTION('ref_axis',(5.30947313395831E-16,1.,0.));
#39896=DIRECTION('',(0.,0.,-1.));
#39897=DIRECTION('center_axis',(0.,0.,1.));
#39898=DIRECTION('ref_axis',(5.30947313395831E-16,1.,0.));
#39899=DIRECTION('',(0.,0.,-1.));
#39900=DIRECTION('center_axis',(0.,0.,1.));
#39901=DIRECTION('ref_axis',(5.30947313395831E-16,1.,0.));
#39902=DIRECTION('',(0.,0.,-1.));
#39903=DIRECTION('center_axis',(0.,0.,1.));
#39904=DIRECTION('ref_axis',(5.30947313395831E-16,1.,0.));
#39905=DIRECTION('center_axis',(0.,0.,1.));
#39906=DIRECTION('ref_axis',(0.700629269222058,-0.7135254915624,0.));
#39907=DIRECTION('center_axis',(-5.15167520928809E-67,1.18789542670764E-48,
1.));
#39908=DIRECTION('ref_axis',(4.33680868994202E-19,-1.,1.18789542670764E-48));
#39909=DIRECTION('center_axis',(5.15167520928809E-67,-1.18789542670764E-48,
-1.));
#39910=DIRECTION('ref_axis',(-4.33680868994202E-19,1.,-1.18789542670764E-48));
#39911=DIRECTION('center_axis',(5.15167520928809E-67,-1.18789542670764E-48,
-1.));
#39912=DIRECTION('ref_axis',(-4.33680868994202E-19,1.,-1.18789542670764E-48));
#39913=DIRECTION('center_axis',(5.15167520928809E-67,-1.18789542670764E-48,
-1.));
#39914=DIRECTION('ref_axis',(-4.33680868994202E-19,1.,-1.18789542670764E-48));
#39915=DIRECTION('center_axis',(1.09747227149895E-48,7.33307527524356E-49,
1.));
#39916=DIRECTION('ref_axis',(1.,4.33680868994202E-19,-1.09747227149895E-48));
#39917=DIRECTION('center_axis',(-0.654448706060852,0.271081529927754,-0.705841126081008));
#39918=DIRECTION('ref_axis',(0.652112169591586,-0.270113704831613,-0.708370174931649));
#39919=DIRECTION('',(1.09747227149895E-48,7.33307527524356E-49,1.));
#39920=DIRECTION('center_axis',(-0.654448706060939,0.271081529927973,0.705841126080843));
#39921=DIRECTION('ref_axis',(0.652112169592024,-0.270113704830126,0.708370174931813));
#39922=DIRECTION('',(1.09747227149895E-48,7.33307527524356E-49,1.));
#39923=DIRECTION('center_axis',(1.12975568624751E-48,8.20815552314688E-49,
1.));
#39924=DIRECTION('ref_axis',(1.,4.33680868994202E-19,-1.12975568624751E-48));
#39925=DIRECTION('center_axis',(-0.673700070814156,0.218898422362917,-0.705841126084352));
#39926=DIRECTION('ref_axis',(0.671294802430975,-0.218116903290839,-0.708370174928316));
#39927=DIRECTION('',(1.12975568624751E-48,8.20815552314688E-49,1.));
#39928=DIRECTION('center_axis',(-0.673700070814201,0.218898422363249,0.705841126084207));
#39929=DIRECTION('ref_axis',(0.671294802430673,-0.218116903291296,0.708370174928462));
#39930=DIRECTION('',(1.12975568624751E-48,8.20815552314688E-49,1.));
#39931=DIRECTION('center_axis',(1.15507378150847E-48,9.10586746597098E-49,
1.));
#39932=DIRECTION('ref_axis',(1.,4.33680868994202E-19,-1.15507378150847E-48));
#39933=DIRECTION('center_axis',(-0.688797850611722,0.165365733230951,-0.705841126079843));
#39934=DIRECTION('ref_axis',(0.686338679579581,-0.164775338502517,-0.708370174932809));
#39935=DIRECTION('',(1.15507378150847E-48,9.10586746597098E-49,1.));
#39936=DIRECTION('center_axis',(-0.688797850609436,0.165365733233163,0.705841126081556));
#39937=DIRECTION('ref_axis',(0.68633867958204,-0.164775338499612,0.708370174931102));
#39938=DIRECTION('',(1.15507378150847E-48,9.10586746597098E-49,1.));
#39939=DIRECTION('center_axis',(1.17327046280542E-48,1.00206764110688E-48,
1.));
#39940=DIRECTION('ref_axis',(1.,4.33680868994202E-19,-1.17327046280542E-48));
#39941=DIRECTION('center_axis',(-0.699648962604041,0.110813509366852,-0.705841126082132));
#39942=DIRECTION('ref_axis',(0.697151050543932,-0.11041787896162,-0.708370174930529));
#39943=DIRECTION('',(1.17327046280542E-48,1.00206764110688E-48,1.));
#39944=DIRECTION('center_axis',(-0.699648962604175,0.110813509367011,0.705841126081974));
#39945=DIRECTION('ref_axis',(0.697151050543496,-0.110417878963368,0.708370174930686));
#39946=DIRECTION('',(1.17327046280542E-48,1.00206764110688E-48,1.));
#39947=DIRECTION('center_axis',(1.18423354154716E-48,1.09469422570891E-48,
1.));
#39948=DIRECTION('ref_axis',(1.,4.33680868994202E-19,-1.18423354154716E-48));
#39949=DIRECTION('center_axis',(-0.706186506088737,0.0555780833649064,-0.705841126081264));
#39950=DIRECTION('ref_axis',(0.703665253451942,-0.0553796564821394,-0.708370174931394));
#39951=DIRECTION('',(1.18423354154716E-48,1.09469422570891E-48,1.));
#39952=DIRECTION('center_axis',(-0.706186506088284,0.0555780833648712,0.705841126081719));
#39953=DIRECTION('ref_axis',(0.703665253452317,-0.0553796564831855,0.70837017493094));
#39954=DIRECTION('',(1.18423354154716E-48,1.09469422570891E-48,1.));
#39955=DIRECTION('center_axis',(1.18789542670764E-48,1.18789542670763E-48,
1.));
#39956=DIRECTION('ref_axis',(1.,4.33680868994202E-19,-1.18789542670764E-48));
#39957=DIRECTION('center_axis',(-0.70837017493089,-1.25340662871076E-13,
-0.70584112608177));
#39958=DIRECTION('ref_axis',(0.70584112608177,-2.88506822019813E-13,-0.708370174930889));
#39959=DIRECTION('',(1.18789542670764E-48,1.18789542670763E-48,1.));
#39960=DIRECTION('center_axis',(-0.70837017493089,1.25340662871076E-13,
0.70584112608177));
#39961=DIRECTION('ref_axis',(0.70584112608177,2.61497947465894E-13,0.708370174930889));
#39962=DIRECTION('',(1.18789542670764E-48,1.18789542670763E-48,1.));
#39963=DIRECTION('center_axis',(1.05842257525003E-48,6.48602188298306E-49,
1.));
#39964=DIRECTION('ref_axis',(1.,4.33680868994202E-19,-1.05842257525003E-48));
#39965=DIRECTION('center_axis',(-0.631162447404585,0.321593329715507,-0.70584112608203));
#39966=DIRECTION('ref_axis',(0.628909048379288,-0.320445165567225,-0.708370174930631));
#39967=DIRECTION('',(1.05842257525003E-48,6.48602188298306E-49,1.));
#39968=DIRECTION('center_axis',(-0.631162447404969,0.32159332971786,0.705841126080614));
#39969=DIRECTION('ref_axis',(0.628909048378923,-0.320445165564824,0.708370174932041));
#39970=DIRECTION('',(1.05842257525003E-48,6.48602188298306E-49,1.));
#39971=DIRECTION('center_axis',(1.01284735186347E-48,5.67221771220248E-49,
1.));
#39972=DIRECTION('ref_axis',(1.,4.33680868994202E-19,-1.01284735186347E-48));
#39973=DIRECTION('center_axis',(-0.603984862377595,0.370122399687911,-0.705841126081486));
#39974=DIRECTION('ref_axis',(0.601828493750374,-0.368800975294447,-0.708370174931173));
#39975=DIRECTION('',(1.01284735186347E-48,5.67221771220248E-49,1.));
#39976=DIRECTION('center_axis',(-0.603984862377492,0.370122399687834,0.705841126081615));
#39977=DIRECTION('ref_axis',(0.60182849375054,-0.368800975294424,0.708370174931044));
#39978=DIRECTION('',(1.01284735186347E-48,5.67221771220248E-49,1.));
#39979=DIRECTION('center_axis',(9.61027587746754E-49,4.89668013623204E-49,
1.));
#39980=DIRECTION('ref_axis',(1.,4.33680868994202E-19,-9.61027587746754E-49));
#39981=DIRECTION('center_axis',(-0.57308350982942,0.416369541987989,-0.705841126080299));
#39982=DIRECTION('ref_axis',(-0.571037466327478,0.414883004371834,0.708370174932355));
#39983=DIRECTION('',(9.61027587746754E-49,4.89668013623204E-49,1.));
#39984=DIRECTION('center_axis',(-0.573083509826005,0.416369541988967,0.705841126082495));
#39985=DIRECTION('ref_axis',(0.571037466331126,-0.41488300437055,0.708370174930167));
#39986=DIRECTION('',(9.61027587746754E-49,4.89668013623204E-49,1.));
#39987=DIRECTION('center_axis',(9.03282768977476E-49,4.16419060212002E-49,
1.));
#39988=DIRECTION('ref_axis',(1.,4.33680868994202E-19,-9.03282768977476E-49));
#39989=DIRECTION('center_axis',(-0.538648906869708,0.460049627603881,-0.705841126082633));
#39990=DIRECTION('ref_axis',(-0.536725803041031,0.458407141763258,0.70837017493003));
#39991=DIRECTION('',(9.03282768977476E-49,4.16419060212002E-49,1.));
#39992=DIRECTION('center_axis',(-0.53864890686968,0.460049627604191,0.705841126082452));
#39993=DIRECTION('ref_axis',(0.536725803040381,-0.45840714176374,0.70837017493021));
#39994=DIRECTION('',(9.03282768977476E-49,4.16419060212002E-49,1.));
#39995=DIRECTION('center_axis',(8.39968911565451E-49,3.47926515142171E-49,
1.));
#39996=DIRECTION('ref_axis',(1.,4.33680868994202E-19,-8.39968911565451E-49));
#39997=DIRECTION('center_axis',(-0.500893354284786,0.500893354283015,-0.705841126081816));
#39998=DIRECTION('ref_axis',(-0.499105046691526,0.499105046694076,0.708370174930843));
#39999=DIRECTION('',(8.39968911565451E-49,3.47926515142171E-49,1.));
#40000=DIRECTION('center_axis',(-0.500893354285066,0.500893354283687,0.70584112608114));
#40001=DIRECTION('ref_axis',(0.49910504669045,-0.499105046694196,0.708370174931517));
#40002=DIRECTION('',(8.39968911565451E-49,3.47926515142171E-49,1.));
#40003=DIRECTION('center_axis',(7.71476366495618E-49,2.84612657730147E-49,
1.));
#40004=DIRECTION('ref_axis',(1.,4.33680868994202E-19,-7.71476366495618E-49));
#40005=DIRECTION('center_axis',(-0.460049627606723,0.538648906869542,-0.705841126080907));
#40006=DIRECTION('ref_axis',(-0.458407141764148,0.536725803038001,0.708370174931749));
#40007=DIRECTION('',(7.71476366495618E-49,2.84612657730147E-49,1.));
#40008=DIRECTION('center_axis',(-0.460049627603276,0.538648906871872,0.705841126081376));
#40009=DIRECTION('ref_axis',(0.458407141768044,-0.53672580303529,0.708370174931282));
#40010=DIRECTION('',(7.71476366495618E-49,2.84612657730147E-49,1.));
#40011=DIRECTION('center_axis',(6.98227413084414E-49,2.26867838960871E-49,
1.));
#40012=DIRECTION('ref_axis',(1.,4.33680868994202E-19,-6.98227413084414E-49));
#40013=DIRECTION('center_axis',(-0.416369541989573,0.573083509826983,-0.705841126081344));
#40014=DIRECTION('ref_axis',(-0.414883004369422,0.571037466330522,0.708370174931314));
#40015=DIRECTION('',(6.98227413084414E-49,2.26867838960871E-49,1.));
#40016=DIRECTION('center_axis',(-0.416369541986537,0.573083509827722,0.705841126082535));
#40017=DIRECTION('ref_axis',(0.414883004374377,-0.571037466328393,0.708370174930127));
#40018=DIRECTION('',(6.98227413084414E-49,2.26867838960871E-49,1.));
#40019=DIRECTION('center_axis',(6.2067365548737E-49,1.75048074844156E-49,
1.));
#40020=DIRECTION('ref_axis',(1.,4.33680868994202E-19,-6.2067365548737E-49));
#40021=DIRECTION('center_axis',(-0.370122399687787,0.603984862376041,-0.70584112608288));
#40022=DIRECTION('ref_axis',(-0.368800975294937,0.60182849375171,0.708370174929783));
#40023=DIRECTION('',(6.2067365548737E-49,1.75048074844156E-49,1.));
#40024=DIRECTION('center_axis',(-0.370122399687792,0.603984862376936,0.705841126082112));
#40025=DIRECTION('ref_axis',(0.368800975294942,-0.601828493750806,0.708370174930549));
#40026=DIRECTION('',(6.2067365548737E-49,1.75048074844156E-49,1.));
#40027=DIRECTION('center_axis',(5.39293238409311E-49,1.29472851457601E-49,
1.));
#40028=DIRECTION('ref_axis',(1.,4.33680868994202E-19,-5.39293238409311E-49));
#40029=DIRECTION('center_axis',(-0.321593329717153,0.63116244740346,-0.705841126082286));
#40030=DIRECTION('ref_axis',(-0.320445165567263,0.628909048379556,0.708370174930376));
#40031=DIRECTION('',(5.39293238409311E-49,1.29472851457601E-49,1.));
#40032=DIRECTION('center_axis',(-0.321593329716558,0.631162447403966,0.705841126082104));
#40033=DIRECTION('ref_axis',(0.320445165566995,-0.628909048379489,0.708370174930556));
#40034=DIRECTION('',(5.39293238409311E-49,1.29472851457601E-49,1.));
#40035=DIRECTION('center_axis',(0.,0.,1.));
#40036=DIRECTION('ref_axis',(1.,4.33680868994202E-19,0.));
#40037=DIRECTION('',(-0.707106781186549,-8.69022643068862E-17,0.707106781186546));
#40038=DIRECTION('center_axis',(0.,0.,1.));
#40039=DIRECTION('ref_axis',(1.,4.33680868994202E-19,0.));
#40040=DIRECTION('center_axis',(5.15167520928809E-67,-1.18789542670764E-48,
-1.));
#40041=DIRECTION('ref_axis',(0.,1.,0.));
#40042=DIRECTION('center_axis',(5.15167520928809E-67,-1.18789542670764E-48,
-1.));
#40043=DIRECTION('ref_axis',(-4.33680868994202E-19,1.,-1.18789542670764E-48));
#40044=DIRECTION('center_axis',(-1.,0.,-5.15167520928809E-67));
#40045=DIRECTION('ref_axis',(0.,-1.,0.));
#40046=DIRECTION('center_axis',(5.15167520928809E-67,-1.18789542670764E-48,
-1.));
#40047=DIRECTION('ref_axis',(-4.33680868994202E-19,1.,-1.18789542670764E-48));
#40048=DIRECTION('center_axis',(5.15167520928809E-67,-1.18789542670764E-48,
-1.));
#40049=DIRECTION('ref_axis',(-4.33680868994202E-19,1.,-1.18789542670764E-48));
#40050=DIRECTION('center_axis',(5.15167520928809E-67,-1.18789542670764E-48,
-1.));
#40051=DIRECTION('ref_axis',(-4.33680868994202E-19,1.,-1.18789542670764E-48));
#40052=DIRECTION('center_axis',(0.0555758110363288,-0.706157633406642,0.705870190622316));
#40053=DIRECTION('ref_axis',(0.0553775799352608,-0.703694571287346,-0.708341212962532));
#40054=DIRECTION('center_axis',(5.15167520928809E-67,-1.18789542670764E-48,
-1.));
#40055=DIRECTION('ref_axis',(-4.33680868994202E-19,1.,-1.18789542670764E-48));
#40056=DIRECTION('center_axis',(0.11080862020158,-0.699618093636883,0.705872490429338));
#40057=DIRECTION('ref_axis',(0.110419233095995,-0.697182591373234,-0.708338921173046));
#40058=DIRECTION('center_axis',(5.15167520928809E-67,-1.18789542670764E-48,
-1.));
#40059=DIRECTION('ref_axis',(-4.33680868994202E-19,1.,-1.18789542670764E-48));
#40060=DIRECTION('center_axis',(0.165358045050138,-0.688765827029971,0.705874176077378));
#40061=DIRECTION('ref_axis',(0.164780094681068,-0.686371526838389,-0.708337241391723));
#40062=DIRECTION('center_axis',(5.15167520928809E-67,-1.18789542670764E-48,
-1.));
#40063=DIRECTION('ref_axis',(-4.33680868994202E-19,1.,-1.18789542670764E-48));
#40064=DIRECTION('center_axis',(0.218887852522913,-0.673667540197498,0.705875451692549));
#40065=DIRECTION('ref_axis',(0.218125006053852,-0.671328261761447,-0.708335970210719));
#40066=DIRECTION('center_axis',(5.15167520928809E-67,-1.18789542670764E-48,
-1.));
#40067=DIRECTION('ref_axis',(-4.33680868994202E-19,1.,-1.18789542670764E-48));
#40068=DIRECTION('center_axis',(0.271068063822855,-0.654416196007407,0.705876439030603));
#40069=DIRECTION('ref_axis',(0.270125073931967,-0.65214568281518,-0.708334986301518));
#40070=DIRECTION('center_axis',(5.15167520928809E-67,-1.18789542670764E-48,
-1.));
#40071=DIRECTION('ref_axis',(-4.33680868994202E-19,1.,-1.18789542670764E-48));
#40072=DIRECTION('center_axis',(0.321577003370555,-0.631130405143931,0.705877214964523));
#40073=DIRECTION('ref_axis',(0.320459697262731,-0.628942147608601,-0.708334213060304));
#40074=DIRECTION('center_axis',(5.15167520928809E-67,-1.18789542670764E-48,
-1.));
#40075=DIRECTION('ref_axis',(-4.33680868994202E-19,1.,-1.18789542670764E-48));
#40076=DIRECTION('center_axis',(0.370103289326652,-0.603953677099404,0.705877830185721));
#40077=DIRECTION('ref_axis',(0.368818543504099,-0.601860775526205,-0.708333599972859));
#40078=DIRECTION('center_axis',(5.15167520928809E-67,-1.18789542670764E-48,
-1.));
#40079=DIRECTION('ref_axis',(-4.33680868994202E-19,1.,-1.18789542670764E-48));
#40080=DIRECTION('center_axis',(0.416347757295498,-0.573053525770462,0.705878319256975));
#40081=DIRECTION('ref_axis',(0.414903461782555,-0.571068576441932,-0.708333112597058));
#40082=DIRECTION('center_axis',(5.15167520928809E-67,-1.18789542670764E-48,
-1.));
#40083=DIRECTION('ref_axis',(-4.33680868994202E-19,1.,-1.18789542670764E-48));
#40084=DIRECTION('center_axis',(0.460025307051016,-0.538620431161506,0.705878706300177));
#40085=DIRECTION('ref_axis',(0.458430320957564,-0.536755427393206,-0.708332726895123));
#40086=DIRECTION('center_axis',(5.15167520928809E-67,-1.18789542670764E-48,
-1.));
#40087=DIRECTION('ref_axis',(-4.33680868994202E-19,1.,-1.18789542670764E-48));
#40088=DIRECTION('center_axis',(0.500866661619323,-0.500866661619323,0.705879008440277));
#40089=DIRECTION('ref_axis',(0.499130761357991,-0.499132905771573,-0.708332425801768));
#40090=DIRECTION('center_axis',(5.15167520928809E-67,-1.18789542670764E-48,
-1.));
#40091=DIRECTION('ref_axis',(-4.33680868994202E-19,1.,-1.18789542670764E-48));
#40092=DIRECTION('center_axis',(0.53862002836901,-0.46002496303376,0.705879237848482));
#40093=DIRECTION('ref_axis',(0.536753849182443,-0.458432987266868,-0.708332197188161));
#40094=DIRECTION('center_axis',(5.15167520928809E-67,-1.18789542670764E-48,
-1.));
#40095=DIRECTION('ref_axis',(-4.33680868994202E-19,1.,-1.18789542670764E-48));
#40096=DIRECTION('center_axis',(0.573052651970297,-0.416347122442612,0.705879403087785));
#40097=DIRECTION('ref_axis',(0.571067623542823,-0.414906617259439,-0.708332032521106));
#40098=DIRECTION('center_axis',(5.15167520928809E-67,-1.18789542670764E-48,
-1.));
#40099=DIRECTION('ref_axis',(-4.33680868994202E-19,1.,-1.18789542670764E-48));
#40100=DIRECTION('center_axis',(0.603952249837211,-0.370102414699222,0.705879509938047));
#40101=DIRECTION('ref_axis',(0.601860526500507,-0.368822164724135,-0.708331926040847));
#40102=DIRECTION('center_axis',(5.15167520928809E-67,-1.18789542670764E-48,
-1.));
#40103=DIRECTION('ref_axis',(-4.33680868994202E-19,1.,-1.18789542670764E-48));
#40104=DIRECTION('center_axis',(0.631128321247012,-0.321575941572045,0.705879561909807));
#40105=DIRECTION('ref_axis',(0.628942707293582,-0.320463768412346,-0.708331874249054));
#40106=DIRECTION('center_axis',(5.15167520928809E-67,-1.18789542670764E-48,
-1.));
#40107=DIRECTION('ref_axis',(-4.33680868994202E-19,1.,-1.18789542670764E-48));
#40108=DIRECTION('center_axis',(0.654413322126613,-0.271066873422487,0.70587956051735));
#40109=DIRECTION('ref_axis',(0.652147192704133,-0.270129585579022,-0.708331875636714));
#40110=DIRECTION('center_axis',(5.15167520928809E-67,-1.18789542670764E-48,
-1.));
#40111=DIRECTION('ref_axis',(-4.33680868994202E-19,1.,-1.18789542670764E-48));
#40112=DIRECTION('center_axis',(0.673663698306673,-0.218886604216949,0.705879505353533));
#40113=DIRECTION('ref_axis',(0.671330916306432,-0.218129954133086,-0.708331930609559));
#40114=DIRECTION('center_axis',(5.15167520928809E-67,-1.18789542670764E-48,
-1.));
#40115=DIRECTION('ref_axis',(-4.33680868994202E-19,1.,-1.18789542670764E-48));
#40116=DIRECTION('center_axis',(0.688760770927107,-0.165356831187235,0.705879393955946));
#40117=DIRECTION('ref_axis',(0.686375600198304,-0.164785479532649,-0.708332041621451));
#40118=DIRECTION('center_axis',(5.15167520928809E-67,-1.18789542670764E-48,
-1.));
#40119=DIRECTION('ref_axis',(-4.33680868994202E-19,1.,-1.18789542670764E-48));
#40120=DIRECTION('center_axis',(0.699611468639781,-0.110807570905153,0.705879221381242));
#40121=DIRECTION('ref_axis',(0.697188483633051,-0.110425058152577,-0.708332213598567));
#40122=DIRECTION('center_axis',(5.15167520928809E-67,-1.18789542670764E-48,
-1.));
#40123=DIRECTION('ref_axis',(-4.33680868994202E-19,1.,-1.18789542670764E-48));
#40124=DIRECTION('center_axis',(0.706148902304913,-0.0555751238837372,0.705878979272562));
#40125=DIRECTION('ref_axis',(0.703702893729778,-0.0553838490533553,-0.708332454868737));
#40126=DIRECTION('center_axis',(5.15167520928809E-67,-1.18789542670764E-48,
-1.));
#40127=DIRECTION('ref_axis',(-4.33680868994202E-19,1.,-1.18789542670764E-48));
#40128=DIRECTION('center_axis',(0.708332577472403,3.07190287735134E-19,
0.705878856243267));
#40129=DIRECTION('ref_axis',(0.705878856242412,-1.55615277571261E-6,-0.708332577471545));
#40130=DIRECTION('center_axis',(5.15167520928809E-67,-1.18789542670764E-48,
-1.));
#40131=DIRECTION('ref_axis',(-4.33680868994202E-19,1.,-1.18789542670764E-48));
#40132=DIRECTION('center_axis',(0.706157633406551,0.0555758110364317,0.705870190622399));
#40133=DIRECTION('ref_axis',(0.703694571287442,0.0553775799351074,-0.70834121296245));
#40134=DIRECTION('center_axis',(5.15167520928809E-67,-1.18789542670764E-48,
-1.));
#40135=DIRECTION('ref_axis',(-4.33680868994202E-19,1.,-1.18789542670764E-48));
#40136=DIRECTION('center_axis',(0.699618093637069,0.110808620201609,0.705872490429149));
#40137=DIRECTION('ref_axis',(0.697182591372912,0.11041923309682,-0.708338921173234));
#40138=DIRECTION('center_axis',(5.15167520928809E-67,-1.18789542670764E-48,
-1.));
#40139=DIRECTION('ref_axis',(-4.33680868994202E-19,1.,-1.18789542670764E-48));
#40140=DIRECTION('center_axis',(0.688765827030135,0.165358045050174,0.705874176077209));
#40141=DIRECTION('ref_axis',(0.686371526838244,0.16478009468095,-0.708337241391891));
#40142=DIRECTION('center_axis',(5.15167520928809E-67,-1.18789542670764E-48,
-1.));
#40143=DIRECTION('ref_axis',(-4.33680868994202E-19,1.,-1.18789542670764E-48));
#40144=DIRECTION('center_axis',(0.673667540197388,0.21888785252289,0.705875451692661));
#40145=DIRECTION('ref_axis',(0.671328261761852,0.21812500605297,-0.708335970210607));
#40146=DIRECTION('center_axis',(5.15167520928809E-67,-1.18789542670764E-48,
-1.));
#40147=DIRECTION('ref_axis',(-4.33680868994202E-19,1.,-1.18789542670764E-48));
#40148=DIRECTION('center_axis',(0.654416196007382,0.271068063822859,0.705876439030624));
#40149=DIRECTION('ref_axis',(0.652145682814771,0.270125073933009,-0.708334986301497));
#40150=DIRECTION('center_axis',(5.15167520928809E-67,-1.18789542670764E-48,
-1.));
#40151=DIRECTION('ref_axis',(-4.33680868994202E-19,1.,-1.18789542670764E-48));
#40152=DIRECTION('center_axis',(0.631130405143941,0.321577003370555,0.705877214964514));
#40153=DIRECTION('ref_axis',(0.628942147608526,0.320459697262857,-0.708334213060313));
#40154=DIRECTION('center_axis',(5.15167520928809E-67,-1.18789542670764E-48,
-1.));
#40155=DIRECTION('ref_axis',(-4.33680868994202E-19,1.,-1.18789542670764E-48));
#40156=DIRECTION('center_axis',(0.603953677099555,0.370103289326611,0.705877830185613));
#40157=DIRECTION('ref_axis',(0.601860775525942,0.368818543504321,-0.708333599972967));
#40158=DIRECTION('center_axis',(5.15167520928809E-67,-1.18789542670764E-48,
-1.));
#40159=DIRECTION('ref_axis',(-4.33680868994202E-19,1.,-1.18789542670764E-48));
#40160=DIRECTION('center_axis',(0.573053525770564,0.41634775729573,0.705878319256755));
#40161=DIRECTION('ref_axis',(-0.571068576442187,-0.414903461781831,0.708333112597277));
#40162=DIRECTION('center_axis',(5.15167520928809E-67,-1.18789542670764E-48,
-1.));
#40163=DIRECTION('ref_axis',(-4.33680868994202E-19,1.,-1.18789542670764E-48));
#40164=DIRECTION('center_axis',(0.538620431161647,0.46002530705115,0.705878706299982));
#40165=DIRECTION('ref_axis',(-0.536755427393011,-0.458430320957492,0.708332726895318));
#40166=DIRECTION('center_axis',(5.15167520928809E-67,-1.18789542670764E-48,
-1.));
#40167=DIRECTION('ref_axis',(-4.33680868994202E-19,1.,-1.18789542670764E-48));
#40168=DIRECTION('center_axis',(0.500866661619527,0.500866661619527,0.705879008439988));
#40169=DIRECTION('ref_axis',(-0.49913290577155,-0.499130761357605,0.708332425802057));
#40170=DIRECTION('center_axis',(5.15167520928809E-67,-1.18789542670764E-48,
-1.));
#40171=DIRECTION('ref_axis',(-4.33680868994202E-19,1.,-1.18789542670764E-48));
#40172=DIRECTION('center_axis',(0.460024963033642,0.538620028368862,0.705879237848672));
#40173=DIRECTION('ref_axis',(-0.45843298726639,-0.536753849183101,0.708332197187972));
#40174=DIRECTION('center_axis',(5.15167520928809E-67,-1.18789542670764E-48,
-1.));
#40175=DIRECTION('ref_axis',(-4.33680868994202E-19,1.,-1.18789542670764E-48));
#40176=DIRECTION('center_axis',(0.416347122442686,0.573052651970292,0.705879403087744));
#40177=DIRECTION('ref_axis',(-0.414906617258984,-0.571067623543104,0.708332032521146));
#40178=DIRECTION('center_axis',(5.15167520928809E-67,-1.18789542670764E-48,
-1.));
#40179=DIRECTION('ref_axis',(-4.33680868994202E-19,1.,-1.18789542670764E-48));
#40180=DIRECTION('center_axis',(0.370102414699172,0.603952249837277,0.705879509938016));
#40181=DIRECTION('ref_axis',(-0.368822164724246,-0.601860526500403,0.708331926040877));
#40182=DIRECTION('center_axis',(5.15167520928809E-67,-1.18789542670764E-48,
-1.));
#40183=DIRECTION('ref_axis',(-4.33680868994202E-19,1.,-1.18789542670764E-48));
#40184=DIRECTION('center_axis',(0.321575941571924,0.631128321246917,0.705879561909948));
#40185=DIRECTION('ref_axis',(-0.320463768412656,-0.628942707293582,0.708331874248914));
#40186=DIRECTION('center_axis',(5.15167520928809E-67,-1.18789542670764E-48,
-1.));
#40187=DIRECTION('ref_axis',(-4.33680868994202E-19,1.,-1.18789542670764E-48));
#40188=DIRECTION('center_axis',(0.271066873422485,0.654413322126598,0.705879560517365));
#40189=DIRECTION('ref_axis',(-0.270129585579224,-0.652147192704065,0.708331875636699));
#40190=DIRECTION('center_axis',(5.15167520928809E-67,-1.18789542670764E-48,
-1.));
#40191=DIRECTION('ref_axis',(-4.33680868994202E-19,1.,-1.18789542670764E-48));
#40192=DIRECTION('center_axis',(0.218886604216952,0.67366369830668,0.705879505353526));
#40193=DIRECTION('ref_axis',(-0.218129954132996,-0.671330916306453,0.708331930609566));
#40194=DIRECTION('center_axis',(5.15167520928809E-67,-1.18789542670764E-48,
-1.));
#40195=DIRECTION('ref_axis',(-4.33680868994202E-19,1.,-1.18789542670764E-48));
#40196=DIRECTION('center_axis',(0.16535683118711,0.68876077092705,0.705879393956031));
#40197=DIRECTION('ref_axis',(-0.164785479532882,-0.686375600198336,0.708332041621366));
#40198=DIRECTION('center_axis',(5.15167520928809E-67,-1.18789542670764E-48,
-1.));
#40199=DIRECTION('ref_axis',(-4.33680868994202E-19,1.,-1.18789542670764E-48));
#40200=DIRECTION('center_axis',(0.110807570905159,0.699611468639805,0.705879221381218));
#40201=DIRECTION('ref_axis',(-0.11042505815257,-0.697188483633028,0.708332213598592));
#40202=DIRECTION('center_axis',(5.15167520928809E-67,-1.18789542670764E-48,
-1.));
#40203=DIRECTION('ref_axis',(-4.33680868994202E-19,1.,-1.18789542670764E-48));
#40204=DIRECTION('center_axis',(0.055575123883674,0.706148902304893,0.705878979272587));
#40205=DIRECTION('ref_axis',(-0.0553838490533958,-0.7037028937298,0.708332454868712));
#40206=DIRECTION('center_axis',(5.15167520928809E-67,-1.18789542670764E-48,
-1.));
#40207=DIRECTION('ref_axis',(-4.33680868994202E-19,1.,-1.18789542670764E-48));
#40208=DIRECTION('center_axis',(4.84352581305682E-13,0.70837017493119,0.705841126081468));
#40209=DIRECTION('ref_axis',(-1.41156745807278E-12,-0.705841126081468,0.70837017493119));
#40210=DIRECTION('center_axis',(5.15167520928809E-67,-1.18789542670764E-48,
-1.));
#40211=DIRECTION('ref_axis',(-4.33680868994202E-19,1.,-1.18789542670764E-48));
#40212=DIRECTION('center_axis',(-0.0555758110363152,0.706157633406656,0.705870190622303));
#40213=DIRECTION('ref_axis',(0.0553775799350914,-0.703694571287347,0.708341212962545));
#40214=DIRECTION('center_axis',(5.15167520928809E-67,-1.18789542670764E-48,
-1.));
#40215=DIRECTION('ref_axis',(-4.33680868994202E-19,1.,-1.18789542670764E-48));
#40216=DIRECTION('center_axis',(-0.110808620201596,0.699618093636976,0.705872490429243));
#40217=DIRECTION('ref_axis',(0.11041923309583,-0.697182591373165,0.70833892117314));
#40218=DIRECTION('center_axis',(5.15167520928809E-67,-1.18789542670764E-48,
-1.));
#40219=DIRECTION('ref_axis',(-4.33680868994202E-19,1.,-1.18789542670764E-48));
#40220=DIRECTION('center_axis',(-0.165358045050154,0.688765827030126,0.705874176077223));
#40221=DIRECTION('ref_axis',(0.164780094680844,-0.686371526838284,0.708337241391878));
#40222=DIRECTION('center_axis',(5.15167520928809E-67,-1.18789542670764E-48,
-1.));
#40223=DIRECTION('ref_axis',(-4.33680868994202E-19,1.,-1.18789542670764E-48));
#40224=DIRECTION('center_axis',(-0.218887852522867,0.673667540197309,0.705875451692744));
#40225=DIRECTION('ref_axis',(0.218125006054104,-0.67132826176157,0.708335970210525));
#40226=DIRECTION('center_axis',(5.15167520928809E-67,-1.18789542670764E-48,
-1.));
#40227=DIRECTION('ref_axis',(-4.33680868994202E-19,1.,-1.18789542670764E-48));
#40228=DIRECTION('center_axis',(-0.271068063822887,0.654416196007496,0.705876439030507));
#40229=DIRECTION('ref_axis',(0.270125073932604,-0.652145682814813,0.708334986301614));
#40230=DIRECTION('center_axis',(5.15167520928809E-67,-1.18789542670764E-48,
-1.));
#40231=DIRECTION('ref_axis',(-4.33680868994202E-19,1.,-1.18789542670764E-48));
#40232=DIRECTION('center_axis',(5.15167520928809E-67,-1.18789542670764E-48,
-1.));
#40233=DIRECTION('ref_axis',(-4.33680868994202E-19,1.,-1.18789542670764E-48));
#40234=DIRECTION('center_axis',(5.15167520928809E-67,-1.18789542670764E-48,
-1.));
#40235=DIRECTION('ref_axis',(-4.33680868994202E-19,1.,-1.18789542670764E-48));
#40236=DIRECTION('center_axis',(5.15167520928809E-67,-1.18789542670764E-48,
-1.));
#40237=DIRECTION('ref_axis',(-4.33680868994202E-19,1.,-1.18789542670764E-48));
#40238=DIRECTION('center_axis',(5.15167520928809E-67,-1.18789542670764E-48,
-1.));
#40239=DIRECTION('ref_axis',(-4.33680868994202E-19,1.,-1.18789542670764E-48));
#40240=DIRECTION('center_axis',(5.15167520928809E-67,-1.18789542670764E-48,
-1.));
#40241=DIRECTION('ref_axis',(-4.33680868994202E-19,1.,-1.18789542670764E-48));
#40242=DIRECTION('center_axis',(5.15167520928809E-67,-1.18789542670764E-48,
-1.));
#40243=DIRECTION('ref_axis',(-4.33680868994202E-19,1.,-1.18789542670764E-48));
#40244=DIRECTION('center_axis',(5.15167520928809E-67,-1.18789542670764E-48,
-1.));
#40245=DIRECTION('ref_axis',(-4.33680868994202E-19,1.,-1.18789542670764E-48));
#40246=DIRECTION('center_axis',(5.15167520928809E-67,-1.18789542670764E-48,
-1.));
#40247=DIRECTION('ref_axis',(-4.33680868994202E-19,1.,-1.18789542670764E-48));
#40248=DIRECTION('center_axis',(5.15167520928809E-67,-1.18789542670764E-48,
-1.));
#40249=DIRECTION('ref_axis',(-4.33680868994202E-19,1.,-1.18789542670764E-48));
#40250=DIRECTION('center_axis',(5.15167520928809E-67,-1.18789542670764E-48,
-1.));
#40251=DIRECTION('ref_axis',(-4.33680868994202E-19,1.,-1.18789542670764E-48));
#40252=DIRECTION('center_axis',(5.15167520928809E-67,-1.18789542670764E-48,
-1.));
#40253=DIRECTION('ref_axis',(-4.33680868994202E-19,1.,-1.18789542670764E-48));
#40254=DIRECTION('center_axis',(5.15167520928809E-67,-1.18789542670764E-48,
-1.));
#40255=DIRECTION('ref_axis',(-4.33680868994202E-19,1.,-1.18789542670764E-48));
#40256=DIRECTION('center_axis',(5.15167520928809E-67,-1.18789542670764E-48,
-1.));
#40257=DIRECTION('ref_axis',(-4.33680868994202E-19,1.,-1.18789542670764E-48));
#40258=DIRECTION('center_axis',(5.15167520928809E-67,-1.18789542670764E-48,
-1.));
#40259=DIRECTION('ref_axis',(-4.33680868994202E-19,1.,-1.18789542670764E-48));
#40260=DIRECTION('center_axis',(5.15167520928809E-67,-1.18789542670764E-48,
-1.));
#40261=DIRECTION('ref_axis',(-4.33680868994202E-19,1.,-1.18789542670764E-48));
#40262=DIRECTION('center_axis',(-0.7061576334064,-0.0555758110363729,0.705870190622555));
#40263=DIRECTION('ref_axis',(0.703694571287618,0.0553775799348557,0.708341212962294));
#40264=DIRECTION('center_axis',(5.15167520928809E-67,-1.18789542670764E-48,
-1.));
#40265=DIRECTION('ref_axis',(-4.33680868994202E-19,1.,-1.18789542670764E-48));
#40266=DIRECTION('center_axis',(-0.699618093637056,-0.110808620201623,0.70587249042916));
#40267=DIRECTION('ref_axis',(0.697182591373085,0.110419233095803,0.708338921173223));
#40268=DIRECTION('center_axis',(5.15167520928809E-67,-1.18789542670764E-48,
-1.));
#40269=DIRECTION('ref_axis',(-4.33680868994202E-19,1.,-1.18789542670764E-48));
#40270=DIRECTION('center_axis',(-0.68876582703002,-0.165358045050145,0.705874176077329));
#40271=DIRECTION('ref_axis',(0.686371526838198,0.164780094681657,0.708337241391772));
#40272=DIRECTION('center_axis',(5.15167520928809E-67,-1.18789542670764E-48,
-1.));
#40273=DIRECTION('ref_axis',(-4.33680868994202E-19,1.,-1.18789542670764E-48));
#40274=DIRECTION('center_axis',(-0.673667540197642,-0.218887852522971,0.705875451692394));
#40275=DIRECTION('ref_axis',(0.671328261761337,0.218125006053688,0.708335970210874));
#40276=DIRECTION('center_axis',(5.15167520928809E-67,-1.18789542670764E-48,
-1.));
#40277=DIRECTION('ref_axis',(-4.33680868994202E-19,1.,-1.18789542670764E-48));
#40278=DIRECTION('center_axis',(-0.654416196007479,-0.271068063822885,0.705876439030525));
#40279=DIRECTION('ref_axis',(0.652145682815046,0.270125073932086,0.708334986301596));
#40280=DIRECTION('center_axis',(5.15167520928809E-67,-1.18789542670764E-48,
-1.));
#40281=DIRECTION('ref_axis',(-4.33680868994202E-19,1.,-1.18789542670764E-48));
#40282=DIRECTION('center_axis',(-0.631130405143739,-0.321577003370466,0.705877214964735));
#40283=DIRECTION('ref_axis',(0.628942147608447,0.3204596972635,0.708334213060093));
#40284=DIRECTION('center_axis',(5.15167520928809E-67,-1.18789542670764E-48,
-1.));
#40285=DIRECTION('ref_axis',(-4.33680868994202E-19,1.,-1.18789542670764E-48));
#40286=DIRECTION('center_axis',(-0.603953677099563,-0.37010328932661,0.705877830185607));
#40287=DIRECTION('ref_axis',(0.601860775526009,0.3688185435042,0.708333599972973));
#40288=DIRECTION('center_axis',(5.15167520928809E-67,-1.18789542670764E-48,
-1.));
#40289=DIRECTION('ref_axis',(-4.33680868994202E-19,1.,-1.18789542670764E-48));
#40290=DIRECTION('center_axis',(-0.573053525770468,-0.416347757295655,0.705878319256877));
#40291=DIRECTION('ref_axis',(-0.571068576442267,-0.414903461781928,-0.708333112597156));
#40292=DIRECTION('center_axis',(5.15167520928809E-67,-1.18789542670764E-48,
-1.));
#40293=DIRECTION('ref_axis',(-4.33680868994202E-19,1.,-1.18789542670764E-48));
#40294=DIRECTION('center_axis',(-0.5386204311615,-0.460025307051025,0.705878706300176));
#40295=DIRECTION('ref_axis',(-0.53675542739315,-0.458430320957627,-0.708332726895124));
#40296=DIRECTION('center_axis',(5.15167520928809E-67,-1.18789542670764E-48,
-1.));
#40297=DIRECTION('ref_axis',(-4.33680868994202E-19,1.,-1.18789542670764E-48));
#40298=DIRECTION('center_axis',(-0.500866661619536,-0.500866661619512,0.705879008439992));
#40299=DIRECTION('ref_axis',(-0.499132905770748,-0.499130761358414,-0.708332425802052));
#40300=DIRECTION('center_axis',(5.15167520928809E-67,-1.18789542670764E-48,
-1.));
#40301=DIRECTION('ref_axis',(-4.33680868994202E-19,1.,-1.18789542670764E-48));
#40302=DIRECTION('center_axis',(-0.460024963033767,-0.538620028369008,0.70587923784848));
#40303=DIRECTION('ref_axis',(-0.45843298726701,-0.536753849182318,-0.708332197188163));
#40304=DIRECTION('center_axis',(5.15167520928809E-67,-1.18789542670764E-48,
-1.));
#40305=DIRECTION('ref_axis',(-4.33680868994202E-19,1.,-1.18789542670764E-48));
#40306=DIRECTION('center_axis',(-0.416347122442742,-0.573052651970378,0.705879403087642));
#40307=DIRECTION('ref_axis',(-0.414906617259033,-0.571067623542942,-0.708332032521248));
#40308=DIRECTION('center_axis',(5.15167520928809E-67,-1.18789542670764E-48,
-1.));
#40309=DIRECTION('ref_axis',(-4.33680868994202E-19,1.,-1.18789542670764E-48));
#40310=DIRECTION('center_axis',(-0.370102414699178,-0.603952249837274,0.705879509938015));
#40311=DIRECTION('ref_axis',(-0.368822164723695,-0.601860526500739,-0.708331926040878));
#40312=DIRECTION('center_axis',(5.15167520928809E-67,-1.18789542670764E-48,
-1.));
#40313=DIRECTION('ref_axis',(-4.33680868994202E-19,1.,-1.18789542670764E-48));
#40314=DIRECTION('center_axis',(-0.321575941572111,-0.631128321247095,0.705879561909702));
#40315=DIRECTION('ref_axis',(-0.320463768412258,-0.628942707293509,-0.708331874249159));
#40316=DIRECTION('center_axis',(5.15167520928809E-67,-1.18789542670764E-48,
-1.));
#40317=DIRECTION('ref_axis',(-4.33680868994202E-19,1.,-1.18789542670764E-48));
#40318=DIRECTION('center_axis',(-0.271066873422704,-0.654413322126826,0.70587956051707));
#40319=DIRECTION('ref_axis',(-0.270129585579653,-0.652147192703568,-0.708331875636993));
#40320=DIRECTION('center_axis',(5.15167520928809E-67,-1.18789542670764E-48,
-1.));
#40321=DIRECTION('ref_axis',(-4.33680868994202E-19,1.,-1.18789542670764E-48));
#40322=DIRECTION('center_axis',(-0.218886604216915,-0.673663698306575,0.705879505353637));
#40323=DIRECTION('ref_axis',(-0.218129954131654,-0.671330916307006,-0.708331930609455));
#40324=DIRECTION('center_axis',(5.15167520928809E-67,-1.18789542670764E-48,
-1.));
#40325=DIRECTION('ref_axis',(-4.33680868994202E-19,1.,-1.18789542670764E-48));
#40326=DIRECTION('center_axis',(-0.165356831187205,-0.688760770926913,0.705879393956142));
#40327=DIRECTION('ref_axis',(-0.164785479532657,-0.686375600198504,-0.708332041621255));
#40328=DIRECTION('center_axis',(5.15167520928809E-67,-1.18789542670764E-48,
-1.));
#40329=DIRECTION('ref_axis',(-4.33680868994202E-19,1.,-1.18789542670764E-48));
#40330=DIRECTION('center_axis',(-0.110807570905278,-0.699611468639872,0.705879221381132));
#40331=DIRECTION('ref_axis',(-0.110425058152835,-0.697188483632899,-0.708332213598677));
#40332=DIRECTION('center_axis',(5.15167520928809E-67,-1.18789542670764E-48,
-1.));
#40333=DIRECTION('ref_axis',(-4.33680868994202E-19,1.,-1.18789542670764E-48));
#40334=DIRECTION('center_axis',(-0.0555751238837442,-0.706148902305009,
0.705878979272465));
#40335=DIRECTION('ref_axis',(-0.0553838490528384,-0.703702893729722,-0.708332454868834));
#40336=DIRECTION('center_axis',(5.15167520928809E-67,-1.18789542670764E-48,
-1.));
#40337=DIRECTION('ref_axis',(-4.33680868994202E-19,1.,-1.18789542670764E-48));
#40338=DIRECTION('',(8.62889469402126E-17,0.707106781186547,0.707106781186548));
#40339=DIRECTION('center_axis',(-5.15167520928809E-67,1.18789542670764E-48,
1.));
#40340=DIRECTION('ref_axis',(4.33680868994202E-19,-1.,1.18789542670764E-48));
#40341=DIRECTION('center_axis',(5.15167520928809E-67,-1.18789542670764E-48,
-1.));
#40342=DIRECTION('ref_axis',(-4.33680868994202E-19,1.,-1.18789542670764E-48));
#40343=DIRECTION('center_axis',(0.0555758110363494,0.706157633406676,-0.705870190622281));
#40344=DIRECTION('ref_axis',(0.0553775799347821,0.703694571287349,0.708341212962568));
#40345=DIRECTION('center_axis',(5.15167520928809E-67,-1.18789542670764E-48,
-1.));
#40346=DIRECTION('ref_axis',(-4.33680868994202E-19,1.,-1.18789542670764E-48));
#40347=DIRECTION('center_axis',(0.110808620201597,0.699618093636782,-0.705872490429435));
#40348=DIRECTION('ref_axis',(0.110419233096536,0.697182591373247,0.708338921172949));
#40349=DIRECTION('center_axis',(5.15167520928809E-67,-1.18789542670764E-48,
-1.));
#40350=DIRECTION('ref_axis',(-4.33680868994202E-19,1.,-1.18789542670764E-48));
#40351=DIRECTION('center_axis',(0.165358045050176,0.688765827030065,-0.705874176077277));
#40352=DIRECTION('ref_axis',(0.164780094681565,0.686371526838166,0.708337241391824));
#40353=DIRECTION('center_axis',(5.15167520928809E-67,-1.18789542670764E-48,
-1.));
#40354=DIRECTION('ref_axis',(-4.33680868994202E-19,1.,-1.18789542670764E-48));
#40355=DIRECTION('center_axis',(0.218887852522828,0.673667540197125,-0.705875451692931));
#40356=DIRECTION('ref_axis',(0.218125006053502,0.671328261761963,0.708335970210338));
#40357=DIRECTION('center_axis',(5.15167520928809E-67,-1.18789542670764E-48,
-1.));
#40358=DIRECTION('ref_axis',(-4.33680868994202E-19,1.,-1.18789542670764E-48));
#40359=DIRECTION('center_axis',(0.271068063822916,0.654416196007463,-0.705876439030527));
#40360=DIRECTION('ref_axis',(0.270125073931817,0.65214568281516,0.708334986301594));
#40361=DIRECTION('center_axis',(5.15167520928809E-67,-1.18789542670764E-48,
-1.));
#40362=DIRECTION('ref_axis',(-4.33680868994202E-19,1.,-1.18789542670764E-48));
#40363=DIRECTION('center_axis',(0.321577003370433,0.631130405143686,-0.705877214964798));
#40364=DIRECTION('ref_axis',(0.320459697263181,0.62894214760868,0.70833421306003));
#40365=DIRECTION('center_axis',(5.15167520928809E-67,-1.18789542670764E-48,
-1.));
#40366=DIRECTION('ref_axis',(-4.33680868994202E-19,1.,-1.18789542670764E-48));
#40367=DIRECTION('center_axis',(0.37010328932647,0.603953677099309,-0.705877830185898));
#40368=DIRECTION('ref_axis',(0.368818543504439,0.601860775526204,0.708333599972683));
#40369=DIRECTION('center_axis',(5.15167520928809E-67,-1.18789542670764E-48,
-1.));
#40370=DIRECTION('ref_axis',(-4.33680868994202E-19,1.,-1.18789542670764E-48));
#40371=DIRECTION('center_axis',(0.416347757295563,0.573053525770315,-0.705878319257056));
#40372=DIRECTION('ref_axis',(0.414903461782186,0.5710685764423,0.708333112596977));
#40373=DIRECTION('center_axis',(5.15167520928809E-67,-1.18789542670764E-48,
-1.));
#40374=DIRECTION('ref_axis',(-4.33680868994202E-19,1.,-1.18789542670764E-48));
#40375=DIRECTION('center_axis',(0.46002530705103,0.538620431161473,-0.705878706300193));
#40376=DIRECTION('ref_axis',(0.458430320957387,0.536755427393379,0.708332726895108));
#40377=DIRECTION('center_axis',(5.15167520928809E-67,-1.18789542670764E-48,
-1.));
#40378=DIRECTION('ref_axis',(-4.33680868994202E-19,1.,-1.18789542670764E-48));
#40379=DIRECTION('center_axis',(0.500866661619595,0.500866661619595,-0.705879008439891));
#40380=DIRECTION('ref_axis',(0.499130761358023,0.499132905770996,0.708332425802153));
#40381=DIRECTION('center_axis',(5.15167520928809E-67,-1.18789542670764E-48,
-1.));
#40382=DIRECTION('ref_axis',(-4.33680868994202E-19,1.,-1.18789542670764E-48));
#40383=DIRECTION('center_axis',(0.538620028368889,0.460024963033635,-0.705879237848656));
#40384=DIRECTION('ref_axis',(0.536753849182959,0.458432987266531,0.708332197187987));
#40385=DIRECTION('center_axis',(5.15167520928809E-67,-1.18789542670764E-48,
-1.));
#40386=DIRECTION('ref_axis',(-4.33680868994202E-19,1.,-1.18789542670764E-48));
#40387=DIRECTION('center_axis',(0.573052651970233,0.416347122442629,-0.705879403087826));
#40388=DIRECTION('ref_axis',(0.57106762354309,0.414906617259142,0.708332032521065));
#40389=DIRECTION('center_axis',(5.15167520928809E-67,-1.18789542670764E-48,
-1.));
#40390=DIRECTION('ref_axis',(-4.33680868994202E-19,1.,-1.18789542670764E-48));
#40391=DIRECTION('center_axis',(0.603952249837032,0.370102414699012,-0.70587950993831));
#40392=DIRECTION('ref_axis',(0.601860526500475,0.36882216472469,0.708331926040585));
#40393=DIRECTION('center_axis',(5.15167520928809E-67,-1.18789542670764E-48,
-1.));
#40394=DIRECTION('ref_axis',(-4.33680868994202E-19,1.,-1.18789542670764E-48));
#40395=DIRECTION('center_axis',(0.631128321246922,0.32157594157199,-0.705879561909913));
#40396=DIRECTION('ref_axis',(0.628942707293632,0.32046376841248,0.708331874248949));
#40397=DIRECTION('center_axis',(5.15167520928809E-67,-1.18789542670764E-48,
-1.));
#40398=DIRECTION('ref_axis',(-4.33680868994202E-19,1.,-1.18789542670764E-48));
#40399=DIRECTION('center_axis',(0.654413322126609,0.271066873422466,-0.705879560517362));
#40400=DIRECTION('ref_axis',(0.652147192704168,0.270129585578968,0.708331875636702));
#40401=DIRECTION('center_axis',(5.15167520928809E-67,-1.18789542670764E-48,
-1.));
#40402=DIRECTION('ref_axis',(-4.33680868994202E-19,1.,-1.18789542670764E-48));
#40403=DIRECTION('center_axis',(0.673663698306398,0.218886604216837,-0.70587950535383));
#40404=DIRECTION('ref_axis',(0.671330916306662,0.218129954133339,0.708331930609263));
#40405=DIRECTION('center_axis',(5.15167520928809E-67,-1.18789542670764E-48,
-1.));
#40406=DIRECTION('ref_axis',(-4.33680868994202E-19,1.,-1.18789542670764E-48));
#40407=DIRECTION('center_axis',(0.688760770927087,0.165356831187229,-0.705879393955967));
#40408=DIRECTION('ref_axis',(0.686375600198292,0.164785479532791,0.70833204162143));
#40409=DIRECTION('center_axis',(5.15167520928809E-67,-1.18789542670764E-48,
-1.));
#40410=DIRECTION('ref_axis',(-4.33680868994202E-19,1.,-1.18789542670764E-48));
#40411=DIRECTION('center_axis',(0.699611468639904,0.110807570905141,-0.705879221381122));
#40412=DIRECTION('ref_axis',(0.697188483632864,0.11042505815299,0.708332213598687));
#40413=DIRECTION('center_axis',(5.15167520928809E-67,-1.18789542670764E-48,
-1.));
#40414=DIRECTION('ref_axis',(-4.33680868994202E-19,1.,-1.18789542670764E-48));
#40415=DIRECTION('center_axis',(0.706148902304704,0.0555751238836885,-0.705878979272775));
#40416=DIRECTION('ref_axis',(0.703702893729991,0.0553838490533688,0.708332454868525));
#40417=DIRECTION('center_axis',(5.15167520928809E-67,-1.18789542670764E-48,
-1.));
#40418=DIRECTION('ref_axis',(-4.33680868994202E-19,1.,-1.18789542670764E-48));
#40419=DIRECTION('center_axis',(0.708332577472139,3.0719028773502E-19,-0.705878856243532));
#40420=DIRECTION('ref_axis',(0.705878856242677,1.5561538090606E-6,0.708332577471281));
#40421=DIRECTION('center_axis',(5.15167520928809E-67,-1.18789542670764E-48,
-1.));
#40422=DIRECTION('ref_axis',(-4.33680868994202E-19,1.,-1.18789542670764E-48));
#40423=DIRECTION('center_axis',(0.706157633406651,-0.0555758110363464,-0.705870190622306));
#40424=DIRECTION('ref_axis',(0.703694571287399,-0.0553775799344575,0.708341212962543));
#40425=DIRECTION('center_axis',(5.15167520928809E-67,-1.18789542670764E-48,
-1.));
#40426=DIRECTION('ref_axis',(-4.33680868994202E-19,1.,-1.18789542670764E-48));
#40427=DIRECTION('center_axis',(0.699618093636944,-0.110808620201621,-0.705872490429271));
#40428=DIRECTION('ref_axis',(0.697182591373154,-0.110419233096072,0.708338921173112));
#40429=DIRECTION('center_axis',(5.15167520928809E-67,-1.18789542670764E-48,
-1.));
#40430=DIRECTION('ref_axis',(-4.33680868994202E-19,1.,-1.18789542670764E-48));
#40431=DIRECTION('center_axis',(0.688765827030149,-0.165358045050179,-0.705874176077195));
#40432=DIRECTION('ref_axis',(0.686371526838092,-0.164780094681522,0.708337241391906));
#40433=DIRECTION('center_axis',(5.15167520928809E-67,-1.18789542670764E-48,
-1.));
#40434=DIRECTION('ref_axis',(-4.33680868994202E-19,1.,-1.18789542670764E-48));
#40435=DIRECTION('center_axis',(0.673667540197491,-0.218887852522947,-0.705875451692545));
#40436=DIRECTION('ref_axis',(0.671328261761432,-0.218125006053886,0.708335970210723));
#40437=DIRECTION('center_axis',(5.15167520928809E-67,-1.18789542670764E-48,
-1.));
#40438=DIRECTION('ref_axis',(-4.33680868994202E-19,1.,-1.18789542670764E-48));
#40439=DIRECTION('center_axis',(0.654416196007489,-0.271068063822922,-0.705876439030501));
#40440=DIRECTION('ref_axis',(0.652145682814786,-0.270125073932652,0.70833498630162));
#40441=DIRECTION('center_axis',(5.15167520928809E-67,-1.18789542670764E-48,
-1.));
#40442=DIRECTION('ref_axis',(-4.33680868994202E-19,1.,-1.18789542670764E-48));
#40443=DIRECTION('center_axis',(0.631130405143858,-0.321577003370522,-0.705877214964604));
#40444=DIRECTION('ref_axis',(0.628942147608515,-0.320459697263077,0.708334213060224));
#40445=DIRECTION('center_axis',(5.15167520928809E-67,-1.18789542670764E-48,
-1.));
#40446=DIRECTION('ref_axis',(-4.33680868994202E-19,1.,-1.18789542670764E-48));
#40447=DIRECTION('center_axis',(0.603953677099314,-0.37010328932649,-0.705877830185883));
#40448=DIRECTION('ref_axis',(0.60186077552563,-0.368818543505346,0.708333599972698));
#40449=DIRECTION('center_axis',(5.15167520928809E-67,-1.18789542670764E-48,
-1.));
#40450=DIRECTION('ref_axis',(-4.33680868994202E-19,1.,-1.18789542670764E-48));
#40451=DIRECTION('center_axis',(0.573053525770311,-0.416347757295561,-0.70587831925706));
#40452=DIRECTION('ref_axis',(-0.571068576442179,0.41490346178236,-0.708333112596973));
#40453=DIRECTION('center_axis',(5.15167520928809E-67,-1.18789542670764E-48,
-1.));
#40454=DIRECTION('ref_axis',(-4.33680868994202E-19,1.,-1.18789542670764E-48));
#40455=DIRECTION('center_axis',(0.53862043116148,-0.460025307051029,-0.705878706300189));
#40456=DIRECTION('ref_axis',(-0.536755427393413,0.45843032095734,-0.708332726895112));
#40457=DIRECTION('center_axis',(5.15167520928809E-67,-1.18789542670764E-48,
-1.));
#40458=DIRECTION('ref_axis',(-4.33680868994202E-19,1.,-1.18789542670764E-48));
#40459=DIRECTION('center_axis',(0.500866661619453,-0.500866661619453,-0.705879008440093));
#40460=DIRECTION('ref_axis',(-0.499132905770974,0.49913076135833,-0.708332425801952));
#40461=DIRECTION('center_axis',(5.15167520928809E-67,-1.18789542670764E-48,
-1.));
#40462=DIRECTION('ref_axis',(-4.33680868994202E-19,1.,-1.18789542670764E-48));
#40463=DIRECTION('center_axis',(0.460024963033751,-0.538620028369041,-0.705879237848464));
#40464=DIRECTION('ref_axis',(-0.458432987266724,0.536753849182542,-0.708332197188179));
#40465=DIRECTION('center_axis',(5.15167520928809E-67,-1.18789542670764E-48,
-1.));
#40466=DIRECTION('ref_axis',(-4.33680868994202E-19,1.,-1.18789542670764E-48));
#40467=DIRECTION('center_axis',(0.416347122442499,-0.573052651970059,-0.705879403088044));
#40468=DIRECTION('ref_axis',(-0.414906617258677,0.571067623543698,-0.708332032520848));
#40469=DIRECTION('center_axis',(5.15167520928809E-67,-1.18789542670764E-48,
-1.));
#40470=DIRECTION('ref_axis',(-4.33680868994202E-19,1.,-1.18789542670764E-48));
#40471=DIRECTION('center_axis',(0.370102414698996,-0.603952249837027,-0.705879509938322));
#40472=DIRECTION('ref_axis',(-0.36882216472453,0.601860526500588,-0.708331926040572));
#40473=DIRECTION('center_axis',(5.15167520928809E-67,-1.18789542670764E-48,
-1.));
#40474=DIRECTION('ref_axis',(-4.33680868994202E-19,1.,-1.18789542670764E-48));
#40475=DIRECTION('center_axis',(0.321575941571994,-0.631128321246919,-0.705879561909914));
#40476=DIRECTION('ref_axis',(-0.320463768412686,0.628942707293528,-0.708331874248948));
#40477=DIRECTION('center_axis',(5.15167520928809E-67,-1.18789542670764E-48,
-1.));
#40478=DIRECTION('ref_axis',(-4.33680868994202E-19,1.,-1.18789542670764E-48));
#40479=DIRECTION('center_axis',(0.27106687342253,-0.654413322126797,-0.705879560517163));
#40480=DIRECTION('ref_axis',(-0.270129585579053,0.652147192703917,-0.7083318756369));
#40481=DIRECTION('center_axis',(5.15167520928809E-67,-1.18789542670764E-48,
-1.));
#40482=DIRECTION('ref_axis',(-4.33680868994202E-19,1.,-1.18789542670764E-48));
#40483=DIRECTION('center_axis',(0.218886604216888,-0.673663698306596,-0.705879505353626));
#40484=DIRECTION('ref_axis',(-0.218129954133397,0.671330916306428,-0.708331930609466));
#40485=DIRECTION('center_axis',(5.15167520928809E-67,-1.18789542670764E-48,
-1.));
#40486=DIRECTION('ref_axis',(-4.33680868994202E-19,1.,-1.18789542670764E-48));
#40487=DIRECTION('center_axis',(0.165356831187193,-0.688760770926925,-0.705879393956133));
#40488=DIRECTION('ref_axis',(-0.164785479532379,0.686375600198561,-0.708332041621264));
#40489=DIRECTION('center_axis',(5.15167520928809E-67,-1.18789542670764E-48,
-1.));
#40490=DIRECTION('ref_axis',(-4.33680868994202E-19,1.,-1.18789542670764E-48));
#40491=DIRECTION('center_axis',(0.110807570905112,-0.699611468639716,-0.705879221381312));
#40492=DIRECTION('ref_axis',(-0.110425058152835,0.697188483633082,-0.708332213598497));
#40493=DIRECTION('center_axis',(5.15167520928809E-67,-1.18789542670764E-48,
-1.));
#40494=DIRECTION('ref_axis',(-4.33680868994202E-19,1.,-1.18789542670764E-48));
#40495=DIRECTION('center_axis',(0.0555751238837179,-0.706148902304883,-0.705878979272593));
#40496=DIRECTION('ref_axis',(-0.0553838490533129,0.703702893729813,-0.708332454868706));
#40497=DIRECTION('center_axis',(5.15167520928809E-67,-1.18789542670764E-48,
-1.));
#40498=DIRECTION('ref_axis',(-4.33680868994202E-19,1.,-1.18789542670764E-48));
#40499=DIRECTION('center_axis',(4.22129745643424E-13,-0.708370174930854,
-0.705841126081805));
#40500=DIRECTION('ref_axis',(-3.47233154276107E-12,0.705841126081805,-0.708370174930854));
#40501=DIRECTION('center_axis',(5.15167520928809E-67,-1.18789542670764E-48,
-1.));
#40502=DIRECTION('ref_axis',(-4.33680868994202E-19,1.,-1.18789542670764E-48));
#40503=DIRECTION('center_axis',(-0.0555758110363383,-0.706157633406556,
-0.705870190622402));
#40504=DIRECTION('ref_axis',(0.0553775799352142,0.703694571287436,-0.708341212962447));
#40505=DIRECTION('center_axis',(5.15167520928809E-67,-1.18789542670764E-48,
-1.));
#40506=DIRECTION('ref_axis',(-4.33680868994202E-19,1.,-1.18789542670764E-48));
#40507=DIRECTION('center_axis',(-0.110808620201578,-0.699618093636773,-0.705872490429447));
#40508=DIRECTION('ref_axis',(0.110419233096311,0.697182591373295,-0.708338921172937));
#40509=DIRECTION('center_axis',(5.15167520928809E-67,-1.18789542670764E-48,
-1.));
#40510=DIRECTION('ref_axis',(-4.33680868994202E-19,1.,-1.18789542670764E-48));
#40511=DIRECTION('center_axis',(-0.165358045050148,-0.688765827029952,-0.705874176077394));
#40512=DIRECTION('ref_axis',(0.164780094682061,0.686371526838168,-0.708337241391707));
#40513=DIRECTION('center_axis',(5.15167520928809E-67,-1.18789542670764E-48,
-1.));
#40514=DIRECTION('ref_axis',(-4.33680868994202E-19,1.,-1.18789542670764E-48));
#40515=DIRECTION('center_axis',(-0.218887852522884,-0.673667540197305,-0.705875451692742));
#40516=DIRECTION('ref_axis',(0.218125006053241,0.671328261761849,-0.708335970210527));
#40517=DIRECTION('center_axis',(5.15167520928809E-67,-1.18789542670764E-48,
-1.));
#40518=DIRECTION('ref_axis',(-4.33680868994202E-19,1.,-1.18789542670764E-48));
#40519=DIRECTION('center_axis',(-0.271068063822912,-0.654416196007481,-0.705876439030512));
#40520=DIRECTION('ref_axis',(0.270125073931987,0.652145682815073,-0.708334986301609));
#40521=DIRECTION('center_axis',(5.15167520928809E-67,-1.18789542670764E-48,
-1.));
#40522=DIRECTION('ref_axis',(-4.33680868994202E-19,1.,-1.18789542670764E-48));
#40523=DIRECTION('center_axis',(-0.321577003370454,-0.631130405143677,-0.705877214964797));
#40524=DIRECTION('ref_axis',(0.32045969726294,0.628942147608801,-0.708334213060031));
#40525=DIRECTION('center_axis',(5.15167520928809E-67,-1.18789542670764E-48,
-1.));
#40526=DIRECTION('ref_axis',(-4.33680868994202E-19,1.,-1.18789542670764E-48));
#40527=DIRECTION('center_axis',(-0.370103289326527,-0.60395367709939,-0.705877830185799));
#40528=DIRECTION('ref_axis',(0.368818543504467,0.601860775526071,-0.708333599972782));
#40529=DIRECTION('center_axis',(5.15167520928809E-67,-1.18789542670764E-48,
-1.));
#40530=DIRECTION('ref_axis',(-4.33680868994202E-19,1.,-1.18789542670764E-48));
#40531=DIRECTION('center_axis',(-0.41634775729562,-0.5730535257704,-0.705878319256953));
#40532=DIRECTION('ref_axis',(0.414903461781904,0.571068576442378,-0.70833311259708));
#40533=DIRECTION('center_axis',(5.15167520928809E-67,-1.18789542670764E-48,
-1.));
#40534=DIRECTION('ref_axis',(-4.33680868994202E-19,1.,-1.18789542670764E-48));
#40535=DIRECTION('center_axis',(-0.460025307050912,-0.538620431161332,-0.705878706300378));
#40536=DIRECTION('ref_axis',(0.458430320957773,0.536755427393291,-0.708332726894923));
#40537=DIRECTION('center_axis',(5.15167520928809E-67,-1.18789542670764E-48,
-1.));
#40538=DIRECTION('ref_axis',(-4.33680868994202E-19,1.,-1.18789542670764E-48));
#40539=DIRECTION('center_axis',(-0.500866661619468,-0.500866661619444,-0.705879008440089));
#40540=DIRECTION('ref_axis',(0.499130761358181,0.499132905771117,-0.708332425801956));
#40541=DIRECTION('center_axis',(5.15167520928809E-67,-1.18789542670764E-48,
-1.));
#40542=DIRECTION('ref_axis',(-4.33680868994202E-19,1.,-1.18789542670764E-48));
#40543=DIRECTION('center_axis',(-0.538620028368883,-0.46002496303363,-0.705879237848664));
#40544=DIRECTION('ref_axis',(0.536753849182796,0.458432987266734,-0.70833219718798));
#40545=DIRECTION('center_axis',(5.15167520928809E-67,-1.18789542670764E-48,
-1.));
#40546=DIRECTION('ref_axis',(-4.33680868994202E-19,1.,-1.18789542670764E-48));
#40547=DIRECTION('center_axis',(-0.573052651970218,-0.416347122442612,-0.705879403087848));
#40548=DIRECTION('ref_axis',(0.571067623543181,0.414906617259055,-0.708332032521043));
#40549=DIRECTION('center_axis',(5.15167520928809E-67,-1.18789542670764E-48,
-1.));
#40550=DIRECTION('ref_axis',(-4.33680868994202E-19,1.,-1.18789542670764E-48));
#40551=DIRECTION('center_axis',(-0.603952249837038,-0.37010241469901,-0.705879509938305));
#40552=DIRECTION('ref_axis',(0.601860526500551,0.368822164724558,-0.708331926040589));
#40553=DIRECTION('center_axis',(5.15167520928809E-67,-1.18789542670764E-48,
-1.));
#40554=DIRECTION('ref_axis',(-4.33680868994202E-19,1.,-1.18789542670764E-48));
#40555=DIRECTION('center_axis',(-0.631128321246897,-0.32157594157199,-0.705879561909935));
#40556=DIRECTION('ref_axis',(0.628942707294004,0.320463768411799,-0.708331874248927));
#40557=DIRECTION('center_axis',(5.15167520928809E-67,-1.18789542670764E-48,
-1.));
#40558=DIRECTION('ref_axis',(-4.33680868994202E-19,1.,-1.18789542670764E-48));
#40559=DIRECTION('center_axis',(-0.654413322126778,-0.271066873422522,-0.705879560517184));
#40560=DIRECTION('ref_axis',(0.65214719270402,0.270129585578859,-0.708331875636879));
#40561=DIRECTION('center_axis',(5.15167520928809E-67,-1.18789542670764E-48,
-1.));
#40562=DIRECTION('ref_axis',(-4.33680868994202E-19,1.,-1.18789542670764E-48));
#40563=DIRECTION('center_axis',(-0.673663698306464,-0.218886604216857,-0.705879505353761));
#40564=DIRECTION('ref_axis',(0.671330916306719,0.218129954132939,-0.708331930609331));
#40565=DIRECTION('center_axis',(5.15167520928809E-67,-1.18789542670764E-48,
-1.));
#40566=DIRECTION('ref_axis',(-4.33680868994202E-19,1.,-1.18789542670764E-48));
#40567=DIRECTION('center_axis',(-0.688760770927255,-0.165356831187267,-0.705879393955794));
#40568=DIRECTION('ref_axis',(0.686375600198197,0.164785479532444,-0.708332041621602));
#40569=DIRECTION('center_axis',(5.15167520928809E-67,-1.18789542670764E-48,
-1.));
#40570=DIRECTION('ref_axis',(-4.33680868994202E-19,1.,-1.18789542670764E-48));
#40571=DIRECTION('center_axis',(-0.699611468639891,-0.110807570905155,-0.705879221381132));
#40572=DIRECTION('ref_axis',(0.697188483632974,0.110425058152362,-0.708332213598677));
#40573=DIRECTION('center_axis',(5.15167520928809E-67,-1.18789542670764E-48,
-1.));
#40574=DIRECTION('ref_axis',(-4.33680868994202E-19,1.,-1.18789542670764E-48));
#40575=DIRECTION('center_axis',(-0.706148902304619,-0.0555751238836977,
-0.705878979272859));
#40576=DIRECTION('ref_axis',(0.703702893730101,0.0553838490530483,-0.708332454868441));
#40577=DIRECTION('center_axis',(5.15167520928809E-67,-1.18789542670764E-48,
-1.));
#40578=DIRECTION('ref_axis',(-4.33680868994202E-19,1.,-1.18789542670764E-48));
#40579=DIRECTION('center_axis',(5.15167520928809E-67,-1.18789542670764E-48,
-1.));
#40580=DIRECTION('ref_axis',(-4.33680868994202E-19,1.,-1.18789542670764E-48));
#40581=DIRECTION('center_axis',(5.15167520928809E-67,-1.18789542670764E-48,
-1.));
#40582=DIRECTION('ref_axis',(-4.33680868994202E-19,1.,-1.18789542670764E-48));
#40583=DIRECTION('center_axis',(5.15167520928809E-67,-1.18789542670764E-48,
-1.));
#40584=DIRECTION('ref_axis',(-4.33680868994202E-19,1.,-1.18789542670764E-48));
#40585=DIRECTION('center_axis',(5.15167520928809E-67,-1.18789542670764E-48,
-1.));
#40586=DIRECTION('ref_axis',(-4.33680868994202E-19,1.,-1.18789542670764E-48));
#40587=DIRECTION('center_axis',(5.15167520928809E-67,-1.18789542670764E-48,
-1.));
#40588=DIRECTION('ref_axis',(-4.33680868994202E-19,1.,-1.18789542670764E-48));
#40589=DIRECTION('center_axis',(5.15167520928809E-67,-1.18789542670764E-48,
-1.));
#40590=DIRECTION('ref_axis',(-4.33680868994202E-19,1.,-1.18789542670764E-48));
#40591=DIRECTION('center_axis',(5.15167520928809E-67,-1.18789542670764E-48,
-1.));
#40592=DIRECTION('ref_axis',(-4.33680868994202E-19,1.,-1.18789542670764E-48));
#40593=DIRECTION('center_axis',(5.15167520928809E-67,-1.18789542670764E-48,
-1.));
#40594=DIRECTION('ref_axis',(-4.33680868994202E-19,1.,-1.18789542670764E-48));
#40595=DIRECTION('center_axis',(5.15167520928809E-67,-1.18789542670764E-48,
-1.));
#40596=DIRECTION('ref_axis',(-4.33680868994202E-19,1.,-1.18789542670764E-48));
#40597=DIRECTION('center_axis',(5.15167520928809E-67,-1.18789542670764E-48,
-1.));
#40598=DIRECTION('ref_axis',(-4.33680868994202E-19,1.,-1.18789542670764E-48));
#40599=DIRECTION('center_axis',(5.15167520928809E-67,-1.18789542670764E-48,
-1.));
#40600=DIRECTION('ref_axis',(-4.33680868994202E-19,1.,-1.18789542670764E-48));
#40601=DIRECTION('center_axis',(5.15167520928809E-67,-1.18789542670764E-48,
-1.));
#40602=DIRECTION('ref_axis',(-4.33680868994202E-19,1.,-1.18789542670764E-48));
#40603=DIRECTION('center_axis',(5.15167520928809E-67,-1.18789542670764E-48,
-1.));
#40604=DIRECTION('ref_axis',(-4.33680868994202E-19,1.,-1.18789542670764E-48));
#40605=DIRECTION('center_axis',(5.15167520928809E-67,-1.18789542670764E-48,
-1.));
#40606=DIRECTION('ref_axis',(-4.33680868994202E-19,1.,-1.18789542670764E-48));
#40607=DIRECTION('center_axis',(5.15167520928809E-67,-1.18789542670764E-48,
-1.));
#40608=DIRECTION('ref_axis',(-4.33680868994202E-19,1.,-1.18789542670764E-48));
#40609=DIRECTION('center_axis',(-0.271066873422527,0.654413322126802,-0.70587956051716));
#40610=DIRECTION('ref_axis',(-0.270129585578839,0.652147192704003,0.708331875636903));
#40611=DIRECTION('center_axis',(5.15167520928809E-67,-1.18789542670764E-48,
-1.));
#40612=DIRECTION('ref_axis',(-4.33680868994202E-19,1.,-1.18789542670764E-48));
#40613=DIRECTION('center_axis',(-0.218886604216929,0.673663698306674,-0.705879505353539));
#40614=DIRECTION('ref_axis',(-0.218129954131946,0.671330916306808,0.708331930609553));
#40615=DIRECTION('center_axis',(5.15167520928809E-67,-1.18789542670764E-48,
-1.));
#40616=DIRECTION('ref_axis',(-4.33680868994202E-19,1.,-1.18789542670764E-48));
#40617=DIRECTION('center_axis',(-0.16535683118721,0.688760770927084,-0.705879393955974));
#40618=DIRECTION('ref_axis',(-0.164785479532737,0.686375600198312,0.708332041621423));
#40619=DIRECTION('center_axis',(5.15167520928809E-67,-1.18789542670764E-48,
-1.));
#40620=DIRECTION('ref_axis',(-4.33680868994202E-19,1.,-1.18789542670764E-48));
#40621=DIRECTION('center_axis',(-0.110807570905113,0.699611468639715,-0.705879221381313));
#40622=DIRECTION('ref_axis',(-0.110425058151779,0.69718848363325,0.708332213598496));
#40623=DIRECTION('center_axis',(5.15167520928809E-67,-1.18789542670764E-48,
-1.));
#40624=DIRECTION('ref_axis',(-4.33680868994202E-19,1.,-1.18789542670764E-48));
#40625=DIRECTION('center_axis',(-0.0555751238836985,0.706148902304822,-0.705878979272656));
#40626=DIRECTION('ref_axis',(-0.0553838490532064,0.703702893729884,0.708332454868643));
#40627=DIRECTION('center_axis',(5.15167520928809E-67,-1.18789542670764E-48,
-1.));
#40628=DIRECTION('ref_axis',(-4.33680868994202E-19,1.,-1.18789542670764E-48));
#40629=DIRECTION('',(8.69022643068848E-17,-0.707106781186538,-0.707106781186557));
#40630=DIRECTION('center_axis',(5.15167520928809E-67,-1.18789542670764E-48,
-1.));
#40631=DIRECTION('ref_axis',(-4.33680868994202E-19,1.,-1.18789542670764E-48));
#40632=DIRECTION('center_axis',(5.15167520928809E-67,-1.18789542670764E-48,
-1.));
#40633=DIRECTION('ref_axis',(-4.33680868994202E-19,1.,-1.18789542670764E-48));
#40634=DIRECTION('center_axis',(5.15167520928809E-67,-1.18789542670764E-48,
-1.));
#40635=DIRECTION('ref_axis',(0.,1.,0.));
#40636=DIRECTION('center_axis',(5.15167520928809E-67,-1.18789542670764E-48,
-1.));
#40637=DIRECTION('ref_axis',(-4.33680868994202E-19,1.,-1.18789542670764E-48));
#40638=DIRECTION('center_axis',(1.,0.,5.15167520928809E-67));
#40639=DIRECTION('ref_axis',(0.,-1.,0.));
#40640=DIRECTION('center_axis',(5.15167520928809E-67,-1.18789542670764E-48,
-1.));
#40641=DIRECTION('ref_axis',(-4.33680868994202E-19,1.,-1.18789542670764E-48));
#40642=DIRECTION('center_axis',(5.15167520928809E-67,-1.18789542670764E-48,
-1.));
#40643=DIRECTION('ref_axis',(-4.33680868994202E-19,1.,-1.18789542670764E-48));
#40644=DIRECTION('',(-5.15167520928809E-67,1.18789542670764E-48,1.));
#40645=DIRECTION('center_axis',(5.15167520928809E-67,-1.18789542670764E-48,
-1.));
#40646=DIRECTION('ref_axis',(0.,1.,0.));
#40647=DIRECTION('center_axis',(5.15167520928809E-67,-1.18789542670764E-48,
-1.));
#40648=DIRECTION('ref_axis',(-4.33680868994202E-19,1.,-1.18789542670764E-48));
#40649=DIRECTION('center_axis',(-1.,0.,-5.15167520928809E-67));
#40650=DIRECTION('ref_axis',(0.,-1.,0.));
#40651=DIRECTION('center_axis',(5.15167520928809E-67,-1.18789542670764E-48,
-1.));
#40652=DIRECTION('ref_axis',(0.,1.,0.));
#40653=DIRECTION('center_axis',(1.,0.,5.15167520928809E-67));
#40654=DIRECTION('ref_axis',(0.,-1.,0.));
#40655=DIRECTION('center_axis',(5.15167520928809E-67,-1.18789542670764E-48,
-1.));
#40656=DIRECTION('ref_axis',(-4.33680868994202E-19,1.,-1.18789542670764E-48));
#40657=DIRECTION('center_axis',(5.15167520928809E-67,-1.18789542670764E-48,
-1.));
#40658=DIRECTION('ref_axis',(0.,1.,0.));
#40659=DIRECTION('center_axis',(-0.726741019926939,-0.686911553067863,9.06501466507717E-5));
#40660=DIRECTION('ref_axis',(0.686840456252471,-0.726663889286196,0.0144837723800636));
#40661=DIRECTION('center_axis',(5.15167520928809E-67,-1.18789542670764E-48,
-1.));
#40662=DIRECTION('ref_axis',(-4.33680868994202E-19,1.,-1.18789542670764E-48));
#40663=DIRECTION('center_axis',(0.0503838293498797,0.99872992276226,0.000105448247773495));
#40664=DIRECTION('ref_axis',(0.998655285166785,-0.0503813543085061,0.012220496982052));
#40665=DIRECTION('center_axis',(5.15167520928809E-67,-1.18789542670764E-48,
-1.));
#40666=DIRECTION('ref_axis',(0.,1.,0.));
#40667=DIRECTION('center_axis',(-0.0281309337977199,0.999604241409737,0.000105448247664664));
#40668=DIRECTION('ref_axis',(0.999529639708461,0.0281275452111534,0.0122204969076063));
#40669=DIRECTION('center_axis',(-0.670606260601171,-0.741813477246852,9.06501467500846E-5));
#40670=DIRECTION('ref_axis',(0.741736547998884,-0.670534945920291,0.0144837723805249));
#40671=DIRECTION('center_axis',(5.15167520928809E-67,-1.18789542670764E-48,
-1.));
#40672=DIRECTION('ref_axis',(-4.33680868994202E-19,1.,-1.18789542670764E-48));
#40673=DIRECTION('center_axis',(5.15167520928809E-67,-1.18789542670764E-48,
-1.));
#40674=DIRECTION('ref_axis',(0.,1.,0.));
#40675=DIRECTION('center_axis',(-0.106472260383779,0.994315667506771,0.000105448247699395));
#40676=DIRECTION('ref_axis',(0.99424156164256,0.106463029061011,0.0122204969504906));
#40677=DIRECTION('center_axis',(-0.610336990679751,-0.792141874660428,9.06501467512865E-5));
#40678=DIRECTION('ref_axis',(0.792059587274889,-0.610271931637935,0.0144837723275367));
#40679=DIRECTION('center_axis',(5.15167520928809E-67,-1.18789542670764E-48,
-1.));
#40680=DIRECTION('ref_axis',(-4.33680868994202E-19,1.,-1.18789542670764E-48));
#40681=DIRECTION('center_axis',(5.15167520928809E-67,-1.18789542670764E-48,
-1.));
#40682=DIRECTION('ref_axis',(0.,1.,0.));
#40683=DIRECTION('center_axis',(-0.18415715007879,0.982896806870144,0.000105448247763879));
#40684=DIRECTION('ref_axis',(0.982823653730846,0.18414213293402,0.0122204969481005));
#40685=DIRECTION('center_axis',(-0.546304790252955,-0.837586454002944,9.06501468511952E-5));
#40686=DIRECTION('ref_axis',(0.837499315807933,-0.546246387960026,0.0144837723631749));
#40687=DIRECTION('center_axis',(5.15167520928809E-67,-1.18789542670764E-48,
-1.));
#40688=DIRECTION('ref_axis',(-4.33680868994202E-19,1.,-1.18789542670764E-48));
#40689=DIRECTION('center_axis',(5.15167520928809E-67,-1.18789542670764E-48,
-1.));
#40690=DIRECTION('ref_axis',(0.,1.,0.));
#40691=DIRECTION('center_axis',(-0.260706649705391,0.965418060572754,0.000105448247684059));
#40692=DIRECTION('ref_axis',(0.965346311171948,0.260685939324359,0.0122204969329739));
#40693=DIRECTION('center_axis',(-0.478904439129961,-0.877867034330466,9.06501466909999E-5));
#40694=DIRECTION('ref_axis',(0.877775582562065,-0.478853053655646,0.0144837723846339));
#40695=DIRECTION('center_axis',(5.15167520928809E-67,-1.18789542670764E-48,
-1.));
#40696=DIRECTION('ref_axis',(-4.33680868994202E-19,1.,-1.18789542670764E-48));
#40697=DIRECTION('center_axis',(5.15167520928809E-67,-1.18789542670764E-48,
-1.));
#40698=DIRECTION('ref_axis',(0.,1.,0.));
#40699=DIRECTION('center_axis',(-0.33564880614276,0.941987190897842,0.000105448247631265));
#40700=DIRECTION('ref_axis',(0.941917287593993,0.335622530211717,0.0122204969563928));
#40701=DIRECTION('center_axis',(-0.408551482887427,-0.912735272471178,9.06501467675252E-5));
#40702=DIRECTION('ref_axis',(0.91264007095957,-0.408507431040139,0.0144837724331839));
#40703=DIRECTION('center_axis',(5.15167520928809E-67,-1.18789542670764E-48,
-1.));
#40704=DIRECTION('ref_axis',(-4.33680868994202E-19,1.,-1.18789542670764E-48));
#40705=DIRECTION('center_axis',(5.15167520928809E-67,-1.18789542670764E-48,
-1.));
#40706=DIRECTION('ref_axis',(0.,1.,0.));
#40707=DIRECTION('center_axis',(-0.408521576075341,0.912748656948662,0.000105448247753309));
#40708=DIRECTION('ref_axis',(0.912681030719062,0.40848989659417,0.0122204969651243));
#40709=DIRECTION('center_axis',(-0.335679670896088,-0.941976194141681,9.06501466394305E-5));
#40710=DIRECTION('ref_axis',(0.941877829837658,-0.335643224270894,0.0144837723450194));
#40711=DIRECTION('center_axis',(5.15167520928809E-67,-1.18789542670764E-48,
-1.));
#40712=DIRECTION('ref_axis',(-4.33680868994202E-19,1.,-1.18789542670764E-48));
#40713=DIRECTION('center_axis',(5.15167520928809E-67,-1.18789542670764E-48,
-1.));
#40714=DIRECTION('ref_axis',(0.,1.,0.));
#40715=DIRECTION('center_axis',(-0.478875674645407,0.877882724009063,0.000105448247283112));
#40716=DIRECTION('ref_axis',(0.877817791790398,0.478838786927794,0.012220497115417));
#40717=DIRECTION('center_axis',(-0.260738282108194,-0.965409519336649,9.06501468435925E-5));
#40718=DIRECTION('ref_axis',(0.965308598687812,-0.260709665410158,0.0144837723364994));
#40719=DIRECTION('center_axis',(5.15167520928809E-67,-1.18789542670764E-48,
-1.));
#40720=DIRECTION('ref_axis',(-4.33680868994202E-19,1.,-1.18789542670764E-48));
#40721=DIRECTION('center_axis',(5.15167520928809E-67,-1.18789542670764E-48,
-1.));
#40722=DIRECTION('ref_axis',(0.,1.,0.));
#40723=DIRECTION('center_axis',(-0.546277345437336,0.837604352151184,0.000105448247639474));
#40724=DIRECTION('ref_axis',(0.837542514276272,0.546235476910692,0.0122204968773897));
#40725=DIRECTION('center_axis',(-0.184189355107295,-0.982890773813505,9.06501468099581E-5));
#40726=DIRECTION('ref_axis',(0.982787919029019,-0.184168744767822,0.0144837723419927));
#40727=DIRECTION('center_axis',(5.15167520928809E-67,-1.18789542670764E-48,
-1.));
#40728=DIRECTION('ref_axis',(-4.33680868994202E-19,1.,-1.18789542670764E-48));
#40729=DIRECTION('center_axis',(5.15167520928809E-67,-1.18789542670764E-48,
-1.));
#40730=DIRECTION('ref_axis',(0.,1.,0.));
#40731=DIRECTION('center_axis',(-0.610311034740724,0.792161870929404,0.000105448247072483));
#40732=DIRECTION('ref_axis',(0.792103508642798,0.610264443533926,0.0122204972891987));
#40733=DIRECTION('center_axis',(-0.106504839483277,-0.994312179825427,9.06501466463657E-5));
#40734=DIRECTION('ref_axis',(0.994208025037708,-0.106492362571804,0.014483772453865));
#40735=DIRECTION('center_axis',(5.15167520928809E-67,-1.18789542670764E-48,
-1.));
#40736=DIRECTION('ref_axis',(-4.33680868994202E-19,1.,-1.18789542670764E-48));
#40737=DIRECTION('center_axis',(5.15167520928809E-67,-1.18789542670764E-48,
-1.));
#40738=DIRECTION('ref_axis',(0.,1.,0.));
#40739=DIRECTION('center_axis',(-0.670581953563772,0.74183544835446,0.000105448247723866));
#40740=DIRECTION('ref_axis',(0.741780921486778,0.670530926933108,0.012220496898794));
#40741=DIRECTION('center_axis',(-0.0281636861068304,-0.999603320606443,
9.06501467794172E-5));
#40742=DIRECTION('ref_axis',(0.999498507966719,-0.0281594195479949,0.0144837724030356));
#40743=DIRECTION('center_axis',(5.15167520928809E-67,-1.18789542670764E-48,
-1.));
#40744=DIRECTION('ref_axis',(-4.33680868994202E-19,1.,-1.18789542670764E-48));
#40745=DIRECTION('center_axis',(5.15167520928809E-67,-1.18789542670764E-48,
-1.));
#40746=DIRECTION('ref_axis',(0.,1.,0.));
#40747=DIRECTION('center_axis',(-0.726718511653027,0.686935363554299,0.000105448247728815));
#40748=DIRECTION('ref_axis',(0.686885008277766,0.726663364191397,0.0122204969332444));
#40749=DIRECTION('center_axis',(0.050351105759542,-0.998731574514065,9.06501467573609E-5));
#40750=DIRECTION('ref_axis',(0.998626750226961,0.0503471356610921,0.014483772362966));
#40751=DIRECTION('center_axis',(5.15167520928809E-67,-1.18789542670764E-48,
-1.));
#40752=DIRECTION('ref_axis',(-4.33680868994202E-19,1.,-1.18789542670764E-48));
#40753=DIRECTION('center_axis',(5.15167520928809E-67,-1.18789542670764E-48,
-1.));
#40754=DIRECTION('ref_axis',(0.,1.,0.));
#40755=DIRECTION('center_axis',(-0.778374608459537,0.627800093808634,0.000105448247783041));
#40756=DIRECTION('ref_axis',(0.627754220580437,0.778315680169477,0.01222049695274));
#40757=DIRECTION('center_axis',(0.128555466315269,-0.991702316152894,9.06501465984867E-5));
#40758=DIRECTION('ref_axis',(0.99159812649388,0.128543284036463,0.0144837724004731));
#40759=DIRECTION('center_axis',(5.15167520928809E-67,-1.18789542670764E-48,
-1.));
#40760=DIRECTION('ref_axis',(-4.33680868994202E-19,1.,-1.18789542670764E-48));
#40761=DIRECTION('center_axis',(5.15167520928809E-67,-1.18789542670764E-48,
-1.));
#40762=DIRECTION('ref_axis',(0.,1.,0.));
#40763=DIRECTION('center_axis',(-0.825231766969855,0.564794227718802,0.000105448247237627));
#40764=DIRECTION('ref_axis',(0.564753119361559,0.825169421162197,0.0122204971352771));
#40765=DIRECTION('center_axis',(0.205967239672467,-0.97855888323813,9.06501466256469E-5));
#40766=DIRECTION('ref_axis',(0.978455970572454,0.205946920321296,0.0144837723432324));
#40767=DIRECTION('center_axis',(5.15167520928809E-67,-1.18789542670764E-48,
-1.));
#40768=DIRECTION('ref_axis',(-4.33680868994202E-19,1.,-1.18789542670764E-48));
#40769=DIRECTION('center_axis',(5.15167520928809E-67,-1.18789542670764E-48,
-1.));
#40770=DIRECTION('ref_axis',(0.,1.,0.));
#40771=DIRECTION('center_axis',(-0.867001097222074,0.498306217396881,0.00010544824406792));
#40772=DIRECTION('ref_axis',(0.498270127350421,0.866935718266621,0.0122204985059196));
#40773=DIRECTION('center_axis',(0.282109156506117,-0.959382309404316,9.06501467341775E-5));
#40774=DIRECTION('ref_axis',(0.959281308220891,0.282080825357731,0.0144837724201092));
#40775=DIRECTION('center_axis',(5.15167520928809E-67,-1.18789542670764E-48,
-1.));
#40776=DIRECTION('ref_axis',(-4.33680868994202E-19,1.,-1.18789542670764E-48));
#40777=DIRECTION('center_axis',(5.15167520928809E-67,-1.18789542670764E-48,
-1.));
#40778=DIRECTION('ref_axis',(0.,1.,0.));
#40779=DIRECTION('center_axis',(-0.903425077395399,0.428745983554114,0.00010544824771057));
#40780=DIRECTION('ref_axis',(0.42871513434286,0.903357068405985,0.0122204969754959));
#40781=DIRECTION('center_axis',(0.356511776578972,-0.934290824606052,9.06501467185522E-5));
#40782=DIRECTION('ref_axis',(0.934192357612503,0.356475608304786,0.0144837723720686));
#40783=DIRECTION('center_axis',(5.15167520928809E-67,-1.18789542670764E-48,
-1.));
#40784=DIRECTION('ref_axis',(-4.33680868994202E-19,1.,-1.18789542670764E-48));
#40785=DIRECTION('center_axis',(5.15167520928809E-67,-1.18789542670764E-48,
-1.));
#40786=DIRECTION('ref_axis',(0.,1.,0.));
#40787=DIRECTION('center_axis',(-0.934279141551227,0.35654238814336,0.000105448247725771));
#40788=DIRECTION('ref_axis',(0.356516969954114,0.934208921810617,0.0122204968876431));
#40789=DIRECTION('center_axis',(0.428716382996855,-0.903439126190938,9.06501466905075E-5));
#40790=DIRECTION('ref_axis',(0.903343800467886,0.428672600585895,0.0144837724078269));
#40791=DIRECTION('center_axis',(5.15167520928809E-67,-1.18789542670764E-48,
-1.));
#40792=DIRECTION('ref_axis',(-4.33680868994202E-19,1.,-1.18789542670764E-48));
#40793=DIRECTION('center_axis',(5.15167520928809E-67,-1.18789542670764E-48,
-1.));
#40794=DIRECTION('ref_axis',(0.,1.,0.));
#40795=DIRECTION('center_axis',(-0.959373064120116,0.282140590347166,0.000105448247704078));
#40796=DIRECTION('ref_axis',(0.282120759890668,0.959301066553995,0.0122204970062476));
#40797=DIRECTION('center_axis',(0.498277810351468,-0.867017425138559,9.06501469271671E-5));
#40798=DIRECTION('ref_axis',(0.86692582840188,0.498226683737388,0.0144837723593644));
#40799=DIRECTION('center_axis',(5.15167520928809E-67,-1.18789542670764E-48,
-1.));
#40800=DIRECTION('ref_axis',(-4.33680868994202E-19,1.,-1.18789542670764E-48));
#40801=DIRECTION('center_axis',(5.15167520928809E-67,-1.18789542670764E-48,
-1.));
#40802=DIRECTION('ref_axis',(0.,1.,0.));
#40803=DIRECTION('center_axis',(-0.978552132724721,0.205999301990486,0.000105448247790145));
#40804=DIRECTION('ref_axis',(0.205985181528783,0.978478801224291,0.0122204969305395));
#40805=DIRECTION('center_axis',(0.564767189310343,-0.825250273348059,9.06501467424166E-5));
#40806=DIRECTION('ref_axis',(0.825162970321744,0.56470903370561,0.0144837723356968));
#40807=DIRECTION('center_axis',(5.15167520928809E-67,-1.18789542670764E-48,
-1.));
#40808=DIRECTION('ref_axis',(-4.33680868994202E-19,1.,-1.18789542670764E-48));
#40809=DIRECTION('center_axis',(5.15167520928809E-67,-1.18789542670764E-48,
-1.));
#40810=DIRECTION('ref_axis',(0.,1.,0.));
#40811=DIRECTION('center_axis',(-0.991698102029505,0.128587959435343,0.000105448247905715));
#40812=DIRECTION('ref_axis',(0.12857963602553,0.991623888707005,0.0122204969268892));
#40813=DIRECTION('center_axis',(0.627774590743107,-0.778395179198763,9.06501466692162E-5));
#40814=DIRECTION('ref_axis',(0.778312708134479,0.627709764696018,0.0144837723553914));
#40815=DIRECTION('center_axis',(5.15167520928809E-67,-1.18789542670764E-48,
-1.));
#40816=DIRECTION('ref_axis',(-4.33680868994202E-19,1.,-1.18789542670764E-48));
#40817=DIRECTION('center_axis',(5.15167520928809E-67,-1.18789542670764E-48,
-1.));
#40818=DIRECTION('ref_axis',(0.,1.,0.));
#40819=DIRECTION('center_axis',(-0.998729922762266,0.05038382934976,0.000105448247701369));
#40820=DIRECTION('ref_axis',(0.0503813543083786,0.998655285166624,0.0122204969957313));
#40821=DIRECTION('center_axis',(0.686911553067687,-0.726741019927105,9.06501465529425E-5));
#40822=DIRECTION('ref_axis',(0.726663889286156,0.686840456252101,0.0144837723995786));
#40823=DIRECTION('center_axis',(5.15167520928809E-67,-1.18789542670764E-48,
-1.));
#40824=DIRECTION('ref_axis',(-4.33680868994202E-19,1.,-1.18789542670764E-48));
#40825=DIRECTION('center_axis',(5.15167520928809E-67,-1.18789542670764E-48,
-1.));
#40826=DIRECTION('ref_axis',(0.,1.,0.));
#40827=DIRECTION('center_axis',(-0.999604241409733,-0.0281309337978441,
0.000105448247608528));
#40828=DIRECTION('ref_axis',(0.0281275452112647,-0.999529639708088,-0.0122204969378127));
#40829=DIRECTION('center_axis',(0.741813477246663,-0.67060626060138,9.06501466416355E-5));
#40830=DIRECTION('ref_axis',(0.670534945920398,0.741736547998582,0.0144837723910712));
#40831=DIRECTION('center_axis',(5.15167520928809E-67,-1.18789542670764E-48,
-1.));
#40832=DIRECTION('ref_axis',(-4.33680868994202E-19,1.,-1.18789542670764E-48));
#40833=DIRECTION('center_axis',(5.15167520928809E-67,-1.18789542670764E-48,
-1.));
#40834=DIRECTION('ref_axis',(0.,1.,0.));
#40835=DIRECTION('center_axis',(-0.994315667506803,-0.106472260383486,0.000105448247832577));
#40836=DIRECTION('ref_axis',(0.10646302906079,-0.994241561643227,-0.0122204968981425));
#40837=DIRECTION('center_axis',(0.792141874660394,-0.610336990679795,9.06501467163515E-5));
#40838=DIRECTION('ref_axis',(0.610271931637984,0.792059587274861,0.0144837723269713));
#40839=DIRECTION('center_axis',(5.15167520928809E-67,-1.18789542670764E-48,
-1.));
#40840=DIRECTION('ref_axis',(-4.33680868994202E-19,1.,-1.18789542670764E-48));
#40841=DIRECTION('center_axis',(5.15167520928809E-67,-1.18789542670764E-48,
-1.));
#40842=DIRECTION('ref_axis',(0.,1.,0.));
#40843=DIRECTION('center_axis',(-0.982896806870098,-0.184157150079038,0.000105448247610839));
#40844=DIRECTION('ref_axis',(0.184142132934261,-0.982823653730751,-0.0122204969521754));
#40845=DIRECTION('center_axis',(0.837586454002892,-0.546304790253034,9.06501468389122E-5));
#40846=DIRECTION('ref_axis',(0.546246387959946,0.837499315807641,0.014483772383082));
#40847=DIRECTION('center_axis',(5.15167520928809E-67,-1.18789542670764E-48,
-1.));
#40848=DIRECTION('ref_axis',(-4.33680868994202E-19,1.,-1.18789542670764E-48));
#40849=DIRECTION('center_axis',(5.15167520928809E-67,-1.18789542670764E-48,
-1.));
#40850=DIRECTION('ref_axis',(0.,1.,0.));
#40851=DIRECTION('center_axis',(-0.965418060572767,-0.260706649705342,0.000105448247695262));
#40852=DIRECTION('ref_axis',(0.260685939324476,-0.965346311172558,-0.0122204968822783));
#40853=DIRECTION('center_axis',(0.877867034330398,-0.478904439130086,9.06501466177592E-5));
#40854=DIRECTION('ref_axis',(0.478853053655353,0.877775582561241,0.0144837724443041));
#40855=DIRECTION('center_axis',(5.15167520928809E-67,-1.18789542670764E-48,
-1.));
#40856=DIRECTION('ref_axis',(-4.33680868994202E-19,1.,-1.18789542670764E-48));
#40857=DIRECTION('center_axis',(5.15167520928809E-67,-1.18789542670764E-48,
-1.));
#40858=DIRECTION('ref_axis',(0.,1.,0.));
#40859=DIRECTION('center_axis',(-0.941987190897914,-0.335648806142557,0.000105448247712849));
#40860=DIRECTION('ref_axis',(0.335622530211483,-0.941917287593983,-0.0122204969636003));
#40861=DIRECTION('center_axis',(0.912735272471151,-0.408551482887487,9.06501467033935E-5));
#40862=DIRECTION('ref_axis',(0.408507431040848,0.912640070960968,0.0144837723251257));
#40863=DIRECTION('center_axis',(5.15167520928809E-67,-1.18789542670764E-48,
-1.));
#40864=DIRECTION('ref_axis',(-4.33680868994202E-19,1.,-1.18789542670764E-48));
#40865=DIRECTION('center_axis',(5.15167520928809E-67,-1.18789542670764E-48,
-1.));
#40866=DIRECTION('ref_axis',(0.,1.,0.));
#40867=DIRECTION('center_axis',(-0.912748656948201,-0.408521576076371,0.000105448247247158));
#40868=DIRECTION('ref_axis',(0.408489896594259,-0.912681030716532,-0.012220497151094));
#40869=DIRECTION('center_axis',(0.941976194141716,-0.335679670895989,9.06501466623777E-5));
#40870=DIRECTION('ref_axis',(0.335643224270751,0.941877829837572,0.0144837723539316));
#40871=DIRECTION('center_axis',(5.15167520928809E-67,-1.18789542670764E-48,
-1.));
#40872=DIRECTION('ref_axis',(-4.33680868994202E-19,1.,-1.18789542670764E-48));
#40873=DIRECTION('center_axis',(5.15167520928809E-67,-1.18789542670764E-48,
-1.));
#40874=DIRECTION('ref_axis',(0.,1.,0.));
#40875=DIRECTION('center_axis',(-0.877882724009451,-0.478875674644697,0.000105448247674909));
#40876=DIRECTION('ref_axis',(0.478838786928496,-0.877817791793333,-0.0122204968770904));
#40877=DIRECTION('center_axis',(0.965409519336493,-0.26073828210877,9.06501465579451E-5));
#40878=DIRECTION('ref_axis',(0.260709665410522,0.965308598686875,0.0144837723924504));
#40879=DIRECTION('center_axis',(5.15167520928809E-67,-1.18789542670764E-48,
-1.));
#40880=DIRECTION('ref_axis',(-4.33680868994202E-19,1.,-1.18789542670764E-48));
#40881=DIRECTION('center_axis',(5.15167520928809E-67,-1.18789542670764E-48,
-1.));
#40882=DIRECTION('ref_axis',(0.,1.,0.));
#40883=DIRECTION('center_axis',(-0.837604352151306,-0.546277345437149,0.00010544824776483));
#40884=DIRECTION('ref_axis',(0.546235476910197,-0.837542514275933,-0.0122204969227218));
#40885=DIRECTION('center_axis',(0.982890773813463,-0.184189355107518,9.06501466980053E-5));
#40886=DIRECTION('ref_axis',(0.184168744767822,0.982787919027818,0.0144837724235038));
#40887=DIRECTION('center_axis',(5.15167520928809E-67,-1.18789542670764E-48,
-1.));
#40888=DIRECTION('ref_axis',(-4.33680868994202E-19,1.,-1.18789542670764E-48));
#40889=DIRECTION('center_axis',(5.15167520928809E-67,-1.18789542670764E-48,
-1.));
#40890=DIRECTION('ref_axis',(0.,1.,0.));
#40891=DIRECTION('center_axis',(-0.792161870930109,-0.610311034739809,0.000105448247597277));
#40892=DIRECTION('ref_axis',(0.610264443535208,-0.792103508646315,-0.0122204969972532));
#40893=DIRECTION('center_axis',(0.994312179825469,-0.106504839482882,9.06501468290203E-5));
#40894=DIRECTION('ref_axis',(0.106492362571566,0.994208025039157,0.0144837723561435));
#40895=DIRECTION('center_axis',(5.15167520928809E-67,-1.18789542670764E-48,
-1.));
#40896=DIRECTION('ref_axis',(-4.33680868994202E-19,1.,-1.18789542670764E-48));
#40897=DIRECTION('center_axis',(5.15167520928809E-67,-1.18789542670764E-48,
-1.));
#40898=DIRECTION('ref_axis',(0.,1.,0.));
#40899=DIRECTION('center_axis',(-0.741835448354634,-0.670581953563579,0.000105448247853962));
#40900=DIRECTION('ref_axis',(0.67053092693267,-0.741780921486687,-0.0122204969283275));
#40901=DIRECTION('center_axis',(0.99960332060645,-0.0281636861065795,9.06501468718404E-5));
#40902=DIRECTION('ref_axis',(0.0281594195477731,0.999498507967606,0.014483772342229));
#40903=DIRECTION('center_axis',(5.15167520928809E-67,-1.18789542670764E-48,
-1.));
#40904=DIRECTION('ref_axis',(-4.33680868994202E-19,1.,-1.18789542670764E-48));
#40905=DIRECTION('center_axis',(5.15167520928809E-67,-1.18789542670764E-48,
-1.));
#40906=DIRECTION('ref_axis',(0.,1.,0.));
#40907=DIRECTION('center_axis',(-0.686935363552547,-0.726718511654683,0.000105448246665782));
#40908=DIRECTION('ref_axis',(0.726663364188996,-0.686885008272227,-0.0122204973873402));
#40909=DIRECTION('center_axis',(0.998731574514055,0.0503511057597249,9.06501467982717E-5));
#40910=DIRECTION('ref_axis',(0.050347135661256,-0.998626750226507,-0.0144837723936806));
#40911=DIRECTION('center_axis',(5.15167520928809E-67,-1.18789542670764E-48,
-1.));
#40912=DIRECTION('ref_axis',(-4.33680868994202E-19,1.,-1.18789542670764E-48));
#40913=DIRECTION('center_axis',(5.15167520928809E-67,-1.18789542670764E-48,
-1.));
#40914=DIRECTION('ref_axis',(0.,1.,0.));
#40915=DIRECTION('center_axis',(-0.627800093808639,-0.778374608459533,0.000105448247779514));
#40916=DIRECTION('ref_axis',(0.778315680170178,-0.627754220581,-0.0122204968791585));
#40917=DIRECTION('center_axis',(0.991702316152886,0.12855546631533,9.06501466251883E-5));
#40918=DIRECTION('ref_axis',(0.128543284036466,-0.991598126493403,-0.0144837724330683));
#40919=DIRECTION('center_axis',(5.15167520928809E-67,-1.18789542670764E-48,
-1.));
#40920=DIRECTION('ref_axis',(-4.33680868994202E-19,1.,-1.18789542670764E-48));
#40921=DIRECTION('center_axis',(5.15167520928809E-67,-1.18789542670764E-48,
-1.));
#40922=DIRECTION('ref_axis',(0.,1.,0.));
#40923=DIRECTION('center_axis',(-0.564794227719968,-0.825231766969057,0.000105448247863909));
#40924=DIRECTION('ref_axis',(0.825169421163414,-0.564753119364088,-0.0122204969362205));
#40925=DIRECTION('center_axis',(0.978558883238036,0.205967239672914,9.06501468463484E-5));
#40926=DIRECTION('ref_axis',(0.205946920321936,-0.978455970573291,-0.014483772277592));
#40927=DIRECTION('center_axis',(5.15167520928809E-67,-1.18789542670764E-48,
-1.));
#40928=DIRECTION('ref_axis',(-4.33680868994202E-19,1.,-1.18789542670764E-48));
#40929=DIRECTION('center_axis',(5.15167520928809E-67,-1.18789542670764E-48,
-1.));
#40930=DIRECTION('ref_axis',(0.,1.,0.));
#40931=DIRECTION('center_axis',(-0.498306217403848,-0.86700109721807,0.000105448247661773));
#40932=DIRECTION('ref_axis',(0.866935718279092,-0.498270127366718,-0.0122204969566953));
#40933=DIRECTION('center_axis',(0.959382309404258,0.282109156506314,9.06501467982869E-5));
#40934=DIRECTION('ref_axis',(0.282080825358155,-0.959281308221622,-0.014483772363392));
#40935=DIRECTION('center_axis',(5.15167520928809E-67,-1.18789542670764E-48,
-1.));
#40936=DIRECTION('ref_axis',(-4.33680868994202E-19,1.,-1.18789542670764E-48));
#40937=DIRECTION('center_axis',(5.15167520928809E-67,-1.18789542670764E-48,
-1.));
#40938=DIRECTION('ref_axis',(0.,1.,0.));
#40939=DIRECTION('center_axis',(-0.428745983554159,-0.903425077395378,0.000105448247692435));
#40940=DIRECTION('ref_axis',(0.903357068405516,-0.428715134342697,-0.0122204970158381));
#40941=DIRECTION('center_axis',(0.934290824605943,0.356511776579256,9.06501468588022E-5));
#40942=DIRECTION('ref_axis',(0.35647560830508,-0.934192357612417,-0.0144837723703894));
#40943=DIRECTION('center_axis',(5.15167520928809E-67,-1.18789542670764E-48,
-1.));
#40944=DIRECTION('ref_axis',(-4.33680868994202E-19,1.,-1.18789542670764E-48));
#40945=DIRECTION('center_axis',(5.15167520928809E-67,-1.18789542670764E-48,
-1.));
#40946=DIRECTION('ref_axis',(0.,1.,0.));
#40947=DIRECTION('center_axis',(-0.356542388142294,-0.934279141551633,0.000105448247232403));
#40948=DIRECTION('ref_axis',(0.934208921807365,-0.356516969951681,-0.0122204972072322));
#40949=DIRECTION('center_axis',(0.903439126190767,0.428716382997215,9.06501468179925E-5));
#40950=DIRECTION('ref_axis',(0.428672600586429,-0.903343800468082,-0.0144837723797852));
#40951=DIRECTION('center_axis',(5.15167520928809E-67,-1.18789542670764E-48,
-1.));
#40952=DIRECTION('ref_axis',(-4.33680868994202E-19,1.,-1.18789542670764E-48));
#40953=DIRECTION('center_axis',(5.15167520928809E-67,-1.18789542670764E-48,
-1.));
#40954=DIRECTION('ref_axis',(0.,1.,0.));
#40955=DIRECTION('center_axis',(-0.282140590347279,-0.959373064120083,0.000105448247741099));
#40956=DIRECTION('ref_axis',(0.959301066555032,-0.282120759891086,-0.012220496915153));
#40957=DIRECTION('center_axis',(0.867017425138588,0.498277810351419,9.06501468672452E-5));
#40958=DIRECTION('ref_axis',(0.498226683737162,-0.866925828401598,-0.0144837723840689));
#40959=DIRECTION('center_axis',(5.15167520928809E-67,-1.18789542670764E-48,
-1.));
#40960=DIRECTION('ref_axis',(-4.33680868994202E-19,1.,-1.18789542670764E-48));
#40961=DIRECTION('center_axis',(5.15167520928809E-67,-1.18789542670764E-48,
-1.));
#40962=DIRECTION('ref_axis',(0.,1.,0.));
#40963=DIRECTION('center_axis',(-0.20599930198994,-0.978552132724836,0.000105448247552452));
#40964=DIRECTION('ref_axis',(0.97847880122346,-0.205985181528044,-0.0122204970095074));
#40965=DIRECTION('center_axis',(0.825250273348004,0.564767189310424,9.06501467639861E-5));
#40966=DIRECTION('ref_axis',(0.56470903370563,-0.825162970321598,-0.0144837723432248));
#40967=DIRECTION('center_axis',(5.15167520928809E-67,-1.18789542670764E-48,
-1.));
#40968=DIRECTION('ref_axis',(-4.33680868994202E-19,1.,-1.18789542670764E-48));
#40969=DIRECTION('center_axis',(5.15167520928809E-67,-1.18789542670764E-48,
-1.));
#40970=DIRECTION('ref_axis',(0.,1.,0.));
#40971=DIRECTION('center_axis',(-0.128587959431095,-0.991698102030056,0.000105448246015545));
#40972=DIRECTION('ref_axis',(0.991623888697772,-0.128579636020076,-0.0122204977334817));
#40973=DIRECTION('center_axis',(0.778395179198649,0.627774590743249,9.06501467187627E-5));
#40974=DIRECTION('ref_axis',(0.62770976469618,-0.778312708134389,-0.0144837723532511));
#40975=DIRECTION('center_axis',(5.15167520928809E-67,-1.18789542670764E-48,
-1.));
#40976=DIRECTION('ref_axis',(-4.33680868994202E-19,1.,-1.18789542670764E-48));
#40977=DIRECTION('center_axis',(5.15167520928809E-67,-1.18789542670764E-48,
-1.));
#40978=DIRECTION('ref_axis',(0.,1.,0.));
#40979=DIRECTION('center_axis',(-0.0503838293498799,-0.99872992276226,0.000105448247790322));
#40980=DIRECTION('ref_axis',(0.998655285167012,-0.050381354308516,-0.0122204969634886));
#40981=DIRECTION('center_axis',(0.726741019926698,0.686911553068118,9.06501468063716E-5));
#40982=DIRECTION('ref_axis',(0.686840456253071,-0.726663889286322,-0.0144837723452766));
#40983=DIRECTION('center_axis',(5.15167520928809E-67,-1.18789542670764E-48,
-1.));
#40984=DIRECTION('ref_axis',(-4.33680868994202E-19,1.,-1.18789542670764E-48));
#40985=DIRECTION('center_axis',(5.15167520928809E-67,-1.18789542670764E-48,
-1.));
#40986=DIRECTION('ref_axis',(0.,1.,0.));
#40987=DIRECTION('center_axis',(0.0281309337977714,-0.999604241409735,0.000105448247661813));
#40988=DIRECTION('ref_axis',(0.999529639707556,0.0281275452111717,-0.0122204969816086));
#40989=DIRECTION('center_axis',(0.670606260601294,0.741813477246741,9.06501466782892E-5));
#40990=DIRECTION('ref_axis',(0.741736547997904,-0.67053494591962,-0.0144837724617815));
#40991=DIRECTION('center_axis',(5.15167520928809E-67,-1.18789542670764E-48,
-1.));
#40992=DIRECTION('ref_axis',(-4.33680868994202E-19,1.,-1.18789542670764E-48));
#40993=DIRECTION('center_axis',(5.15167520928809E-67,-1.18789542670764E-48,
-1.));
#40994=DIRECTION('ref_axis',(0.,1.,0.));
#40995=DIRECTION('center_axis',(0.106472260384112,-0.994315667506736,0.000105448247531298));
#40996=DIRECTION('ref_axis',(0.994241561642015,0.106463029061287,-0.01222049699245));
#40997=DIRECTION('center_axis',(0.610336990679746,0.792141874660432,9.06501467541659E-5));
#40998=DIRECTION('ref_axis',(0.792059587274579,-0.610271931637685,-0.0144837723550388));
#40999=DIRECTION('center_axis',(5.15167520928809E-67,-1.18789542670764E-48,
-1.));
#41000=DIRECTION('ref_axis',(-4.33680868994202E-19,1.,-1.18789542670764E-48));
#41001=DIRECTION('center_axis',(5.15167520928809E-67,-1.18789542670764E-48,
-1.));
#41002=DIRECTION('ref_axis',(0.,1.,0.));
#41003=DIRECTION('center_axis',(0.184157150078655,-0.982896806870169,0.000105448247826086));
#41004=DIRECTION('ref_axis',(0.982823653731041,0.184142132933918,-0.01222049693405));
#41005=DIRECTION('center_axis',(0.546304790253063,0.837586454002874,9.06501468026834E-5));
#41006=DIRECTION('ref_axis',(0.837499315807096,-0.546246387959628,-0.0144837724265968));
#41007=DIRECTION('center_axis',(5.15167520928809E-67,-1.18789542670764E-48,
-1.));
#41008=DIRECTION('ref_axis',(-4.33680868994202E-19,1.,-1.18789542670764E-48));
#41009=DIRECTION('center_axis',(5.15167520928809E-67,-1.18789542670764E-48,
-1.));
#41010=DIRECTION('ref_axis',(0.,1.,0.));
#41011=DIRECTION('center_axis',(0.260706649723291,-0.965418060567921,0.000105448239312411));
#41012=DIRECTION('ref_axis',(0.965346311124436,0.260685939330442,-0.0122205005564138));
#41013=DIRECTION('center_axis',(0.478904439129984,0.877867034330454,9.06501466836614E-5));
#41014=DIRECTION('ref_axis',(0.877775582561938,-0.478853053655605,-0.0144837723936657));
#41015=DIRECTION('center_axis',(5.15167520928809E-67,-1.18789542670764E-48,
-1.));
#41016=DIRECTION('ref_axis',(-4.33680868994202E-19,1.,-1.18789542670764E-48));
#41017=DIRECTION('center_axis',(5.15167520928809E-67,-1.18789542670764E-48,
-1.));
#41018=DIRECTION('ref_axis',(0.,1.,0.));
#41019=DIRECTION('center_axis',(0.335648806142683,-0.941987190897869,0.000105448247681778));
#41020=DIRECTION('ref_axis',(0.941917287594608,0.335622530211854,-0.012220496905163));
#41021=DIRECTION('center_axis',(0.408551482887321,0.912735272471225,9.06501468104788E-5));
#41022=DIRECTION('ref_axis',(0.912640070960436,-0.408507431040405,-0.014483772371131));
#41023=DIRECTION('center_axis',(5.15167520928809E-67,-1.18789542670764E-48,
-1.));
#41024=DIRECTION('ref_axis',(-4.33680868994202E-19,1.,-1.18789542670764E-48));
#41025=DIRECTION('center_axis',(5.15167520928809E-67,-1.18789542670764E-48,
-1.));
#41026=DIRECTION('ref_axis',(0.,1.,0.));
#41027=DIRECTION('center_axis',(0.408521576076219,-0.912748656948269,0.000105448247344423));
#41028=DIRECTION('ref_axis',(0.912681030717311,0.408489896594431,-0.0122204970871443));
#41029=DIRECTION('center_axis',(0.335679670895796,0.941976194141785,9.06501467685389E-5));
#41030=DIRECTION('ref_axis',(0.941877829836932,-0.335643224270299,-0.0144837724059784));
#41031=DIRECTION('center_axis',(5.15167520928809E-67,-1.18789542670764E-48,
-1.));
#41032=DIRECTION('ref_axis',(-4.33680868994202E-19,1.,-1.18789542670764E-48));
#41033=DIRECTION('center_axis',(5.15167520928809E-67,-1.18789542670764E-48,
-1.));
#41034=DIRECTION('ref_axis',(0.,1.,0.));
#41035=DIRECTION('center_axis',(0.478875674644822,-0.877882724009383,0.000105448247602163));
#41036=DIRECTION('ref_axis',(0.877817791792273,0.47883878692807,-0.0122204969699355));
#41037=DIRECTION('center_axis',(0.260738282108074,0.965409519336681,9.06501468936573E-5));
#41038=DIRECTION('ref_axis',(0.965308598687316,-0.260709665409891,-0.0144837723743816));
#41039=DIRECTION('center_axis',(5.15167520928809E-67,-1.18789542670764E-48,
-1.));
#41040=DIRECTION('ref_axis',(-4.33680868994202E-19,1.,-1.18789542670764E-48));
#41041=DIRECTION('center_axis',(5.15167520928809E-67,-1.18789542670764E-48,
-1.));
#41042=DIRECTION('ref_axis',(0.,1.,0.));
#41043=DIRECTION('center_axis',(0.546277345437349,-0.837604352151176,0.000105448247639465));
#41044=DIRECTION('ref_axis',(0.837542514275712,0.546235476910338,-0.0122204969316073));
#41045=DIRECTION('center_axis',(0.184189355107516,0.982890773813463,9.06501467024073E-5));
#41046=DIRECTION('ref_axis',(0.982787919028468,-0.184168744767946,-0.0144837723778112));
#41047=DIRECTION('center_axis',(5.15167520928809E-67,-1.18789542670764E-48,
-1.));
#41048=DIRECTION('ref_axis',(-4.33680868994202E-19,1.,-1.18789542670764E-48));
#41049=DIRECTION('center_axis',(5.15167520928809E-67,-1.18789542670764E-48,
-1.));
#41050=DIRECTION('ref_axis',(0.,1.,0.));
#41051=DIRECTION('center_axis',(0.610311034750668,-0.792161870921744,0.000105448241406271));
#41052=DIRECTION('ref_axis',(0.79210350861157,0.610264443525473,-0.0122204997355093));
#41053=DIRECTION('center_axis',(0.106504839483129,0.994312179825443,9.06501467375791E-5));
#41054=DIRECTION('ref_axis',(0.994208025038601,-0.106492362571754,-0.0144837723929676));
#41055=DIRECTION('center_axis',(5.15167520928809E-67,-1.18789542670764E-48,
-1.));
#41056=DIRECTION('ref_axis',(-4.33680868994202E-19,1.,-1.18789542670764E-48));
#41057=DIRECTION('center_axis',(5.15167520928809E-67,-1.18789542670764E-48,
-1.));
#41058=DIRECTION('ref_axis',(0.,1.,0.));
#41059=DIRECTION('center_axis',(0.670581953563674,-0.741835448354548,0.000105448247759945));
#41060=DIRECTION('ref_axis',(0.741780921486581,0.670530926932748,-0.0122204969305506));
#41061=DIRECTION('center_axis',(0.0281636861069903,0.999603320606438,9.06501466992701E-5));
#41062=DIRECTION('ref_axis',(0.999498507967367,-0.0281594195481785,-0.0144837723579484));
#41063=DIRECTION('center_axis',(5.15167520928809E-67,-1.18789542670764E-48,
-1.));
#41064=DIRECTION('ref_axis',(-4.33680868994202E-19,1.,-1.18789542670764E-48));
#41065=DIRECTION('center_axis',(5.15167520928809E-67,-1.18789542670764E-48,
-1.));
#41066=DIRECTION('ref_axis',(0.,1.,0.));
#41067=DIRECTION('center_axis',(0.726718511653026,-0.6869353635543,0.000105448247761845));
#41068=DIRECTION('ref_axis',(0.686885008277897,0.726663364191536,-0.0122204969175564));
#41069=DIRECTION('center_axis',(-0.0503511057596336,0.99873157451406,9.06501467774672E-5));
#41070=DIRECTION('ref_axis',(0.998626750226755,0.0503471356611751,-0.0144837723768601));
#41071=DIRECTION('center_axis',(5.15167520928809E-67,-1.18789542670764E-48,
-1.));
#41072=DIRECTION('ref_axis',(-4.33680868994202E-19,1.,-1.18789542670764E-48));
#41073=DIRECTION('center_axis',(5.15167520928809E-67,-1.18789542670764E-48,
-1.));
#41074=DIRECTION('ref_axis',(0.,1.,0.));
#41075=DIRECTION('center_axis',(0.778374608459656,-0.627800093808486,0.000105448247696036));
#41076=DIRECTION('ref_axis',(0.627754220580537,0.778315680169911,-0.0122204969200215));
#41077=DIRECTION('center_axis',(-0.128555466315276,0.991702316152893,9.06501466266556E-5));
#41078=DIRECTION('ref_axis',(0.991598126493641,0.128543284036441,-0.0144837724170315));
#41079=DIRECTION('center_axis',(5.15167520928809E-67,-1.18789542670764E-48,
-1.));
#41080=DIRECTION('ref_axis',(-4.33680868994202E-19,1.,-1.18789542670764E-48));
#41081=DIRECTION('center_axis',(5.15167520928809E-67,-1.18789542670764E-48,
-1.));
#41082=DIRECTION('ref_axis',(0.,1.,0.));
#41083=DIRECTION('center_axis',(0.825231766969182,-0.564794227719785,0.000105448247768853));
#41084=DIRECTION('ref_axis',(0.564753119363901,0.825169421163535,-0.0122204969367096));
#41085=DIRECTION('center_axis',(-0.205967239672835,0.978558883238052,9.06501467925213E-5));
#41086=DIRECTION('ref_axis',(0.978455970572528,0.205946920321698,-0.0144837723325158));
#41087=DIRECTION('center_axis',(5.15167520928809E-67,-1.18789542670764E-48,
-1.));
#41088=DIRECTION('ref_axis',(-4.33680868994202E-19,1.,-1.18789542670764E-48));
#41089=DIRECTION('center_axis',(5.15167520928809E-67,-1.18789542670764E-48,
-1.));
#41090=DIRECTION('ref_axis',(0.,1.,0.));
#41091=DIRECTION('center_axis',(0.867001097218019,-0.498306217403936,0.000105448247742928));
#41092=DIRECTION('ref_axis',(0.498270127367224,0.866935718279781,-0.0122204968872419));
#41093=DIRECTION('center_axis',(-0.282109156506148,0.959382309404307,9.06501467249393E-5));
#41094=DIRECTION('ref_axis',(0.959281308221143,0.282080825357837,-0.0144837724013445));
#41095=DIRECTION('center_axis',(5.15167520928809E-67,-1.18789542670764E-48,
-1.));
#41096=DIRECTION('ref_axis',(-4.33680868994202E-19,1.,-1.18789542670764E-48));
#41097=DIRECTION('center_axis',(5.15167520928809E-67,-1.18789542670764E-48,
-1.));
#41098=DIRECTION('ref_axis',(0.,1.,0.));
#41099=DIRECTION('center_axis',(0.903425077395463,-0.428745983553979,0.000105448247628158));
#41100=DIRECTION('ref_axis',(0.428715134343002,0.903357068406648,-0.0122204969215573));
#41101=DIRECTION('center_axis',(-0.356511776579108,0.934290824606,9.06501467950618E-5));
#41102=DIRECTION('ref_axis',(0.934192357613078,0.356475608305158,-0.0144837723258434));
#41103=DIRECTION('center_axis',(5.15167520928809E-67,-1.18789542670764E-48,
-1.));
#41104=DIRECTION('ref_axis',(-4.33680868994202E-19,1.,-1.18789542670764E-48));
#41105=DIRECTION('center_axis',(5.15167520928809E-67,-1.18789542670764E-48,
-1.));
#41106=DIRECTION('ref_axis',(0.,1.,0.));
#41107=DIRECTION('center_axis',(0.93427914155167,-0.356542388142199,0.000105448247170392));
#41108=DIRECTION('ref_axis',(0.356516969951772,0.934208921807903,-0.012220497163456));
#41109=DIRECTION('center_axis',(-0.428716382997142,0.903439126190801,9.06501468381065E-5));
#41110=DIRECTION('ref_axis',(0.903343800468038,0.42867260058632,-0.0144837723857595));
#41111=DIRECTION('center_axis',(5.15167520928809E-67,-1.18789542670764E-48,
-1.));
#41112=DIRECTION('ref_axis',(-4.33680868994202E-19,1.,-1.18789542670764E-48));
#41113=DIRECTION('center_axis',(5.15167520928809E-67,-1.18789542670764E-48,
-1.));
#41114=DIRECTION('ref_axis',(0.,1.,0.));
#41115=DIRECTION('center_axis',(0.959373064120116,-0.282140590347164,0.000105448247729292));
#41116=DIRECTION('ref_axis',(0.282120759890968,0.959301066555056,-0.0122204969160199));
#41117=DIRECTION('center_axis',(-0.498277810351142,0.867017425138747,9.06501467342992E-5));
#41118=DIRECTION('ref_axis',(0.866925828401964,0.498226683737,-0.0144837723677419));
#41119=DIRECTION('center_axis',(5.15167520928809E-67,-1.18789542670764E-48,
-1.));
#41120=DIRECTION('ref_axis',(-4.33680868994202E-19,1.,-1.18789542670764E-48));
#41121=DIRECTION('center_axis',(5.15167520928809E-67,-1.18789542670764E-48,
-1.));
#41122=DIRECTION('ref_axis',(0.,1.,0.));
#41123=DIRECTION('center_axis',(0.978552132724802,-0.205999301990102,0.000105448247615573));
#41124=DIRECTION('ref_axis',(0.205985181528349,0.978478801224133,-0.0122204969505153));
#41125=DIRECTION('center_axis',(-0.564767189310334,0.825250273348065,9.0650146758551E-5));
#41126=DIRECTION('ref_axis',(0.82516297032109,0.564709033705155,-0.014483772390721));
#41127=DIRECTION('center_axis',(5.15167520928809E-67,-1.18789542670764E-48,
-1.));
#41128=DIRECTION('ref_axis',(-4.33680868994202E-19,1.,-1.18789542670764E-48));
#41129=DIRECTION('center_axis',(5.15167520928809E-67,-1.18789542670764E-48,
-1.));
#41130=DIRECTION('ref_axis',(0.,1.,0.));
#41131=DIRECTION('center_axis',(0.991698102030069,-0.128587959430995,0.000105448245943976));
#41132=DIRECTION('ref_axis',(0.128579636019992,0.99162388869792,-0.0122204977223251));
#41133=DIRECTION('center_axis',(-0.627774590743336,0.778395179198579,9.06501467764949E-5));
#41134=DIRECTION('ref_axis',(0.778312708134504,0.627709764696415,-0.014483772336843));
#41135=DIRECTION('center_axis',(5.15167520928809E-67,-1.18789542670764E-48,
-1.));
#41136=DIRECTION('ref_axis',(-4.33680868994202E-19,1.,-1.18789542670764E-48));
#41137=DIRECTION('center_axis',(5.15167520928809E-67,-1.18789542670764E-48,
-1.));
#41138=DIRECTION('ref_axis',(0.,1.,0.));
#41139=DIRECTION('center_axis',(0.998729922762269,-0.0503838293497056,0.000105448247690158));
#41140=DIRECTION('ref_axis',(0.0503813543083624,0.998655285167543,-0.0122204969206726));
#41141=DIRECTION('center_axis',(-0.686911553068082,0.726741019926732,9.065014676939E-5));
#41142=DIRECTION('ref_axis',(0.726663889285701,0.686840456252424,-0.0144837724071123));
#41143=DIRECTION('center_axis',(5.15167520928809E-67,-1.18789542670764E-48,
-1.));
#41144=DIRECTION('ref_axis',(-4.33680868994202E-19,1.,-1.18789542670764E-48));
#41145=DIRECTION('center_axis',(5.15167520928809E-67,-1.18789542670764E-48,
-1.));
#41146=DIRECTION('ref_axis',(0.,1.,0.));
#41147=DIRECTION('center_axis',(0.999604241409737,0.0281309337977193,0.000105448247673278));
#41148=DIRECTION('ref_axis',(0.0281275452111183,-0.999529639707527,0.0122204969841135));
#41149=DIRECTION('center_axis',(-0.741813477246845,0.670606260601179,9.06501467534462E-5));
#41150=DIRECTION('ref_axis',(0.670534945920493,0.741736547999089,-0.0144837723606804));
#41151=DIRECTION('center_axis',(5.15167520928809E-67,-1.18789542670764E-48,
-1.));
#41152=DIRECTION('ref_axis',(-4.33680868994202E-19,1.,-1.18789542670764E-48));
#41153=DIRECTION('center_axis',(5.15167520928809E-67,-1.18789542670764E-48,
-1.));
#41154=DIRECTION('ref_axis',(0.,1.,0.));
#41155=DIRECTION('center_axis',(0.994315667506773,0.106472260383761,0.000105448247684943));
#41156=DIRECTION('ref_axis',(0.106463029060952,-0.994241561642206,0.0122204969798675));
#41157=DIRECTION('center_axis',(-0.792141874660476,0.610336990679688,9.06501468075157E-5));
#41158=DIRECTION('ref_axis',(0.610271931637649,0.792059587274653,-0.0144837723525293));
#41159=DIRECTION('center_axis',(5.15167520928809E-67,-1.18789542670764E-48,
-1.));
#41160=DIRECTION('ref_axis',(-4.33680868994202E-19,1.,-1.18789542670764E-48));
#41161=DIRECTION('center_axis',(5.15167520928809E-67,-1.18789542670764E-48,
-1.));
#41162=DIRECTION('ref_axis',(0.,1.,0.));
#41163=DIRECTION('center_axis',(0.982896806870138,0.184157150078822,0.000105448247739781));
#41164=DIRECTION('ref_axis',(0.184142132934029,-0.982823653730722,0.0122204969580191));
#41165=DIRECTION('center_axis',(-0.837586454002804,0.546304790253169,9.06501467452083E-5));
#41166=DIRECTION('ref_axis',(0.546246387960594,0.837499315808325,-0.0144837723191043));
#41167=DIRECTION('center_axis',(5.15167520928809E-67,-1.18789542670764E-48,
-1.));
#41168=DIRECTION('ref_axis',(-4.33680868994202E-19,1.,-1.18789542670764E-48));
#41169=DIRECTION('center_axis',(5.15167520928809E-67,-1.18789542670764E-48,
-1.));
#41170=DIRECTION('ref_axis',(0.,1.,0.));
#41171=DIRECTION('center_axis',(-0.778395179198544,-0.62777459074338,9.06501468008605E-5));
#41172=DIRECTION('ref_axis',(0.62770976469586,-0.778312708133716,0.0144837724032618));
#41173=DIRECTION('center_axis',(5.15167520928809E-67,-1.18789542670764E-48,
-1.));
#41174=DIRECTION('ref_axis',(-4.33680868994202E-19,1.,-1.18789542670764E-48));
#41175=DIRECTION('center_axis',(0.128587959434843,0.991698102029569,0.000105448247713068));
#41176=DIRECTION('ref_axis',(0.991623888707174,-0.128579636025041,0.0122204969182792));
#41177=DIRECTION('center_axis',(5.15167520928809E-67,-1.18789542670764E-48,
-1.));
#41178=DIRECTION('ref_axis',(0.,1.,0.));
#41179=DIRECTION('center_axis',(-0.82525027334801,-0.564767189310415,9.06501467887519E-5));
#41180=DIRECTION('ref_axis',(0.56470903370554,-0.825162970321483,0.0144837723533119));
#41181=DIRECTION('center_axis',(5.15167520928809E-67,-1.18789542670764E-48,
-1.));
#41182=DIRECTION('ref_axis',(-4.33680868994202E-19,1.,-1.18789542670764E-48));
#41183=DIRECTION('center_axis',(0.205999301990312,0.978552132724757,0.000105448247717959));
#41184=DIRECTION('ref_axis',(0.978478801224664,-0.205985181528676,0.0122204969024898));
#41185=DIRECTION('center_axis',(5.15167520928809E-67,-1.18789542670764E-48,
-1.));
#41186=DIRECTION('ref_axis',(0.,1.,0.));
#41187=DIRECTION('center_axis',(-0.867017425138643,-0.498277810351323,9.06501468256068E-5));
#41188=DIRECTION('ref_axis',(0.498226683737087,-0.866925828401692,0.014483772381015));
#41189=DIRECTION('center_axis',(5.15167520928809E-67,-1.18789542670764E-48,
-1.));
#41190=DIRECTION('ref_axis',(-4.33680868994202E-19,1.,-1.18789542670764E-48));
#41191=DIRECTION('center_axis',(0.282140590347035,0.959373064120154,0.000105448247634384));
#41192=DIRECTION('ref_axis',(0.959301066555324,-0.282120759890904,0.0122204968965099));
#41193=DIRECTION('center_axis',(5.15167520928809E-67,-1.18789542670764E-48,
-1.));
#41194=DIRECTION('ref_axis',(0.,1.,0.));
#41195=DIRECTION('center_axis',(-0.903439126190879,-0.428716382996979,9.06501467301661E-5));
#41196=DIRECTION('ref_axis',(0.428672600586422,-0.903343800468688,0.0144837723422516));
#41197=DIRECTION('center_axis',(5.15167520928809E-67,-1.18789542670764E-48,
-1.));
#41198=DIRECTION('ref_axis',(-4.33680868994202E-19,1.,-1.18789542670764E-48));
#41199=DIRECTION('center_axis',(0.356542388143256,0.934279141551266,0.000105448247681697));
#41200=DIRECTION('ref_axis',(0.934208921810558,-0.356516969953973,0.0122204968962765));
#41201=DIRECTION('center_axis',(5.15167520928809E-67,-1.18789542670764E-48,
-1.));
#41202=DIRECTION('ref_axis',(0.,1.,0.));
#41203=DIRECTION('center_axis',(-0.934290824606111,-0.356511776578816,9.06501466618288E-5));
#41204=DIRECTION('ref_axis',(0.356475608304419,-0.934192357612002,0.0144837724134131));
#41205=DIRECTION('center_axis',(5.15167520928809E-67,-1.18789542670764E-48,
-1.));
#41206=DIRECTION('ref_axis',(-4.33680868994202E-19,1.,-1.18789542670764E-48));
#41207=DIRECTION('center_axis',(0.428745983554273,0.903425077395324,0.000105448247749283));
#41208=DIRECTION('ref_axis',(0.903357068406257,-0.428715134343181,0.0122204969441668));
#41209=DIRECTION('center_axis',(5.15167520928809E-67,-1.18789542670764E-48,
-1.));
#41210=DIRECTION('ref_axis',(0.,1.,0.));
#41211=DIRECTION('center_axis',(-0.959382309404256,-0.282109156506322,9.06501468215648E-5));
#41212=DIRECTION('ref_axis',(0.282080825358184,-0.959281308221691,0.0144837723582998));
#41213=DIRECTION('center_axis',(5.15167520928809E-67,-1.18789542670764E-48,
-1.));
#41214=DIRECTION('ref_axis',(-4.33680868994202E-19,1.,-1.18789542670764E-48));
#41215=DIRECTION('center_axis',(0.498306217397306,0.86700109722183,0.000105448244261109));
#41216=DIRECTION('ref_axis',(0.866935718266673,-0.498270127351015,0.0122204984779969));
#41217=DIRECTION('center_axis',(5.15167520928809E-67,-1.18789542670764E-48,
-1.));
#41218=DIRECTION('ref_axis',(0.,1.,0.));
#41219=DIRECTION('center_axis',(-0.978558883238081,-0.205967239672699,9.06501467769327E-5));
#41220=DIRECTION('ref_axis',(0.205946920321355,-0.978455970571544,0.0144837724038677));
#41221=DIRECTION('center_axis',(5.15167520928809E-67,-1.18789542670764E-48,
-1.));
#41222=DIRECTION('ref_axis',(-4.33680868994202E-19,1.,-1.18789542670764E-48));
#41223=DIRECTION('center_axis',(0.564794227718686,0.825231766969935,0.000105448247134299));
#41224=DIRECTION('ref_axis',(0.825169421162366,-0.564753119361502,0.0122204971264834));
#41225=DIRECTION('center_axis',(5.15167520928809E-67,-1.18789542670764E-48,
-1.));
#41226=DIRECTION('ref_axis',(0.,1.,0.));
#41227=DIRECTION('center_axis',(-0.991702316152861,-0.128555466315523,9.06501467288715E-5));
#41228=DIRECTION('ref_axis',(0.12854328403675,-0.991598126494102,0.0144837723826971));
#41229=DIRECTION('center_axis',(5.15167520928809E-67,-1.18789542670764E-48,
-1.));
#41230=DIRECTION('ref_axis',(-4.33680868994202E-19,1.,-1.18789542670764E-48));
#41231=DIRECTION('center_axis',(0.627800093808552,0.778374608459603,0.000105448247728723));
#41232=DIRECTION('ref_axis',(0.778315680170199,-0.627754220580874,0.0122204968843025));
#41233=DIRECTION('center_axis',(5.15167520928809E-67,-1.18789542670764E-48,
-1.));
#41234=DIRECTION('ref_axis',(0.,1.,0.));
#41235=DIRECTION('center_axis',(-0.998731574514058,-0.0503511057596628,
9.06501468007229E-5));
#41236=DIRECTION('ref_axis',(0.0503471356611987,-0.998626750226619,0.0144837723861814));
#41237=DIRECTION('center_axis',(5.15167520928809E-67,-1.18789542670764E-48,
-1.));
#41238=DIRECTION('ref_axis',(-4.33680868994202E-19,1.,-1.18789542670764E-48));
#41239=DIRECTION('center_axis',(0.686935363554282,0.726718511653043,0.000105448247718559));
#41240=DIRECTION('ref_axis',(0.726663364191442,-0.686885008277775,0.012220496930023));
#41241=DIRECTION('center_axis',(5.15167520928809E-67,-1.18789542670764E-48,
-1.));
#41242=DIRECTION('ref_axis',(0.,1.,0.));
#41243=DIRECTION('center_axis',(-0.99960332060644,0.0281636861069471,9.06501467308329E-5));
#41244=DIRECTION('ref_axis',(0.0281594195481261,0.999498507967114,-0.0144837723754724));
#41245=DIRECTION('center_axis',(5.15167520928809E-67,-1.18789542670764E-48,
-1.));
#41246=DIRECTION('ref_axis',(-4.33680868994202E-19,1.,-1.18789542670764E-48));
#41247=DIRECTION('center_axis',(0.741835448354451,0.670581953563782,0.00010544824772104));
#41248=DIRECTION('ref_axis',(0.670530926933101,-0.74178092148675,0.0122204969008548));
#41249=DIRECTION('center_axis',(5.15167520928809E-67,-1.18789542670764E-48,
-1.));
#41250=DIRECTION('ref_axis',(0.,1.,0.));
#41251=DIRECTION('center_axis',(-0.994312179825441,0.106504839483146,9.06501467381912E-5));
#41252=DIRECTION('ref_axis',(0.106492362571802,0.99420802503887,-0.0144837723741357));
#41253=DIRECTION('center_axis',(5.15167520928809E-67,-1.18789542670764E-48,
-1.));
#41254=DIRECTION('ref_axis',(-4.33680868994202E-19,1.,-1.18789542670764E-48));
#41255=DIRECTION('center_axis',(0.792161870929241,0.610311034740936,0.000105448246928053));
#41256=DIRECTION('ref_axis',(0.610264443534212,-0.792103508642726,0.0122204972796185));
#41257=DIRECTION('center_axis',(5.15167520928809E-67,-1.18789542670764E-48,
-1.));
#41258=DIRECTION('ref_axis',(0.,1.,0.));
#41259=DIRECTION('center_axis',(-0.982890773813477,0.184189355107443,9.06501467544422E-5));
#41260=DIRECTION('ref_axis',(0.184168744767819,0.982787919028209,-0.0144837723970302));
#41261=DIRECTION('center_axis',(5.15167520928809E-67,-1.18789542670764E-48,
-1.));
#41262=DIRECTION('ref_axis',(-4.33680868994202E-19,1.,-1.18789542670764E-48));
#41263=DIRECTION('center_axis',(0.837604352151223,0.546277345437276,0.000105448247675196));
#41264=DIRECTION('ref_axis',(0.546235476910048,-0.837542514275434,0.0122204969635834));
#41265=DIRECTION('center_axis',(5.15167520928809E-67,-1.18789542670764E-48,
-1.));
#41266=DIRECTION('ref_axis',(0.,1.,0.));
#41267=DIRECTION('center_axis',(-0.96540951933663,0.260738282108263,9.06501468112521E-5));
#41268=DIRECTION('ref_axis',(0.26070966540993,0.965308598686718,-0.0144837724135372));
#41269=DIRECTION('center_axis',(5.15167520928809E-67,-1.18789542670764E-48,
-1.));
#41270=DIRECTION('ref_axis',(-4.33680868994202E-19,1.,-1.18789542670764E-48));
#41271=DIRECTION('center_axis',(0.877882724009476,0.478875674644651,0.000105448247670176));
#41272=DIRECTION('ref_axis',(0.478838786927941,-0.877817791792444,0.0122204969627255));
#41273=DIRECTION('center_axis',(5.15167520928809E-67,-1.18789542670764E-48,
-1.));
#41274=DIRECTION('ref_axis',(0.,1.,0.));
#41275=DIRECTION('center_axis',(-0.941976194141744,0.33567967089591,9.06501467361574E-5));
#41276=DIRECTION('ref_axis',(0.335643224270696,0.941877829837669,-0.0144837723488913));
#41277=DIRECTION('center_axis',(5.15167520928809E-67,-1.18789542670764E-48,
-1.));
#41278=DIRECTION('ref_axis',(-4.33680868994202E-19,1.,-1.18789542670764E-48));
#41279=DIRECTION('center_axis',(0.912748656948457,0.408521576075799,0.000105448247549386));
#41280=DIRECTION('ref_axis',(0.408489896594413,-0.912681030718381,0.0122204970078645));
#41281=DIRECTION('center_axis',(5.15167520928809E-67,-1.18789542670764E-48,
-1.));
#41282=DIRECTION('ref_axis',(0.,1.,0.));
#41283=DIRECTION('center_axis',(0.965418060567994,0.260706649723021,0.000105448239440975));
#41284=DIRECTION('ref_axis',(0.260685939330027,-0.965346311123993,0.0122205006002244));
#41285=DIRECTION('center_axis',(-0.877867034330543,0.478904439129822,9.06501467527618E-5));
#41286=DIRECTION('ref_axis',(0.478853053655558,0.877775582562237,-0.014483772377146));
#41287=DIRECTION('center_axis',(5.15167520928809E-67,-1.18789542670764E-48,
-1.));
#41288=DIRECTION('ref_axis',(-4.33680868994202E-19,1.,-1.18789542670764E-48));
#41289=DIRECTION('center_axis',(5.15167520928809E-67,-1.18789542670764E-48,
-1.));
#41290=DIRECTION('ref_axis',(-4.33680868994202E-19,1.,-1.18789542670764E-48));
#41291=DIRECTION('',(5.15167520928809E-67,-1.18789542670764E-48,-1.));
#41292=DIRECTION('center_axis',(5.15167520928809E-67,-1.18789542670764E-48,
-1.));
#41293=DIRECTION('ref_axis',(-4.33680868994202E-19,1.,-1.18789542670764E-48));
#41294=DIRECTION('',(-5.15167520928809E-67,1.18789542670764E-48,1.));
#41295=DIRECTION('center_axis',(5.15167520928809E-67,-1.18789542670764E-48,
-1.));
#41296=DIRECTION('ref_axis',(-4.33680868994202E-19,1.,-1.18789542670764E-48));
#41297=DIRECTION('',(-5.15167520928809E-67,1.18789542670764E-48,1.));
#41298=DIRECTION('',(5.15167520928809E-67,-1.18789542670764E-48,-1.));
#41299=DIRECTION('center_axis',(5.15167520928809E-67,-1.18789542670764E-48,
-1.));
#41300=DIRECTION('ref_axis',(-4.33680868994202E-19,1.,-1.18789542670764E-48));
#41301=DIRECTION('center_axis',(5.15167520928809E-67,-1.18789542670764E-48,
-1.));
#41302=DIRECTION('ref_axis',(-4.33680868994202E-19,1.,-1.18789542670764E-48));
#41303=DIRECTION('',(-5.15167520928809E-67,1.18789542670764E-48,1.));
#41304=DIRECTION('',(5.15167520928809E-67,-1.18789542670764E-48,-1.));
#41305=DIRECTION('center_axis',(5.15167520928809E-67,-1.18789542670764E-48,
-1.));
#41306=DIRECTION('ref_axis',(-4.33680868994202E-19,1.,-1.18789542670764E-48));
#41307=DIRECTION('center_axis',(5.15167520928809E-67,-1.18789542670764E-48,
-1.));
#41308=DIRECTION('ref_axis',(-4.33680868994202E-19,1.,-1.18789542670764E-48));
#41309=DIRECTION('',(-5.15167520928809E-67,1.18789542670764E-48,1.));
#41310=DIRECTION('',(5.15167520928809E-67,-1.18789542670764E-48,-1.));
#41311=DIRECTION('center_axis',(5.15167520928809E-67,-1.18789542670764E-48,
-1.));
#41312=DIRECTION('ref_axis',(-4.33680868994202E-19,1.,-1.18789542670764E-48));
#41313=DIRECTION('center_axis',(5.15167520928809E-67,-1.18789542670764E-48,
-1.));
#41314=DIRECTION('ref_axis',(-4.33680868994202E-19,1.,-1.18789542670764E-48));
#41315=DIRECTION('',(-5.15167520928809E-67,1.18789542670764E-48,1.));
#41316=DIRECTION('',(5.15167520928809E-67,-1.18789542670764E-48,-1.));
#41317=DIRECTION('center_axis',(5.15167520928809E-67,-1.18789542670764E-48,
-1.));
#41318=DIRECTION('ref_axis',(-4.33680868994202E-19,1.,-1.18789542670764E-48));
#41319=DIRECTION('center_axis',(5.15167520928809E-67,-1.18789542670764E-48,
-1.));
#41320=DIRECTION('ref_axis',(-4.33680868994202E-19,1.,-1.18789542670764E-48));
#41321=DIRECTION('',(-5.15167520928809E-67,1.18789542670764E-48,1.));
#41322=DIRECTION('',(5.15167520928809E-67,-1.18789542670764E-48,-1.));
#41323=DIRECTION('center_axis',(5.15167520928809E-67,-1.18789542670764E-48,
-1.));
#41324=DIRECTION('ref_axis',(-4.33680868994202E-19,1.,-1.18789542670764E-48));
#41325=DIRECTION('center_axis',(5.15167520928809E-67,-1.18789542670764E-48,
-1.));
#41326=DIRECTION('ref_axis',(-4.33680868994202E-19,1.,-1.18789542670764E-48));
#41327=DIRECTION('',(-5.15167520928809E-67,1.18789542670764E-48,1.));
#41328=DIRECTION('',(5.15167520928809E-67,-1.18789542670764E-48,-1.));
#41329=DIRECTION('center_axis',(5.15167520928809E-67,-1.18789542670764E-48,
-1.));
#41330=DIRECTION('ref_axis',(-4.33680868994202E-19,1.,-1.18789542670764E-48));
#41331=DIRECTION('center_axis',(5.15167520928809E-67,-1.18789542670764E-48,
-1.));
#41332=DIRECTION('ref_axis',(-4.33680868994202E-19,1.,-1.18789542670764E-48));
#41333=DIRECTION('',(-5.15167520928809E-67,1.18789542670764E-48,1.));
#41334=DIRECTION('',(5.15167520928809E-67,-1.18789542670764E-48,-1.));
#41335=DIRECTION('center_axis',(5.15167520928809E-67,-1.18789542670764E-48,
-1.));
#41336=DIRECTION('ref_axis',(-4.33680868994202E-19,1.,-1.18789542670764E-48));
#41337=DIRECTION('center_axis',(5.15167520928809E-67,-1.18789542670764E-48,
-1.));
#41338=DIRECTION('ref_axis',(-4.33680868994202E-19,1.,-1.18789542670764E-48));
#41339=DIRECTION('',(-5.15167520928809E-67,1.18789542670764E-48,1.));
#41340=DIRECTION('',(5.15167520928809E-67,-1.18789542670764E-48,-1.));
#41341=DIRECTION('center_axis',(5.15167520928809E-67,-1.18789542670764E-48,
-1.));
#41342=DIRECTION('ref_axis',(-4.33680868994202E-19,1.,-1.18789542670764E-48));
#41343=DIRECTION('center_axis',(5.15167520928809E-67,-1.18789542670764E-48,
-1.));
#41344=DIRECTION('ref_axis',(-4.33680868994202E-19,1.,-1.18789542670764E-48));
#41345=DIRECTION('',(-5.15167520928809E-67,1.18789542670764E-48,1.));
#41346=DIRECTION('',(5.15167520928809E-67,-1.18789542670764E-48,-1.));
#41347=DIRECTION('center_axis',(5.15167520928809E-67,-1.18789542670764E-48,
-1.));
#41348=DIRECTION('ref_axis',(-4.33680868994202E-19,1.,-1.18789542670764E-48));
#41349=DIRECTION('center_axis',(5.15167520928809E-67,-1.18789542670764E-48,
-1.));
#41350=DIRECTION('ref_axis',(-4.33680868994202E-19,1.,-1.18789542670764E-48));
#41351=DIRECTION('',(-5.15167520928809E-67,1.18789542670764E-48,1.));
#41352=DIRECTION('',(5.15167520928809E-67,-1.18789542670764E-48,-1.));
#41353=DIRECTION('center_axis',(5.15167520928809E-67,-1.18789542670764E-48,
-1.));
#41354=DIRECTION('ref_axis',(-4.33680868994202E-19,1.,-1.18789542670764E-48));
#41355=DIRECTION('center_axis',(5.15167520928809E-67,-1.18789542670764E-48,
-1.));
#41356=DIRECTION('ref_axis',(-4.33680868994202E-19,1.,-1.18789542670764E-48));
#41357=DIRECTION('',(-5.15167520928809E-67,1.18789542670764E-48,1.));
#41358=DIRECTION('',(5.15167520928809E-67,-1.18789542670764E-48,-1.));
#41359=DIRECTION('center_axis',(5.15167520928809E-67,-1.18789542670764E-48,
-1.));
#41360=DIRECTION('ref_axis',(-4.33680868994202E-19,1.,-1.18789542670764E-48));
#41361=DIRECTION('center_axis',(5.15167520928809E-67,-1.18789542670764E-48,
-1.));
#41362=DIRECTION('ref_axis',(-4.33680868994202E-19,1.,-1.18789542670764E-48));
#41363=DIRECTION('',(-5.15167520928809E-67,1.18789542670764E-48,1.));
#41364=DIRECTION('',(5.15167520928809E-67,-1.18789542670764E-48,-1.));
#41365=DIRECTION('center_axis',(5.15167520928809E-67,-1.18789542670764E-48,
-1.));
#41366=DIRECTION('ref_axis',(-4.33680868994202E-19,1.,-1.18789542670764E-48));
#41367=DIRECTION('center_axis',(5.15167520928809E-67,-1.18789542670764E-48,
-1.));
#41368=DIRECTION('ref_axis',(-4.33680868994202E-19,1.,-1.18789542670764E-48));
#41369=DIRECTION('',(-5.15167520928809E-67,1.18789542670764E-48,1.));
#41370=DIRECTION('',(5.15167520928809E-67,-1.18789542670764E-48,-1.));
#41371=DIRECTION('center_axis',(5.15167520928809E-67,-1.18789542670764E-48,
-1.));
#41372=DIRECTION('ref_axis',(-4.33680868994202E-19,1.,-1.18789542670764E-48));
#41373=DIRECTION('center_axis',(5.15167520928809E-67,-1.18789542670764E-48,
-1.));
#41374=DIRECTION('ref_axis',(-4.33680868994202E-19,1.,-1.18789542670764E-48));
#41375=DIRECTION('',(-5.15167520928809E-67,1.18789542670764E-48,1.));
#41376=DIRECTION('',(5.15167520928809E-67,-1.18789542670764E-48,-1.));
#41377=DIRECTION('center_axis',(5.15167520928809E-67,-1.18789542670764E-48,
-1.));
#41378=DIRECTION('ref_axis',(-4.33680868994202E-19,1.,-1.18789542670764E-48));
#41379=DIRECTION('center_axis',(5.15167520928809E-67,-1.18789542670764E-48,
-1.));
#41380=DIRECTION('ref_axis',(-4.33680868994202E-19,1.,-1.18789542670764E-48));
#41381=DIRECTION('',(-5.15167520928809E-67,1.18789542670764E-48,1.));
#41382=DIRECTION('',(5.15167520928809E-67,-1.18789542670764E-48,-1.));
#41383=DIRECTION('center_axis',(5.15167520928809E-67,-1.18789542670764E-48,
-1.));
#41384=DIRECTION('ref_axis',(-4.33680868994202E-19,1.,-1.18789542670764E-48));
#41385=DIRECTION('center_axis',(5.15167520928809E-67,-1.18789542670764E-48,
-1.));
#41386=DIRECTION('ref_axis',(-4.33680868994202E-19,1.,-1.18789542670764E-48));
#41387=DIRECTION('',(-5.15167520928809E-67,1.18789542670764E-48,1.));
#41388=DIRECTION('',(5.15167520928809E-67,-1.18789542670764E-48,-1.));
#41389=DIRECTION('center_axis',(5.15167520928809E-67,-1.18789542670764E-48,
-1.));
#41390=DIRECTION('ref_axis',(-4.33680868994202E-19,1.,-1.18789542670764E-48));
#41391=DIRECTION('center_axis',(5.15167520928809E-67,-1.18789542670764E-48,
-1.));
#41392=DIRECTION('ref_axis',(-4.33680868994202E-19,1.,-1.18789542670764E-48));
#41393=DIRECTION('',(-5.15167520928809E-67,1.18789542670764E-48,1.));
#41394=DIRECTION('',(5.15167520928809E-67,-1.18789542670764E-48,-1.));
#41395=DIRECTION('center_axis',(5.15167520928809E-67,-1.18789542670764E-48,
-1.));
#41396=DIRECTION('ref_axis',(-4.33680868994202E-19,1.,-1.18789542670764E-48));
#41397=DIRECTION('center_axis',(5.15167520928809E-67,-1.18789542670764E-48,
-1.));
#41398=DIRECTION('ref_axis',(-4.33680868994202E-19,1.,-1.18789542670764E-48));
#41399=DIRECTION('',(-5.15167520928809E-67,1.18789542670764E-48,1.));
#41400=DIRECTION('',(5.15167520928809E-67,-1.18789542670764E-48,-1.));
#41401=DIRECTION('center_axis',(5.15167520928809E-67,-1.18789542670764E-48,
-1.));
#41402=DIRECTION('ref_axis',(-4.33680868994202E-19,1.,-1.18789542670764E-48));
#41403=DIRECTION('center_axis',(5.15167520928809E-67,-1.18789542670764E-48,
-1.));
#41404=DIRECTION('ref_axis',(-4.33680868994202E-19,1.,-1.18789542670764E-48));
#41405=DIRECTION('',(-5.15167520928809E-67,1.18789542670764E-48,1.));
#41406=DIRECTION('',(5.15167520928809E-67,-1.18789542670764E-48,-1.));
#41407=DIRECTION('center_axis',(5.15167520928809E-67,-1.18789542670764E-48,
-1.));
#41408=DIRECTION('ref_axis',(-4.33680868994202E-19,1.,-1.18789542670764E-48));
#41409=DIRECTION('center_axis',(5.15167520928809E-67,-1.18789542670764E-48,
-1.));
#41410=DIRECTION('ref_axis',(-4.33680868994202E-19,1.,-1.18789542670764E-48));
#41411=DIRECTION('',(-5.15167520928809E-67,1.18789542670764E-48,1.));
#41412=DIRECTION('',(5.15167520928809E-67,-1.18789542670764E-48,-1.));
#41413=DIRECTION('center_axis',(5.15167520928809E-67,-1.18789542670764E-48,
-1.));
#41414=DIRECTION('ref_axis',(-4.33680868994202E-19,1.,-1.18789542670764E-48));
#41415=DIRECTION('center_axis',(5.15167520928809E-67,-1.18789542670764E-48,
-1.));
#41416=DIRECTION('ref_axis',(-4.33680868994202E-19,1.,-1.18789542670764E-48));
#41417=DIRECTION('',(-5.15167520928809E-67,1.18789542670764E-48,1.));
#41418=DIRECTION('',(5.15167520928809E-67,-1.18789542670764E-48,-1.));
#41419=DIRECTION('center_axis',(5.15167520928809E-67,-1.18789542670764E-48,
-1.));
#41420=DIRECTION('ref_axis',(-4.33680868994202E-19,1.,-1.18789542670764E-48));
#41421=DIRECTION('center_axis',(5.15167520928809E-67,-1.18789542670764E-48,
-1.));
#41422=DIRECTION('ref_axis',(-4.33680868994202E-19,1.,-1.18789542670764E-48));
#41423=DIRECTION('',(-5.15167520928809E-67,1.18789542670764E-48,1.));
#41424=DIRECTION('',(5.15167520928809E-67,-1.18789542670764E-48,-1.));
#41425=DIRECTION('center_axis',(5.15167520928809E-67,-1.18789542670764E-48,
-1.));
#41426=DIRECTION('ref_axis',(-4.33680868994202E-19,1.,-1.18789542670764E-48));
#41427=DIRECTION('center_axis',(5.15167520928809E-67,-1.18789542670764E-48,
-1.));
#41428=DIRECTION('ref_axis',(-4.33680868994202E-19,1.,-1.18789542670764E-48));
#41429=DIRECTION('',(-5.15167520928809E-67,1.18789542670764E-48,1.));
#41430=DIRECTION('',(5.15167520928809E-67,-1.18789542670764E-48,-1.));
#41431=DIRECTION('center_axis',(5.15167520928809E-67,-1.18789542670764E-48,
-1.));
#41432=DIRECTION('ref_axis',(-4.33680868994202E-19,1.,-1.18789542670764E-48));
#41433=DIRECTION('center_axis',(5.15167520928809E-67,-1.18789542670764E-48,
-1.));
#41434=DIRECTION('ref_axis',(-4.33680868994202E-19,1.,-1.18789542670764E-48));
#41435=DIRECTION('',(-5.15167520928809E-67,1.18789542670764E-48,1.));
#41436=DIRECTION('',(5.15167520928809E-67,-1.18789542670764E-48,-1.));
#41437=DIRECTION('center_axis',(5.15167520928809E-67,-1.18789542670764E-48,
-1.));
#41438=DIRECTION('ref_axis',(-4.33680868994202E-19,1.,-1.18789542670764E-48));
#41439=DIRECTION('center_axis',(5.15167520928809E-67,-1.18789542670764E-48,
-1.));
#41440=DIRECTION('ref_axis',(-4.33680868994202E-19,1.,-1.18789542670764E-48));
#41441=DIRECTION('',(-5.15167520928809E-67,1.18789542670764E-48,1.));
#41442=DIRECTION('',(5.15167520928809E-67,-1.18789542670764E-48,-1.));
#41443=DIRECTION('center_axis',(5.15167520928809E-67,-1.18789542670764E-48,
-1.));
#41444=DIRECTION('ref_axis',(-4.33680868994202E-19,1.,-1.18789542670764E-48));
#41445=DIRECTION('center_axis',(5.15167520928809E-67,-1.18789542670764E-48,
-1.));
#41446=DIRECTION('ref_axis',(-4.33680868994202E-19,1.,-1.18789542670764E-48));
#41447=DIRECTION('',(-5.15167520928809E-67,1.18789542670764E-48,1.));
#41448=DIRECTION('',(5.15167520928809E-67,-1.18789542670764E-48,-1.));
#41449=DIRECTION('center_axis',(5.15167520928809E-67,-1.18789542670764E-48,
-1.));
#41450=DIRECTION('ref_axis',(-4.33680868994202E-19,1.,-1.18789542670764E-48));
#41451=DIRECTION('center_axis',(5.15167520928809E-67,-1.18789542670764E-48,
-1.));
#41452=DIRECTION('ref_axis',(-4.33680868994202E-19,1.,-1.18789542670764E-48));
#41453=DIRECTION('',(-5.15167520928809E-67,1.18789542670764E-48,1.));
#41454=DIRECTION('',(5.15167520928809E-67,-1.18789542670764E-48,-1.));
#41455=DIRECTION('center_axis',(5.15167520928809E-67,-1.18789542670764E-48,
-1.));
#41456=DIRECTION('ref_axis',(-4.33680868994202E-19,1.,-1.18789542670764E-48));
#41457=DIRECTION('center_axis',(5.15167520928809E-67,-1.18789542670764E-48,
-1.));
#41458=DIRECTION('ref_axis',(-4.33680868994202E-19,1.,-1.18789542670764E-48));
#41459=DIRECTION('',(-5.15167520928809E-67,1.18789542670764E-48,1.));
#41460=DIRECTION('',(5.15167520928809E-67,-1.18789542670764E-48,-1.));
#41461=DIRECTION('center_axis',(5.15167520928809E-67,-1.18789542670764E-48,
-1.));
#41462=DIRECTION('ref_axis',(-4.33680868994202E-19,1.,-1.18789542670764E-48));
#41463=DIRECTION('center_axis',(5.15167520928809E-67,-1.18789542670764E-48,
-1.));
#41464=DIRECTION('ref_axis',(-4.33680868994202E-19,1.,-1.18789542670764E-48));
#41465=DIRECTION('',(-5.15167520928809E-67,1.18789542670764E-48,1.));
#41466=DIRECTION('',(5.15167520928809E-67,-1.18789542670764E-48,-1.));
#41467=DIRECTION('center_axis',(5.15167520928809E-67,-1.18789542670764E-48,
-1.));
#41468=DIRECTION('ref_axis',(-4.33680868994202E-19,1.,-1.18789542670764E-48));
#41469=DIRECTION('center_axis',(5.15167520928809E-67,-1.18789542670764E-48,
-1.));
#41470=DIRECTION('ref_axis',(-4.33680868994202E-19,1.,-1.18789542670764E-48));
#41471=DIRECTION('',(-5.15167520928809E-67,1.18789542670764E-48,1.));
#41472=DIRECTION('',(5.15167520928809E-67,-1.18789542670764E-48,-1.));
#41473=DIRECTION('center_axis',(5.15167520928809E-67,-1.18789542670764E-48,
-1.));
#41474=DIRECTION('ref_axis',(-4.33680868994202E-19,1.,-1.18789542670764E-48));
#41475=DIRECTION('center_axis',(5.15167520928809E-67,-1.18789542670764E-48,
-1.));
#41476=DIRECTION('ref_axis',(-4.33680868994202E-19,1.,-1.18789542670764E-48));
#41477=DIRECTION('',(-5.15167520928809E-67,1.18789542670764E-48,1.));
#41478=DIRECTION('',(5.15167520928809E-67,-1.18789542670764E-48,-1.));
#41479=DIRECTION('center_axis',(5.15167520928809E-67,-1.18789542670764E-48,
-1.));
#41480=DIRECTION('ref_axis',(-4.33680868994202E-19,1.,-1.18789542670764E-48));
#41481=DIRECTION('center_axis',(5.15167520928809E-67,-1.18789542670764E-48,
-1.));
#41482=DIRECTION('ref_axis',(-4.33680868994202E-19,1.,-1.18789542670764E-48));
#41483=DIRECTION('',(-5.15167520928809E-67,1.18789542670764E-48,1.));
#41484=DIRECTION('',(5.15167520928809E-67,-1.18789542670764E-48,-1.));
#41485=DIRECTION('center_axis',(5.15167520928809E-67,-1.18789542670764E-48,
-1.));
#41486=DIRECTION('ref_axis',(-4.33680868994202E-19,1.,-1.18789542670764E-48));
#41487=DIRECTION('center_axis',(5.15167520928809E-67,-1.18789542670764E-48,
-1.));
#41488=DIRECTION('ref_axis',(-4.33680868994202E-19,1.,-1.18789542670764E-48));
#41489=DIRECTION('',(-5.15167520928809E-67,1.18789542670764E-48,1.));
#41490=DIRECTION('',(5.15167520928809E-67,-1.18789542670764E-48,-1.));
#41491=DIRECTION('center_axis',(5.15167520928809E-67,-1.18789542670764E-48,
-1.));
#41492=DIRECTION('ref_axis',(-4.33680868994202E-19,1.,-1.18789542670764E-48));
#41493=DIRECTION('center_axis',(5.15167520928809E-67,-1.18789542670764E-48,
-1.));
#41494=DIRECTION('ref_axis',(-4.33680868994202E-19,1.,-1.18789542670764E-48));
#41495=DIRECTION('',(-5.15167520928809E-67,1.18789542670764E-48,1.));
#41496=DIRECTION('',(5.15167520928809E-67,-1.18789542670764E-48,-1.));
#41497=DIRECTION('center_axis',(5.15167520928809E-67,-1.18789542670764E-48,
-1.));
#41498=DIRECTION('ref_axis',(-4.33680868994202E-19,1.,-1.18789542670764E-48));
#41499=DIRECTION('center_axis',(5.15167520928809E-67,-1.18789542670764E-48,
-1.));
#41500=DIRECTION('ref_axis',(-4.33680868994202E-19,1.,-1.18789542670764E-48));
#41501=DIRECTION('',(-5.15167520928809E-67,1.18789542670764E-48,1.));
#41502=DIRECTION('',(5.15167520928809E-67,-1.18789542670764E-48,-1.));
#41503=DIRECTION('center_axis',(5.15167520928809E-67,-1.18789542670764E-48,
-1.));
#41504=DIRECTION('ref_axis',(-4.33680868994202E-19,1.,-1.18789542670764E-48));
#41505=DIRECTION('center_axis',(5.15167520928809E-67,-1.18789542670764E-48,
-1.));
#41506=DIRECTION('ref_axis',(-4.33680868994202E-19,1.,-1.18789542670764E-48));
#41507=DIRECTION('',(-5.15167520928809E-67,1.18789542670764E-48,1.));
#41508=DIRECTION('',(5.15167520928809E-67,-1.18789542670764E-48,-1.));
#41509=DIRECTION('center_axis',(5.15167520928809E-67,-1.18789542670764E-48,
-1.));
#41510=DIRECTION('ref_axis',(-4.33680868994202E-19,1.,-1.18789542670764E-48));
#41511=DIRECTION('center_axis',(5.15167520928809E-67,-1.18789542670764E-48,
-1.));
#41512=DIRECTION('ref_axis',(-4.33680868994202E-19,1.,-1.18789542670764E-48));
#41513=DIRECTION('',(-5.15167520928809E-67,1.18789542670764E-48,1.));
#41514=DIRECTION('',(5.15167520928809E-67,-1.18789542670764E-48,-1.));
#41515=DIRECTION('center_axis',(5.15167520928809E-67,-1.18789542670764E-48,
-1.));
#41516=DIRECTION('ref_axis',(-4.33680868994202E-19,1.,-1.18789542670764E-48));
#41517=DIRECTION('center_axis',(5.15167520928809E-67,-1.18789542670764E-48,
-1.));
#41518=DIRECTION('ref_axis',(-4.33680868994202E-19,1.,-1.18789542670764E-48));
#41519=DIRECTION('',(-5.15167520928809E-67,1.18789542670764E-48,1.));
#41520=DIRECTION('',(5.15167520928809E-67,-1.18789542670764E-48,-1.));
#41521=DIRECTION('center_axis',(5.15167520928809E-67,-1.18789542670764E-48,
-1.));
#41522=DIRECTION('ref_axis',(-4.33680868994202E-19,1.,-1.18789542670764E-48));
#41523=DIRECTION('center_axis',(5.15167520928809E-67,-1.18789542670764E-48,
-1.));
#41524=DIRECTION('ref_axis',(-4.33680868994202E-19,1.,-1.18789542670764E-48));
#41525=DIRECTION('',(-5.15167520928809E-67,1.18789542670764E-48,1.));
#41526=DIRECTION('',(5.15167520928809E-67,-1.18789542670764E-48,-1.));
#41527=DIRECTION('center_axis',(5.15167520928809E-67,-1.18789542670764E-48,
-1.));
#41528=DIRECTION('ref_axis',(-4.33680868994202E-19,1.,-1.18789542670764E-48));
#41529=DIRECTION('center_axis',(5.15167520928809E-67,-1.18789542670764E-48,
-1.));
#41530=DIRECTION('ref_axis',(-4.33680868994202E-19,1.,-1.18789542670764E-48));
#41531=DIRECTION('',(-5.15167520928809E-67,1.18789542670764E-48,1.));
#41532=DIRECTION('',(5.15167520928809E-67,-1.18789542670764E-48,-1.));
#41533=DIRECTION('center_axis',(5.15167520928809E-67,-1.18789542670764E-48,
-1.));
#41534=DIRECTION('ref_axis',(-4.33680868994202E-19,1.,-1.18789542670764E-48));
#41535=DIRECTION('center_axis',(5.15167520928809E-67,-1.18789542670764E-48,
-1.));
#41536=DIRECTION('ref_axis',(-4.33680868994202E-19,1.,-1.18789542670764E-48));
#41537=DIRECTION('',(-5.15167520928809E-67,1.18789542670764E-48,1.));
#41538=DIRECTION('',(5.15167520928809E-67,-1.18789542670764E-48,-1.));
#41539=DIRECTION('center_axis',(5.15167520928809E-67,-1.18789542670764E-48,
-1.));
#41540=DIRECTION('ref_axis',(-4.33680868994202E-19,1.,-1.18789542670764E-48));
#41541=DIRECTION('center_axis',(5.15167520928809E-67,-1.18789542670764E-48,
-1.));
#41542=DIRECTION('ref_axis',(-4.33680868994202E-19,1.,-1.18789542670764E-48));
#41543=DIRECTION('',(-5.15167520928809E-67,1.18789542670764E-48,1.));
#41544=DIRECTION('',(5.15167520928809E-67,-1.18789542670764E-48,-1.));
#41545=DIRECTION('center_axis',(5.15167520928809E-67,-1.18789542670764E-48,
-1.));
#41546=DIRECTION('ref_axis',(-4.33680868994202E-19,1.,-1.18789542670764E-48));
#41547=DIRECTION('center_axis',(5.15167520928809E-67,-1.18789542670764E-48,
-1.));
#41548=DIRECTION('ref_axis',(-4.33680868994202E-19,1.,-1.18789542670764E-48));
#41549=DIRECTION('',(-5.15167520928809E-67,1.18789542670764E-48,1.));
#41550=DIRECTION('',(5.15167520928809E-67,-1.18789542670764E-48,-1.));
#41551=DIRECTION('center_axis',(5.15167520928809E-67,-1.18789542670764E-48,
-1.));
#41552=DIRECTION('ref_axis',(-4.33680868994202E-19,1.,-1.18789542670764E-48));
#41553=DIRECTION('center_axis',(5.15167520928809E-67,-1.18789542670764E-48,
-1.));
#41554=DIRECTION('ref_axis',(-4.33680868994202E-19,1.,-1.18789542670764E-48));
#41555=DIRECTION('',(-5.15167520928809E-67,1.18789542670764E-48,1.));
#41556=DIRECTION('',(5.15167520928809E-67,-1.18789542670764E-48,-1.));
#41557=DIRECTION('center_axis',(5.15167520928809E-67,-1.18789542670764E-48,
-1.));
#41558=DIRECTION('ref_axis',(-4.33680868994202E-19,1.,-1.18789542670764E-48));
#41559=DIRECTION('center_axis',(5.15167520928809E-67,-1.18789542670764E-48,
-1.));
#41560=DIRECTION('ref_axis',(-4.33680868994202E-19,1.,-1.18789542670764E-48));
#41561=DIRECTION('',(-5.15167520928809E-67,1.18789542670764E-48,1.));
#41562=DIRECTION('',(5.15167520928809E-67,-1.18789542670764E-48,-1.));
#41563=DIRECTION('center_axis',(5.15167520928809E-67,-1.18789542670764E-48,
-1.));
#41564=DIRECTION('ref_axis',(-4.33680868994202E-19,1.,-1.18789542670764E-48));
#41565=DIRECTION('center_axis',(5.15167520928809E-67,-1.18789542670764E-48,
-1.));
#41566=DIRECTION('ref_axis',(-4.33680868994202E-19,1.,-1.18789542670764E-48));
#41567=DIRECTION('',(-5.15167520928809E-67,1.18789542670764E-48,1.));
#41568=DIRECTION('',(5.15167520928809E-67,-1.18789542670764E-48,-1.));
#41569=DIRECTION('center_axis',(5.15167520928809E-67,-1.18789542670764E-48,
-1.));
#41570=DIRECTION('ref_axis',(-4.33680868994202E-19,1.,-1.18789542670764E-48));
#41571=DIRECTION('center_axis',(5.15167520928809E-67,-1.18789542670764E-48,
-1.));
#41572=DIRECTION('ref_axis',(-4.33680868994202E-19,1.,-1.18789542670764E-48));
#41573=DIRECTION('',(-5.15167520928809E-67,1.18789542670764E-48,1.));
#41574=DIRECTION('',(5.15167520928809E-67,-1.18789542670764E-48,-1.));
#41575=DIRECTION('center_axis',(5.15167520928809E-67,-1.18789542670764E-48,
-1.));
#41576=DIRECTION('ref_axis',(-4.33680868994202E-19,1.,-1.18789542670764E-48));
#41577=DIRECTION('center_axis',(5.15167520928809E-67,-1.18789542670764E-48,
-1.));
#41578=DIRECTION('ref_axis',(-4.33680868994202E-19,1.,-1.18789542670764E-48));
#41579=DIRECTION('',(-5.15167520928809E-67,1.18789542670764E-48,1.));
#41580=DIRECTION('',(5.15167520928809E-67,-1.18789542670764E-48,-1.));
#41581=DIRECTION('center_axis',(5.15167520928809E-67,-1.18789542670764E-48,
-1.));
#41582=DIRECTION('ref_axis',(-4.33680868994202E-19,1.,-1.18789542670764E-48));
#41583=DIRECTION('center_axis',(5.15167520928809E-67,-1.18789542670764E-48,
-1.));
#41584=DIRECTION('ref_axis',(-4.33680868994202E-19,1.,-1.18789542670764E-48));
#41585=DIRECTION('',(-5.15167520928809E-67,1.18789542670764E-48,1.));
#41586=DIRECTION('',(5.15167520928809E-67,-1.18789542670764E-48,-1.));
#41587=DIRECTION('center_axis',(5.15167520928809E-67,-1.18789542670764E-48,
-1.));
#41588=DIRECTION('ref_axis',(-4.33680868994202E-19,1.,-1.18789542670764E-48));
#41589=DIRECTION('center_axis',(5.15167520928809E-67,-1.18789542670764E-48,
-1.));
#41590=DIRECTION('ref_axis',(-4.33680868994202E-19,1.,-1.18789542670764E-48));
#41591=DIRECTION('',(-5.15167520928809E-67,1.18789542670764E-48,1.));
#41592=DIRECTION('',(5.15167520928809E-67,-1.18789542670764E-48,-1.));
#41593=DIRECTION('center_axis',(5.15167520928809E-67,-1.18789542670764E-48,
-1.));
#41594=DIRECTION('ref_axis',(-4.33680868994202E-19,1.,-1.18789542670764E-48));
#41595=DIRECTION('center_axis',(5.15167520928809E-67,-1.18789542670764E-48,
-1.));
#41596=DIRECTION('ref_axis',(-4.33680868994202E-19,1.,-1.18789542670764E-48));
#41597=DIRECTION('',(-5.15167520928809E-67,1.18789542670764E-48,1.));
#41598=DIRECTION('',(5.15167520928809E-67,-1.18789542670764E-48,-1.));
#41599=DIRECTION('center_axis',(5.15167520928809E-67,-1.18789542670764E-48,
-1.));
#41600=DIRECTION('ref_axis',(-4.33680868994202E-19,1.,-1.18789542670764E-48));
#41601=DIRECTION('center_axis',(5.15167520928809E-67,-1.18789542670764E-48,
-1.));
#41602=DIRECTION('ref_axis',(-4.33680868994202E-19,1.,-1.18789542670764E-48));
#41603=DIRECTION('',(-5.15167520928809E-67,1.18789542670764E-48,1.));
#41604=DIRECTION('',(5.15167520928809E-67,-1.18789542670764E-48,-1.));
#41605=DIRECTION('center_axis',(5.15167520928809E-67,-1.18789542670764E-48,
-1.));
#41606=DIRECTION('ref_axis',(-4.33680868994202E-19,1.,-1.18789542670764E-48));
#41607=DIRECTION('center_axis',(5.15167520928809E-67,-1.18789542670764E-48,
-1.));
#41608=DIRECTION('ref_axis',(-4.33680868994202E-19,1.,-1.18789542670764E-48));
#41609=DIRECTION('',(-5.15167520928809E-67,1.18789542670764E-48,1.));
#41610=DIRECTION('',(5.15167520928809E-67,-1.18789542670764E-48,-1.));
#41611=DIRECTION('center_axis',(5.15167520928809E-67,-1.18789542670764E-48,
-1.));
#41612=DIRECTION('ref_axis',(-4.33680868994202E-19,1.,-1.18789542670764E-48));
#41613=DIRECTION('center_axis',(5.15167520928809E-67,-1.18789542670764E-48,
-1.));
#41614=DIRECTION('ref_axis',(-4.33680868994202E-19,1.,-1.18789542670764E-48));
#41615=DIRECTION('',(-5.15167520928809E-67,1.18789542670764E-48,1.));
#41616=DIRECTION('',(5.15167520928809E-67,-1.18789542670764E-48,-1.));
#41617=DIRECTION('center_axis',(5.15167520928809E-67,-1.18789542670764E-48,
-1.));
#41618=DIRECTION('ref_axis',(-4.33680868994202E-19,1.,-1.18789542670764E-48));
#41619=DIRECTION('center_axis',(5.15167520928809E-67,-1.18789542670764E-48,
-1.));
#41620=DIRECTION('ref_axis',(-4.33680868994202E-19,1.,-1.18789542670764E-48));
#41621=DIRECTION('',(-5.15167520928809E-67,1.18789542670764E-48,1.));
#41622=DIRECTION('',(5.15167520928809E-67,-1.18789542670764E-48,-1.));
#41623=DIRECTION('center_axis',(5.15167520928809E-67,-1.18789542670764E-48,
-1.));
#41624=DIRECTION('ref_axis',(-4.33680868994202E-19,1.,-1.18789542670764E-48));
#41625=DIRECTION('center_axis',(5.15167520928809E-67,-1.18789542670764E-48,
-1.));
#41626=DIRECTION('ref_axis',(-4.33680868994202E-19,1.,-1.18789542670764E-48));
#41627=DIRECTION('',(-5.15167520928809E-67,1.18789542670764E-48,1.));
#41628=DIRECTION('',(5.15167520928809E-67,-1.18789542670764E-48,-1.));
#41629=DIRECTION('center_axis',(5.15167520928809E-67,-1.18789542670764E-48,
-1.));
#41630=DIRECTION('ref_axis',(-4.33680868994202E-19,1.,-1.18789542670764E-48));
#41631=DIRECTION('center_axis',(5.15167520928809E-67,-1.18789542670764E-48,
-1.));
#41632=DIRECTION('ref_axis',(-4.33680868994202E-19,1.,-1.18789542670764E-48));
#41633=DIRECTION('',(-5.15167520928809E-67,1.18789542670764E-48,1.));
#41634=DIRECTION('',(5.15167520928809E-67,-1.18789542670764E-48,-1.));
#41635=DIRECTION('center_axis',(5.15167520928809E-67,-1.18789542670764E-48,
-1.));
#41636=DIRECTION('ref_axis',(-4.33680868994202E-19,1.,-1.18789542670764E-48));
#41637=DIRECTION('center_axis',(5.15167520928809E-67,-1.18789542670764E-48,
-1.));
#41638=DIRECTION('ref_axis',(-4.33680868994202E-19,1.,-1.18789542670764E-48));
#41639=DIRECTION('',(-5.15167520928809E-67,1.18789542670764E-48,1.));
#41640=DIRECTION('',(5.15167520928809E-67,-1.18789542670764E-48,-1.));
#41641=DIRECTION('center_axis',(5.15167520928809E-67,-1.18789542670764E-48,
-1.));
#41642=DIRECTION('ref_axis',(-4.33680868994202E-19,1.,-1.18789542670764E-48));
#41643=DIRECTION('center_axis',(5.15167520928809E-67,-1.18789542670764E-48,
-1.));
#41644=DIRECTION('ref_axis',(-4.33680868994202E-19,1.,-1.18789542670764E-48));
#41645=DIRECTION('',(-5.15167520928809E-67,1.18789542670764E-48,1.));
#41646=DIRECTION('',(5.15167520928809E-67,-1.18789542670764E-48,-1.));
#41647=DIRECTION('center_axis',(5.15167520928809E-67,-1.18789542670764E-48,
-1.));
#41648=DIRECTION('ref_axis',(-4.33680868994202E-19,1.,-1.18789542670764E-48));
#41649=DIRECTION('center_axis',(5.15167520928809E-67,-1.18789542670764E-48,
-1.));
#41650=DIRECTION('ref_axis',(-4.33680868994202E-19,1.,-1.18789542670764E-48));
#41651=DIRECTION('',(-5.15167520928809E-67,1.18789542670764E-48,1.));
#41652=DIRECTION('',(5.15167520928809E-67,-1.18789542670764E-48,-1.));
#41653=DIRECTION('center_axis',(5.15167520928809E-67,-1.18789542670764E-48,
-1.));
#41654=DIRECTION('ref_axis',(-4.33680868994202E-19,1.,-1.18789542670764E-48));
#41655=DIRECTION('center_axis',(5.15167520928809E-67,-1.18789542670764E-48,
-1.));
#41656=DIRECTION('ref_axis',(-4.33680868994202E-19,1.,-1.18789542670764E-48));
#41657=DIRECTION('',(-5.15167520928809E-67,1.18789542670764E-48,1.));
#41658=DIRECTION('',(5.15167520928809E-67,-1.18789542670764E-48,-1.));
#41659=DIRECTION('center_axis',(5.15167520928809E-67,-1.18789542670764E-48,
-1.));
#41660=DIRECTION('ref_axis',(-4.33680868994202E-19,1.,-1.18789542670764E-48));
#41661=DIRECTION('center_axis',(5.15167520928809E-67,-1.18789542670764E-48,
-1.));
#41662=DIRECTION('ref_axis',(-4.33680868994202E-19,1.,-1.18789542670764E-48));
#41663=DIRECTION('',(-5.15167520928809E-67,1.18789542670764E-48,1.));
#41664=DIRECTION('',(5.15167520928809E-67,-1.18789542670764E-48,-1.));
#41665=DIRECTION('center_axis',(5.15167520928809E-67,-1.18789542670764E-48,
-1.));
#41666=DIRECTION('ref_axis',(-4.33680868994202E-19,1.,-1.18789542670764E-48));
#41667=DIRECTION('center_axis',(5.15167520928809E-67,-1.18789542670764E-48,
-1.));
#41668=DIRECTION('ref_axis',(-4.33680868994202E-19,1.,-1.18789542670764E-48));
#41669=DIRECTION('',(-5.15167520928809E-67,1.18789542670764E-48,1.));
#41670=DIRECTION('',(5.15167520928809E-67,-1.18789542670764E-48,-1.));
#41671=DIRECTION('center_axis',(5.15167520928809E-67,-1.18789542670764E-48,
-1.));
#41672=DIRECTION('ref_axis',(-4.33680868994202E-19,1.,-1.18789542670764E-48));
#41673=DIRECTION('center_axis',(5.15167520928809E-67,-1.18789542670764E-48,
-1.));
#41674=DIRECTION('ref_axis',(-4.33680868994202E-19,1.,-1.18789542670764E-48));
#41675=DIRECTION('',(5.15167520928809E-67,-1.18789542670764E-48,-1.));
#41676=DIRECTION('center_axis',(5.15167520928809E-67,-1.18789542670764E-48,
-1.));
#41677=DIRECTION('ref_axis',(-4.33680868994202E-19,1.,-1.18789542670764E-48));
#41678=DIRECTION('',(-5.15167520928809E-67,1.18789542670764E-48,1.));
#41679=DIRECTION('center_axis',(5.15167520928809E-67,-1.18789542670764E-48,
-1.));
#41680=DIRECTION('ref_axis',(-4.33680868994202E-19,1.,-1.18789542670764E-48));
#41681=DIRECTION('',(5.15167520928809E-67,-1.18789542670764E-48,-1.));
#41682=DIRECTION('center_axis',(5.15167520928809E-67,-1.18789542670764E-48,
-1.));
#41683=DIRECTION('ref_axis',(-4.33680868994202E-19,1.,-1.18789542670764E-48));
#41684=DIRECTION('',(-5.15167520928809E-67,1.18789542670764E-48,1.));
#41685=DIRECTION('center_axis',(5.15167520928809E-67,-1.18789542670764E-48,
-1.));
#41686=DIRECTION('ref_axis',(-4.33680868994202E-19,1.,-1.18789542670764E-48));
#41687=DIRECTION('',(5.15167520928809E-67,-1.18789542670764E-48,-1.));
#41688=DIRECTION('center_axis',(5.15167520928809E-67,-1.18789542670764E-48,
-1.));
#41689=DIRECTION('ref_axis',(-4.33680868994202E-19,1.,-1.18789542670764E-48));
#41690=DIRECTION('',(-5.15167520928809E-67,1.18789542670764E-48,1.));
#41691=DIRECTION('center_axis',(5.15167520928809E-67,-1.18789542670764E-48,
-1.));
#41692=DIRECTION('ref_axis',(-4.33680868994202E-19,1.,-1.18789542670764E-48));
#41693=DIRECTION('',(5.15167520928809E-67,-1.18789542670764E-48,-1.));
#41694=DIRECTION('center_axis',(5.15167520928809E-67,-1.18789542670764E-48,
-1.));
#41695=DIRECTION('ref_axis',(-4.33680868994202E-19,1.,-1.18789542670764E-48));
#41696=DIRECTION('',(-5.15167520928809E-67,1.18789542670764E-48,1.));
#41697=DIRECTION('center_axis',(5.15167520928809E-67,-1.18789542670764E-48,
-1.));
#41698=DIRECTION('ref_axis',(-4.33680868994202E-19,1.,-1.18789542670764E-48));
#41699=DIRECTION('',(5.15167520928809E-67,-1.18789542670764E-48,-1.));
#41700=DIRECTION('center_axis',(5.15167520928809E-67,-1.18789542670764E-48,
-1.));
#41701=DIRECTION('ref_axis',(-4.33680868994202E-19,1.,-1.18789542670764E-48));
#41702=DIRECTION('',(-5.15167520928809E-67,1.18789542670764E-48,1.));
#41703=DIRECTION('center_axis',(5.15167520928809E-67,-1.18789542670764E-48,
-1.));
#41704=DIRECTION('ref_axis',(-4.33680868994202E-19,1.,-1.18789542670764E-48));
#41705=DIRECTION('',(5.15167520928809E-67,-1.18789542670764E-48,-1.));
#41706=DIRECTION('center_axis',(5.15167520928809E-67,-1.18789542670764E-48,
-1.));
#41707=DIRECTION('ref_axis',(-4.33680868994202E-19,1.,-1.18789542670764E-48));
#41708=DIRECTION('',(-5.15167520928809E-67,1.18789542670764E-48,1.));
#41709=DIRECTION('center_axis',(5.15167520928809E-67,-1.18789542670764E-48,
-1.));
#41710=DIRECTION('ref_axis',(-4.33680868994202E-19,1.,-1.18789542670764E-48));
#41711=DIRECTION('',(5.15167520928809E-67,-1.18789542670764E-48,-1.));
#41712=DIRECTION('center_axis',(5.15167520928809E-67,-1.18789542670764E-48,
-1.));
#41713=DIRECTION('ref_axis',(-4.33680868994202E-19,1.,-1.18789542670764E-48));
#41714=DIRECTION('',(-5.15167520928809E-67,1.18789542670764E-48,1.));
#41715=DIRECTION('center_axis',(5.15167520928809E-67,-1.18789542670764E-48,
-1.));
#41716=DIRECTION('ref_axis',(-4.33680868994202E-19,1.,-1.18789542670764E-48));
#41717=DIRECTION('',(5.15167520928809E-67,-1.18789542670764E-48,-1.));
#41718=DIRECTION('center_axis',(5.15167520928809E-67,-1.18789542670764E-48,
-1.));
#41719=DIRECTION('ref_axis',(-4.33680868994202E-19,1.,-1.18789542670764E-48));
#41720=DIRECTION('',(-5.15167520928809E-67,1.18789542670764E-48,1.));
#41721=DIRECTION('center_axis',(5.15167520928809E-67,-1.18789542670764E-48,
-1.));
#41722=DIRECTION('ref_axis',(-4.33680868994202E-19,1.,-1.18789542670764E-48));
#41723=DIRECTION('',(5.15167520928809E-67,-1.18789542670764E-48,-1.));
#41724=DIRECTION('center_axis',(5.15167520928809E-67,-1.18789542670764E-48,
-1.));
#41725=DIRECTION('ref_axis',(-4.33680868994202E-19,1.,-1.18789542670764E-48));
#41726=DIRECTION('',(-5.15167520928809E-67,1.18789542670764E-48,1.));
#41727=DIRECTION('center_axis',(5.15167520928809E-67,-1.18789542670764E-48,
-1.));
#41728=DIRECTION('ref_axis',(-4.33680868994202E-19,1.,-1.18789542670764E-48));
#41729=DIRECTION('',(5.15167520928809E-67,-1.18789542670764E-48,-1.));
#41730=DIRECTION('center_axis',(5.15167520928809E-67,-1.18789542670764E-48,
-1.));
#41731=DIRECTION('ref_axis',(-4.33680868994202E-19,1.,-1.18789542670764E-48));
#41732=DIRECTION('',(-5.15167520928809E-67,1.18789542670764E-48,1.));
#41733=DIRECTION('center_axis',(5.15167520928809E-67,-1.18789542670764E-48,
-1.));
#41734=DIRECTION('ref_axis',(-4.33680868994202E-19,1.,-1.18789542670764E-48));
#41735=DIRECTION('',(5.15167520928809E-67,-1.18789542670764E-48,-1.));
#41736=DIRECTION('center_axis',(5.15167520928809E-67,-1.18789542670764E-48,
-1.));
#41737=DIRECTION('ref_axis',(-4.33680868994202E-19,1.,-1.18789542670764E-48));
#41738=DIRECTION('',(-5.15167520928809E-67,1.18789542670764E-48,1.));
#41739=DIRECTION('center_axis',(5.15167520928809E-67,-1.18789542670764E-48,
-1.));
#41740=DIRECTION('ref_axis',(-4.33680868994202E-19,1.,-1.18789542670764E-48));
#41741=DIRECTION('',(5.15167520928809E-67,-1.18789542670764E-48,-1.));
#41742=DIRECTION('center_axis',(5.15167520928809E-67,-1.18789542670764E-48,
-1.));
#41743=DIRECTION('ref_axis',(-4.33680868994202E-19,1.,-1.18789542670764E-48));
#41744=DIRECTION('',(-5.15167520928809E-67,1.18789542670764E-48,1.));
#41745=DIRECTION('center_axis',(5.15167520928809E-67,-1.18789542670764E-48,
-1.));
#41746=DIRECTION('ref_axis',(-4.33680868994202E-19,1.,-1.18789542670764E-48));
#41747=DIRECTION('',(5.15167520928809E-67,-1.18789542670764E-48,-1.));
#41748=DIRECTION('center_axis',(5.15167520928809E-67,-1.18789542670764E-48,
-1.));
#41749=DIRECTION('ref_axis',(-4.33680868994202E-19,1.,-1.18789542670764E-48));
#41750=DIRECTION('',(-5.15167520928809E-67,1.18789542670764E-48,1.));
#41751=DIRECTION('center_axis',(5.15167520928809E-67,-1.18789542670764E-48,
-1.));
#41752=DIRECTION('ref_axis',(-4.33680868994202E-19,1.,-1.18789542670764E-48));
#41753=DIRECTION('',(5.15167520928809E-67,-1.18789542670764E-48,-1.));
#41754=DIRECTION('center_axis',(5.15167520928809E-67,-1.18789542670764E-48,
-1.));
#41755=DIRECTION('ref_axis',(-4.33680868994202E-19,1.,-1.18789542670764E-48));
#41756=DIRECTION('',(-5.15167520928809E-67,1.18789542670764E-48,1.));
#41757=DIRECTION('center_axis',(5.15167520928809E-67,-1.18789542670764E-48,
-1.));
#41758=DIRECTION('ref_axis',(-4.33680868994202E-19,1.,-1.18789542670764E-48));
#41759=DIRECTION('',(-5.15167520928809E-67,1.18789542670764E-48,1.));
#41760=DIRECTION('',(5.15167520928809E-67,-1.18789542670764E-48,-1.));
#41761=DIRECTION('center_axis',(5.15167520928809E-67,-1.18789542670764E-48,
-1.));
#41762=DIRECTION('ref_axis',(-4.33680868994202E-19,1.,-1.18789542670764E-48));
#41763=DIRECTION('center_axis',(5.15167520928809E-67,-1.18789542670764E-48,
-1.));
#41764=DIRECTION('ref_axis',(0.,1.,0.));
#41765=DIRECTION('center_axis',(-0.726718511656259,-0.686935363550879,-0.000105448246390915));
#41766=DIRECTION('ref_axis',(0.686885008270217,-0.726663364190208,-0.0122204974282148));
#41767=DIRECTION('center_axis',(0.0503511057571476,0.998731574514185,-9.06501463958382E-5));
#41768=DIRECTION('ref_axis',(0.998626750226923,-0.0503471356586858,-0.0144837723739379));
#41769=DIRECTION('center_axis',(5.15167520928809E-67,-1.18789542670764E-48,
-1.));
#41770=DIRECTION('ref_axis',(0.,1.,0.));
#41771=DIRECTION('center_axis',(-0.0281636861094737,0.999603320606368,-9.06501463234301E-5));
#41772=DIRECTION('ref_axis',(0.999498507968587,0.0281594195507115,-0.0144837722688343));
#41773=DIRECTION('center_axis',(-0.670581953565459,-0.741835448352935,-0.000105448247414229));
#41774=DIRECTION('ref_axis',(0.741780921484837,-0.670530926934418,-0.0122204969447688));
#41775=DIRECTION('center_axis',(5.15167520928809E-67,-1.18789542670764E-48,
-1.));
#41776=DIRECTION('ref_axis',(0.,1.,0.));
#41777=DIRECTION('center_axis',(-0.106504839485416,0.994312179825198,-9.06501464431132E-5));
#41778=DIRECTION('ref_axis',(0.994208025038947,0.106492362574112,-0.014483772351861));
#41779=DIRECTION('center_axis',(-0.610311034741592,-0.792161870928735,-0.000105448247339917));
#41780=DIRECTION('ref_axis',(0.792103508645573,-0.610264443537491,-0.0122204969313235));
#41781=DIRECTION('center_axis',(5.15167520928809E-67,-1.18789542670764E-48,
-1.));
#41782=DIRECTION('ref_axis',(0.,1.,0.));
#41783=DIRECTION('center_axis',(-0.184189355109993,0.982890773812999,-9.06501463311491E-5));
#41784=DIRECTION('ref_axis',(0.982787919029266,0.184168744770673,-0.0144837722890199));
#41785=DIRECTION('center_axis',(-0.546277345439217,-0.837604352149957,-0.000105448247410497));
#41786=DIRECTION('ref_axis',(0.837542514274823,-0.546235476912428,-0.0122204968991007));
#41787=DIRECTION('center_axis',(5.15167520928809E-67,-1.18789542670764E-48,
-1.));
#41788=DIRECTION('ref_axis',(0.,1.,0.));
#41789=DIRECTION('center_axis',(-0.260738282110594,0.965409519336,-9.0650146457266E-5));
#41790=DIRECTION('ref_axis',(0.965308598686112,0.260709665412272,-0.0144837724117514));
#41791=DIRECTION('center_axis',(-0.478875674647023,-0.877882724008182,-0.000105448247224529));
#41792=DIRECTION('ref_axis',(0.877817791791478,-0.478838786930502,-0.0122204969317693));
#41793=DIRECTION('center_axis',(5.15167520928809E-67,-1.18789542670764E-48,
-1.));
#41794=DIRECTION('ref_axis',(0.,1.,0.));
#41795=DIRECTION('center_axis',(-0.335679670898074,0.941976194140973,-9.06501464082373E-5));
#41796=DIRECTION('ref_axis',(0.941877829837014,0.335643224272907,-0.014483772340284));
#41797=DIRECTION('center_axis',(-0.40852157607848,-0.912748656947257,-0.000105448246964389));
#41798=DIRECTION('ref_axis',(0.912681030716442,-0.408489896596762,-0.0122204970741974));
#41799=DIRECTION('center_axis',(5.15167520928809E-67,-1.18789542670764E-48,
-1.));
#41800=DIRECTION('ref_axis',(0.,1.,0.));
#41801=DIRECTION('center_axis',(-0.408551482889657,0.91273527247018,-9.06501463992171E-5));
#41802=DIRECTION('ref_axis',(0.91264007096006,0.408507431043052,-0.014483772320157));
#41803=DIRECTION('center_axis',(-0.335648806144879,-0.941987190897087,-0.000105448247367288));
#41804=DIRECTION('ref_axis',(0.941917287594001,-0.335622530214118,-0.0122204968897907));
#41805=DIRECTION('center_axis',(5.15167520928809E-67,-1.18789542670764E-48,
-1.));
#41806=DIRECTION('ref_axis',(0.,1.,0.));
#41807=DIRECTION('center_axis',(-0.478904439132113,0.877867034329292,-9.06501463430316E-5));
#41808=DIRECTION('ref_axis',(0.877775582560928,0.478853053657823,-0.0144837723815965));
#41809=DIRECTION('center_axis',(-0.260706649707894,-0.965418060572078,-0.000105448247265905));
#41810=DIRECTION('ref_axis',(0.965346311170054,-0.260685939326527,-0.0122204970363453));
#41811=DIRECTION('center_axis',(5.15167520928809E-67,-1.18789542670764E-48,
-1.));
#41812=DIRECTION('ref_axis',(0.,1.,0.));
#41813=DIRECTION('center_axis',(-0.546304790255147,0.837586454001514,-9.06501464163507E-5));
#41814=DIRECTION('ref_axis',(0.837499315806636,0.546246387962313,-0.0144837723519214));
#41815=DIRECTION('center_axis',(-0.184157150081311,-0.982896806869672,-0.00010544824733539));
#41816=DIRECTION('ref_axis',(0.982823653730718,-0.184142132936614,-0.012220496919376));
#41817=DIRECTION('center_axis',(5.15167520928809E-67,-1.18789542670764E-48,
-1.));
#41818=DIRECTION('ref_axis',(0.,1.,0.));
#41819=DIRECTION('center_axis',(-0.610336990681852,0.792141874658809,-9.06501463120476E-5));
#41820=DIRECTION('ref_axis',(0.792059587273495,0.610271931640219,-0.0144837723075503));
#41821=DIRECTION('center_axis',(-0.106472260385922,-0.994315667506542,-0.000105448247451369));
#41822=DIRECTION('ref_axis',(0.994241561642557,-0.106463029063183,-0.0122204969318448));
#41823=DIRECTION('center_axis',(5.15167520928809E-67,-1.18789542670764E-48,
-1.));
#41824=DIRECTION('ref_axis',(0.,1.,0.));
#41825=DIRECTION('center_axis',(-0.670606260603123,0.741813477245087,-9.06501463072396E-5));
#41826=DIRECTION('ref_axis',(0.741736547997548,0.670534945922644,-0.0144837723400245));
#41827=DIRECTION('center_axis',(-0.0281309338001256,-0.999604241409669,
-0.000105448247349234));
#41828=DIRECTION('ref_axis',(0.999529639708615,-0.0281275452135709,-0.012220496889411));
#41829=DIRECTION('center_axis',(5.15167520928809E-67,-1.18789542670764E-48,
-1.));
#41830=DIRECTION('ref_axis',(0.,1.,0.));
#41831=DIRECTION('center_axis',(-0.726741019928497,0.686911553066215,-9.0650146372247E-5));
#41832=DIRECTION('ref_axis',(0.686840456250864,0.726663889287803,-0.014483772375632));
#41833=DIRECTION('center_axis',(0.0503838293471008,-0.9987299227624,-0.000105448247268434));
#41834=DIRECTION('ref_axis',(0.998655285167451,0.0503813543057433,-0.0122204969390446));
#41835=DIRECTION('center_axis',(5.15167520928809E-67,-1.18789542670764E-48,
-1.));
#41836=DIRECTION('ref_axis',(0.,1.,0.));
#41837=DIRECTION('center_axis',(-0.77839517919999,0.627774590741587,-9.06501465192481E-5));
#41838=DIRECTION('ref_axis',(0.62770976469511,0.778312708136478,-0.0144837722873138));
#41839=DIRECTION('center_axis',(0.128587959432554,-0.991698102029866,-0.000105448247403937));
#41840=DIRECTION('ref_axis',(0.991623888707038,0.128579636022696,-0.0122204969540051));
#41841=DIRECTION('center_axis',(5.15167520928809E-67,-1.18789542670764E-48,
-1.));
#41842=DIRECTION('ref_axis',(0.,1.,0.));
#41843=DIRECTION('center_axis',(-0.825250273349494,0.564767189308247,-9.06501463546308E-5));
#41844=DIRECTION('ref_axis',(0.564709033703414,0.82516297032304,-0.0144837723475052));
#41845=DIRECTION('center_axis',(0.205999301987418,-0.978552132725367,-0.000105448247113811));
#41846=DIRECTION('ref_axis',(0.978478801224233,0.205985181525565,-0.0122204969893998));
#41847=DIRECTION('center_axis',(5.15167520928809E-67,-1.18789542670764E-48,
-1.));
#41848=DIRECTION('ref_axis',(0.,1.,0.));
#41849=DIRECTION('center_axis',(-0.867017425140065,0.498277810348848,-9.06501462870057E-5));
#41850=DIRECTION('ref_axis',(0.498226683734515,0.866925828402957,-0.0144837723937473));
#41851=DIRECTION('center_axis',(0.282140590344591,-0.959373064120873,-0.000105448247263863));
#41852=DIRECTION('ref_axis',(0.959301066555575,0.282120759888322,-0.0122204969363817));
#41853=DIRECTION('center_axis',(5.15167520928809E-67,-1.18789542670764E-48,
-1.));
#41854=DIRECTION('ref_axis',(0.,1.,0.));
#41855=DIRECTION('center_axis',(-0.903439126191882,0.428716382994866,-9.06501464245823E-5));
#41856=DIRECTION('ref_axis',(0.42867260058449,0.903343800470088,-0.0144837723120868));
#41857=DIRECTION('center_axis',(0.356542388140961,-0.934279141552142,-0.000105448247299974));
#41858=DIRECTION('ref_axis',(0.934208921811354,0.356516969951643,-0.0122204969034503));
#41859=DIRECTION('center_axis',(5.15167520928809E-67,-1.18789542670764E-48,
-1.));
#41860=DIRECTION('ref_axis',(0.,1.,0.));
#41861=DIRECTION('center_axis',(-0.934290824606917,0.356511776576704,-9.06501463905499E-5));
#41862=DIRECTION('ref_axis',(0.356475608302988,0.934192357614636,-0.0144837722787681));
#41863=DIRECTION('center_axis',(0.428745983551553,-0.903425077396614,-0.000105448247174382));
#41864=DIRECTION('ref_axis',(0.903357068407879,0.428715134340607,-0.0122204969145006));
#41865=DIRECTION('center_axis',(5.15167520928809E-67,-1.18789542670764E-48,
-1.));
#41866=DIRECTION('ref_axis',(0.,1.,0.));
#41867=DIRECTION('center_axis',(-0.959382309405018,0.282109156503729,-9.06501463332588E-5));
#41868=DIRECTION('ref_axis',(0.282080825355611,0.959281308222547,-0.0144837723517365));
#41869=DIRECTION('center_axis',(0.498306217395032,-0.867001097223137,-0.000105448243846677));
#41870=DIRECTION('ref_axis',(0.866935718268405,0.498270127348975,-0.0122204984383232));
#41871=DIRECTION('center_axis',(5.15167520928809E-67,-1.18789542670764E-48,
-1.));
#41872=DIRECTION('ref_axis',(0.,1.,0.));
#41873=DIRECTION('center_axis',(-0.978558883238511,0.205967239670656,-9.06501465473592E-5));
#41874=DIRECTION('ref_axis',(0.205946920319669,0.978455970573743,-0.0144837722792749));
#41875=DIRECTION('center_axis',(0.564794227716619,-0.825231766971349,-0.000105448246777006));
#41876=DIRECTION('ref_axis',(0.825169421163283,0.564753119359096,-0.01222049717581));
#41877=DIRECTION('center_axis',(5.15167520928809E-67,-1.18789542670764E-48,
-1.));
#41878=DIRECTION('ref_axis',(0.,1.,0.));
#41879=DIRECTION('center_axis',(-0.991702316153162,0.128555466313202,-9.0650146420716E-5));
#41880=DIRECTION('ref_axis',(0.128543284034494,0.991598126494967,-0.0144837723435229));
#41881=DIRECTION('center_axis',(0.627800093806525,-0.778374608461238,-0.000105448247294656));
#41882=DIRECTION('ref_axis',(0.778315680171741,0.627754220578766,-0.012220496894383));
#41883=DIRECTION('center_axis',(5.15167520928809E-67,-1.18789542670764E-48,
-1.));
#41884=DIRECTION('ref_axis',(0.,1.,0.));
#41885=DIRECTION('center_axis',(-0.998731574514195,0.0503511057569474,-9.06501463044587E-5));
#41886=DIRECTION('ref_axis',(0.0503471356585215,0.998626750227776,-0.0144837723156803));
#41887=DIRECTION('center_axis',(0.686935363552588,-0.726718511654644,-0.000105448247440854));
#41888=DIRECTION('ref_axis',(0.726663364192637,0.6868850082757,-0.0122204969756106));
#41889=DIRECTION('center_axis',(5.15167520928809E-67,-1.18789542670764E-48,
-1.));
#41890=DIRECTION('ref_axis',(0.,1.,0.));
#41891=DIRECTION('center_axis',(-0.99960332060638,-0.0281636861090561,-9.06501465204533E-5));
#41892=DIRECTION('ref_axis',(0.0281594195503036,-0.999498507968962,0.0144837722437162));
#41893=DIRECTION('center_axis',(0.741835448352776,-0.670581953565635,-0.000105448247295083));
#41894=DIRECTION('ref_axis',(0.67053092693442,0.741780921484487,-0.0122204969658991));
#41895=DIRECTION('center_axis',(5.15167520928809E-67,-1.18789542670764E-48,
-1.));
#41896=DIRECTION('ref_axis',(0.,1.,0.));
#41897=DIRECTION('center_axis',(-0.994312179825187,-0.106504839485521,-9.0650146389517E-5));
#41898=DIRECTION('ref_axis',(0.106492362574174,-0.994208025038546,0.0144837723789195));
#41899=DIRECTION('center_axis',(0.792161870927703,-0.610311034742932,-0.000105448246562834));
#41900=DIRECTION('ref_axis',(0.610264443536631,0.792103508641721,-0.0122204972240042));
#41901=DIRECTION('center_axis',(5.15167520928809E-67,-1.18789542670764E-48,
-1.));
#41902=DIRECTION('ref_axis',(0.,1.,0.));
#41903=DIRECTION('center_axis',(-0.982890773812962,-0.18418935511019,-9.06501462458389E-5));
#41904=DIRECTION('ref_axis',(0.184168744770736,-0.982787919028534,0.0144837723378535));
#41905=DIRECTION('center_axis',(0.837604352149828,-0.546277345439416,-0.000105448247288724));
#41906=DIRECTION('ref_axis',(0.546235476912052,0.837542514273825,-0.0122204969843265));
#41907=DIRECTION('center_axis',(5.15167520928809E-67,-1.18789542670764E-48,
-1.));
#41908=DIRECTION('ref_axis',(0.,1.,0.));
#41909=DIRECTION('center_axis',(-0.965409519335916,-0.260738282110905,-9.06501463158079E-5));
#41910=DIRECTION('ref_axis',(0.260709665413015,-0.965308598687581,0.0144837723005081));
#41911=DIRECTION('center_axis',(0.877882724007609,-0.478875674648073,-0.000105448246644854));
#41912=DIRECTION('ref_axis',(0.47883878693024,0.877817791788535,-0.012220497153411));
#41913=DIRECTION('center_axis',(5.15167520928809E-67,-1.18789542670764E-48,
-1.));
#41914=DIRECTION('ref_axis',(0.,1.,0.));
#41915=DIRECTION('center_axis',(-0.941976194141077,-0.335679670897783,-9.06501465752214E-5));
#41916=DIRECTION('ref_axis',(0.335643224272825,-0.941877829837701,0.0144837722974511));
#41917=DIRECTION('center_axis',(0.912748656947635,-0.408521576077636,-0.000105448247395522));
#41918=DIRECTION('ref_axis',(0.408489896596716,0.912681030718573,-0.0122204969165703));
#41919=DIRECTION('center_axis',(5.15167520928809E-67,-1.18789542670764E-48,
-1.));
#41920=DIRECTION('ref_axis',(0.,1.,0.));
#41921=DIRECTION('center_axis',(-0.912735272470059,-0.408551482889927,-9.0650146236208E-5));
#41922=DIRECTION('ref_axis',(0.408507431042893,-0.912640070958992,0.0144837723919199));
#41923=DIRECTION('center_axis',(0.941987190897161,-0.335648806144671,-0.000105448247475279));
#41924=DIRECTION('ref_axis',(0.335622530214028,0.941917287594399,-0.0122204968616106));
#41925=DIRECTION('center_axis',(5.15167520928809E-67,-1.18789542670764E-48,
-1.));
#41926=DIRECTION('ref_axis',(0.,1.,0.));
#41927=DIRECTION('center_axis',(-0.877867034329361,-0.478904439131988,-9.06501463610722E-5));
#41928=DIRECTION('ref_axis',(0.478853053657853,-0.877775582561276,0.0144837723595397));
#41929=DIRECTION('center_axis',(0.965418060572122,-0.260706649707733,-0.000105448247352975));
#41930=DIRECTION('ref_axis',(0.260685939326823,0.965346311171741,-0.012220496896787));
#41931=DIRECTION('center_axis',(5.15167520928809E-67,-1.18789542670764E-48,
-1.));
#41932=DIRECTION('ref_axis',(0.,1.,0.));
#41933=DIRECTION('center_axis',(-0.837586454001461,-0.546304790255229,-9.06501463408637E-5));
#41934=DIRECTION('ref_axis',(0.54624638796239,-0.837499315806573,0.0144837723526967));
#41935=DIRECTION('center_axis',(0.982896806869685,-0.184157150081241,-0.000105448247384682));
#41936=DIRECTION('ref_axis',(0.184142132936524,0.982823653730634,-0.0122204969274716));
#41937=DIRECTION('center_axis',(5.15167520928809E-67,-1.18789542670764E-48,
-1.));
#41938=DIRECTION('ref_axis',(0.,1.,0.));
#41939=DIRECTION('center_axis',(-0.792141874658961,-0.610336990681655,-9.06501464140886E-5));
#41940=DIRECTION('ref_axis',(0.610271931639049,-0.792059587272402,0.0144837724166105));
#41941=DIRECTION('center_axis',(0.994315667506523,-0.1064722603861,-0.000105448247372999));
#41942=DIRECTION('ref_axis',(0.106463029063429,0.994241561643113,-0.0122204968844733));
#41943=DIRECTION('center_axis',(5.15167520928809E-67,-1.18789542670764E-48,
-1.));
#41944=DIRECTION('ref_axis',(0.,1.,0.));
#41945=DIRECTION('center_axis',(-0.741813477245026,-0.670606260603191,-9.06501462657205E-5));
#41946=DIRECTION('ref_axis',(0.670534945922615,-0.741736547997381,0.0144837723499451));
#41947=DIRECTION('center_axis',(0.999604241409683,-0.0281309337996267,-0.000105448247542078));
#41948=DIRECTION('ref_axis',(0.0281275452130772,0.999529639708833,-0.0122204968727785));
#41949=DIRECTION('center_axis',(5.15167520928809E-67,-1.18789542670764E-48,
-1.));
#41950=DIRECTION('ref_axis',(0.,1.,0.));
#41951=DIRECTION('center_axis',(-0.686911553066313,-0.726741019928404,-9.0650146445407E-5));
#41952=DIRECTION('ref_axis',(0.726663889287897,-0.686840456251137,0.0144837723579623));
#41953=DIRECTION('center_axis',(0.998729922762429,0.0503838293465177,-0.00010544824700806));
#41954=DIRECTION('ref_axis',(0.0503813543051317,-0.998655285166875,0.0122204969886123));
#41955=DIRECTION('center_axis',(5.15167520928809E-67,-1.18789542670764E-48,
-1.));
#41956=DIRECTION('ref_axis',(0.,1.,0.));
#41957=DIRECTION('center_axis',(-0.627774590741284,-0.778395179200234,-9.06501463091932E-5));
#41958=DIRECTION('ref_axis',(0.778312708136324,-0.627709764694486,0.014483772322638));
#41959=DIRECTION('center_axis',(0.991698102029894,0.128587959432343,-0.000105448247307732));
#41960=DIRECTION('ref_axis',(0.128579636022594,-0.991623888707978,0.0122204968787672));
#41961=DIRECTION('center_axis',(5.15167520928809E-67,-1.18789542670764E-48,
-1.));
#41962=DIRECTION('ref_axis',(0.,1.,0.));
#41963=DIRECTION('center_axis',(-0.564767189308512,-0.825250273349312,-9.06501464604225E-5));
#41964=DIRECTION('ref_axis',(0.825162970323365,-0.564709033704023,0.014483772305219));
#41965=DIRECTION('center_axis',(0.978552132725239,0.205999301988023,-0.000105448247439453));
#41966=DIRECTION('ref_axis',(0.205985181526365,-0.978478801225051,0.0122204969104439));
#41967=DIRECTION('center_axis',(5.15167520928809E-67,-1.18789542670764E-48,
-1.));
#41968=DIRECTION('ref_axis',(0.,1.,0.));
#41969=DIRECTION('center_axis',(-0.498277810349565,-0.867017425139653,-9.06501466563663E-5));
#41970=DIRECTION('ref_axis',(0.86692582840462,-0.498226683736414,0.0144837722289047));
#41971=DIRECTION('center_axis',(0.959373064120893,0.282140590344525,-0.00010544824722367));
#41972=DIRECTION('ref_axis',(0.282120759888269,-0.959301066555644,0.0122204969322086));
#41973=DIRECTION('center_axis',(5.15167520928809E-67,-1.18789542670764E-48,
-1.));
#41974=DIRECTION('ref_axis',(0.,1.,0.));
#41975=DIRECTION('center_axis',(-0.428716382994794,-0.903439126191916,-9.06501464376821E-5));
#41976=DIRECTION('ref_axis',(0.903343800470677,-0.428672600584677,0.0144837722698243));
#41977=DIRECTION('center_axis',(0.934279141552165,0.356542388140901,-0.000105448247303552));
#41978=DIRECTION('ref_axis',(0.356516969951467,-0.934208921811066,0.0122204969306124));
#41979=DIRECTION('center_axis',(5.15167520928809E-67,-1.18789542670764E-48,
-1.));
#41980=DIRECTION('ref_axis',(0.,1.,0.));
#41981=DIRECTION('center_axis',(-0.356511776576584,-0.934290824606963,-9.06501462973138E-5));
#41982=DIRECTION('ref_axis',(0.9341923576135,-0.356475608302424,0.0144837723659048));
#41983=DIRECTION('center_axis',(0.903425077396469,0.42874598355186,-0.000105448247323971));
#41984=DIRECTION('ref_axis',(0.428715134340782,-0.903357068407445,0.0122204969404582));
#41985=DIRECTION('center_axis',(5.15167520928809E-67,-1.18789542670764E-48,
-1.));
#41986=DIRECTION('ref_axis',(0.,1.,0.));
#41987=DIRECTION('center_axis',(-0.282109156503611,-0.959382309405053,-9.06501462853803E-5));
#41988=DIRECTION('ref_axis',(0.959281308222382,-0.282080825355435,0.0144837723660616));
#41989=DIRECTION('center_axis',(0.867001097223284,0.498306217394775,-0.000105448243705777));
#41990=DIRECTION('ref_axis',(0.498270127348596,-0.86693571826834,0.0122204984583659));
#41991=DIRECTION('center_axis',(5.15167520928809E-67,-1.18789542670764E-48,
-1.));
#41992=DIRECTION('ref_axis',(0.,1.,0.));
#41993=DIRECTION('center_axis',(-0.205967239670074,-0.978558883238633,-9.06501462899978E-5));
#41994=DIRECTION('ref_axis',(0.978455970573443,-0.205946920318997,0.0144837723091262));
#41995=DIRECTION('center_axis',(0.825231766971361,0.564794227716602,-0.000105448246768021));
#41996=DIRECTION('ref_axis',(0.56475311935916,-0.825169421163415,0.0122204971638891));
#41997=DIRECTION('center_axis',(5.15167520928809E-67,-1.18789542670764E-48,
-1.));
#41998=DIRECTION('ref_axis',(0.,1.,0.));
#41999=DIRECTION('center_axis',(-0.128555466313085,-0.991702316153177,-9.06501463759606E-5));
#42000=DIRECTION('ref_axis',(0.991598126495219,-0.128543284034406,0.014483772327091));
#42001=DIRECTION('center_axis',(0.778374608461285,0.627800093806467,-0.000105448247278628));
#42002=DIRECTION('ref_axis',(0.627754220578617,-0.778315680171672,0.0122204969064386));
#42003=DIRECTION('center_axis',(5.15167520928809E-67,-1.18789542670764E-48,
-1.));
#42004=DIRECTION('ref_axis',(0.,1.,0.));
#42005=DIRECTION('center_axis',(-0.0503511057568215,-0.998731574514202,
-9.06501462140748E-5));
#42006=DIRECTION('ref_axis',(0.998626750226433,-0.0503471356583347,0.0144837724089729));
#42007=DIRECTION('center_axis',(0.72671851165485,0.686935363552371,-0.000105448247305609));
#42008=DIRECTION('ref_axis',(0.68688500827568,-0.726663364193057,0.0122204969517677));
#42009=DIRECTION('center_axis',(5.15167520928809E-67,-1.18789542670764E-48,
-1.));
#42010=DIRECTION('ref_axis',(0.,1.,0.));
#42011=DIRECTION('center_axis',(0.028163686109212,-0.999603320606376,-9.06501464412085E-5));
#42012=DIRECTION('ref_axis',(0.999498507967367,0.0281594195504058,0.0144837723535955));
#42013=DIRECTION('center_axis',(0.670581953565646,0.741835448352765,-0.000105448247317749));
#42014=DIRECTION('ref_axis',(0.741780921484837,-0.670530926934763,0.0122204969257884));
#42015=DIRECTION('center_axis',(5.15167520928809E-67,-1.18789542670764E-48,
-1.));
#42016=DIRECTION('ref_axis',(0.,1.,0.));
#42017=DIRECTION('center_axis',(0.106504839485654,-0.994312179825173,-9.06501463242885E-5));
#42018=DIRECTION('ref_axis',(0.994208025039066,0.106492362574368,0.0144837723417732));
#42019=DIRECTION('center_axis',(0.610311034742769,0.792161870927829,-0.000105448246632335));
#42020=DIRECTION('ref_axis',(0.792103508641049,-0.610264443535841,0.012220497306985));
#42021=DIRECTION('center_axis',(5.15167520928809E-67,-1.18789542670764E-48,
-1.));
#42022=DIRECTION('ref_axis',(0.,1.,0.));
#42023=DIRECTION('center_axis',(0.184189355110076,-0.982890773812984,-9.06501463014399E-5));
#42024=DIRECTION('ref_axis',(0.982787919027527,0.184168744770422,0.0144837724102069));
#42025=DIRECTION('center_axis',(0.546277345439608,0.837604352149702,-0.000105448247164003));
#42026=DIRECTION('ref_axis',(0.837542514274121,-0.546235476912526,0.0122204969428009));
#42027=DIRECTION('center_axis',(5.15167520928809E-67,-1.18789542670764E-48,
-1.));
#42028=DIRECTION('ref_axis',(0.,1.,0.));
#42029=DIRECTION('center_axis',(0.260738282110494,-0.965409519336027,-9.06501465102787E-5));
#42030=DIRECTION('ref_axis',(0.965308598687087,0.260709665412434,0.0144837723438797));
#42031=DIRECTION('center_axis',(0.47887567464682,0.877882724008293,-0.000105448247318393));
#42032=DIRECTION('ref_axis',(0.877817791791359,-0.47883878693017,0.0122204969532827));
#42033=DIRECTION('center_axis',(5.15167520928809E-67,-1.18789542670764E-48,
-1.));
#42034=DIRECTION('ref_axis',(0.,1.,0.));
#42035=DIRECTION('center_axis',(0.335679670898317,-0.941976194140886,-9.06501463025926E-5));
#42036=DIRECTION('ref_axis',(0.941877829837149,0.335643224273232,0.0144837723239312));
#42037=DIRECTION('center_axis',(0.408521576078182,0.912748656947391,-0.000105448247109452));
#42038=DIRECTION('ref_axis',(0.912681030717227,-0.408489896596761,0.0122204970155898));
#42039=DIRECTION('center_axis',(5.15167520928809E-67,-1.18789542670764E-48,
-1.));
#42040=DIRECTION('ref_axis',(0.,1.,0.));
#42041=DIRECTION('center_axis',(0.40855148288974,-0.912735272470143,-9.06501463607514E-5));
#42042=DIRECTION('ref_axis',(0.912640070959719,0.408507431042997,0.0144837723432182));
#42043=DIRECTION('center_axis',(0.33564880614496,0.941987190897058,-0.00010544824731253));
#42044=DIRECTION('ref_axis',(0.941917287593217,-0.335622530213924,0.0122204969555834));
#42045=DIRECTION('center_axis',(5.15167520928809E-67,-1.18789542670764E-48,
-1.));
#42046=DIRECTION('ref_axis',(0.,1.,0.));
#42047=DIRECTION('center_axis',(0.47890443913187,-0.877867034329425,-9.06501464476592E-5));
#42048=DIRECTION('ref_axis',(0.877775582561568,0.47885305365786,0.0144837723415746));
#42049=DIRECTION('center_axis',(0.260706649725499,0.965418060567325,-0.000105448239035086));
#42050=DIRECTION('ref_axis',(0.965346311123191,-0.260685939332472,0.0122205006114622));
#42051=DIRECTION('center_axis',(5.15167520928809E-67,-1.18789542670764E-48,
-1.));
#42052=DIRECTION('ref_axis',(0.,1.,0.));
#42053=DIRECTION('center_axis',(0.546304790255255,-0.837586454001444,-9.0650146342598E-5));
#42054=DIRECTION('ref_axis',(0.837499315807156,0.546246387962813,0.0144837723030219));
#42055=DIRECTION('center_axis',(0.184157150081292,0.982896806869675,-0.000105448247335927));
#42056=DIRECTION('ref_axis',(0.982823653730575,-0.184142132936566,0.0122204969315608));
#42057=DIRECTION('center_axis',(5.15167520928809E-67,-1.18789542670764E-48,
-1.));
#42058=DIRECTION('ref_axis',(0.,1.,0.));
#42059=DIRECTION('center_axis',(0.610336990681674,-0.792141874658946,-9.06501464101343E-5));
#42060=DIRECTION('ref_axis',(0.792059587273886,0.610271931640238,0.0144837722853376));
#42061=DIRECTION('center_axis',(0.106472260386401,0.99431566750649,-0.000105448247238185));
#42062=DIRECTION('ref_axis',(0.994241561642249,-0.106463029063635,0.0122204969529716));
#42063=DIRECTION('center_axis',(5.15167520928809E-67,-1.18789542670764E-48,
-1.));
#42064=DIRECTION('ref_axis',(0.,1.,0.));
#42065=DIRECTION('center_axis',(0.670606260602894,-0.741813477245294,-9.06501464627064E-5));
#42066=DIRECTION('ref_axis',(0.741736547997723,0.670534945922382,0.0144837723432088));
#42067=DIRECTION('center_axis',(0.0281309337999561,0.999604241409674,-0.000105448247417899));
#42068=DIRECTION('ref_axis',(0.999529639708026,-0.0281275452133787,0.0122204969380853));
#42069=DIRECTION('center_axis',(5.15167520928809E-67,-1.18789542670764E-48,
-1.));
#42070=DIRECTION('ref_axis',(0.,1.,0.));
#42071=DIRECTION('center_axis',(0.726741019928368,-0.686911553066351,-9.0650146471134E-5));
#42072=DIRECTION('ref_axis',(0.686840456251459,0.726663889288164,0.0144837723292476));
#42073=DIRECTION('center_axis',(-0.050383829347144,0.998729922762398,-0.000105448247269544));
#42074=DIRECTION('ref_axis',(0.998655285167744,0.0503813543057988,0.0122204969148411));
#42075=DIRECTION('center_axis',(5.15167520928809E-67,-1.18789542670764E-48,
-1.));
#42076=DIRECTION('ref_axis',(0.,1.,0.));
#42077=DIRECTION('center_axis',(0.778395179200218,-0.627774590741304,-9.06501463631465E-5));
#42078=DIRECTION('ref_axis',(0.627709764694807,0.778312708136684,0.0144837722894029));
#42079=DIRECTION('center_axis',(-0.12858795942834,0.991698102030413,-0.000105448245500489));
#42080=DIRECTION('ref_axis',(0.991623888698102,0.128579636017312,0.0122204977357358));
#42081=DIRECTION('center_axis',(5.15167520928809E-67,-1.18789542670764E-48,
-1.));
#42082=DIRECTION('ref_axis',(0.,1.,0.));
#42083=DIRECTION('center_axis',(0.825250273349428,-0.564767189308343,-9.06501464028957E-5));
#42084=DIRECTION('ref_axis',(0.564709033703531,0.825162970323003,0.0144837723450398));
#42085=DIRECTION('center_axis',(-0.205999301987628,0.978552132725322,-0.000105448247257059));
#42086=DIRECTION('ref_axis',(0.978478801225208,0.205985181525983,0.0122204969042825));
#42087=DIRECTION('center_axis',(5.15167520928809E-67,-1.18789542670764E-48,
-1.));
#42088=DIRECTION('ref_axis',(0.,1.,0.));
#42089=DIRECTION('center_axis',(0.867017425139937,-0.498277810349071,-9.06501464136658E-5));
#42090=DIRECTION('ref_axis',(0.498226683735389,0.866925828403975,0.0144837723027363));
#42091=DIRECTION('center_axis',(-0.282140590344626,0.959373064120863,-0.000105448247277017));
#42092=DIRECTION('ref_axis',(0.959301066555094,0.282120759888223,0.0122204969764503));
#42093=DIRECTION('center_axis',(5.15167520928809E-67,-1.18789542670764E-48,
-1.));
#42094=DIRECTION('ref_axis',(0.,1.,0.));
#42095=DIRECTION('center_axis',(0.90343912619187,-0.42871638299489,-9.06501464260602E-5));
#42096=DIRECTION('ref_axis',(0.428672600584421,0.903343800469878,0.0144837723272369));
#42097=DIRECTION('center_axis',(-0.356542388139781,0.934279141552593,-0.000105448246761887));
#42098=DIRECTION('ref_axis',(0.934208921809314,0.35651696994953,0.012220497120973));
#42099=DIRECTION('center_axis',(5.15167520928809E-67,-1.18789542670764E-48,
-1.));
#42100=DIRECTION('ref_axis',(0.,1.,0.));
#42101=DIRECTION('center_axis',(0.934290824606888,-0.35651177657678,-9.06501464134324E-5));
#42102=DIRECTION('ref_axis',(0.356475608302711,0.934192357613664,0.0144837723482609));
#42103=DIRECTION('center_axis',(-0.428745983551679,0.903425077396555,-0.000105448247222545));
#42104=DIRECTION('ref_axis',(0.903357068407448,0.428715134340562,0.0122204969479439));
#42105=DIRECTION('center_axis',(5.15167520928809E-67,-1.18789542670764E-48,
-1.));
#42106=DIRECTION('ref_axis',(0.,1.,0.));
#42107=DIRECTION('center_axis',(0.959382309405034,-0.282109156503675,-9.06501462956451E-5));
#42108=DIRECTION('ref_axis',(0.282080825355574,0.959281308222623,0.0144837723473633));
#42109=DIRECTION('center_axis',(-0.498306217401744,0.867001097219279,-0.000105448247347347));
#42110=DIRECTION('ref_axis',(0.866935718280794,0.498270127364887,0.0122204969106369));
#42111=DIRECTION('center_axis',(5.15167520928809E-67,-1.18789542670764E-48,
-1.));
#42112=DIRECTION('ref_axis',(0.,1.,0.));
#42113=DIRECTION('center_axis',(0.978558883238587,-0.205967239670296,-9.06501464061553E-5));
#42114=DIRECTION('ref_axis',(0.205946920319019,0.978455970572407,0.0144837723787919));
#42115=DIRECTION('center_axis',(-0.564794227717559,0.825231766970706,-0.000105448247271081));
#42116=DIRECTION('ref_axis',(0.825169421165301,0.564753119361831,0.0122204969131223));
#42117=DIRECTION('center_axis',(5.15167520928809E-67,-1.18789542670764E-48,
-1.));
#42118=DIRECTION('ref_axis',(0.,1.,0.));
#42119=DIRECTION('center_axis',(0.99170231615319,-0.128555466312983,-9.06501463191467E-5));
#42120=DIRECTION('ref_axis',(0.128543284034309,0.991598126495285,0.014483772323378));
#42121=DIRECTION('center_axis',(-0.627800093806562,0.778374608461208,-0.000105448247350595));
#42122=DIRECTION('ref_axis',(0.778315680171392,0.627754220578551,0.0122204969276863));
#42123=DIRECTION('center_axis',(5.15167520928809E-67,-1.18789542670764E-48,
-1.));
#42124=DIRECTION('ref_axis',(0.,1.,0.));
#42125=DIRECTION('center_axis',(0.998731574514188,-0.0503511057570843,-9.06501463742907E-5));
#42126=DIRECTION('ref_axis',(0.0503471356586318,0.998626750227146,0.0144837723587898));
#42127=DIRECTION('center_axis',(-0.686935363552425,0.726718511654798,-0.000105448247333776));
#42128=DIRECTION('ref_axis',(0.726663364192883,0.686885008275621,0.0122204969654078));
#42129=DIRECTION('center_axis',(5.15167520928809E-67,-1.18789542670764E-48,
-1.));
#42130=DIRECTION('ref_axis',(0.,1.,0.));
#42131=DIRECTION('center_axis',(0.999603320606373,0.0281636861093081,-9.0650146390368E-5));
#42132=DIRECTION('ref_axis',(0.0281594195505035,-0.99949850796739,-0.0144837723518616));
#42133=DIRECTION('center_axis',(-0.741835448352795,0.670581953565614,-0.000105448247334273));
#42134=DIRECTION('ref_axis',(0.670530926935027,0.741780921485189,0.0122204968899333));
#42135=DIRECTION('center_axis',(5.15167520928809E-67,-1.18789542670764E-48,
-1.));
#42136=DIRECTION('ref_axis',(0.,1.,0.));
#42137=DIRECTION('center_axis',(0.994312179825183,0.106504839485559,-9.06501463756277E-5));
#42138=DIRECTION('ref_axis',(0.106492362574294,-0.994208025039266,-0.0144837723286163));
#42139=DIRECTION('center_axis',(-0.792161870920044,0.610311034752874,-0.00010544824088436));
#42140=DIRECTION('ref_axis',(0.610264443527485,0.792103508609612,0.0122204997619462));
#42141=DIRECTION('center_axis',(5.15167520928809E-67,-1.18789542670764E-48,
-1.));
#42142=DIRECTION('ref_axis',(0.,1.,0.));
#42143=DIRECTION('center_axis',(0.982890773813025,0.184189355109853,-9.06501463812825E-5));
#42144=DIRECTION('ref_axis',(0.184168744770323,-0.982787919028214,-0.0144837723648623));
#42145=DIRECTION('center_axis',(-0.837604352149864,0.54627734543936,-0.00010544824728987));
#42146=DIRECTION('ref_axis',(0.546235476912709,0.837542514274935,0.0122204968788532));
#42147=DIRECTION('center_axis',(5.15167520928809E-67,-1.18789542670764E-48,
-1.));
#42148=DIRECTION('ref_axis',(0.,1.,0.));
#42149=DIRECTION('center_axis',(-0.778374608461274,-0.62780009380648,-0.000105448247267533));
#42150=DIRECTION('ref_axis',(0.627754220578446,-0.77831568017143,-0.0122204969306265));
#42151=DIRECTION('center_axis',(0.128555466313028,0.991702316153185,-9.06501463500336E-5));
#42152=DIRECTION('ref_axis',(0.991598126495177,-0.128543284034342,-0.0144837723304925));
#42153=DIRECTION('center_axis',(5.15167520928809E-67,-1.18789542670764E-48,
-1.));
#42154=DIRECTION('ref_axis',(0.,1.,0.));
#42155=DIRECTION('center_axis',(-0.825231766970672,-0.564794227717608,-0.000105448247309068));
#42156=DIRECTION('ref_axis',(0.564753119361638,-0.825169421164907,-0.012220496948613));
#42157=DIRECTION('center_axis',(0.205967239670274,0.978558883238591,-9.0650146374353E-5));
#42158=DIRECTION('ref_axis',(0.978455970572943,-0.205946920319105,-0.0144837723413512));
#42159=DIRECTION('center_axis',(5.15167520928809E-67,-1.18789542670764E-48,
-1.));
#42160=DIRECTION('ref_axis',(0.,1.,0.));
#42161=DIRECTION('center_axis',(-0.86700109721932,-0.498306217401672,-0.00010544824729092));
#42162=DIRECTION('ref_axis',(0.498270127364739,-0.8669357182807,-0.0122204969233888));
#42163=DIRECTION('center_axis',(0.282109156504052,0.959382309404923,-9.06501464701313E-5));
#42164=DIRECTION('ref_axis',(0.959281308222407,-0.282080825355923,-0.0144837723548786));
#42165=DIRECTION('center_axis',(5.15167520928809E-67,-1.18789542670764E-48,
-1.));
#42166=DIRECTION('ref_axis',(0.,1.,0.));
#42167=DIRECTION('center_axis',(-0.903425077396529,-0.428745983551733,-0.000105448247249315));
#42168=DIRECTION('ref_axis',(0.428715134340504,-0.903357068407182,-0.0122204969696425));
#42169=DIRECTION('center_axis',(0.356511776576785,0.934290824606886,-9.06501464239672E-5));
#42170=DIRECTION('ref_axis',(0.934192357613866,-0.356475608302793,-0.0144837723332318));
#42171=DIRECTION('center_axis',(5.15167520928809E-67,-1.18789542670764E-48,
-1.));
#42172=DIRECTION('ref_axis',(0.,1.,0.));
#42173=DIRECTION('center_axis',(-0.934279141552621,-0.356542388139705,-0.000105448246733279));
#42174=DIRECTION('ref_axis',(0.356516969949183,-0.934208921808614,-0.0122204971846563));
#42175=DIRECTION('center_axis',(0.428716382994808,0.903439126191909,-9.06501463770139E-5));
#42176=DIRECTION('ref_axis',(0.903343800469329,-0.428672600584064,-0.0144837723720362));
#42177=DIRECTION('center_axis',(5.15167520928809E-67,-1.18789542670764E-48,
-1.));
#42178=DIRECTION('ref_axis',(0.,1.,0.));
#42179=DIRECTION('center_axis',(-0.959373064120865,-0.282140590344618,-0.000105448247270857));
#42180=DIRECTION('ref_axis',(0.282120759888191,-0.959301066555013,-0.0122204969835453));
#42181=DIRECTION('center_axis',(0.498277810349034,0.867017425139958,-9.06501463569771E-5));
#42182=DIRECTION('ref_axis',(0.866925828403698,-0.498226683735182,-0.0144837723264648));
#42183=DIRECTION('center_axis',(5.15167520928809E-67,-1.18789542670764E-48,
-1.));
#42184=DIRECTION('ref_axis',(0.,1.,0.));
#42185=DIRECTION('center_axis',(-0.978552132725285,-0.205999301987804,-0.000105448247338301));
#42186=DIRECTION('ref_axis',(0.205985181526041,-0.978478801224581,-0.0122204969535068));
#42187=DIRECTION('center_axis',(0.564767189308271,0.825250273349477,-9.06501463565956E-5));
#42188=DIRECTION('ref_axis',(0.825162970322881,-0.564709033703342,-0.0144837723594094));
#42189=DIRECTION('center_axis',(5.15167520928809E-67,-1.18789542670764E-48,
-1.));
#42190=DIRECTION('ref_axis',(0.,1.,0.));
#42191=DIRECTION('center_axis',(-0.991698102030424,-0.128587959428258,-0.000105448245434831));
#42192=DIRECTION('ref_axis',(0.128579636017166,-0.991623888697594,-0.0122204977785004));
#42193=DIRECTION('center_axis',(0.627774590741263,0.778395179200251,-9.06501463298504E-5));
#42194=DIRECTION('ref_axis',(0.778312708136619,-0.627709764694687,-0.0144837722981268));
#42195=DIRECTION('center_axis',(5.15167520928809E-67,-1.18789542670764E-48,
-1.));
#42196=DIRECTION('ref_axis',(0.,1.,0.));
#42197=DIRECTION('center_axis',(-0.998729922762387,-0.0503838293473624,
-0.000105448247373321));
#42198=DIRECTION('ref_axis',(0.0503813543060242,-0.998655285167869,-0.0122204969036645));
#42199=DIRECTION('center_axis',(0.686911553066443,0.726741019928282,-9.06501464895761E-5));
#42200=DIRECTION('ref_axis',(0.726663889287984,-0.686840456251464,-0.0144837723380814));
#42201=DIRECTION('center_axis',(5.15167520928809E-67,-1.18789542670764E-48,
-1.));
#42202=DIRECTION('ref_axis',(0.,1.,0.));
#42203=DIRECTION('center_axis',(-0.999604241409666,0.0281309338002504,-0.00010544824728445));
#42204=DIRECTION('ref_axis',(0.0281275452136831,0.999529639708247,0.0122204969192793));
#42205=DIRECTION('center_axis',(0.741813477245179,0.670606260603021,-9.06501463486941E-5));
#42206=DIRECTION('ref_axis',(0.670534945922386,-0.741736547997471,-0.0144837723559454));
#42207=DIRECTION('center_axis',(5.15167520928809E-67,-1.18789542670764E-48,
-1.));
#42208=DIRECTION('ref_axis',(0.,1.,0.));
#42209=DIRECTION('center_axis',(-0.994315667506492,0.106472260386385,-0.000105448247246095));
#42210=DIRECTION('ref_axis',(0.106463029063669,0.99424156164268,0.0122204969176238));
#42211=DIRECTION('center_axis',(0.792141874658893,0.610336990681743,-9.06501463537118E-5));
#42212=DIRECTION('ref_axis',(0.610271931639807,-0.792059587273192,-0.0144837723414781));
#42213=DIRECTION('center_axis',(5.15167520928809E-67,-1.18789542670764E-48,
-1.));
#42214=DIRECTION('ref_axis',(0.,1.,0.));
#42215=DIRECTION('center_axis',(-0.98289680686965,0.184157150081429,-0.000105448247288298));
#42216=DIRECTION('ref_axis',(0.184142132936832,0.982823653731204,0.0122204968770007));
#42217=DIRECTION('center_axis',(0.837586454001503,0.546304790255165,-9.06501464022278E-5));
#42218=DIRECTION('ref_axis',(0.546246387962582,-0.837499315807004,-0.0144837723204838));
#42219=DIRECTION('center_axis',(5.15167520928809E-67,-1.18789542670764E-48,
-1.));
#42220=DIRECTION('ref_axis',(0.,1.,0.));
#42221=DIRECTION('center_axis',(-0.965418060567323,0.260706649725506,-0.000105448239021929));
#42222=DIRECTION('ref_axis',(0.260685939332638,0.965346311123758,0.0122205005631217));
#42223=DIRECTION('center_axis',(0.877867034329392,0.478904439131931,-9.06501464072983E-5));
#42224=DIRECTION('ref_axis',(0.478853053658107,-0.87777558256187,-0.0144837723150808));
#42225=DIRECTION('center_axis',(5.15167520928809E-67,-1.18789542670764E-48,
-1.));
#42226=DIRECTION('ref_axis',(0.,1.,0.));
#42227=DIRECTION('center_axis',(-0.94198719089703,0.335648806145038,-0.000105448247300868));
#42228=DIRECTION('ref_axis',(0.335622530213848,0.941917287592769,0.0122204969921728));
#42229=DIRECTION('center_axis',(0.912735272470196,0.40855148288962,-9.06501464040206E-5));
#42230=DIRECTION('ref_axis',(0.408507431043198,-0.912640070960478,-0.01448377228974));
#42231=DIRECTION('center_axis',(5.15167520928809E-67,-1.18789542670764E-48,
-1.));
#42232=DIRECTION('ref_axis',(0.,1.,0.));
#42233=DIRECTION('center_axis',(0.965409519335958,0.260738282110751,-9.06501464007405E-5));
#42234=DIRECTION('ref_axis',(0.260709665412327,-0.965308598685698,-0.0144837724383535));
#42235=DIRECTION('center_axis',(-0.87788272400828,0.478875674646843,-0.000105448247307507));
#42236=DIRECTION('ref_axis',(0.478838786930294,0.877817791791527,0.0122204969363654));
#42237=DIRECTION('center_axis',(5.15167520928809E-67,-1.18789542670764E-48,
-1.));
#42238=DIRECTION('ref_axis',(-4.33680868994202E-19,1.,-1.18789542670764E-48));
#42239=DIRECTION('center_axis',(5.15167520928809E-67,-1.18789542670764E-48,
-1.));
#42240=DIRECTION('ref_axis',(-4.33680868994202E-19,1.,-1.18789542670764E-48));
#42241=DIRECTION('center_axis',(5.15167520928809E-67,-1.18789542670764E-48,
-1.));
#42242=DIRECTION('ref_axis',(0.,1.,0.));
#42243=DIRECTION('center_axis',(0.941987190897879,0.335648806142656,0.000105448247691596));
#42244=DIRECTION('ref_axis',(0.335622530211987,-0.941917287595053,0.0122204968672344));
#42245=DIRECTION('center_axis',(-0.912735272471169,0.408551482887447,9.06501467246596E-5));
#42246=DIRECTION('ref_axis',(0.408507431040732,0.912640070960819,-0.0144837723377799));
#42247=DIRECTION('center_axis',(5.15167520928809E-67,-1.18789542670764E-48,
-1.));
#42248=DIRECTION('ref_axis',(-4.33680868994202E-19,1.,-1.18789542670764E-48));
#42249=DIRECTION('center_axis',(5.15167520928809E-67,-1.18789542670764E-48,
-1.));
#42250=DIRECTION('ref_axis',(-4.33680868994202E-19,1.,-1.18789542670764E-48));
#42251=DIRECTION('',(-5.15167520928809E-67,1.18789542670764E-48,1.));
#42252=DIRECTION('',(5.15167520928809E-67,-1.18789542670764E-48,-1.));
#42253=DIRECTION('center_axis',(5.15167520928809E-67,-1.18789542670764E-48,
-1.));
#42254=DIRECTION('ref_axis',(-4.33680868994202E-19,1.,-1.18789542670764E-48));
#42255=DIRECTION('center_axis',(5.15167520928809E-67,-1.18789542670764E-48,
-1.));
#42256=DIRECTION('ref_axis',(0.,1.,0.));
#42257=DIRECTION('center_axis',(0.941976194140935,0.33567967089818,-9.06501463865783E-5));
#42258=DIRECTION('ref_axis',(0.335643224273153,-0.94187782983736,-0.014483772312066));
#42259=DIRECTION('center_axis',(-0.912748656947277,0.408521576078436,-0.000105448246989675));
#42260=DIRECTION('ref_axis',(0.408489896596946,0.91268103071696,0.012220497029356));
#42261=DIRECTION('center_axis',(-5.15167520928809E-67,1.18789542670764E-48,
1.));
#42262=DIRECTION('ref_axis',(4.33680868994202E-19,-1.,1.18789542670764E-48));
#42263=DIRECTION('center_axis',(0.,0.,1.));
#42264=DIRECTION('ref_axis',(1.,4.33680868994202E-19,0.));
#42265=DIRECTION('',(0.866025403784438,0.5,0.));
#42266=DIRECTION('',(-4.33680868994202E-19,1.,0.));
#42267=DIRECTION('',(-0.866025403784439,0.499999999999999,0.));
#42268=DIRECTION('',(-0.866025403784439,-0.5,0.));
#42269=DIRECTION('',(6.01359520363859E-16,-1.,0.));
#42270=DIRECTION('',(0.866025403784439,-0.5,0.));
#42271=DIRECTION('center_axis',(1.,4.33680868994202E-19,0.));
#42272=DIRECTION('ref_axis',(0.,0.,-1.));
#42273=DIRECTION('',(0.,0.,1.));
#42274=DIRECTION('',(0.,0.,1.));
#42275=DIRECTION('center_axis',(0.499999999999999,0.866025403784439,0.));
#42276=DIRECTION('ref_axis',(-0.866025403784439,0.499999999999999,0.));
#42277=DIRECTION('',(0.,0.,1.));
#42278=DIRECTION('center_axis',(-0.5,0.866025403784439,0.));
#42279=DIRECTION('ref_axis',(-0.866025403784439,-0.5,0.));
#42280=DIRECTION('',(0.,0.,1.));
#42281=DIRECTION('center_axis',(-1.,-6.01359520363859E-16,0.));
#42282=DIRECTION('ref_axis',(6.01359520363859E-16,-1.,0.));
#42283=DIRECTION('',(0.,0.,1.));
#42284=DIRECTION('center_axis',(-0.5,-0.866025403784439,0.));
#42285=DIRECTION('ref_axis',(0.866025403784439,-0.5,0.));
#42286=DIRECTION('',(0.,0.,1.));
#42287=DIRECTION('center_axis',(0.5,-0.866025403784439,0.));
#42288=DIRECTION('ref_axis',(0.866025403784439,0.5,0.));
#42289=DIRECTION('',(1.0568194522281E-16,0.866025403784468,-0.499999999999949));
#42290=DIRECTION('center_axis',(4.70261923768679E-35,-1.08435016942139E-16,
1.));
#42291=DIRECTION('ref_axis',(0.378466979033695,0.925614793410903,1.00369055805406E-16));
#42292=DIRECTION('center_axis',(0.912653256146669,-0.408734674385332,0.));
#42293=DIRECTION('ref_axis',(0.408734674385332,0.912653256146669,0.));
#42294=DIRECTION('',(0.,0.,1.));
#42295=DIRECTION('center_axis',(0.,0.,1.));
#42296=DIRECTION('ref_axis',(1.,4.33680868994202E-19,0.));
#42297=DIRECTION('',(0.,0.,1.));
#42298=DIRECTION('center_axis',(-0.912653256146668,-0.408734674385334,0.));
#42299=DIRECTION('ref_axis',(0.408734674385334,-0.912653256146668,0.));
#42300=DIRECTION('center_axis',(0.877770897795706,-0.479080630982844,8.35636401295593E-50));
#42301=DIRECTION('ref_axis',(0.479080630982844,0.877770897795706,2.97282767021015E-66));
#42302=DIRECTION('',(-9.32012009987243E-50,3.66188516048321E-51,1.));
#42303=DIRECTION('center_axis',(-9.32012009987243E-50,3.66188516048321E-51,
1.));
#42304=DIRECTION('ref_axis',(1.,4.33680868994202E-19,9.32012009987243E-50));
#42305=DIRECTION('',(-9.32012009987243E-50,3.66188516048321E-51,1.));
#42306=DIRECTION('center_axis',(-0.941908803685482,-0.335868732602165,-8.65571190069724E-50));
#42307=DIRECTION('ref_axis',(0.335868732602165,-0.941908803685482,-2.86613947502886E-66));
#42308=DIRECTION('center_axis',(0.941908803685478,-0.335868732602176,-8.65571190069562E-50));
#42309=DIRECTION('ref_axis',(0.335868732602176,0.941908803685478,5.69318196416785E-66));
#42310=DIRECTION('',(9.32012009987071E-50,3.66188516048189E-51,1.));
#42311=DIRECTION('center_axis',(9.32012009987071E-50,3.66188516048189E-51,
1.));
#42312=DIRECTION('ref_axis',(1.,4.33680868994202E-19,-9.32012009987071E-50));
#42313=DIRECTION('',(9.32012009987071E-50,3.66188516048189E-51,1.));
#42314=DIRECTION('center_axis',(-0.877770897795712,-0.479080630982834,8.35636401295441E-50));
#42315=DIRECTION('ref_axis',(0.479080630982834,-0.877770897795712,-1.78392693329902E-66));
#42316=DIRECTION('center_axis',(0.965357170233111,-0.260932048394827,-1.75574063469501E-49));
#42317=DIRECTION('ref_axis',(0.260932048394827,0.965357170233111,-8.03239509524584E-66));
#42318=DIRECTION('',(1.85827785600731E-49,1.46249639022155E-50,1.));
#42319=DIRECTION('center_axis',(1.8582778560073E-49,1.46249639022155E-50,
1.));
#42320=DIRECTION('ref_axis',(1.,4.33680868994202E-19,-1.8582778560073E-49));
#42321=DIRECTION('',(1.85827785600731E-49,1.46249639022155E-50,1.));
#42322=DIRECTION('center_axis',(-0.837476789971396,-0.546472896179862,1.63618603752562E-49));
#42323=DIRECTION('ref_axis',(0.546472896179862,-0.837476789971396,1.23627039651628E-65));
#42324=DIRECTION('center_axis',(0.982853788812423,-0.184386631340412,-2.66502014323869E-49));
#42325=DIRECTION('ref_axis',(0.184386631340412,0.982853788812423,-4.59929189808117E-66));
#42326=DIRECTION('',(2.77308680110516E-49,3.28216451991643E-50,1.));
#42327=DIRECTION('center_axis',(2.77308680110516E-49,3.28216451991643E-50,
1.));
#42328=DIRECTION('ref_axis',(1.,4.33680868994202E-19,-2.77308680110516E-49));
#42329=DIRECTION('',(2.77308680110516E-49,3.28216451991643E-50,1.));
#42330=DIRECTION('center_axis',(-0.792019359247614,-0.610495974251263,2.39671325397326E-49));
#42331=DIRECTION('ref_axis',(0.610495974251263,-0.792019359247614,-2.26955332198497E-65));
#42332=DIRECTION('center_axis',(0.994290786951656,-0.106704409389008,-3.5878037051643E-49));
#42333=DIRECTION('ref_axis',(0.106704409389008,0.994290786951656,1.37166247450949E-66));
#42334=DIRECTION('',(3.67079874392927E-49,5.81397404601223E-50,1.));
#42335=DIRECTION('center_axis',(3.67079874392927E-49,5.81397404601223E-50,
1.));
#42336=DIRECTION('ref_axis',(1.,4.33680868994202E-19,-3.67079874392927E-49));
#42337=DIRECTION('',(3.67079874392927E-49,5.81397404601223E-50,1.));
#42338=DIRECTION('center_axis',(-0.741678865800908,-0.670755141630892,3.11252914744798E-49));
#42339=DIRECTION('ref_axis',(0.670755141630892,-0.741678865800908,-3.59898235302298E-65));
#42340=DIRECTION('center_axis',(0.999597651754094,-0.028364319270904,-4.5184020529559E-49));
#42341=DIRECTION('ref_axis',(0.028364319270904,0.999597651754094,-3.26521667006146E-66));
#42342=DIRECTION('',(4.54587899183259E-49,9.04231552086841E-50,1.));
#42343=DIRECTION('center_axis',(4.54587899183259E-49,9.04231552086841E-50,
1.));
#42344=DIRECTION('ref_axis',(1.,4.33680868994202E-19,-4.54587899183259E-49));
#42345=DIRECTION('',(4.54587899183259E-49,9.04231552086841E-50,1.));
#42346=DIRECTION('center_axis',(-0.68676567551329,-0.726878880513649,3.77922047493358E-49));
#42347=DIRECTION('ref_axis',(0.726878880513649,-0.68676567551329,8.44347396578498E-67));
#42348=DIRECTION('center_axis',(0.998741664633518,0.0501506463075991,-5.45107773834402E-49));
#42349=DIRECTION('ref_axis',(-0.0501506463075991,0.998741664633518,-5.68155672720376E-65));
#42350=DIRECTION('center_axis',(-0.62761834646337,-0.778521169386283,4.39267686269876E-49));
#42351=DIRECTION('ref_axis',(0.778521169386283,-0.62761834646337,2.86838711888421E-65));
#42352=DIRECTION('center_axis',(0.991728103035171,0.128356416474834,-6.38008050558209E-49));
#42353=DIRECTION('ref_axis',(-0.128356416474834,0.991728103035171,2.64164793875071E-66));
#42354=DIRECTION('center_axis',(-0.564601541603225,-0.825363616365092,4.94911614811798E-49));
#42355=DIRECTION('ref_axis',(0.825363616365092,-0.564601541603225,-1.21982614064914E-65));
#42356=DIRECTION('center_axis',(0.978600207898554,0.20577082665166,-7.29968274368531E-49));
#42357=DIRECTION('ref_axis',(-0.20577082665166,0.978600207898554,7.99368498149713E-66));
#42358=DIRECTION('center_axis',(-0.498103780490032,-0.867117422187756,5.44510769796179E-49));
#42359=DIRECTION('ref_axis',(0.867117422187756,-0.498103780490032,-1.67935322369464E-65));
#42360=DIRECTION('center_axis',(0.95943891706265,0.281916591256437,-8.20421479905702E-49));
#42361=DIRECTION('ref_axis',(-0.281916591256437,0.95943891706265,1.24589067679861E-65));
#42362=DIRECTION('center_axis',(-0.428535043933802,-0.903525160756829,5.87759355939149E-49));
#42363=DIRECTION('ref_axis',(0.903525160756829,-0.428535043933802,-8.86364012879408E-65));
#42364=DIRECTION('center_axis',(0.93436236625724,0.356324246329338,-9.08809993078841E-49));
#42365=DIRECTION('ref_axis',(-0.356324246329338,0.93436236625724,-2.69950222050985E-65));
#42366=DIRECTION('center_axis',(-0.356324246329358,-0.934362366257233,6.24390731325522E-49));
#42367=DIRECTION('ref_axis',(0.934362366257233,-0.356324246329358,4.50754916861586E-65));
#42368=DIRECTION('center_axis',(0.903525160756839,0.428535043933782,-9.94588869312071E-49));
#42369=DIRECTION('ref_axis',(-0.428535043933782,0.903525160756839,-3.06876799885187E-65));
#42370=DIRECTION('center_axis',(-0.281916591256458,-0.959438917062644,6.54179051344872E-49));
#42371=DIRECTION('ref_axis',(0.959438917062644,-0.281916591256458,5.46345068117847E-65));
#42372=DIRECTION('center_axis',(0.867117422187767,0.498103780490012,-1.07722925330905E-48));
#42373=DIRECTION('ref_axis',(-0.498103780490012,0.867117422187767,2.63677046246647E-65));
#42374=DIRECTION('center_axis',(-0.205770826651682,-0.978600207898549,6.76940661098659E-49));
#42375=DIRECTION('ref_axis',(0.978600207898549,-0.205770826651682,1.20007194121145E-65));
#42376=DIRECTION('center_axis',(0.825363616365104,0.564601541603207,-1.15622163962171E-48));
#42377=DIRECTION('ref_axis',(-0.564601541603207,0.825363616365104,5.34857418276646E-65));
#42378=DIRECTION('center_axis',(-0.128356416474855,-0.991728103035168,6.92535227693746E-49));
#42379=DIRECTION('ref_axis',(0.991728103035168,-0.128356416474855,1.05782428992148E-64));
#42380=DIRECTION('center_axis',(0.778521169386297,0.627618346463353,-1.2310790139208E-48));
#42381=DIRECTION('ref_axis',(-0.627618346463353,0.778521169386297,-3.24299836420865E-65));
#42382=DIRECTION('center_axis',(-0.0501506463076206,-0.998741664633517,
7.00866605441356E-49));
#42383=DIRECTION('ref_axis',(0.998741664633517,-0.0501506463076206,5.61717615944791E-66));
#42384=DIRECTION('center_axis',(0.83747678997139,-0.546472896179871,1.63618603752577E-49));
#42385=DIRECTION('ref_axis',(0.546472896179871,0.83747678997139,8.18221406165844E-66));
#42386=DIRECTION('',(-1.85827785600747E-49,1.46249639022181E-50,1.));
#42387=DIRECTION('center_axis',(-1.85827785600747E-49,1.46249639022181E-50,
1.));
#42388=DIRECTION('ref_axis',(1.,4.33680868994202E-19,1.85827785600747E-49));
#42389=DIRECTION('',(-1.85827785600747E-49,1.46249639022181E-50,1.));
#42390=DIRECTION('center_axis',(-0.965357170233114,-0.260932048394816,-1.75574063469517E-49));
#42391=DIRECTION('ref_axis',(0.260932048394816,-0.965357170233114,4.85072620126884E-66));
#42392=DIRECTION('center_axis',(0.792019359247608,-0.610495974251272,2.39671325397339E-49));
#42393=DIRECTION('ref_axis',(0.610495974251272,0.792019359247608,6.86514884131891E-66));
#42394=DIRECTION('',(-2.77308680110532E-49,3.28216451991683E-50,1.));
#42395=DIRECTION('center_axis',(-2.77308680110532E-49,3.28216451991683E-50,
1.));
#42396=DIRECTION('ref_axis',(1.,4.33680868994202E-19,2.77308680110532E-49));
#42397=DIRECTION('',(-2.77308680110532E-49,3.28216451991683E-50,1.));
#42398=DIRECTION('center_axis',(-0.982853788812425,-0.184386631340402,-2.66502014323885E-49));
#42399=DIRECTION('ref_axis',(0.184386631340402,-0.982853788812425,5.0100483719309E-66));
#42400=DIRECTION('center_axis',(0.741678865800901,-0.6707551416309,3.11252914744811E-49));
#42401=DIRECTION('ref_axis',(0.6707551416309,0.741678865800901,2.48321099822104E-65));
#42402=DIRECTION('',(-3.67079874392942E-49,5.81397404601274E-50,1.));
#42403=DIRECTION('center_axis',(-3.67079874392942E-49,5.81397404601274E-50,
1.));
#42404=DIRECTION('ref_axis',(1.,4.33680868994202E-19,3.67079874392942E-49));
#42405=DIRECTION('',(-3.67079874392942E-49,5.81397404601274E-50,1.));
#42406=DIRECTION('center_axis',(-0.994290786951657,-0.106704409388997,-3.58780370516446E-49));
#42407=DIRECTION('ref_axis',(0.106704409388997,-0.994290786951657,8.97464790050996E-66));
#42408=DIRECTION('center_axis',(0.686765675513281,-0.726878880513656,3.77922047493371E-49));
#42409=DIRECTION('ref_axis',(0.726878880513657,0.686765675513281,3.1589153081368E-66));
#42410=DIRECTION('',(-4.54587899183275E-49,9.04231552086907E-50,1.));
#42411=DIRECTION('center_axis',(-4.54587899183275E-49,9.04231552086907E-50,
1.));
#42412=DIRECTION('ref_axis',(1.,4.33680868994202E-19,4.54587899183275E-49));
#42413=DIRECTION('',(-4.54587899183275E-49,9.04231552086907E-50,1.));
#42414=DIRECTION('center_axis',(-0.999597651754094,-0.0283643192708926,
-4.51840205295607E-49));
#42415=DIRECTION('ref_axis',(0.0283643192708926,-0.999597651754094,-3.99287521021606E-67));
#42416=DIRECTION('center_axis',(0.627618346463361,-0.77852116938629,4.39267686269887E-49));
#42417=DIRECTION('ref_axis',(0.77852116938629,0.627618346463361,3.8324092947301E-66));
#42418=DIRECTION('',(-5.39293238409326E-49,1.29472851457609E-49,1.));
#42419=DIRECTION('center_axis',(-5.39293238409326E-49,1.29472851457609E-49,
1.));
#42420=DIRECTION('ref_axis',(-0.453990499739606,-0.891006524188338,-1.29472851457643E-49));
#42421=DIRECTION('',(-5.39293238409326E-49,1.29472851457609E-49,1.));
#42422=DIRECTION('center_axis',(-0.998741664633517,0.0501506463076103,-5.45107773834419E-49));
#42423=DIRECTION('ref_axis',(-0.0501506463076103,-0.998741664633517,1.75141110323522E-67));
#42424=DIRECTION('center_axis',(0.564601541603216,-0.825363616365098,4.94911614811808E-49));
#42425=DIRECTION('ref_axis',(0.825363616365098,0.564601541603216,-2.63676715352381E-65));
#42426=DIRECTION('',(-6.20673655487384E-49,1.75048074844164E-49,1.));
#42427=DIRECTION('center_axis',(-6.20673655487384E-49,1.75048074844164E-49,
1.));
#42428=DIRECTION('ref_axis',(-0.52249856471585,-0.852640164354153,-1.75048074844092E-49));
#42429=DIRECTION('',(-6.20673655487384E-49,1.75048074844164E-49,1.));
#42430=DIRECTION('center_axis',(-0.99172810303517,0.128356416474844,-6.38008050558225E-49));
#42431=DIRECTION('ref_axis',(-0.128356416474844,-0.99172810303517,-6.45104663994926E-66));
#42432=DIRECTION('center_axis',(0.498103780490022,-0.867117422187761,5.44510769796189E-49));
#42433=DIRECTION('ref_axis',(0.867117422187761,0.498103780490022,4.62928424055004E-65));
#42434=DIRECTION('',(-6.98227413084428E-49,2.26867838960881E-49,1.));
#42435=DIRECTION('center_axis',(-6.98227413084428E-49,2.26867838960881E-49,
1.));
#42436=DIRECTION('ref_axis',(-0.587785252292493,-0.809016994374933,-2.26867838960897E-49));
#42437=DIRECTION('',(-6.98227413084428E-49,2.26867838960881E-49,1.));
#42438=DIRECTION('center_axis',(-0.978600207898551,0.205770826651671,-7.29968274368548E-49));
#42439=DIRECTION('ref_axis',(-0.205770826651671,-0.978600207898551,-8.37640359713844E-66));
#42440=DIRECTION('center_axis',(0.428535043933792,-0.903525160756834,5.87759355939158E-49));
#42441=DIRECTION('ref_axis',(0.903525160756834,0.428535043933792,-6.0990810847752E-65));
#42442=DIRECTION('',(-7.71476366495631E-49,2.84612657730158E-49,1.));
#42443=DIRECTION('center_axis',(-7.71476366495631E-49,2.84612657730158E-49,
1.));
#42444=DIRECTION('ref_axis',(-0.649448048330161,-0.76040596560005,-2.84612657730134E-49));
#42445=DIRECTION('',(-7.71476366495631E-49,2.84612657730158E-49,1.));
#42446=DIRECTION('center_axis',(-0.959438917062647,0.281916591256448,-8.20421479905718E-49));
#42447=DIRECTION('ref_axis',(-0.281916591256448,-0.959438917062647,-3.25299225253391E-65));
#42448=DIRECTION('center_axis',(0.356324246329348,-0.934362366257237,6.2439073132553E-49));
#42449=DIRECTION('ref_axis',(0.934362366257237,0.356324246329348,-6.3916346242107E-66));
#42450=DIRECTION('',(-8.39968911565463E-49,3.47926515142182E-49,1.));
#42451=DIRECTION('center_axis',(-8.39968911565463E-49,3.47926515142182E-49,
1.));
#42452=DIRECTION('ref_axis',(-0.707106781186566,-0.707106781186529,-3.47926515142204E-49));
#42453=DIRECTION('',(-8.39968911565463E-49,3.47926515142182E-49,1.));
#42454=DIRECTION('center_axis',(-0.934362366257236,0.356324246329348,-9.08809993078856E-49));
#42455=DIRECTION('ref_axis',(-0.356324246329348,-0.934362366257236,-6.41640199023417E-65));
#42456=DIRECTION('center_axis',(0.281916591256447,-0.959438917062647,6.54179051344879E-49));
#42457=DIRECTION('ref_axis',(0.959438917062647,0.281916591256447,-1.09781434718078E-65));
#42458=DIRECTION('',(-9.03282768977487E-49,4.16419060212015E-49,1.));
#42459=DIRECTION('center_axis',(-9.03282768977487E-49,4.16419060212015E-49,
1.));
#42460=DIRECTION('ref_axis',(-0.760405965599942,-0.649448048330288,-4.16419060211889E-49));
#42461=DIRECTION('',(-9.03282768977487E-49,4.16419060212015E-49,1.));
#42462=DIRECTION('center_axis',(-0.903525160756834,0.428535043933793,-9.94588869312087E-49));
#42463=DIRECTION('ref_axis',(-0.428535043933793,-0.903525160756834,3.14193955482054E-65));
#42464=DIRECTION('center_axis',(0.205770826651671,-0.978600207898551,6.76940661098664E-49));
#42465=DIRECTION('ref_axis',(0.978600207898551,0.205770826651671,1.21103353553181E-65));
#42466=DIRECTION('',(-9.61027587746764E-49,4.89668013623218E-49,1.));
#42467=DIRECTION('center_axis',(-9.61027587746764E-49,4.89668013623218E-49,
1.));
#42468=DIRECTION('ref_axis',(-0.809016994374948,-0.587785252292472,-4.89668013623217E-49));
#42469=DIRECTION('',(-9.61027587746764E-49,4.89668013623218E-49,1.));
#42470=DIRECTION('center_axis',(-0.867117422187761,0.498103780490022,-1.07722925330906E-48));
#42471=DIRECTION('ref_axis',(-0.498103780490022,-0.867117422187761,1.20400755006059E-65));
#42472=DIRECTION('center_axis',(0.128356416474844,-0.99172810303517,6.92535227693751E-49));
#42473=DIRECTION('ref_axis',(0.99172810303517,0.128356416474844,1.37955244398014E-65));
#42474=DIRECTION('',(-1.01284735186348E-48,5.67221771220262E-49,1.));
#42475=DIRECTION('center_axis',(-1.01284735186348E-48,5.67221771220262E-49,
1.));
#42476=DIRECTION('ref_axis',(-0.852640164354111,-0.522498564715917,-5.67221771220297E-49));
#42477=DIRECTION('',(-1.01284735186348E-48,5.67221771220262E-49,1.));
#42478=DIRECTION('center_axis',(-0.825363616365097,0.564601541603216,-1.15622163962172E-48));
#42479=DIRECTION('ref_axis',(-0.564601541603216,-0.825363616365097,3.75089637720347E-65));
#42480=DIRECTION('center_axis',(0.0501506463076098,-0.998741664633517,7.0086660544136E-49));
#42481=DIRECTION('ref_axis',(0.998741664633517,0.0501506463076098,-1.39822384050416E-65));
#42482=DIRECTION('',(-1.05842257525004E-48,6.4860218829832E-49,1.));
#42483=DIRECTION('center_axis',(-1.05842257525004E-48,6.4860218829832E-49,
1.));
#42484=DIRECTION('ref_axis',(-0.891006524188326,-0.453990499739629,-6.48602188298224E-49));
#42485=DIRECTION('',(-1.05842257525004E-48,6.4860218829832E-49,1.));
#42486=DIRECTION('center_axis',(-0.77852116938629,0.627618346463361,-1.23107901392082E-48));
#42487=DIRECTION('ref_axis',(-0.627618346463361,-0.77852116938629,-1.0235164758246E-65));
#42488=DIRECTION('center_axis',(-0.0283643192708931,-0.999597651754094,
7.01883428627214E-49));
#42489=DIRECTION('ref_axis',(0.999597651754094,-0.0283643192708931,-4.40612052675408E-66));
#42490=DIRECTION('',(-1.09747227149895E-48,7.33307527524372E-49,1.));
#42491=DIRECTION('center_axis',(-1.09747227149895E-48,7.33307527524372E-49,
1.));
#42492=DIRECTION('ref_axis',(-0.923879532511259,-0.382683432365157,-7.33307527524286E-49));
#42493=DIRECTION('',(-1.09747227149895E-48,7.33307527524372E-49,1.));
#42494=DIRECTION('center_axis',(-0.726878880513656,0.686765675513282,-1.30133985560119E-48));
#42495=DIRECTION('ref_axis',(-0.686765675513282,-0.726878880513656,-1.0460740182702E-64));
#42496=DIRECTION('center_axis',(-0.106704409388998,-0.994290786951657,6.95579428198243E-49));
#42497=DIRECTION('ref_axis',(0.994290786951657,-0.106704409388998,-7.09717408543387E-66));
#42498=DIRECTION('',(-1.12975568624752E-48,8.20815552314704E-49,1.));
#42499=DIRECTION('center_axis',(-1.12975568624752E-48,8.20815552314704E-49,
1.));
#42500=DIRECTION('ref_axis',(-0.951056516295187,-0.309016994374844,-8.20815552314827E-49));
#42501=DIRECTION('',(-1.12975568624752E-48,8.20815552314704E-49,1.));
#42502=DIRECTION('center_axis',(-0.6707551416309,0.741678865800901,-1.36657098320978E-48));
#42503=DIRECTION('ref_axis',(-0.741678865800901,-0.6707551416309,3.57211103088032E-65));
#42504=DIRECTION('center_axis',(-0.184386631340402,-0.982853788812425,6.81993470413386E-49));
#42505=DIRECTION('ref_axis',(0.982853788812425,-0.184386631340402,2.71684956354986E-65));
#42506=DIRECTION('',(-1.15507378150848E-48,9.10586746597114E-49,1.));
#42507=DIRECTION('center_axis',(-1.15507378150848E-48,9.10586746597114E-49,
1.));
#42508=DIRECTION('ref_axis',(-0.972369920397692,-0.233445363855843,-9.1058674659719E-49));
#42509=DIRECTION('',(-1.15507378150848E-48,9.10586746597114E-49,1.));
#42510=DIRECTION('center_axis',(-0.610495974251271,0.792019359247608,-1.42637022515333E-48));
#42511=DIRECTION('ref_axis',(-0.792019359247608,-0.610495974251271,3.09249712984754E-64));
#42512=DIRECTION('center_axis',(-0.260932048394816,-0.965357170233114,6.61209317220174E-49));
#42513=DIRECTION('ref_axis',(0.965357170233114,-0.260932048394816,1.42679734120621E-65));
#42514=DIRECTION('',(-1.17327046280543E-48,1.0020676411069E-48,1.));
#42515=DIRECTION('center_axis',(-1.17327046280543E-48,1.0020676411069E-48,
1.));
#42516=DIRECTION('ref_axis',(-0.987688340595155,-0.156434465040119,-1.00206764110703E-48));
#42517=DIRECTION('',(-1.17327046280543E-48,1.0020676411069E-48,1.));
#42518=DIRECTION('center_axis',(-0.546472896179871,0.83747678997139,-1.48036889921999E-48));
#42519=DIRECTION('ref_axis',(-0.83747678997139,-0.546472896179871,5.98336102584152E-65));
#42520=DIRECTION('center_axis',(-0.335868732602165,-0.941908803685482,6.33355109834478E-49));
#42521=DIRECTION('ref_axis',(0.941908803685482,-0.335868732602165,5.83703495410428E-65));
#42522=DIRECTION('',(-1.18423354154716E-48,1.09469422570892E-48,1.));
#42523=DIRECTION('center_axis',(-1.18423354154716E-48,1.09469422570892E-48,
1.));
#42524=DIRECTION('ref_axis',(-0.996917333733132,-0.0784590957277897,-1.09469422570898E-48));
#42525=DIRECTION('',(-1.18423354154716E-48,1.09469422570892E-48,1.));
#42526=DIRECTION('center_axis',(-0.479080630982844,0.877770897795706,-1.52823408562776E-48));
#42527=DIRECTION('ref_axis',(-0.877770897795706,-0.479080630982844,-1.85065299173653E-65));
#42528=DIRECTION('center_axis',(-0.408734674385335,-0.912653256146667,5.98602578707292E-49));
#42529=DIRECTION('ref_axis',(0.912653256146667,-0.408734674385335,-4.742731066544E-66));
#42530=DIRECTION('',(-1.18789542670764E-48,1.18789542670765E-48,1.));
#42531=DIRECTION('center_axis',(-1.18789542670764E-48,1.18789542670765E-48,
1.));
#42532=DIRECTION('ref_axis',(4.33680868994202E-19,-1.,1.18789542670765E-48));
#42533=DIRECTION('',(-1.18789542670764E-48,1.18789542670765E-48,1.));
#42534=DIRECTION('center_axis',(-0.408734674385331,0.912653256146669,-1.56967067958564E-48));
#42535=DIRECTION('ref_axis',(-0.912653256146669,-0.408734674385331,-1.44539080722799E-64));
#42536=DIRECTION('center_axis',(-0.479080630982847,-0.877770897795704,5.57165984749406E-49));
#42537=DIRECTION('ref_axis',(0.877770897795704,-0.479080630982847,-3.32989513528092E-65));
#42538=DIRECTION('',(-1.18423354154716E-48,1.28109662770637E-48,1.));
#42539=DIRECTION('center_axis',(-1.18423354154716E-48,1.28109662770637E-48,
1.));
#42540=DIRECTION('ref_axis',(4.33680868994202E-19,-1.,1.28109662770637E-48));
#42541=DIRECTION('',(-1.18423354154716E-48,1.28109662770637E-48,1.));
#42542=DIRECTION('center_axis',(-0.335868732602161,0.941908803685483,-1.60442321071283E-48));
#42543=DIRECTION('ref_axis',(-0.941908803685483,-0.335868732602161,-1.10077185323049E-64));
#42544=DIRECTION('center_axis',(-0.546472896179874,-0.837476789971388,5.09300798341636E-49));
#42545=DIRECTION('ref_axis',(0.837476789971388,-0.546472896179874,-4.24396990687181E-65));
#42546=DIRECTION('',(-1.17327046280542E-48,1.37372321230839E-48,1.));
#42547=DIRECTION('center_axis',(-1.17327046280542E-48,1.37372321230839E-48,
1.));
#42548=DIRECTION('ref_axis',(4.33680868994202E-19,-1.,1.37372321230839E-48));
#42549=DIRECTION('',(-1.17327046280542E-48,1.37372321230839E-48,1.));
#42550=DIRECTION('center_axis',(-0.260932048394812,0.965357170233115,-1.63227741809852E-48));
#42551=DIRECTION('ref_axis',(-0.965357170233115,-0.260932048394812,1.79840374663787E-65));
#42552=DIRECTION('center_axis',(-0.610495974251274,-0.792019359247605,4.55302124274975E-49));
#42553=DIRECTION('ref_axis',(0.792019359247605,-0.610495974251274,-1.92107929694605E-65));
#42554=DIRECTION('',(-1.15507378150847E-48,1.46520410681818E-48,1.));
#42555=DIRECTION('center_axis',(-1.15507378150847E-48,1.46520410681818E-48,
1.));
#42556=DIRECTION('ref_axis',(4.33680868994202E-19,-1.,1.46520410681818E-48));
#42557=DIRECTION('',(-1.15507378150847E-48,1.46520410681818E-48,1.));
#42558=DIRECTION('center_axis',(-0.184386631340398,0.982853788812426,-1.65306157129174E-48));
#42559=DIRECTION('ref_axis',(-0.982853788812426,-0.184386631340398,3.00112067034686E-65));
#42560=DIRECTION('center_axis',(-0.670755141630903,-0.741678865800898,3.95502882331426E-49));
#42561=DIRECTION('ref_axis',(0.741678865800898,-0.670755141630903,1.84878394507284E-65));
#42562=DIRECTION('',(-1.12975568624751E-48,1.55497530110059E-48,1.));
#42563=DIRECTION('center_axis',(-1.12975568624751E-48,1.55497530110059E-48,
1.));
#42564=DIRECTION('ref_axis',(4.33680868994202E-19,-1.,1.55497530110059E-48));
#42565=DIRECTION('',(-1.12975568624751E-48,1.55497530110059E-48,1.));
#42566=DIRECTION('center_axis',(-0.106704409388993,0.994290786951657,-1.66664752907659E-48));
#42567=DIRECTION('ref_axis',(-0.994290786951658,-0.106704409388993,-2.84767254643969E-65));
#42568=DIRECTION('center_axis',(-0.726878880513659,-0.686765675513279,3.30271754722836E-49));
#42569=DIRECTION('ref_axis',(0.686765675513279,-0.726878880513659,1.35737227185702E-66));
#42570=DIRECTION('',(-1.09747227149895E-48,1.64248332589092E-48,1.));
#42571=DIRECTION('center_axis',(-1.09747227149895E-48,1.64248332589092E-48,
1.));
#42572=DIRECTION('ref_axis',(4.33680868994202E-19,-1.,1.64248332589092E-48));
#42573=DIRECTION('',(-1.09747227149895E-48,1.64248332589092E-48,1.));
#42574=DIRECTION('center_axis',(-0.0283643192708891,0.999597651754094,-1.67295152950556E-48));
#42575=DIRECTION('ref_axis',(-0.999597651754094,-0.0283643192708891,-1.01926051780483E-65));
#42576=DIRECTION('center_axis',(-0.778521169386292,-0.627618346463358,2.60010913042463E-49));
#42577=DIRECTION('ref_axis',(0.627618346463358,-0.778521169386292,-1.77736454987801E-64));
#42578=DIRECTION('',(-1.05842257525003E-48,1.72718866511697E-48,1.));
#42579=DIRECTION('center_axis',(-1.05842257525003E-48,1.72718866511697E-48,
1.));
#42580=DIRECTION('ref_axis',(-0.891006524188322,0.453990499739636,-1.72718866511707E-48));
#42581=DIRECTION('',(-1.05842257525003E-48,1.72718866511697E-48,1.));
#42582=DIRECTION('center_axis',(0.050150646307614,0.998741664633517,-1.67193470631971E-48));
#42583=DIRECTION('ref_axis',(-0.998741664633517,0.050150646307614,1.52017605534737E-65));
#42584=DIRECTION('center_axis',(-0.8253636163651,-0.564601541603213,1.85153538743368E-49));
#42585=DIRECTION('ref_axis',(0.564601541603213,-0.8253636163651,-7.9609822926636E-66));
#42586=DIRECTION('',(-1.01284735186348E-48,1.80856908219503E-48,1.));
#42587=DIRECTION('center_axis',(-1.01284735186348E-48,1.80856908219503E-48,
1.));
#42588=DIRECTION('ref_axis',(-0.852640164354107,0.522498564715924,-1.808569082195E-48));
#42589=DIRECTION('',(-1.01284735186348E-48,1.80856908219503E-48,1.));
#42590=DIRECTION('center_axis',(0.128356416474848,0.991728103035169,-1.6636033285721E-48));
#42591=DIRECTION('ref_axis',(-0.991728103035169,0.128356416474848,-6.99057875847398E-66));
#42592=DIRECTION('center_axis',(-0.867117422187763,-0.498103780490019,1.06161152430708E-49));
#42593=DIRECTION('ref_axis',(0.498103780490019,-0.867117422187763,1.00088346227585E-65));
#42594=DIRECTION('',(-9.61027587746759E-49,1.88612283979207E-48,1.));
#42595=DIRECTION('center_axis',(-9.61027587746759E-49,1.88612283979207E-48,
1.));
#42596=DIRECTION('ref_axis',(-0.809016994374894,0.587785252292546,-1.88612283979215E-48));
#42597=DIRECTION('',(-9.61027587746759E-49,1.88612283979207E-48,1.));
#42598=DIRECTION('center_axis',(0.205770826651675,0.978600207898551,-1.64800876197701E-48));
#42599=DIRECTION('ref_axis',(-0.978600207898551,0.205770826651675,2.0991990898783E-65));
#42600=DIRECTION('center_axis',(-0.903525160756836,-0.428535043933789,2.35207684337335E-50));
#42601=DIRECTION('ref_axis',(0.428535043933789,-0.903525160756836,-9.18347163738211E-68));
#42602=DIRECTION('',(-9.03282768977482E-49,1.95937179320328E-48,1.));
#42603=DIRECTION('center_axis',(-9.03282768977482E-49,1.95937179320328E-48,
1.));
#42604=DIRECTION('ref_axis',(-0.760405965599999,0.649448048330221,-1.95937179320332E-48));
#42605=DIRECTION('',(-9.03282768977482E-49,1.95937179320328E-48,1.));
#42606=DIRECTION('center_axis',(0.281916591256451,0.959438917062646,-1.62524715222323E-48));
#42607=DIRECTION('ref_axis',(-0.959438917062646,0.281916591256451,8.99283719863503E-66));
#42608=DIRECTION('center_axis',(-0.934362366257238,-0.356324246329344,-6.22581077994971E-50));
#42609=DIRECTION('ref_axis',(0.356324246329344,-0.934362366257238,-2.14283631075808E-67));
#42610=DIRECTION('',(-8.39968911565457E-49,2.02786433827311E-48,1.));
#42611=DIRECTION('center_axis',(-8.39968911565457E-49,2.02786433827311E-48,
1.));
#42612=DIRECTION('ref_axis',(-0.707106781186559,0.707106781186536,-2.02786433827309E-48));
#42613=DIRECTION('',(-8.39968911565457E-49,2.02786433827311E-48,1.));
#42614=DIRECTION('center_axis',(0.356324246329351,0.934362366257235,-1.59545883220388E-48));
#42615=DIRECTION('ref_axis',(-0.934362366257235,0.356324246329351,6.60900149289003E-65));
#42616=DIRECTION('center_axis',(-0.959438917062648,-0.281916591256444,-1.50646620972636E-49));
#42617=DIRECTION('ref_axis',(0.281916591256444,-0.959438917062648,3.84808191287826E-66));
#42618=DIRECTION('',(-7.71476366495624E-49,2.09117819568513E-48,1.));
#42619=DIRECTION('center_axis',(-7.71476366495624E-49,2.09117819568513E-48,
1.));
#42620=DIRECTION('ref_axis',(-0.649448048330135,0.760405965600073,-2.09117819568518E-48));
#42621=DIRECTION('',(-7.71476366495624E-49,2.09117819568513E-48,1.));
#42622=DIRECTION('center_axis',(0.428535043933796,0.903525160756832,-1.5588274568175E-48));
#42623=DIRECTION('ref_axis',(-0.903525160756832,0.428535043933796,-3.10862492143316E-66));
#42624=DIRECTION('center_axis',(-0.978600207898552,-0.205770826651667,-2.41099826509806E-49));
#42625=DIRECTION('ref_axis',(0.205770826651667,-0.978600207898552,1.22158844253494E-66));
#42626=DIRECTION('',(-6.98227413084421E-49,2.14892301445441E-48,1.));
#42627=DIRECTION('center_axis',(-6.98227413084421E-49,2.14892301445441E-48,
1.));
#42628=DIRECTION('ref_axis',(-0.587785252292501,0.809016994374927,-2.14892301445438E-48));
#42629=DIRECTION('',(-6.98227413084421E-49,2.14892301445441E-48,1.));
#42630=DIRECTION('center_axis',(0.498103780490025,0.867117422187759,-1.51557887067454E-48));
#42631=DIRECTION('ref_axis',(-0.867117422187759,0.498103780490025,2.99504754920617E-65));
#42632=DIRECTION('center_axis',(-0.99172810303517,-0.128356416474841,-3.33060050320128E-49));
#42633=DIRECTION('ref_axis',(0.128356416474841,-0.99172810303517,-3.10963647347836E-66));
#42634=DIRECTION('',(-6.20673655487377E-49,2.20074277857113E-48,1.));
#42635=DIRECTION('center_axis',(-6.20673655487377E-49,2.20074277857113E-48,
1.));
#42636=DIRECTION('ref_axis',(-0.522498564715884,0.852640164354132,-2.20074277857117E-48));
#42637=DIRECTION('',(-6.20673655487377E-49,2.20074277857113E-48,1.));
#42638=DIRECTION('center_axis',(0.564601541603219,0.825363616365096,-1.46597971569015E-48));
#42639=DIRECTION('ref_axis',(-0.825363616365096,0.564601541603219,-1.28895308917342E-64));
#42640=DIRECTION('center_axis',(-0.998741664633517,-0.0501506463076061,
-4.25960327043935E-49));
#42641=DIRECTION('ref_axis',(0.0501506463076061,-0.998741664633517,-2.80568036684895E-66));
#42642=DIRECTION('',(-5.39293238409318E-49,2.24631800195768E-48,1.));
#42643=DIRECTION('center_axis',(-5.39293238409318E-49,2.24631800195768E-48,
1.));
#42644=DIRECTION('ref_axis',(-0.453990499739489,0.891006524188397,-2.24631800195771E-48));
#42645=DIRECTION('',(-5.39293238409318E-49,2.24631800195768E-48,1.));
#42646=DIRECTION('center_axis',(0.627618346463364,0.778521169386287,-1.41033578714823E-48));
#42647=DIRECTION('ref_axis',(-0.778521169386288,0.627618346463364,5.07659402759256E-65));
#42648=DIRECTION('center_axis',(-0.999597651754094,0.0283643192708965,-5.19227895582746E-49));
#42649=DIRECTION('ref_axis',(-0.0283643192708965,-0.999597651754094,2.50391620144835E-67));
#42650=DIRECTION('',(-4.54587899183267E-49,2.2853676982066E-48,1.));
#42651=DIRECTION('center_axis',(-4.54587899183267E-49,2.2853676982066E-48,
1.));
#42652=DIRECTION('ref_axis',(-0.382683432365006,0.923879532511321,-2.28536769820664E-48));
#42653=DIRECTION('',(-4.54587899183267E-49,2.2853676982066E-48,1.));
#42654=DIRECTION('center_axis',(0.686765675513284,0.726878880513654,-1.34899014837172E-48));
#42655=DIRECTION('ref_axis',(-0.726878880513654,0.686765675513284,4.51664321804638E-65));
#42656=DIRECTION('center_axis',(-0.994290786951657,0.106704409389001,-6.12287730361908E-49));
#42657=DIRECTION('ref_axis',(-0.106704409389001,-0.994290786951657,-3.36897451344462E-66));
#42658=DIRECTION('',(-3.67079874392934E-49,2.31765111295516E-48,1.));
#42659=DIRECTION('center_axis',(-3.67079874392934E-49,2.31765111295516E-48,
1.));
#42660=DIRECTION('ref_axis',(-0.309016994374936,0.951056516295157,-2.31765111295516E-48));
#42661=DIRECTION('',(-3.67079874392934E-49,2.31765111295516E-48,1.));
#42662=DIRECTION('center_axis',(0.741678865800904,0.670755141630897,-1.28232101562316E-48));
#42663=DIRECTION('ref_axis',(-0.670755141630897,0.741678865800904,-7.13448931820408E-65));
#42664=DIRECTION('center_axis',(-0.982853788812424,0.184386631340406,-7.04566086554469E-49));
#42665=DIRECTION('ref_axis',(-0.184386631340406,-0.982853788812424,1.03257498418151E-65));
#42666=DIRECTION('',(-2.77308680110524E-49,2.34296920821612E-48,1.));
#42667=DIRECTION('center_axis',(-2.77308680110524E-49,2.34296920821612E-48,
1.));
#42668=DIRECTION('ref_axis',(-0.233445363855831,0.972369920397695,-2.34296920821614E-48));
#42669=DIRECTION('',(-2.77308680110524E-49,2.34296920821612E-48,1.));
#42670=DIRECTION('center_axis',(0.79201935924761,0.610495974251268,-1.21073942627568E-48));
#42671=DIRECTION('ref_axis',(-0.610495974251268,0.79201935924761,-4.36775682720849E-65));
#42672=DIRECTION('center_axis',(-0.965357170233113,0.260932048394819,-7.95494037408836E-49));
#42673=DIRECTION('ref_axis',(-0.260932048394819,-0.965357170233113,-3.47978634051958E-65));
#42674=DIRECTION('',(-1.85827785600739E-49,2.36116588951307E-48,1.));
#42675=DIRECTION('center_axis',(-1.85827785600739E-49,2.36116588951307E-48,
1.));
#42676=DIRECTION('ref_axis',(-0.156434465040246,0.987688340595135,-2.36116588951307E-48));
#42677=DIRECTION('',(-1.85827785600739E-49,2.36116588951307E-48,1.));
#42678=DIRECTION('center_axis',(0.837476789971392,0.546472896179868,-1.13468670463092E-48));
#42679=DIRECTION('ref_axis',(-0.546472896179868,0.837476789971392,7.35185048458512E-65));
#42680=DIRECTION('center_axis',(-0.94190880368548,0.335868732602169,-8.84510981871381E-49));
#42681=DIRECTION('ref_axis',(-0.335868732602169,-0.94190880368548,-2.80378683690505E-64));
#42682=DIRECTION('',(-9.32012009987159E-50,2.3721289682548E-48,1.));
#42683=DIRECTION('center_axis',(-9.32012009987159E-50,2.3721289682548E-48,
1.));
#42684=DIRECTION('ref_axis',(-0.0784590957277844,0.996917333733133,-2.3721289682548E-48));
#42685=DIRECTION('',(-9.32012009987159E-50,2.3721289682548E-48,1.));
#42686=DIRECTION('center_axis',(0.877770897795708,0.47908063098284,-1.0546317410079E-48));
#42687=DIRECTION('ref_axis',(-0.47908063098284,0.877770897795708,-1.46432166581228E-64));
#42688=DIRECTION('center_axis',(-0.912653256146669,0.408734674385332,-9.71068100878346E-49));
#42689=DIRECTION('ref_axis',(-0.408734674385332,-0.912653256146669,4.78015562106795E-65));
#42690=DIRECTION('',(-1.03033504185762E-66,2.37579085341529E-48,1.));
#42691=DIRECTION('center_axis',(-1.03033504185762E-66,2.37579085341529E-48,
1.));
#42692=DIRECTION('ref_axis',(-5.51899603821915E-14,1.,-2.37579085341529E-48));
#42693=DIRECTION('',(-1.03033504185762E-66,2.37579085341529E-48,1.));
#42694=DIRECTION('center_axis',(0.912653256146668,0.408734674385334,-9.71068100878352E-49));
#42695=DIRECTION('ref_axis',(-0.408734674385334,0.912653256146668,-3.97320112854764E-64));
#42696=DIRECTION('center_axis',(-0.877770897795703,0.47908063098285,-1.05463174100791E-48));
#42697=DIRECTION('ref_axis',(-0.47908063098285,-0.877770897795703,8.5181126283276E-66));
#42698=DIRECTION('',(9.32012009987329E-50,2.3721289682548E-48,1.));
#42699=DIRECTION('center_axis',(9.32012009987329E-50,2.3721289682548E-48,
1.));
#42700=DIRECTION('ref_axis',(0.078459095727909,0.996917333733123,-2.37212896825479E-48));
#42701=DIRECTION('',(9.32012009987329E-50,2.3721289682548E-48,1.));
#42702=DIRECTION('center_axis',(0.941908803685484,0.335868732602158,-8.84510981871371E-49));
#42703=DIRECTION('ref_axis',(-0.335868732602158,0.941908803685484,-1.44601818635795E-65));
#42704=DIRECTION('center_axis',(-0.837476789971386,0.546472896179877,-1.13468670463093E-48));
#42705=DIRECTION('ref_axis',(-0.546472896179877,-0.837476789971386,1.1507371701338E-64));
#42706=DIRECTION('',(1.85827785600756E-49,2.36116588951307E-48,1.));
#42707=DIRECTION('center_axis',(1.85827785600756E-49,2.36116588951307E-48,
1.));
#42708=DIRECTION('ref_axis',(0.156434465040226,0.987688340595138,-2.36116588951307E-48));
#42709=DIRECTION('',(1.85827785600756E-49,2.36116588951307E-48,1.));
#42710=DIRECTION('center_axis',(0.965357170233116,0.260932048394809,-7.95494037408827E-49));
#42711=DIRECTION('ref_axis',(-0.260932048394809,0.965357170233116,-4.20694512990981E-65));
#42712=DIRECTION('center_axis',(-0.792019359247603,0.610495974251277,-1.21073942627569E-48));
#42713=DIRECTION('ref_axis',(-0.610495974251277,-0.792019359247603,-2.13945998802071E-65));
#42714=DIRECTION('',(2.7730868011054E-49,2.34296920821612E-48,1.));
#42715=DIRECTION('center_axis',(2.7730868011054E-49,2.34296920821612E-48,
1.));
#42716=DIRECTION('ref_axis',(0.233445363855898,0.972369920397678,-2.34296920821612E-48));
#42717=DIRECTION('',(2.7730868011054E-49,2.34296920821612E-48,1.));
#42718=DIRECTION('center_axis',(0.982853788812426,0.184386631340395,-7.04566086554459E-49));
#42719=DIRECTION('ref_axis',(-0.184386631340395,0.982853788812426,-1.76256118611904E-65));
#42720=DIRECTION('center_axis',(-0.741678865800896,0.670755141630906,-1.28232101562316E-48));
#42721=DIRECTION('ref_axis',(-0.670755141630906,-0.741678865800896,1.75561258236883E-65));
#42722=DIRECTION('',(3.6707987439295E-49,2.31765111295516E-48,1.));
#42723=DIRECTION('center_axis',(3.6707987439295E-49,2.31765111295516E-48,
1.));
#42724=DIRECTION('ref_axis',(0.309016994374949,0.951056516295153,-2.31765111295516E-48));
#42725=DIRECTION('',(3.6707987439295E-49,2.31765111295516E-48,1.));
#42726=DIRECTION('center_axis',(0.994290786951658,0.10670440938899,-6.12287730361897E-49));
#42727=DIRECTION('ref_axis',(-0.10670440938899,0.994290786951658,-7.83421067979577E-66));
#42728=DIRECTION('center_axis',(-0.686765675513276,0.726878880513661,-1.34899014837172E-48));
#42729=DIRECTION('ref_axis',(-0.726878880513661,-0.686765675513276,5.3563970103269E-65));
#42730=DIRECTION('',(4.54587899183282E-49,2.28536769820659E-48,1.));
#42731=DIRECTION('center_axis',(4.54587899183282E-49,2.28536769820659E-48,
1.));
#42732=DIRECTION('ref_axis',(0.382683432365024,0.923879532511314,-2.28536769820663E-48));
#42733=DIRECTION('',(4.54587899183282E-49,2.28536769820659E-48,1.));
#42734=DIRECTION('center_axis',(0.999597651754094,0.0283643192708856,-5.19227895582736E-49));
#42735=DIRECTION('ref_axis',(-0.0283643192708856,0.999597651754094,1.94568536261846E-66));
#42736=DIRECTION('center_axis',(-0.627618346463355,0.778521169386295,-1.41033578714824E-48));
#42737=DIRECTION('ref_axis',(-0.778521169386295,-0.627618346463355,-4.32781502974933E-65));
#42738=DIRECTION('',(5.39293238409334E-49,2.24631800195767E-48,1.));
#42739=DIRECTION('center_axis',(5.39293238409334E-49,2.24631800195767E-48,
1.));
#42740=DIRECTION('ref_axis',(0.45399049973962,0.89100652418833,-2.24631800195763E-48));
#42741=DIRECTION('',(5.39293238409334E-49,2.24631800195767E-48,1.));
#42742=DIRECTION('center_axis',(0.998741664633517,-0.0501506463076175,-4.25960327043925E-49));
#42743=DIRECTION('ref_axis',(0.0501506463076175,0.998741664633517,-4.14088422014228E-66));
#42744=DIRECTION('center_axis',(-0.56460154160321,0.825363616365102,-1.46597971569016E-48));
#42745=DIRECTION('ref_axis',(-0.825363616365102,-0.56460154160321,7.97777118454868E-65));
#42746=DIRECTION('',(6.20673655487391E-49,2.20074277857112E-48,1.));
#42747=DIRECTION('center_axis',(6.20673655487391E-49,2.20074277857112E-48,
1.));
#42748=DIRECTION('ref_axis',(0.522498564715976,0.852640164354076,-2.20074277857111E-48));
#42749=DIRECTION('',(6.20673655487391E-49,2.20074277857112E-48,1.));
#42750=DIRECTION('center_axis',(0.991728103035169,-0.128356416474851,-3.33060050320119E-49));
#42751=DIRECTION('ref_axis',(0.128356416474851,0.991728103035169,2.08257490756294E-67));
#42752=DIRECTION('center_axis',(-0.498103780490015,0.867117422187765,-1.51557887067454E-48));
#42753=DIRECTION('ref_axis',(-0.867117422187765,-0.498103780490015,2.18779707200991E-65));
#42754=DIRECTION('',(6.98227413084436E-49,2.1489230144544E-48,1.));
#42755=DIRECTION('center_axis',(6.98227413084435E-49,2.1489230144544E-48,
1.));
#42756=DIRECTION('ref_axis',(0.587785252292489,0.809016994374936,-2.14892301445439E-48));
#42757=DIRECTION('',(6.98227413084436E-49,2.1489230144544E-48,1.));
#42758=DIRECTION('center_axis',(0.97860020789855,-0.205770826651679,-2.41099826509796E-49));
#42759=DIRECTION('ref_axis',(0.205770826651679,0.97860020789855,-2.74077973100627E-66));
#42760=DIRECTION('center_axis',(-0.428535043933785,0.903525160756837,-1.55882745681751E-48));
#42761=DIRECTION('ref_axis',(-0.903525160756837,-0.428535043933785,-8.73188639847288E-65));
#42762=DIRECTION('',(7.71476366495637E-49,2.09117819568512E-48,1.));
#42763=DIRECTION('center_axis',(7.71476366495637E-49,2.09117819568512E-48,
1.));
#42764=DIRECTION('ref_axis',(0.649448048330186,0.760405965600029,-2.09117819568512E-48));
#42765=DIRECTION('',(7.71476366495637E-49,2.09117819568512E-48,1.));
#42766=DIRECTION('center_axis',(0.959438917062645,-0.281916591256455,-1.50646620972626E-49));
#42767=DIRECTION('ref_axis',(0.281916591256455,0.959438917062645,-2.91844467010393E-67));
#42768=DIRECTION('center_axis',(-0.356324246329341,0.934362366257239,-1.59545883220388E-48));
#42769=DIRECTION('ref_axis',(-0.934362366257239,-0.356324246329341,1.49301625507406E-64));
#42770=DIRECTION('',(8.39968911565469E-49,2.0278643382731E-48,1.));
#42771=DIRECTION('center_axis',(8.39968911565469E-49,2.0278643382731E-48,
1.));
#42772=DIRECTION('ref_axis',(0.707106781186573,0.707106781186522,-2.02786433827308E-48));
#42773=DIRECTION('',(8.39968911565469E-49,2.0278643382731E-48,1.));
#42774=DIRECTION('center_axis',(0.934362366257234,-0.356324246329355,-6.22581077994883E-50));
#42775=DIRECTION('ref_axis',(0.356324246329355,0.934362366257234,-4.97582464336991E-66));
#42776=DIRECTION('center_axis',(-0.28191659125644,0.959438917062649,-1.62524715222323E-48));
#42777=DIRECTION('ref_axis',(-0.959438917062649,-0.28191659125644,-5.29515836320384E-66));
#42778=DIRECTION('',(9.03282768977493E-49,1.95937179320326E-48,1.));
#42779=DIRECTION('center_axis',(9.03282768977493E-49,1.95937179320326E-48,
1.));
#42780=DIRECTION('ref_axis',(0.760405965600079,0.649448048330127,-1.9593717932032E-48));
#42781=DIRECTION('',(9.03282768977493E-49,1.95937179320326E-48,1.));
#42782=DIRECTION('center_axis',(0.903525160756831,-0.428535043933799,2.35207684337425E-50));
#42783=DIRECTION('ref_axis',(0.428535043933799,0.903525160756831,3.46790681006673E-67));
#42784=DIRECTION('center_axis',(-0.205770826651664,0.978600207898553,-1.64800876197701E-48));
#42785=DIRECTION('ref_axis',(-0.978600207898553,-0.205770826651664,-5.70930081633759E-65));
#42786=DIRECTION('',(9.61027587746769E-49,1.88612283979206E-48,1.));
#42787=DIRECTION('center_axis',(9.61027587746769E-49,1.88612283979206E-48,
1.));
#42788=DIRECTION('ref_axis',(0.809016994374978,0.587785252292432,-1.88612283979202E-48));
#42789=DIRECTION('',(9.61027587746769E-49,1.88612283979206E-48,1.));
#42790=DIRECTION('center_axis',(0.867117422187757,-0.498103780490029,1.06161152430717E-49));
#42791=DIRECTION('ref_axis',(0.498103780490029,0.867117422187757,8.6756046158998E-66));
#42792=DIRECTION('center_axis',(-0.128356416474837,0.991728103035171,-1.6636033285721E-48));
#42793=DIRECTION('ref_axis',(-0.991728103035171,-0.128356416474837,3.98742758462882E-65));
#42794=DIRECTION('',(1.01284735186348E-48,1.80856908219502E-48,1.));
#42795=DIRECTION('center_axis',(1.01284735186348E-48,1.80856908219502E-48,
1.));
#42796=DIRECTION('ref_axis',(0.852640164354111,0.522498564715918,-1.80856908219499E-48));
#42797=DIRECTION('',(1.01284735186348E-48,1.80856908219502E-48,1.));
#42798=DIRECTION('center_axis',(0.825363616365094,-0.564601541603222,1.85153538743376E-49));
#42799=DIRECTION('ref_axis',(0.564601541603222,0.825363616365094,-1.20460226317478E-65));
#42800=DIRECTION('center_axis',(-0.0501506463076026,0.998741664633518,-1.67193470631971E-48));
#42801=DIRECTION('ref_axis',(-0.998741664633518,-0.0501506463076026,9.17993822873344E-66));
#42802=DIRECTION('',(1.05842257525004E-48,1.72718866511696E-48,1.));
#42803=DIRECTION('center_axis',(1.05842257525004E-48,1.72718866511696E-48,
1.));
#42804=DIRECTION('ref_axis',(0.891006524188331,0.453990499739619,-1.72718866511705E-48));
#42805=DIRECTION('',(1.05842257525004E-48,1.72718866511696E-48,1.));
#42806=DIRECTION('center_axis',(0.778521169386285,-0.627618346463367,2.6001091304247E-49));
#42807=DIRECTION('ref_axis',(0.627618346463367,0.778521169386285,-2.38387219843189E-65));
#42808=DIRECTION('center_axis',(0.0283643192709005,0.999597651754094,-1.67295152950556E-48));
#42809=DIRECTION('ref_axis',(-0.999597651754094,0.0283643192709005,5.71503284305285E-66));
#42810=DIRECTION('',(1.09747227149896E-48,1.6424833258909E-48,1.));
#42811=DIRECTION('center_axis',(1.09747227149896E-48,1.6424833258909E-48,
1.));
#42812=DIRECTION('ref_axis',(4.33680868994202E-19,-1.,1.6424833258909E-48));
#42813=DIRECTION('',(1.09747227149896E-48,1.6424833258909E-48,1.));
#42814=DIRECTION('center_axis',(0.726878880513651,-0.686765675513287,3.30271754722842E-49));
#42815=DIRECTION('ref_axis',(0.686765675513287,0.726878880513651,-2.02185804836064E-65));
#42816=DIRECTION('center_axis',(0.106704409389004,0.994290786951656,-1.66664752907659E-48));
#42817=DIRECTION('ref_axis',(-0.994290786951656,0.106704409389004,-7.60908949083185E-66));
#42818=DIRECTION('',(1.12975568624752E-48,1.55497530110057E-48,1.));
#42819=DIRECTION('center_axis',(1.12975568624752E-48,1.55497530110057E-48,
1.));
#42820=DIRECTION('ref_axis',(4.33680868994202E-19,-1.,1.55497530110057E-48));
#42821=DIRECTION('',(1.12975568624752E-48,1.55497530110057E-48,1.));
#42822=DIRECTION('center_axis',(0.670755141630895,-0.741678865800906,3.95502882331431E-49));
#42823=DIRECTION('ref_axis',(0.741678865800906,0.670755141630895,-5.99583083400171E-67));
#42824=DIRECTION('center_axis',(0.184386631340409,0.982853788812424,-1.65306157129173E-48));
#42825=DIRECTION('ref_axis',(-0.982853788812424,0.184386631340409,2.90870213757036E-65));
#42826=DIRECTION('',(1.15507378150848E-48,1.46520410681816E-48,1.));
#42827=DIRECTION('center_axis',(1.15507378150848E-48,1.46520410681816E-48,
1.));
#42828=DIRECTION('ref_axis',(4.33680868994202E-19,-1.,1.46520410681816E-48));
#42829=DIRECTION('',(1.15507378150848E-48,1.46520410681816E-48,1.));
#42830=DIRECTION('center_axis',(0.610495974251266,-0.792019359247612,4.5530212427498E-49));
#42831=DIRECTION('ref_axis',(0.792019359247612,0.610495974251266,2.91962028883906E-65));
#42832=DIRECTION('center_axis',(0.260932048394823,0.965357170233112,-1.63227741809852E-48));
#42833=DIRECTION('ref_axis',(-0.965357170233112,0.260932048394823,3.06323067308603E-65));
#42834=DIRECTION('',(1.17327046280543E-48,1.37372321230838E-48,1.));
#42835=DIRECTION('center_axis',(1.17327046280543E-48,1.37372321230838E-48,
1.));
#42836=DIRECTION('ref_axis',(4.33680868994202E-19,-1.,1.37372321230838E-48));
#42837=DIRECTION('',(1.17327046280543E-48,1.37372321230838E-48,1.));
#42838=DIRECTION('center_axis',(0.546472896179865,-0.837476789971394,5.0930079834164E-49));
#42839=DIRECTION('ref_axis',(0.837476789971394,0.546472896179865,-4.56422939014991E-65));
#42840=DIRECTION('center_axis',(0.335868732602171,0.94190880368548,-1.60442321071282E-48));
#42841=DIRECTION('ref_axis',(-0.94190880368548,0.335868732602171,4.87630450545203E-65));
#42842=DIRECTION('',(1.18423354154716E-48,1.28109662770635E-48,1.));
#42843=DIRECTION('center_axis',(1.18423354154716E-48,1.28109662770635E-48,
1.));
#42844=DIRECTION('ref_axis',(4.33680868994202E-19,-1.,1.28109662770635E-48));
#42845=DIRECTION('',(1.18423354154716E-48,1.28109662770635E-48,1.));
#42846=DIRECTION('center_axis',(0.479080630982838,-0.87777089779571,5.57165984749409E-49));
#42847=DIRECTION('ref_axis',(0.87777089779571,0.479080630982838,-3.73128804317402E-67));
#42848=DIRECTION('center_axis',(0.408734674385341,0.912653256146664,-1.56967067958563E-48));
#42849=DIRECTION('ref_axis',(-0.912653256146664,0.408734674385341,1.45818743306131E-64));
#42850=DIRECTION('center_axis',(0.408734674385325,-0.912653256146672,5.98602578707294E-49));
#42851=DIRECTION('ref_axis',(0.912653256146672,0.408734674385325,1.90174553100142E-65));
#42852=DIRECTION('center_axis',(0.479080630982853,0.877770897795701,-1.52823408562775E-48));
#42853=DIRECTION('ref_axis',(-0.877770897795701,0.479080630982853,5.61428358120402E-65));
#42854=DIRECTION('center_axis',(0.335868732602155,-0.941908803685485,6.33355109834479E-49));
#42855=DIRECTION('ref_axis',(0.941908803685485,0.335868732602155,-2.18452554190007E-64));
#42856=DIRECTION('center_axis',(0.54647289617988,0.837476789971384,-1.48036889921998E-48));
#42857=DIRECTION('ref_axis',(-0.837476789971384,0.54647289617988,1.0038841655118E-64));
#42858=DIRECTION('center_axis',(0.260932048394805,-0.965357170233117,6.61209317220175E-49));
#42859=DIRECTION('ref_axis',(0.965357170233117,0.260932048394805,-1.34731391844263E-65));
#42860=DIRECTION('center_axis',(0.61049597425128,0.792019359247601,-1.42637022515332E-48));
#42861=DIRECTION('ref_axis',(-0.792019359247601,0.61049597425128,4.68595517840464E-65));
#42862=DIRECTION('center_axis',(0.184386631340391,-0.982853788812427,6.81993470413385E-49));
#42863=DIRECTION('ref_axis',(0.982853788812427,0.184386631340391,-4.82159387328582E-66));
#42864=DIRECTION('center_axis',(0.670755141630908,0.741678865800894,-1.36657098320977E-48));
#42865=DIRECTION('ref_axis',(-0.741678865800894,0.670755141630908,-1.20021806126158E-65));
#42866=DIRECTION('center_axis',(0.106704409388986,-0.994290786951658,6.95579428198241E-49));
#42867=DIRECTION('ref_axis',(0.994290786951658,0.106704409388986,-5.2899598259714E-66));
#42868=DIRECTION('center_axis',(0.726878880513664,0.686765675513273,-1.30133985560118E-48));
#42869=DIRECTION('ref_axis',(-0.686765675513273,0.726878880513664,8.56568901676031E-65));
#42870=DIRECTION('center_axis',(0.0283643192708817,-0.999597651754094,7.01883428627211E-49));
#42871=DIRECTION('ref_axis',(0.999597651754094,0.0283643192708817,4.29698701010715E-68));
#55931=CARTESIAN_POINT('',(0.,0.,0.));
#55932=CARTESIAN_POINT('Origin',(30.,-1.32966554433622E-14,16.));
#55933=CARTESIAN_POINT('',(29.9999999999999,-1.50000000000001,30.25));
#55934=CARTESIAN_POINT('',(30.,-1.50000000000001,30.3125));
#55935=CARTESIAN_POINT('',(30.,-1.50000000000001,16.));
#55936=CARTESIAN_POINT('',(30.,-1.50000000000002,30.75));
#55937=CARTESIAN_POINT('Ctrl Pts',(29.9999999999999,-1.50000000000001,30.25));
#55938=CARTESIAN_POINT('Ctrl Pts',(30.1658036138247,-1.50000000000003,30.2579772300895));
#55939=CARTESIAN_POINT('Ctrl Pts',(30.3306771390814,-1.47251502213024,30.2666731828795));
#55940=CARTESIAN_POINT('Ctrl Pts',(30.6740051197163,-1.35441705513551,30.2864720571327));
#55941=CARTESIAN_POINT('Ctrl Pts',(30.8456956760641,-1.25440329321601,30.2975106829297));
#55942=CARTESIAN_POINT('Ctrl Pts',(31.1355371924707,-0.998320157723232,
30.31856910982));
#55943=CARTESIAN_POINT('Ctrl Pts',(31.2526807741055,-0.846671576374736,
30.3279626902015));
#55944=CARTESIAN_POINT('Ctrl Pts',(31.4282014939959,-0.499786966349004,
30.3472340574251));
#55945=CARTESIAN_POINT('Ctrl Pts',(31.4817951924464,-0.306278304449559,
30.3579845386417));
#55946=CARTESIAN_POINT('Ctrl Pts',(31.5101111597472,0.0860175204635018,
30.3797787511369));
#55947=CARTESIAN_POINT('Ctrl Pts',(31.4862462216493,0.280921846793951,30.3906067692664));
#55948=CARTESIAN_POINT('Ctrl Pts',(31.3664146176937,0.647698903970874,30.4109832724428));
#55949=CARTESIAN_POINT('Ctrl Pts',(31.2727727808063,0.816486916731949,30.4197772164968));
#55950=CARTESIAN_POINT('Ctrl Pts',(31.0215777110749,1.11639419547156,30.440193602667));
#55951=CARTESIAN_POINT('Ctrl Pts',(30.8638920671928,1.2424306705166,30.4512812699412));
#55952=CARTESIAN_POINT('Ctrl Pts',(30.51519869364,1.4218077371841,30.4730404839947));
#55953=CARTESIAN_POINT('Ctrl Pts',(30.3288784064271,1.47608428096084,30.4835125047644));
#55954=CARTESIAN_POINT('Ctrl Pts',(29.9417076474062,1.51169090841865,30.5031293395779));
#55955=CARTESIAN_POINT('Ctrl Pts',(29.7444133180912,1.49107258678014,30.5125449036674));
#55956=CARTESIAN_POINT('Ctrl Pts',(29.3680874803138,1.37464650826943,30.5338849467157));
#55957=CARTESIAN_POINT('Ctrl Pts',(29.192868275455,1.27964935682832,30.5449539944024));
#55958=CARTESIAN_POINT('Ctrl Pts',(28.8948089362382,1.03185947909864,30.5661774332058));
#55959=CARTESIAN_POINT('Ctrl Pts',(28.7730426891403,0.883581363472215,30.5759121464738));
#55960=CARTESIAN_POINT('Ctrl Pts',(28.5872420086988,0.541893735862482,30.5948947924521));
#55961=CARTESIAN_POINT('Ctrl Pts',(28.5279457886126,0.350092848014275,30.6055503973326));
#55962=CARTESIAN_POINT('Ctrl Pts',(28.4879441501424,-0.0417086531130522,
30.6273171473952));
#55963=CARTESIAN_POINT('Ctrl Pts',(28.5061747163527,-0.237794814766365,
30.6382108230426));
#55964=CARTESIAN_POINT('Ctrl Pts',(28.6154381406337,-0.60772707143957,30.65876261508));
#55965=CARTESIAN_POINT('Ctrl Pts',(28.7037802077497,-0.77855877037785,30.6675955620118));
#55966=CARTESIAN_POINT('Ctrl Pts',(28.9458348287961,-1.08578773838532,30.687775558397));
#55967=CARTESIAN_POINT('Ctrl Pts',(29.1002278810903,-1.21679626071423,30.6988429232091));
#55968=CARTESIAN_POINT('Ctrl Pts',(29.3881527190005,-1.37554036843891,30.7171052719799));
#55969=CARTESIAN_POINT('Ctrl Pts',(29.5080276522,-1.42282651307167,30.7241862614101));
#55970=CARTESIAN_POINT('Ctrl Pts',(29.7526687702711,-1.48465507368766,30.7376740227083));
#55971=CARTESIAN_POINT('Ctrl Pts',(29.8761199631302,-1.50000000000009,30.7440398189472));
#55972=CARTESIAN_POINT('Ctrl Pts',(30.0000000000009,-1.50000000000001,30.75));
#55973=CARTESIAN_POINT('',(30.,-1.50000000000001,30.85));
#55974=CARTESIAN_POINT('',(30.,-1.50000000000001,16.));
#55975=CARTESIAN_POINT('Origin',(30.,-1.32966554433622E-14,30.85));
#55976=CARTESIAN_POINT('',(28.9490560961666,-1.07028823734334,30.75));
#55977=CARTESIAN_POINT('Origin',(30.,-1.5916987375435E-14,30.75));
#55978=CARTESIAN_POINT('Ctrl Pts',(28.9490560961666,-1.07028823734332,30.75));
#55979=CARTESIAN_POINT('Ctrl Pts',(28.8761609488349,-0.998710593084209,
30.7445045626927));
#55980=CARTESIAN_POINT('Ctrl Pts',(28.8107674297946,-0.919873442584925,
30.7391683946938));
#55981=CARTESIAN_POINT('Ctrl Pts',(28.6983154051604,-0.752052754529888,
30.7290963583567));
#55982=CARTESIAN_POINT('Ctrl Pts',(28.6511686993163,-0.663795554008335,
30.7243775307781));
#55983=CARTESIAN_POINT('Ctrl Pts',(28.5395598759442,-0.392939439769756,
30.709329968876));
#55984=CARTESIAN_POINT('Ctrl Pts',(28.5011631241701,-0.201888114570883,
30.6987160063649));
#55985=CARTESIAN_POINT('Ctrl Pts',(28.4988436150777,0.191908857459164,30.6768383968077));
#55986=CARTESIAN_POINT('Ctrl Pts',(28.5379718270057,0.390884408078152,30.6657841995511));
#55987=CARTESIAN_POINT('Ctrl Pts',(28.6882496652404,0.752033457565058,30.6457203634686));
#55988=CARTESIAN_POINT('Ctrl Pts',(28.7941652988744,0.912256576314666,30.6368419553212));
#55989=CARTESIAN_POINT('Ctrl Pts',(29.0637866570552,1.18813740110581,30.6162064354332));
#55990=CARTESIAN_POINT('Ctrl Pts',(29.2263162356668,1.29983562680085,30.6052839989448));
#55991=CARTESIAN_POINT('Ctrl Pts',(29.5881540142218,1.45598200117754,30.5835376714189));
#55992=CARTESIAN_POINT('Ctrl Pts',(29.7845106480132,1.49769538170803,30.5729317534561));
#55993=CARTESIAN_POINT('Ctrl Pts',(30.1735918421599,1.5020241460186,30.5540918323215));
#55994=CARTESIAN_POINT('Ctrl Pts',(30.3626153088868,1.46791385953203,30.544162381137));
#55995=CARTESIAN_POINT('Ctrl Pts',(30.7246797057952,1.32812661690519,30.5228595707569));
#55996=CARTESIAN_POINT('Ctrl Pts',(30.8932233177541,1.2211620663456,30.5117792749302));
#55997=CARTESIAN_POINT('Ctrl Pts',(31.1776737025205,0.949411483501645,30.4905450221109));
#55998=CARTESIAN_POINT('Ctrl Pts',(31.2913339229655,0.787872571372875,30.4812706984095));
#55999=CARTESIAN_POINT('Ctrl Pts',(31.4489779041399,0.433069950768308,30.4615594417092));
#56000=CARTESIAN_POINT('Ctrl Pts',(31.4925441992832,0.243681023738972,30.451037834652));
#56001=CARTESIAN_POINT('Ctrl Pts',(31.5059639907605,-0.148777135728896,
30.4292346035705));
#56002=CARTESIAN_POINT('Ctrl Pts',(31.4726973264507,-0.348194823891665,
30.418155843117));
#56003=CARTESIAN_POINT('Ctrl Pts',(31.3331360295961,-0.713588890875335,
30.3978561727291));
#56004=CARTESIAN_POINT('Ctrl Pts',(31.2315888806866,-0.877298264710928,
30.3890521180742));
#56005=CARTESIAN_POINT('Ctrl Pts',(30.969887909143,-1.16071911064266,30.3685882229343));
#56006=CARTESIAN_POINT('Ctrl Pts',(30.8111118646049,-1.27673016594729,30.3577265776157));
#56007=CARTESIAN_POINT('Ctrl Pts',(30.4544959445291,-1.44324278722566,30.3359435355702));
#56008=CARTESIAN_POINT('Ctrl Pts',(30.2594138454525,-1.49071962728781,30.3252388425894));
#56009=CARTESIAN_POINT('Ctrl Pts',(30.0404799678322,-1.49959063127059,30.3144589647139));
#56010=CARTESIAN_POINT('Ctrl Pts',(30.0202329450965,-1.50000000000001,30.3134734580248));
#56011=CARTESIAN_POINT('Ctrl Pts',(30.,-1.50000000000001,30.3125));
#56012=CARTESIAN_POINT('Origin',(30.,-1.32966554433622E-14,16.));
#56013=CARTESIAN_POINT('',(30.0000000422953,-1.50000000000001,29.7500000040699));
#56014=CARTESIAN_POINT('',(30.0000000000001,-1.50000000000001,29.8125));
#56015=CARTESIAN_POINT('',(30.,-1.50000000000001,16.));
#56016=CARTESIAN_POINT('Ctrl Pts',(30.0000000423936,-1.50000000000001,29.7500000020397));
#56017=CARTESIAN_POINT('Ctrl Pts',(30.195284159332,-1.49999999448081,29.7593956136499));
#56018=CARTESIAN_POINT('Ctrl Pts',(30.3888046451199,-1.46186371850976,29.7697657133627));
#56019=CARTESIAN_POINT('Ctrl Pts',(30.7506676874449,-1.3133124636612,29.7913022808498));
#56020=CARTESIAN_POINT('Ctrl Pts',(30.9154176613495,-1.20428706546983,29.8022573009481));
#56021=CARTESIAN_POINT('Ctrl Pts',(31.18981388205,-0.933008136594988,29.8229947210741));
#56022=CARTESIAN_POINT('Ctrl Pts',(31.2983679232815,-0.774850228387389,
29.8319527650896));
#56023=CARTESIAN_POINT('Ctrl Pts',(31.4541476549185,-0.418353419581691,
29.8517581433566));
#56024=CARTESIAN_POINT('Ctrl Pts',(31.4967395542031,-0.22207441884915,29.8626625322862));
#56025=CARTESIAN_POINT('Ctrl Pts',(31.5028167108854,0.170195075492689,29.8844552819718));
#56026=CARTESIAN_POINT('Ctrl Pts',(31.4683656451658,0.362410265994727,29.8951339036664));
#56027=CARTESIAN_POINT('Ctrl Pts',(31.3284167977355,0.722950513431523,29.9151639174129));
#56028=CARTESIAN_POINT('Ctrl Pts',(31.2243440361084,0.887881539566768,29.9240904295301));
#56029=CARTESIAN_POINT('Ctrl Pts',(30.9555499935672,1.17320843290826,29.9449485359688));
#56030=CARTESIAN_POINT('Ctrl Pts',(30.7918896841479,1.28933944326239,29.9560485076758));
#56031=CARTESIAN_POINT('Ctrl Pts',(30.4356884609645,1.44801470954154,29.9775938933022));
#56032=CARTESIAN_POINT('Ctrl Pts',(30.24769400318,1.49172420709908,29.9878529335795));
#56033=CARTESIAN_POINT('Ctrl Pts',(29.8564383086953,1.50648133745832,30.007087152245));
#56034=CARTESIAN_POINT('Ctrl Pts',(29.6568006042803,1.4738887523207,30.0172375010609));
#56035=CARTESIAN_POINT('Ctrl Pts',(29.2858871639067,1.33362042993594,30.0389794245699));
#56036=CARTESIAN_POINT('Ctrl Pts',(29.1177424716204,1.22887149382963,30.049978982519));
#56037=CARTESIAN_POINT('Ctrl Pts',(28.8358984689122,0.964859074366596,30.0708728867402));
#56038=CARTESIAN_POINT('Ctrl Pts',(28.7232154667205,0.809870978335536,30.0800071678703));
#56039=CARTESIAN_POINT('Ctrl Pts',(28.5578456280088,0.457982195266601,30.0995565447074));
#56040=CARTESIAN_POINT('Ctrl Pts',(28.5099042682065,0.262965364708001,30.1103908130718));
#56041=CARTESIAN_POINT('Ctrl Pts',(28.4930631778567,-0.129475272168894,
30.1321930706761));
#56042=CARTESIAN_POINT('Ctrl Pts',(28.5224126203679,-0.323064053208287,
30.142948002956));
#56043=CARTESIAN_POINT('Ctrl Pts',(28.6526173206986,-0.686662322858743,
30.1631479068255));
#56044=CARTESIAN_POINT('Ctrl Pts',(28.7515795011674,-0.85345907766542,30.1719758706799));
#56045=CARTESIAN_POINT('Ctrl Pts',(29.0118186458561,-1.14595641051804,30.1926215582791));
#56046=CARTESIAN_POINT('Ctrl Pts',(29.172636650331,-1.26695599442051,30.2037200176798));
#56047=CARTESIAN_POINT('Ctrl Pts',(29.5253217759949,-1.43577307549295,30.2253779520631));
#56048=CARTESIAN_POINT('Ctrl Pts',(29.7125728326969,-1.48464476779679,30.2357446197376));
#56049=CARTESIAN_POINT('Ctrl Pts',(29.9359811243456,-1.49897644179293,30.2468914582366));
#56050=CARTESIAN_POINT('Ctrl Pts',(29.9680065223165,-1.50000000000001,30.2484607130873));
#56051=CARTESIAN_POINT('Ctrl Pts',(29.9999999999999,-1.50000000000001,30.25));
#56052=CARTESIAN_POINT('Ctrl Pts',(30.,-1.50000000000001,30.3125));
#56053=CARTESIAN_POINT('Ctrl Pts',(29.8305649734084,-1.50000000000001,30.3043480534823));
#56054=CARTESIAN_POINT('Ctrl Pts',(29.6621927434306,-1.471296371185,30.2954499177677));
#56055=CARTESIAN_POINT('Ctrl Pts',(29.3161242189391,-1.34950305066004,30.2754165403276));
#56056=CARTESIAN_POINT('Ctrl Pts',(29.1449154106261,-1.2480688680691,30.264361636514));
#56057=CARTESIAN_POINT('Ctrl Pts',(28.8512754656375,-0.984586302069753,
30.242914917907));
#56058=CARTESIAN_POINT('Ctrl Pts',(28.7318299827785,-0.825047829175388,
30.2333359905097));
#56059=CARTESIAN_POINT('Ctrl Pts',(28.5638630976012,-0.47370253085421,30.2138168072696));
#56060=CARTESIAN_POINT('Ctrl Pts',(28.5150825240157,-0.286153024679847,
30.2033973902599));
#56061=CARTESIAN_POINT('Ctrl Pts',(28.4904050702493,0.104624550291977,30.1816875249837));
#56062=CARTESIAN_POINT('Ctrl Pts',(28.5176966903753,0.304322584656878,30.1705931897412));
#56063=CARTESIAN_POINT('Ctrl Pts',(28.6462704703314,0.673930577459572,30.1500594123633));
#56064=CARTESIAN_POINT('Ctrl Pts',(28.7433931121189,0.841252262459088,30.141257075347));
#56065=CARTESIAN_POINT('Ctrl Pts',(28.9970706151381,1.13219704351489,30.1209702113185));
#56066=CARTESIAN_POINT('Ctrl Pts',(29.1519620886259,1.25242080149054,30.1101784429931));
#56067=CARTESIAN_POINT('Ctrl Pts',(29.5030294160994,1.42917820121841,30.0883777805545));
#56068=CARTESIAN_POINT('Ctrl Pts',(29.696654967539,1.48240812812318,30.0775833577866));
#56069=CARTESIAN_POINT('Ctrl Pts',(30.0844620336651,1.50960977413546,30.0581693803401));
#56070=CARTESIAN_POINT('Ctrl Pts',(30.2746950762916,1.48681483093204,30.0489174722834));
#56071=CARTESIAN_POINT('Ctrl Pts',(30.642872277816,1.3694262764412,30.0279427452356));
#56072=CARTESIAN_POINT('Ctrl Pts',(30.8165454300566,1.27352463490858,30.0169229573155));
#56073=CARTESIAN_POINT('Ctrl Pts',(31.1192034235311,1.01839257572982,29.9952743161713));
#56074=CARTESIAN_POINT('Ctrl Pts',(31.2444516003803,0.860842115189833,29.9853245619549));
#56075=CARTESIAN_POINT('Ctrl Pts',(31.4225185229473,0.51295924874081,29.9659977360411));
#56076=CARTESIAN_POINT('Ctrl Pts',(31.476317491186,0.327339595503408,29.9556855330835));
#56077=CARTESIAN_POINT('Ctrl Pts',(31.5118899575654,-0.0614966036299657,
29.9340835220205));
#56078=CARTESIAN_POINT('Ctrl Pts',(31.49041063713,-0.261302093346022,29.9229832170363));
#56079=CARTESIAN_POINT('Ctrl Pts',(31.3726040951777,-0.63490434793495,29.9022275362258));
#56080=CARTESIAN_POINT('Ctrl Pts',(31.2797800327084,-0.805795593106099,
29.8933569012793));
#56081=CARTESIAN_POINT('Ctrl Pts',(31.0338687856651,-1.10392432463312,29.873244137236));
#56082=CARTESIAN_POINT('Ctrl Pts',(30.8828092373533,-1.22807490132932,29.8625276541988));
#56083=CARTESIAN_POINT('Ctrl Pts',(30.5373473005298,-1.41449618106684,29.8407282401322));
#56084=CARTESIAN_POINT('Ctrl Pts',(30.3452845785499,-1.47320733373471,29.8298567527606));
#56085=CARTESIAN_POINT('Ctrl Pts',(30.0982962322989,-1.49758712755237,29.8172963039161));
#56086=CARTESIAN_POINT('Ctrl Pts',(30.0491225084885,-1.50000000000001,29.8148634077916));
#56087=CARTESIAN_POINT('Ctrl Pts',(30.0000000000002,-1.50000000000001,29.8125));
#56088=CARTESIAN_POINT('Origin',(30.,-1.32966554433622E-14,16.));
#56089=CARTESIAN_POINT('',(30.,-1.50000000000001,29.25));
#56090=CARTESIAN_POINT('',(30.,-1.50000000000001,29.3125));
#56091=CARTESIAN_POINT('',(30.,-1.50000000000001,16.));
#56092=CARTESIAN_POINT('Ctrl Pts',(30.0000000000001,-1.50000000000001,29.25));
#56093=CARTESIAN_POINT('Ctrl Pts',(30.0257058009192,-1.50000000000001,29.2512367709234));
#56094=CARTESIAN_POINT('Ctrl Pts',(30.0514327409082,-1.49933922123128,29.2524929138666));
#56095=CARTESIAN_POINT('Ctrl Pts',(30.2757518694164,-1.4877855903611,29.2636064071598));
#56096=CARTESIAN_POINT('Ctrl Pts',(30.4703136581261,-1.43816783024051,29.2743455366981));
#56097=CARTESIAN_POINT('Ctrl Pts',(30.8249043497727,-1.26783071251083,29.2961373759079));
#56098=CARTESIAN_POINT('Ctrl Pts',(30.9822510518058,-1.15024113589767,29.3069740997672));
#56099=CARTESIAN_POINT('Ctrl Pts',(31.2409808029183,-0.864020908483806,
29.3273728025942));
#56100=CARTESIAN_POINT('Ctrl Pts',(31.3408899715229,-0.698983488656709,
29.3361675839636));
#56101=CARTESIAN_POINT('Ctrl Pts',(31.4763980403227,-0.332018378933428,
29.3565545345038));
#56102=CARTESIAN_POINT('Ctrl Pts',(31.5074559153656,-0.132477013527386,
29.3676401659153));
#56103=CARTESIAN_POINT('Ctrl Pts',(31.4898677318573,0.259397054955175,29.3894109474976));
#56104=CARTESIAN_POINT('Ctrl Pts',(31.444367356687,0.448123046557066,29.3998957248088));
#56105=CARTESIAN_POINT('Ctrl Pts',(31.2829132867175,0.801659109129801,29.419536617174));
#56106=CARTESIAN_POINT('Ctrl Pts',(31.1671346623852,0.962462537199801,29.4289146111855));
#56107=CARTESIAN_POINT('Ctrl Pts',(30.8792964511142,1.23119218867364,29.4502279461232));
#56108=CARTESIAN_POINT('Ctrl Pts',(30.7097525390342,1.33613064071083,29.4613000883974));
#56109=CARTESIAN_POINT('Ctrl Pts',(30.346523773562,1.47177468007876,29.4825438305068));
#56110=CARTESIAN_POINT('Ctrl Pts',(30.1572989096959,1.50379960302192,29.4923264081504));
#56111=CARTESIAN_POINT('Ctrl Pts',(29.7684168962525,1.49529312487305,29.5112727938055));
#56112=CARTESIAN_POINT('Ctrl Pts',(29.5725063077327,1.45146676708809,29.5219159452176));
#56113=CARTESIAN_POINT('Ctrl Pts',(29.2125442219205,1.29150806105852,29.5436779265358));
#56114=CARTESIAN_POINT('Ctrl Pts',(29.051374885103,1.17821798386326,29.5545791364576));
#56115=CARTESIAN_POINT('Ctrl Pts',(28.784644635234,0.899571593555892,29.5751523790963));
#56116=CARTESIAN_POINT('Ctrl Pts',(28.6803243600253,0.738084850822973,29.5839952860653));
#56117=CARTESIAN_POINT('Ctrl Pts',(28.5339435846744,0.375376943196454,29.6041457253779));
#56118=CARTESIAN_POINT('Ctrl Pts',(28.4969501646145,0.176221200716502,29.6152099332935));
#56119=CARTESIAN_POINT('Ctrl Pts',(28.5033188891713,-0.217123692718195,
29.6370624273732));
#56120=CARTESIAN_POINT('Ctrl Pts',(28.5436046203998,-0.407585858885439,
29.6476436588269));
#56121=CARTESIAN_POINT('Ctrl Pts',(28.6948329707667,-0.764496194056087,
29.6674720107808));
#56122=CARTESIAN_POINT('Ctrl Pts',(28.8049699824855,-0.927268122072015,
29.6765948726435));
#56123=CARTESIAN_POINT('Ctrl Pts',(29.0837280295094,-1.20402609540407,29.6976943469156));
#56124=CARTESIAN_POINT('Ctrl Pts',(29.2505451199729,-1.31436112105669,29.7087851997463));
#56125=CARTESIAN_POINT('Ctrl Pts',(29.6105129505334,-1.46104267840857,29.7301786477734));
#56126=CARTESIAN_POINT('Ctrl Pts',(29.799201008928,-1.49868271487424,29.7403024627842));
#56127=CARTESIAN_POINT('Ctrl Pts',(29.9932712661576,-1.49998868274459,29.7496759492739));
#56128=CARTESIAN_POINT('Ctrl Pts',(29.9966359009771,-1.50000000009509,29.7498381447076));
#56129=CARTESIAN_POINT('Ctrl Pts',(30.0000000423936,-1.50000000000001,29.7500000020397));
#56130=CARTESIAN_POINT('Ctrl Pts',(30.0000000000002,-1.50000000000001,29.8125));
#56131=CARTESIAN_POINT('Ctrl Pts',(29.8597537134085,-1.50000000000001,29.8057523973903));
#56132=CARTESIAN_POINT('Ctrl Pts',(29.7199776172616,-1.48033650865739,29.798481208736));
#56133=CARTESIAN_POINT('Ctrl Pts',(29.396444095828,-1.38712528602054,29.7803259942996));
#56134=CARTESIAN_POINT('Ctrl Pts',(29.2206000446906,-1.29650603057681,29.7693484919046));
#56135=CARTESIAN_POINT('Ctrl Pts',(28.911420128637,-1.05097346611518,29.747652717245));
#56136=CARTESIAN_POINT('Ctrl Pts',(28.7818724475201,-0.897590413872414,
29.737366134104));
#56137=CARTESIAN_POINT('Ctrl Pts',(28.5939020851709,-0.556198210295242,
29.7183999005719));
#56138=CARTESIAN_POINT('Ctrl Pts',(28.5345980064858,-0.372882477899534,
29.7082156932166));
#56139=CARTESIAN_POINT('Ctrl Pts',(28.4870031451474,0.0134445146485481,
29.6867530825195));
#56140=CARTESIAN_POINT('Ctrl Pts',(28.502033993864,0.213177772539474,29.6756567904145));
#56141=CARTESIAN_POINT('Ctrl Pts',(28.6077791980133,0.591085049341038,29.6546619417033));
#56142=CARTESIAN_POINT('Ctrl Pts',(28.6958240597398,0.766015662165753,29.6456356480104));
#56143=CARTESIAN_POINT('Ctrl Pts',(28.9331445661562,1.07197536298372,29.6257186792435));
#56144=CARTESIAN_POINT('Ctrl Pts',(29.079894739921,1.20029258347643,29.6150937909803));
#56145=CARTESIAN_POINT('Ctrl Pts',(29.4205899711736,1.39807482372058,29.5932081329061));
#56146=CARTESIAN_POINT('Ctrl Pts',(29.6127784235583,1.46301280498413,29.5821576288666));
#56147=CARTESIAN_POINT('Ctrl Pts',(30.000882127086,1.51202551870596,29.5621235164545));
#56148=CARTESIAN_POINT('Ctrl Pts',(30.1924980276144,1.49972435337029,29.5532307774773));
#56149=CARTESIAN_POINT('Ctrl Pts',(30.565900986819,1.40283604422102,29.5325740773055));
#56150=CARTESIAN_POINT('Ctrl Pts',(30.7436552900603,1.31725598082702,29.5216446454201));
#56151=CARTESIAN_POINT('Ctrl Pts',(31.0589827795059,1.08076551025951,29.4999042647726));
#56152=CARTESIAN_POINT('Ctrl Pts',(31.1927323157941,0.931082658468895,29.4893113802134));
#56153=CARTESIAN_POINT('Ctrl Pts',(31.3898152208091,0.595521362119493,29.470508077404));
#56154=CARTESIAN_POINT('Ctrl Pts',(31.454132752542,0.414466978649508,29.4605259432583));
#56155=CARTESIAN_POINT('Ctrl Pts',(31.5126702779257,0.0306540870738048,
29.4392030048374));
#56156=CARTESIAN_POINT('Ctrl Pts',(31.5035323460368,-0.168835937693657,
29.4281202256837));
#56157=CARTESIAN_POINT('Ctrl Pts',(31.4089367798935,-0.550558804938134,
29.4069133997257));
#56158=CARTESIAN_POINT('Ctrl Pts',(31.3252882833553,-0.729258932876967,
29.3976724363492));
#56159=CARTESIAN_POINT('Ctrl Pts',(31.095809753143,-1.04226364925314,29.3779370699617));
#56160=CARTESIAN_POINT('Ctrl Pts',(30.9530486497371,-1.17422022183269,29.3674030128222));
#56161=CARTESIAN_POINT('Ctrl Pts',(30.6189939852,-1.38091973480463,29.3455891471428));
#56162=CARTESIAN_POINT('Ctrl Pts',(30.429320489981,-1.45113472826307,29.3345130603643));
#56163=CARTESIAN_POINT('Ctrl Pts',(30.1547092959792,-1.49402062264703,29.3201095482887));
#56164=CARTESIAN_POINT('Ctrl Pts',(30.0773321028638,-1.50000000000001,29.3162206425338));
#56165=CARTESIAN_POINT('Ctrl Pts',(30.,-1.50000000000001,29.3125));
#56166=CARTESIAN_POINT('Origin',(30.,-1.32966554433622E-14,16.));
#56167=CARTESIAN_POINT('',(30.0000000000001,-1.50000000000001,28.75));
#56168=CARTESIAN_POINT('',(30.,-1.50000000000001,28.8125));
#56169=CARTESIAN_POINT('',(30.,-1.50000000000001,16.));
#56170=CARTESIAN_POINT('Ctrl Pts',(30.0000000000002,-1.50000000000001,28.75));
#56171=CARTESIAN_POINT('Ctrl Pts',(30.0540853804301,-1.50000000000001,28.7526021840792));
#56172=CARTESIAN_POINT('Ctrl Pts',(30.1082259230801,-1.49707499170992,28.7552882723823));
#56173=CARTESIAN_POINT('Ctrl Pts',(30.3599293953789,-1.46969892581938,28.7681588076143));
#56174=CARTESIAN_POINT('Ctrl Pts',(30.551406195325,-1.40907643365525,28.7790551975627));
#56175=CARTESIAN_POINT('Ctrl Pts',(30.8948389562126,-1.21930777033508,28.8008499657338));
#56176=CARTESIAN_POINT('Ctrl Pts',(31.0445316684251,-1.09380802186036,28.8115381638324));
#56177=CARTESIAN_POINT('Ctrl Pts',(31.2877030940359,-0.793168713090864,
28.8315888464123));
#56178=CARTESIAN_POINT('Ctrl Pts',(31.379006293082,-0.620999590881335,28.8405000227289));
#56179=CARTESIAN_POINT('Ctrl Pts',(31.4929834420294,-0.246010850263539,
28.861332730541));
#56180=CARTESIAN_POINT('Ctrl Pts',(31.5124077516471,-0.0462064671363202,
28.872432974048));
#56181=CARTESIAN_POINT('Ctrl Pts',(31.472996504913,0.34187077296362,28.8939928207202));
#56182=CARTESIAN_POINT('Ctrl Pts',(31.4174359900152,0.526774847879437,28.9042652693267));
#56183=CARTESIAN_POINT('Ctrl Pts',(31.2357811865968,0.873408443354475,28.9235226912975));
#56184=CARTESIAN_POINT('Ctrl Pts',(31.1084372252019,1.03024288184359,28.9336214802999));
#56185=CARTESIAN_POINT('Ctrl Pts',(30.8025714917792,1.28234443647017,28.9553402732223));
#56186=CARTESIAN_POINT('Ctrl Pts',(30.6280587815183,1.37625325113107,28.9663450980946));
#56187=CARTESIAN_POINT('Ctrl Pts',(30.2588396849677,1.48965870484553,28.9872593116519));
#56188=CARTESIAN_POINT('Ctrl Pts',(30.068359262301,1.51042753130005,28.996421409812));
#56189=CARTESIAN_POINT('Ctrl Pts',(29.6808324457,1.4790834395187,29.015936971685));
#56190=CARTESIAN_POINT('Ctrl Pts',(29.4877765738488,1.42378431516532,29.0267614634377));
#56191=CARTESIAN_POINT('Ctrl Pts',(29.1387883585853,1.24336756773843,29.0485637430906));
#56192=CARTESIAN_POINT('Ctrl Pts',(28.9853282851658,1.12165139698337,29.0593280990587));
#56193=CARTESIAN_POINT('Ctrl Pts',(28.7345675292747,0.827996981331758,29.0795498986531));
#56194=CARTESIAN_POINT('Ctrl Pts',(28.6390572969471,0.659343561113025,29.0883698021604));
#56195=CARTESIAN_POINT('Ctrl Pts',(28.5145121329283,0.288224890453508,29.108987506086));
#56196=CARTESIAN_POINT('Ctrl Pts',(28.4894007489509,0.0884674237606763,
29.1200851431244));
#56197=CARTESIAN_POINT('Ctrl Pts',(28.5181714945435,-0.301617414497863,
29.1417565230277));
#56198=CARTESIAN_POINT('Ctrl Pts',(28.5688407456957,-0.488459284239858,
29.1521366269022));
#56199=CARTESIAN_POINT('Ctrl Pts',(28.7405885892344,-0.838517734954907,
29.1715843186086));
#56200=CARTESIAN_POINT('Ctrl Pts',(28.8621896492638,-0.99731625641509,29.1812936366545));
#56201=CARTESIAN_POINT('Ctrl Pts',(29.1592029920166,-1.25770358504828,29.2028166791214));
#56202=CARTESIAN_POINT('Ctrl Pts',(29.3313514615525,-1.35708034159287,29.2138596416832));
#56203=CARTESIAN_POINT('Ctrl Pts',(29.6732716198879,-1.47316539526991,29.2335348677957));
#56204=CARTESIAN_POINT('Ctrl Pts',(29.836171069295,-1.50000000000001,29.2421177768964));
#56205=CARTESIAN_POINT('Ctrl Pts',(30.0000000000001,-1.50000000000001,29.25));
#56206=CARTESIAN_POINT('Ctrl Pts',(30.,-1.50000000000001,29.3125));
#56207=CARTESIAN_POINT('Ctrl Pts',(29.8873008443269,-1.50000000000001,29.3070777593446));
#56208=CARTESIAN_POINT('Ctrl Pts',(29.7747317592542,-1.48730209620256,29.3013090571639));
#56209=CARTESIAN_POINT('Ctrl Pts',(29.4744632015876,-1.41837586794508,29.2849477619958));
#56210=CARTESIAN_POINT('Ctrl Pts',(29.294837753903,-1.33817655775596,29.2740777699983));
#56211=CARTESIAN_POINT('Ctrl Pts',(28.9731315511867,-1.11133054751215,29.2522983950411));
#56212=CARTESIAN_POINT('Ctrl Pts',(28.8350302040853,-0.965600487241644,
29.241605933651));
#56213=CARTESIAN_POINT('Ctrl Pts',(28.6283822605559,-0.636211572057215,
29.2225138877439));
#56214=CARTESIAN_POINT('Ctrl Pts',(28.5588803689078,-0.457503373167084,
29.2129168540649));
#56215=CARTESIAN_POINT('Ctrl Pts',(28.4890373687744,-0.0765943370343735,
29.1917552409464));
#56216=CARTESIAN_POINT('Ctrl Pts',(28.4920613555339,0.122462822378066,29.1806965098678));
#56217=CARTESIAN_POINT('Ctrl Pts',(28.5749385187676,0.508021327520356,29.1592765929154));
#56218=CARTESIAN_POINT('Ctrl Pts',(28.6539760022703,0.690715131611738,29.1497407450183));
#56219=CARTESIAN_POINT('Ctrl Pts',(28.8753117279029,1.01093295253508,29.1301967854836));
#56220=CARTESIAN_POINT('Ctrl Pts',(29.0138845897616,1.14650161502305,29.1197638993787));
#56221=CARTESIAN_POINT('Ctrl Pts',(29.3408853293963,1.36213850199283,29.0980411554306));
#56222=CARTESIAN_POINT('Ctrl Pts',(29.5278326261113,1.43768005817386,29.0869482728631));
#56223=CARTESIAN_POINT('Ctrl Pts',(29.9124519842907,1.50965487695232,29.0664439648431));
#56224=CARTESIAN_POINT('Ctrl Pts',(30.1057978761999,1.50848592114141,29.0576455173396));
#56225=CARTESIAN_POINT('Ctrl Pts',(30.4842893221004,1.43290905070853,29.0373359816462));
#56226=CARTESIAN_POINT('Ctrl Pts',(30.6656448486515,1.3581864320247,29.02653488151));
#56227=CARTESIAN_POINT('Ctrl Pts',(30.9934995933557,1.14126552935963,29.0047353821212));
#56228=CARTESIAN_POINT('Ctrl Pts',(31.1358790692293,0.999664672511309,28.9939517892597));
#56229=CARTESIAN_POINT('Ctrl Pts',(31.3521306759684,0.67660748989115,28.974573568351));
#56230=CARTESIAN_POINT('Ctrl Pts',(31.426848104494,0.500181082019829,28.9652878378899));
#56231=CARTESIAN_POINT('Ctrl Pts',(31.5078778462889,0.122255781263764,28.9442919878479));
#56232=CARTESIAN_POINT('Ctrl Pts',(31.5109056485428,-0.0761896933508503,
28.9332672392582));
#56233=CARTESIAN_POINT('Ctrl Pts',(31.4398008862795,-0.46541654048851,28.9116435255283));
#56234=CARTESIAN_POINT('Ctrl Pts',(31.3653977766762,-0.65214948337147,28.9017441343992));
#56235=CARTESIAN_POINT('Ctrl Pts',(31.1521444486118,-0.979425287841449,
28.8823929843003));
#56236=CARTESIAN_POINT('Ctrl Pts',(31.0177656624447,-1.1184106596764,28.8720669771632));
#56237=CARTESIAN_POINT('Ctrl Pts',(30.6979072153004,-1.34258973369453,28.8504505839492));
#56238=CARTESIAN_POINT('Ctrl Pts',(30.5137720633169,-1.42326028628083,28.8393505286358));
#56239=CARTESIAN_POINT('Ctrl Pts',(30.2141280739392,-1.48853135114915,28.8231208153399));
#56240=CARTESIAN_POINT('Ctrl Pts',(30.107104215103,-1.50000000000001,28.8176530539518));
#56241=CARTESIAN_POINT('Ctrl Pts',(30.,-1.50000000000001,28.8125));
#56242=CARTESIAN_POINT('Origin',(30.,-1.32966554433622E-14,16.));
#56243=CARTESIAN_POINT('',(30.,-1.50000000000001,28.25));
#56244=CARTESIAN_POINT('',(29.9999999999999,-1.50000000000001,28.3125));
#56245=CARTESIAN_POINT('',(30.,-1.50000000000001,16.));
#56246=CARTESIAN_POINT('Ctrl Pts',(30.,-1.50000000000001,28.25));
#56247=CARTESIAN_POINT('Ctrl Pts',(30.0829658981124,-1.50000000000001,28.2539916986341));
#56248=CARTESIAN_POINT('Ctrl Pts',(30.1659646402018,-1.49311778203419,28.258176150196));
#56249=CARTESIAN_POINT('Ctrl Pts',(30.4454386189069,-1.44623695759697,28.272924593389));
#56250=CARTESIAN_POINT('Ctrl Pts',(30.6341065114148,-1.37401296366571,28.2840081036532));
#56251=CARTESIAN_POINT('Ctrl Pts',(30.9655430066945,-1.16393488515826,28.305789851648));
#56252=CARTESIAN_POINT('Ctrl Pts',(31.1067439460802,-1.03060853555517,28.3162868947229));
#56253=CARTESIAN_POINT('Ctrl Pts',(31.3331794991128,-0.714896180931114,
28.3359510679762));
#56254=CARTESIAN_POINT('Ctrl Pts',(31.4151109522262,-0.5347128589249,28.3452937300598));
#56255=CARTESIAN_POINT('Ctrl Pts',(31.5053441166005,-0.151540941191815,
28.3665810588227));
#56256=CARTESIAN_POINT('Ctrl Pts',(31.5121960357138,0.047808853319833,28.3776560474067));
#56257=CARTESIAN_POINT('Ctrl Pts',(31.4494295470438,0.430548940590616,28.3989193855884));
#56258=CARTESIAN_POINT('Ctrl Pts',(31.3831821322801,0.610720967506089,28.4087494232854));
#56259=CARTESIAN_POINT('Ctrl Pts',(31.1825379493516,0.943999251999173,28.4276606511623));
#56260=CARTESIAN_POINT('Ctrl Pts',(31.047158086339,1.09222920702457,28.4382916166091));
#56261=CARTESIAN_POINT('Ctrl Pts',(30.7294268326579,1.32515752881874,28.4600486998403));
#56262=CARTESIAN_POINT('Ctrl Pts',(30.550958922042,1.4087432384851,28.4709570664618));
#56263=CARTESIAN_POINT('Ctrl Pts',(30.1765920486677,1.5017020595339,28.4915509905286));
#56264=CARTESIAN_POINT('Ctrl Pts',(29.9846796160604,1.51197023290498,28.5004045958464));
#56265=CARTESIAN_POINT('Ctrl Pts',(29.5971747277955,1.45876321333926,28.5205264062414));
#56266=CARTESIAN_POINT('Ctrl Pts',(29.4058997547266,1.39186434368365,28.5315874296089));
#56267=CARTESIAN_POINT('Ctrl Pts',(29.0676327101079,1.19076140439435,28.5534485031393));
#56268=CARTESIAN_POINT('Ctrl Pts',(28.9223466869136,1.06108495094317,28.5640407038963));
#56269=CARTESIAN_POINT('Ctrl Pts',(28.6879155980949,0.752518131365587,28.5838910754598));
#56270=CARTESIAN_POINT('Ctrl Pts',(28.6014862328755,0.576207606788701,28.5929884662895));
#56271=CARTESIAN_POINT('Ctrl Pts',(28.499833643426,0.196881228217823,28.6140621539879));
#56272=CARTESIAN_POINT('Ctrl Pts',(28.4869739372834,-0.00278217893022192,
28.6251545654961));
#56273=CARTESIAN_POINT('Ctrl Pts',(28.5386011115484,-0.388179803466622,
28.646565544637));
#56274=CARTESIAN_POINT('Ctrl Pts',(28.5997438056181,-0.57068109411198,28.6567045052284));
#56275=CARTESIAN_POINT('Ctrl Pts',(28.7910752661536,-0.909939730661663,
28.6755522072589));
#56276=CARTESIAN_POINT('Ctrl Pts',(28.9221594106395,-1.06198129449833,28.6859751842018));
#56277=CARTESIAN_POINT('Ctrl Pts',(29.2336502066539,-1.30423330232361,28.7076910145522));
#56278=CARTESIAN_POINT('Ctrl Pts',(29.4102115046891,-1.39300789458955,28.7186517848609));
#56279=CARTESIAN_POINT('Ctrl Pts',(29.7297304238973,-1.48169043732429,28.7364880499937));
#56280=CARTESIAN_POINT('Ctrl Pts',(29.8646679236608,-1.50000000000001,28.7434888324413));
#56281=CARTESIAN_POINT('Ctrl Pts',(30.0000000000002,-1.50000000000001,28.75));
#56282=CARTESIAN_POINT('Ctrl Pts',(30.,-1.50000000000001,28.8125));
#56283=CARTESIAN_POINT('Ctrl Pts',(29.915383015882,-1.50000000000001,28.8084288634535));
#56284=CARTESIAN_POINT('Ctrl Pts',(29.8307352254749,-1.4928411598692,28.8041573880682));
#56285=CARTESIAN_POINT('Ctrl Pts',(29.5559284168413,-1.44580747389306,28.7896292480462));
#56286=CARTESIAN_POINT('Ctrl Pts',(29.3730572440495,-1.37640415455312,28.7789029846613));
#56287=CARTESIAN_POINT('Ctrl Pts',(29.0395563050654,-1.16922544646275,28.7571024491396));
#56288=CARTESIAN_POINT('Ctrl Pts',(28.8931654598463,-1.03173520870096,28.7462400430439));
#56289=CARTESIAN_POINT('Ctrl Pts',(28.6676984257239,-0.714888535897263,
28.7265909588401));
#56290=CARTESIAN_POINT('Ctrl Pts',(28.5879546245725,-0.540586509645268,
28.7175325838691));
#56291=CARTESIAN_POINT('Ctrl Pts',(28.4963360655409,-0.165582907317607,
28.6966990504065));
#56292=CARTESIAN_POINT('Ctrl Pts',(28.4875887561367,0.032114568158461,28.6857158573245));
#56293=CARTESIAN_POINT('Ctrl Pts',(28.5470557852483,0.422500942588754,28.6640277254117));
#56294=CARTESIAN_POINT('Ctrl Pts',(28.6157998677826,0.611145026803925,28.6537877758344));
#56295=CARTESIAN_POINT('Ctrl Pts',(28.8187186237447,0.943964110383672,28.6347798680923));
#56296=CARTESIAN_POINT('Ctrl Pts',(28.9483973542157,1.08655537048085,28.6245798289275));
#56297=CARTESIAN_POINT('Ctrl Pts',(29.2601643471919,1.31985362966521,28.6030994252846));
#56298=CARTESIAN_POINT('Ctrl Pts',(29.4410566887989,1.40604402433623,28.5920020608114));
#56299=CARTESIAN_POINT('Ctrl Pts',(29.8214920682634,1.50190823479761,28.5710354603478));
#56300=CARTESIAN_POINT('Ctrl Pts',(30.0168727428654,1.5123834847247,28.5620321954671));
#56301=CARTESIAN_POINT('Ctrl Pts',(30.4002098002625,1.45848214178997,28.5420916231679));
#56302=CARTESIAN_POINT('Ctrl Pts',(30.5845472296663,1.39485738401663,28.531455330078));
#56303=CARTESIAN_POINT('Ctrl Pts',(30.9255768985555,1.19735876148644,28.5095614596354));
#56304=CARTESIAN_POINT('Ctrl Pts',(31.0774615143075,1.06275841541511,28.4985150091509));
#56305=CARTESIAN_POINT('Ctrl Pts',(31.3127681711381,0.750226996476014,28.4785123840417));
#56306=CARTESIAN_POINT('Ctrl Pts',(31.3972426471779,0.57785906771898,28.4696032815399));
#56307=CARTESIAN_POINT('Ctrl Pts',(31.4986444188222,0.205636520695856,28.4489242511497));
#56308=CARTESIAN_POINT('Ctrl Pts',(31.5126593744967,0.00877624847217685,
28.4379875693595));
#56309=CARTESIAN_POINT('Ctrl Pts',(31.4639817400215,-0.38243148199871,28.4162538065556));
#56310=CARTESIAN_POINT('Ctrl Pts',(31.4004868863224,-0.572852347631721,
28.405674869576));
#56311=CARTESIAN_POINT('Ctrl Pts',(31.2070793636249,-0.910612756316215,
28.3869104024268));
#56312=CARTESIAN_POINT('Ctrl Pts',(31.0818178721223,-1.05640050494828,28.3768711948362));
#56313=CARTESIAN_POINT('Ctrl Pts',(30.7776023551779,-1.29787423387296,28.3555270153716));
#56314=CARTESIAN_POINT('Ctrl Pts',(30.5998203088742,-1.38901510440857,28.3444417818325));
#56315=CARTESIAN_POINT('Ctrl Pts',(30.2759956104928,-1.48090471471267,28.3263092695923));
#56316=CARTESIAN_POINT('Ctrl Pts',(30.1382050521625,-1.50000000000003,28.3191493936725));
#56317=CARTESIAN_POINT('Ctrl Pts',(29.9999999999998,-1.50000000000001,28.3125));
#56318=CARTESIAN_POINT('Origin',(30.,-1.32966554433622E-14,16.));
#56319=CARTESIAN_POINT('',(30.,-1.50000000000001,27.75));
#56320=CARTESIAN_POINT('',(29.9999999999999,-1.50000000000001,27.8125));
#56321=CARTESIAN_POINT('',(30.,-1.50000000000001,16.));
#56322=CARTESIAN_POINT('Ctrl Pts',(30.,-1.50000000000001,27.75));
#56323=CARTESIAN_POINT('Ctrl Pts',(30.1124415068704,-1.50000000000002,27.7554098445216));
#56324=CARTESIAN_POINT('Ctrl Pts',(30.2247618661566,-1.48736003703784,27.7611649704098));
#56325=CARTESIAN_POINT('Ctrl Pts',(30.5287085515254,-1.41774990238772,27.7777222269793));
#56326=CARTESIAN_POINT('Ctrl Pts',(30.7117935692984,-1.3352484713228,27.7888226154224));
#56327=CARTESIAN_POINT('Ctrl Pts',(31.0290158327245,-1.10803593258209,27.810396438097));
#56328=CARTESIAN_POINT('Ctrl Pts',(31.1618575965723,-0.967846133863366,
27.8206819515156));
#56329=CARTESIAN_POINT('Ctrl Pts',(31.3721629460689,-0.6380210664967,27.8399620797878));
#56330=CARTESIAN_POINT('Ctrl Pts',(31.4448593309443,-0.449797513993593,
27.8500112492227));
#56331=CARTESIAN_POINT('Ctrl Pts',(31.5116357099559,-0.0592694964018678,
27.8717072502));
#56332=CARTESIAN_POINT('Ctrl Pts',(31.5064070816201,0.138907825669745,27.8827171014262));
#56333=CARTESIAN_POINT('Ctrl Pts',(31.4213057895144,0.515720730899333,27.9036511517167));
#56334=CARTESIAN_POINT('Ctrl Pts',(31.3446665574137,0.691326301909506,27.9128415418121));
#56335=CARTESIAN_POINT('Ctrl Pts',(31.1248857141117,1.01202109760975,27.9323239413351));
#56336=CARTESIAN_POINT('Ctrl Pts',(30.9809587395189,1.15206471718701,27.9431387316727));
#56337=CARTESIAN_POINT('Ctrl Pts',(30.6509116511972,1.36527940308072,27.964940759777));
#56338=CARTESIAN_POINT('Ctrl Pts',(30.4689587309927,1.43797198007731,27.9757142119819));
#56339=CARTESIAN_POINT('Ctrl Pts',(30.0895559298121,1.50958056680736,27.9959573651739));
#56340=CARTESIAN_POINT('Ctrl Pts',(29.8958570870542,1.50864454830606,28.0047704518936));
#56341=CARTESIAN_POINT('Ctrl Pts',(29.5119529197823,1.43233602869983,28.0253607308535));
#56342=CARTESIAN_POINT('Ctrl Pts',(29.326059536573,1.35483178794297,28.0364574259998));
#56343=CARTESIAN_POINT('Ctrl Pts',(29.0017503691465,1.13591853977073,28.058141681653));
#56344=CARTESIAN_POINT('Ctrl Pts',(28.8647633102306,0.999035130825837,28.0685347915132));
#56345=CARTESIAN_POINT('Ctrl Pts',(28.6464909172802,0.676130375169667,28.0880060034614));
#56346=CARTESIAN_POINT('Ctrl Pts',(28.5692025798653,0.491914163630282,28.097671435354));
#56347=CARTESIAN_POINT('Ctrl Pts',(28.4907708909632,0.10494838810591,28.1191695339942));
#56348=CARTESIAN_POINT('Ctrl Pts',(28.4900432259905,-0.0938982867387415,
28.1302165714856));
#56349=CARTESIAN_POINT('Ctrl Pts',(28.5641302538219,-0.473688030944453,
28.1513160017192));
#56350=CARTESIAN_POINT('Ctrl Pts',(28.6356001259049,-0.65152593371875,28.1607865563875));
#56351=CARTESIAN_POINT('Ctrl Pts',(28.845875335272,-0.978539657712538,28.1799871416705));
#56352=CARTESIAN_POINT('Ctrl Pts',(28.9856037255401,-1.12272886979256,28.1907150828729));
#56353=CARTESIAN_POINT('Ctrl Pts',(29.3096631032409,-1.34585412683097,28.2125043207586));
#56354=CARTESIAN_POINT('Ctrl Pts',(29.4899597666947,-1.42399330666579,28.2233493807965));
#56355=CARTESIAN_POINT('Ctrl Pts',(29.7854687062271,-1.48848755634025,28.2393585682142));
#56356=CARTESIAN_POINT('Ctrl Pts',(29.8926913234913,-1.50000000000001,28.2448371088943));
#56357=CARTESIAN_POINT('Ctrl Pts',(30.,-1.50000000000001,28.25));
#56358=CARTESIAN_POINT('Ctrl Pts',(29.9999999999998,-1.50000000000001,28.3125));
#56359=CARTESIAN_POINT('Ctrl Pts',(29.9436942937174,-1.50000000000001,28.3097909904434));
#56360=CARTESIAN_POINT('Ctrl Pts',(29.8873283119117,-1.49682992210333,28.3069910231599));
#56361=CARTESIAN_POINT('Ctrl Pts',(29.6396724584349,-1.46877643215582,28.2942964117443));
#56362=CARTESIAN_POINT('Ctrl Pts',(29.4541661443778,-1.41038581308707,28.2837492734071));
#56363=CARTESIAN_POINT('Ctrl Pts',(29.1087260311914,-1.22301113475657,28.2619244260365));
#56364=CARTESIAN_POINT('Ctrl Pts',(28.9535330490943,-1.09318251992373,28.250851349792));
#56365=CARTESIAN_POINT('Ctrl Pts',(28.7092889328235,-0.787692454984111,
28.2306143141317));
#56366=CARTESIAN_POINT('Ctrl Pts',(28.6196840987504,-0.61735395437333,28.2217974419096));
#56367=CARTESIAN_POINT('Ctrl Pts',(28.5078809954767,-0.248171981043882,
28.2012873322802));
#56368=CARTESIAN_POINT('Ctrl Pts',(28.4882926923279,-0.0523550997824531,
28.1904086166545));
#56369=CARTESIAN_POINT('Ctrl Pts',(28.5254878247544,0.339597077669009,28.168633495685));
#56370=CARTESIAN_POINT('Ctrl Pts',(28.5834194437059,0.531823926835376,28.1579542262869));
#56371=CARTESIAN_POINT('Ctrl Pts',(28.7667554264755,0.874769226053054,28.1389017096637));
#56372=CARTESIAN_POINT('Ctrl Pts',(28.8874031082008,1.02385470321529,28.129256101159));
#56373=CARTESIAN_POINT('Ctrl Pts',(29.1834814070674,1.27365788399194,28.1080720501192));
#56374=CARTESIAN_POINT('Ctrl Pts',(29.3578610118793,1.36987818467188,28.0970094213409));
#56375=CARTESIAN_POINT('Ctrl Pts',(29.7335617480327,1.48922788034193,28.0756182419206));
#56376=CARTESIAN_POINT('Ctrl Pts',(29.9311376367095,1.51130087803589,28.0661270552772));
#56377=CARTESIAN_POINT('Ctrl Pts',(30.3188296259211,1.47827076732948,28.0465567126743));
#56378=CARTESIAN_POINT('Ctrl Pts',(30.5053902810264,1.4253063260919,28.0361095744917));
#56379=CARTESIAN_POINT('Ctrl Pts',(30.8550820522802,1.24848731142734,28.0143733820065));
#56380=CARTESIAN_POINT('Ctrl Pts',(31.0135429189334,1.12366789185429,28.0032822239058));
#56381=CARTESIAN_POINT('Ctrl Pts',(31.2669421658592,0.825551327222966,27.9828095312695));
#56382=CARTESIAN_POINT('Ctrl Pts',(31.3618736710286,0.657250577679458,27.9740139209821));
#56383=CARTESIAN_POINT('Ctrl Pts',(31.4842407851538,0.291243414392501,27.9536801896884));
#56384=CARTESIAN_POINT('Ctrl Pts',(31.509450941646,0.0966465287303217,27.9428692515961));
#56385=CARTESIAN_POINT('Ctrl Pts',(31.4839402912682,-0.295715862316101,
27.9210713409824));
#56386=CARTESIAN_POINT('Ctrl Pts',(31.4317236332783,-0.489608696036187,
27.9102995168868));
#56387=CARTESIAN_POINT('Ctrl Pts',(31.2586786377253,-0.837725609348495,
27.8909596883695));
#56388=CARTESIAN_POINT('Ctrl Pts',(31.1426320784322,-0.99018742000189,27.8816363720611));
#56389=CARTESIAN_POINT('Ctrl Pts',(30.8547518896528,-1.24822771259633,27.8606179441152));
#56390=CARTESIAN_POINT('Ctrl Pts',(30.683921012954,-1.3494162779034,27.8495880462471));
#56391=CARTESIAN_POINT('Ctrl Pts',(30.3380948295812,-1.47125624803439,27.8295650326271));
#56392=CARTESIAN_POINT('Ctrl Pts',(30.1695563642114,-1.50000000000003,27.8206577843767));
#56393=CARTESIAN_POINT('Ctrl Pts',(29.9999999999999,-1.50000000000001,27.8125));
#56394=CARTESIAN_POINT('Origin',(30.,-1.32966554433622E-14,16.));
#56395=CARTESIAN_POINT('',(29.9999999999999,-1.50000000000001,27.25));
#56396=CARTESIAN_POINT('',(30.0000000001561,-1.50000000000001,27.312500000015));
#56397=CARTESIAN_POINT('',(30.,-1.50000000000001,16.));
#56398=CARTESIAN_POINT('Ctrl Pts',(29.9999999999998,-1.50000000000001,27.25));
#56399=CARTESIAN_POINT('Ctrl Pts',(30.1442714687728,-1.50000000000004,27.2569412642777));
#56400=CARTESIAN_POINT('Ctrl Pts',(30.2880340149987,-1.4791914741294,27.2644360576155));
#56401=CARTESIAN_POINT('Ctrl Pts',(30.6163114314673,-1.38174334274362,27.2829372047179));
#56402=CARTESIAN_POINT('Ctrl Pts',(30.7927900386128,-1.28861749288707,27.2940148648257));
#56403=CARTESIAN_POINT('Ctrl Pts',(31.0938533402203,-1.04389816914467,27.3152975386708));
#56404=CARTESIAN_POINT('Ctrl Pts',(31.2173213404585,-0.896838599044721,
27.3251756333865));
#56405=CARTESIAN_POINT('Ctrl Pts',(31.4068435879888,-0.557063752560209,
27.3440520137467));
#56406=CARTESIAN_POINT('Ctrl Pts',(31.4681965573585,-0.365925712559008,
27.3546707937468));
#56407=CARTESIAN_POINT('Ctrl Pts',(31.5124404667227,0.0256096349450533,
27.376422757497));
#56408=CARTESIAN_POINT('Ctrl Pts',(31.4962677243898,0.222085336897189,27.3873380742721));
#56409=CARTESIAN_POINT('Ctrl Pts',(31.3908461160845,0.593142920619804,27.4079523844789));
#56410=CARTESIAN_POINT('Ctrl Pts',(31.304401721973,0.764723471695272,27.4168175948822));
#56411=CARTESIAN_POINT('Ctrl Pts',(31.0656503667188,1.07455866625052,27.4369110579998));
#56412=CARTESIAN_POINT('Ctrl Pts',(30.9124772117446,1.20733392111332,27.4479688063785));
#56413=CARTESIAN_POINT('Ctrl Pts',(30.5697179509117,1.40095220523075,27.4698381046742));
#56414=CARTESIAN_POINT('Ctrl Pts',(30.3849139570494,1.46256729268532,27.4804410211816));
#56415=CARTESIAN_POINT('Ctrl Pts',(30.0007344874447,1.51254230178002,27.5003130592281));
#56416=CARTESIAN_POINT('Ctrl Pts',(29.8049569216954,1.49991645600797,27.5093863351468));
#56417=CARTESIAN_POINT('Ctrl Pts',(29.4253565109394,1.3996692288739,27.5304345136228));
#56418=CARTESIAN_POINT('Ctrl Pts',(29.245638701995,1.31157237616612,27.5415283255346));
#56419=CARTESIAN_POINT('Ctrl Pts',(28.9367683949736,1.07514318986943,27.562956332507));
#56420=CARTESIAN_POINT('Ctrl Pts',(28.8087599369318,0.93132448347984,27.5731101063824));
#56421=CARTESIAN_POINT('Ctrl Pts',(28.6094708234815,0.596592375009914,27.591996522448));
#56422=CARTESIAN_POINT('Ctrl Pts',(28.5427132787644,0.407261741609369,27.6023743476884));
#56423=CARTESIAN_POINT('Ctrl Pts',(28.4873635075659,0.0164898797776363,
27.624083895568));
#56424=CARTESIAN_POINT('Ctrl Pts',(28.4981279946982,-0.180903932406258,
27.6350502184671));
#56425=CARTESIAN_POINT('Ctrl Pts',(28.5934885065557,-0.554852956622451,
27.6558251642568));
#56426=CARTESIAN_POINT('Ctrl Pts',(28.6750314181996,-0.72841210507679,27.6648194223046));
#56427=CARTESIAN_POINT('Ctrl Pts',(28.9037835277885,-1.04301134033857,27.6845641309549));
#56428=CARTESIAN_POINT('Ctrl Pts',(29.0515807305306,-1.17900166318454,27.6954525361552));
#56429=CARTESIAN_POINT('Ctrl Pts',(29.3870321030576,-1.38265756586298,27.7172490562487));
#56430=CARTESIAN_POINT('Ctrl Pts',(29.570408592882,-1.45015060314336,27.7279465683201));
#56431=CARTESIAN_POINT('Ctrl Pts',(29.8405845073873,-1.49365112485936,27.7421537608929));
#56432=CARTESIAN_POINT('Ctrl Pts',(29.920314098353,-1.50000000000001,27.7461661102695));
#56433=CARTESIAN_POINT('Ctrl Pts',(30.,-1.50000000000001,27.75));
#56434=CARTESIAN_POINT('Ctrl Pts',(29.9999999999999,-1.50000000000001,27.8125));
#56435=CARTESIAN_POINT('Ctrl Pts',(29.9712572824709,-1.50000000000001,27.8111171153581));
#56436=CARTESIAN_POINT('Ctrl Pts',(29.9424874969812,-1.49917387170699,27.8097099804002));
#56437=CARTESIAN_POINT('Ctrl Pts',(29.7223735770152,-1.48649276547853,27.7987674915373));
#56438=CARTESIAN_POINT('Ctrl Pts',(29.5349257292356,-1.43889608772887,27.7884267728186));
#56439=CARTESIAN_POINT('Ctrl Pts',(29.1813453265204,-1.27257887490163,27.7667952051828));
#56440=CARTESIAN_POINT('Ctrl Pts',(29.0198117779222,-1.15277654761383,27.7556955762776));
#56441=CARTESIAN_POINT('Ctrl Pts',(28.7574522908629,-0.862041024530384,
27.7349968128188));
#56442=CARTESIAN_POINT('Ctrl Pts',(28.6572312223829,-0.695708343276581,
27.7261504635153));
#56443=CARTESIAN_POINT('Ctrl Pts',(28.524605736016,-0.332863036208749,27.7059923909005));
#56444=CARTESIAN_POINT('Ctrl Pts',(28.4939840388333,-0.139603136099824,
27.6952557297833));
#56445=CARTESIAN_POINT('Ctrl Pts',(28.508148989394,0.25282273238934,27.673454292645));
#56446=CARTESIAN_POINT('Ctrl Pts',(28.5547646373704,0.44816718663467,27.6626018229647));
#56447=CARTESIAN_POINT('Ctrl Pts',(28.7177569938957,0.801209312950165,27.6429883715028));
#56448=CARTESIAN_POINT('Ctrl Pts',(28.8294090431484,0.956981758536969,27.6339039237114));
#56449=CARTESIAN_POINT('Ctrl Pts',(29.1093968787388,1.22281551664853,27.6130487316321));
#56450=CARTESIAN_POINT('Ctrl Pts',(29.2767036270498,1.32864238149993,27.6020595468161));
#56451=CARTESIAN_POINT('Ctrl Pts',(29.6469534397504,1.47162694755714,27.5802741008953));
#56452=CARTESIAN_POINT('Ctrl Pts',(29.8468632228895,1.50560128622732,27.570023387908));
#56453=CARTESIAN_POINT('Ctrl Pts',(30.2385607914922,1.49319741260661,27.5508332778069));
#56454=CARTESIAN_POINT('Ctrl Pts',(30.4267058309758,1.45067195878526,27.540599882768));
#56455=CARTESIAN_POINT('Ctrl Pts',(30.7836729511717,1.29433057010809,27.5190824778378));
#56456=CARTESIAN_POINT('Ctrl Pts',(30.9479647504538,1.17932417828325,27.5079833629642));
#56457=CARTESIAN_POINT('Ctrl Pts',(31.2187102492265,0.89565657574078,27.4870774584548));
#56458=CARTESIAN_POINT('Ctrl Pts',(31.3239608540741,0.731149127851972,27.4781193959917));
#56459=CARTESIAN_POINT('Ctrl Pts',(31.4661242989034,0.37131396030254,27.4581285533501));
#56460=CARTESIAN_POINT('Ctrl Pts',(31.5017272578984,0.179429293592902,27.4474682940885));
#56461=CARTESIAN_POINT('Ctrl Pts',(31.4980926781097,-0.21275991516766,27.4256800047129));
#56462=CARTESIAN_POINT('Ctrl Pts',(31.4567210643059,-0.409304691427262,
27.4147608504762));
#56463=CARTESIAN_POINT('Ctrl Pts',(31.3031284414201,-0.766835781066652,
27.394898012163));
#56464=CARTESIAN_POINT('Ctrl Pts',(31.1955054411838,-0.925718941221814,
27.3859710339898));
#56465=CARTESIAN_POINT('Ctrl Pts',(30.9227930606553,-1.19862566676885,27.3652694110877));
#56466=CARTESIAN_POINT('Ctrl Pts',(30.75882230211,-1.30859982122977,27.354325526665));
#56467=CARTESIAN_POINT('Ctrl Pts',(30.3950972752779,-1.46060207029247,27.3326035134561));
#56468=CARTESIAN_POINT('Ctrl Pts',(30.198484714314,-1.4999999999587,27.3220496002711));
#56469=CARTESIAN_POINT('Ctrl Pts',(30.0000000003122,-1.50000000000001,27.312500000015));
#56470=CARTESIAN_POINT('Origin',(30.,-1.32966554433622E-14,16.));
#56471=CARTESIAN_POINT('',(30.,-1.50000000000001,26.75));
#56472=CARTESIAN_POINT('',(30.0000000000001,-1.50000000000001,26.8125));
#56473=CARTESIAN_POINT('',(30.,-1.50000000000001,16.));
#56474=CARTESIAN_POINT('Ctrl Pts',(29.9999999999999,-1.50000000000002,26.75));
#56475=CARTESIAN_POINT('Ctrl Pts',(30.1755630845093,-1.50000000000003,26.7584467828418));
#56476=CARTESIAN_POINT('Ctrl Pts',(30.3499584064833,-1.46918259215549,26.7676934207892));
#56477=CARTESIAN_POINT('Ctrl Pts',(30.6997034276012,-1.3412672085792,26.7880737410627));
#56478=CARTESIAN_POINT('Ctrl Pts',(30.8691431470038,-1.23821435243508,26.7990884927007));
#56479=CARTESIAN_POINT('Ctrl Pts',(31.1538803669515,-0.977054933639417,
26.8200423468827));
#56480=CARTESIAN_POINT('Ctrl Pts',(31.2681733329846,-0.823282264050392,
26.8292620964417));
#56481=CARTESIAN_POINT('Ctrl Pts',(31.4372326110993,-0.473197410553428,
26.8487112549693));
#56482=CARTESIAN_POINT('Ctrl Pts',(31.4872301101415,-0.278708237309613,
26.8595162090384));
#56483=CARTESIAN_POINT('Ctrl Pts',(31.5082331683214,0.113718878171538,26.881317715454));
#56484=CARTESIAN_POINT('Ctrl Pts',(31.4808674747884,0.307802550913579,26.8921001417175));
#56485=CARTESIAN_POINT('Ctrl Pts',(31.3544261384598,0.67256246632588,26.9123645814626));
#56486=CARTESIAN_POINT('Ctrl Pts',(31.2574072539999,0.840081862517357,26.9211719059107));
#56487=CARTESIAN_POINT('Ctrl Pts',(31.0004574791989,1.1352928844589,26.9417347138799));
#56488=CARTESIAN_POINT('Ctrl Pts',(30.8407636896231,1.25813738072432,26.9528303320317));
#56489=CARTESIAN_POINT('Ctrl Pts',(30.4894980147219,1.43081423936239,26.9745271891017));
#56490=CARTESIAN_POINT('Ctrl Pts',(30.302568408204,1.48165789304525,26.984933167702));
#56491=CARTESIAN_POINT('Ctrl Pts',(29.9140424353861,1.51051713966446,27.0044277780243));
#56492=CARTESIAN_POINT('Ctrl Pts',(29.7160053760103,1.48607476032932,27.0140505099305));
#56493=CARTESIAN_POINT('Ctrl Pts',(29.3413420123945,1.36197834203437,27.0355236321475));
#56494=CARTESIAN_POINT('Ctrl Pts',(29.1683424827117,1.26378814603618,27.0465745813446));
#56495=CARTESIAN_POINT('Ctrl Pts',(28.87548492057,1.01073104588063,27.0676940612658));
#56496=CARTESIAN_POINT('Ctrl Pts',(28.7566499301147,0.860326156686485,27.0772041024063));
#56497=CARTESIAN_POINT('Ctrl Pts',(28.5773390955292,0.515342682333064,27.0963698509815));
#56498=CARTESIAN_POINT('Ctrl Pts',(28.5216397715234,0.322442560698391,27.1070865244057));
#56499=CARTESIAN_POINT('Ctrl Pts',(28.4890218615652,-0.0697120082430973,
27.1288728893469));
#56500=CARTESIAN_POINT('Ctrl Pts',(28.510818362855,-0.265069960572926,27.1397261089208));
#56501=CARTESIAN_POINT('Ctrl Pts',(28.6267610927498,-0.633018179794785,
27.1601676766553));
#56502=CARTESIAN_POINT('Ctrl Pts',(28.7184387624141,-0.802555681667626,
27.1689674029211));
#56503=CARTESIAN_POINT('Ctrl Pts',(28.9662614123549,-1.10518359683465,27.1892971067025));
#56504=CARTESIAN_POINT('Ctrl Pts',(29.1227466839353,-1.23306866661795,27.2003783708913));
#56505=CARTESIAN_POINT('Ctrl Pts',(29.4698813680168,-1.416339226716,27.2221707450579));
#56506=CARTESIAN_POINT('Ctrl Pts',(29.6558172836666,-1.47261637710131,27.232679845148));
#56507=CARTESIAN_POINT('Ctrl Pts',(29.8981460836565,-1.49740948534734,27.2450275924248));
#56508=CARTESIAN_POINT('Ctrl Pts',(29.9491012405249,-1.5,27.247551132293));
#56509=CARTESIAN_POINT('Ctrl Pts',(29.9999999999998,-1.50000000000001,27.25));
#56510=CARTESIAN_POINT('Ctrl Pts',(30.0000000003122,-1.50000000000001,27.312500000015));
#56511=CARTESIAN_POINT('Ctrl Pts',(29.9998020603292,-1.50000000000005,27.3124904766232));
#56512=CARTESIAN_POINT('Ctrl Pts',(29.9996041185888,-1.49999996081992,27.3124809520584));
#56513=CARTESIAN_POINT('Ctrl Pts',(29.8088160951652,-1.49992443102837,27.3032995609518));
#56514=CARTESIAN_POINT('Ctrl Pts',(29.6200100906951,-1.46352575850992,27.2932045535897));
#56515=CARTESIAN_POINT('Ctrl Pts',(29.2593205849108,-1.31930644298838,27.2718447795537));
#56516=CARTESIAN_POINT('Ctrl Pts',(29.0918823606668,-1.21016636340677,27.2607572353565));
#56517=CARTESIAN_POINT('Ctrl Pts',(28.8110979291704,-0.935181294724627,
27.2396095139674));
#56518=CARTESIAN_POINT('Ctrl Pts',(28.6997118002275,-0.772848068745042,
27.2304360038192));
#56519=CARTESIAN_POINT('Ctrl Pts',(28.5461974612702,-0.416685157506792,
27.210649175417));
#56520=CARTESIAN_POINT('Ctrl Pts',(28.5047394765833,-0.226599155889903,
27.2000888419939));
#56521=CARTESIAN_POINT('Ctrl Pts',(28.4958539389935,0.166443777601294,27.1782531234666));
#56522=CARTESIAN_POINT('Ctrl Pts',(28.5315184967694,0.365700597221805,27.1671833001544));
#56523=CARTESIAN_POINT('Ctrl Pts',(28.6754701753172,0.729371435414476,27.1469793646992));
#56524=CARTESIAN_POINT('Ctrl Pts',(28.7788000491734,0.891648198610453,27.1381536711784));
#56525=CARTESIAN_POINT('Ctrl Pts',(29.0437345128306,1.17200464814443,27.1176193266989));
#56526=CARTESIAN_POINT('Ctrl Pts',(29.2040531543845,1.2862733419873,27.1067318620762));
#56527=CARTESIAN_POINT('Ctrl Pts',(29.5628324377282,1.44858368838945,27.0849614650246));
#56528=CARTESIAN_POINT('Ctrl Pts',(29.7584548095726,1.49371725552991,27.0742958690726));
#56529=CARTESIAN_POINT('Ctrl Pts',(30.1472060622831,1.50481186242553,27.055283882181));
#56530=CARTESIAN_POINT('Ctrl Pts',(30.3365600149074,1.47407427722924,27.045587089767));
#56531=CARTESIAN_POINT('Ctrl Pts',(30.7004989886168,1.34098519143669,27.0243801486806));
#56532=CARTESIAN_POINT('Ctrl Pts',(30.8706482413977,1.23730103012925,27.0133137233474));
#56533=CARTESIAN_POINT('Ctrl Pts',(31.1605713571455,0.970446090199086,26.991952153717));
#56534=CARTESIAN_POINT('Ctrl Pts',(31.2776619344983,0.810096307036669,26.9825053503909));
#56535=CARTESIAN_POINT('Ctrl Pts',(31.4414580755822,0.457344311316898,26.9629080172954));
#56536=CARTESIAN_POINT('Ctrl Pts',(31.4881418689773,0.269035150966863,26.9524463972759));
#56537=CARTESIAN_POINT('Ctrl Pts',(31.508284818313,-0.122458793694974,26.9306967336836));
#56538=CARTESIAN_POINT('Ctrl Pts',(31.478582774639,-0.322064434897177,26.9196075313946));
#56539=CARTESIAN_POINT('Ctrl Pts',(31.3455674834561,-0.689986184900448,
26.8991674341722));
#56540=CARTESIAN_POINT('Ctrl Pts',(31.246662212612,-0.855842984261559,26.8903733141072));
#56541=CARTESIAN_POINT('Ctrl Pts',(30.9897531567272,-1.14377092738595,26.8700147729728));
#56542=CARTESIAN_POINT('Ctrl Pts',(30.8332877383797,-1.26231706455743,26.8591938787678));
#56543=CARTESIAN_POINT('Ctrl Pts',(30.4799553603842,-1.43498001100993,26.8373979738484));
#56544=CARTESIAN_POINT('Ctrl Pts',(30.2857235516143,-1.48590367409306,26.8266384453951));
#56545=CARTESIAN_POINT('Ctrl Pts',(30.0581276265954,-1.49915605873645,26.8153201095514));
#56546=CARTESIAN_POINT('Ctrl Pts',(30.0290509426437,-1.50000000000001,26.8138977141296));
#56547=CARTESIAN_POINT('Ctrl Pts',(30.0000000000001,-1.50000000000001,26.8125));
#56548=CARTESIAN_POINT('Origin',(30.,-1.32966554433622E-14,16.));
#56549=CARTESIAN_POINT('',(30.,-1.50000000000001,26.25));
#56550=CARTESIAN_POINT('',(30.0000000000001,-1.50000000000001,26.3125));
#56551=CARTESIAN_POINT('',(30.,-1.50000000000001,16.));
#56552=CARTESIAN_POINT('Ctrl Pts',(30.,-1.50000000000001,26.25));
#56553=CARTESIAN_POINT('Ctrl Pts',(30.0056194401817,-1.50000000000001,26.2502703654418));
#56554=CARTESIAN_POINT('Ctrl Pts',(30.0112401600052,-1.49996842190559,26.2505416696197));
#56555=CARTESIAN_POINT('Ctrl Pts',(30.2156637559459,-1.49767029707552,26.2604408412659));
#56556=CARTESIAN_POINT('Ctrl Pts',(30.4120156853044,-1.45593401100177,26.2710471691517));
#56557=CARTESIAN_POINT('Ctrl Pts',(30.7738333695248,-1.29974623576057,26.2927936799124));
#56558=CARTESIAN_POINT('Ctrl Pts',(30.9363483004055,-1.18803068750778,26.3037158928437));
#56559=CARTESIAN_POINT('Ctrl Pts',(31.2059383925193,-0.91211987124096,26.3243507415389));
#56560=CARTESIAN_POINT('Ctrl Pts',(31.3118367658411,-0.751883140819906,
26.3332287143989));
#56561=CARTESIAN_POINT('Ctrl Pts',(31.4620725484111,-0.390717177178761,
26.3532934901568));
#56562=CARTESIAN_POINT('Ctrl Pts',(31.5011777050095,-0.191739563198423,
26.3643478020445));
#56563=CARTESIAN_POINT('Ctrl Pts',(31.4988144256802,0.202052743889533,26.3862251524383));
#56564=CARTESIAN_POINT('Ctrl Pts',(31.4603972352794,0.393097806012914,26.3968387670007));
#56565=CARTESIAN_POINT('Ctrl Pts',(31.3127984325509,0.751186708707084,26.4167325949282));
#56566=CARTESIAN_POINT('Ctrl Pts',(31.2046306350456,0.914654115967526,26.4257825736587));
#56567=CARTESIAN_POINT('Ctrl Pts',(30.929085340333,1.1942016269637,26.4468049614706));
#56568=CARTESIAN_POINT('Ctrl Pts',(30.763267624326,1.30642002708729,26.4579000478329));
#56569=CARTESIAN_POINT('Ctrl Pts',(30.4044749371868,1.4569895622401,26.479344956129));
#56570=CARTESIAN_POINT('Ctrl Pts',(30.2159899848526,1.49659297949806,26.4895135375502));
#56571=CARTESIAN_POINT('Ctrl Pts',(29.8264040657205,1.50311771775866,26.5084387415533));
#56572=CARTESIAN_POINT('Ctrl Pts',(29.6289313228251,1.46692091172634,26.5187719136178));
#56573=CARTESIAN_POINT('Ctrl Pts',(29.2622864534942,1.32066065000658,26.5404749081659));
#56574=CARTESIAN_POINT('Ctrl Pts',(29.0963152488665,1.21314636529189,26.5514467093804));
#56575=CARTESIAN_POINT('Ctrl Pts',(28.8192613253014,0.944447852152411,26.5722403200802));
#56576=CARTESIAN_POINT('Ctrl Pts',(28.7092361098565,0.787428080615722,26.5812539955214));
#56577=CARTESIAN_POINT('Ctrl Pts',(28.5500186537103,0.4325695152731,26.6009683602626));
#56578=CARTESIAN_POINT('Ctrl Pts',(28.5055087117716,0.236724815037938,26.6118486213868));
#56579=CARTESIAN_POINT('Ctrl Pts',(28.4955827399852,-0.155640049113208,
26.6336466693952));
#56580=CARTESIAN_POINT('Ctrl Pts',(28.5282144121142,-0.348361913823613,
26.6443534396569));
#56581=CARTESIAN_POINT('Ctrl Pts',(28.6646766132005,-0.710004687419899,
26.6644447048566));
#56582=CARTESIAN_POINT('Ctrl Pts',(28.7669073789545,-0.875602741749661,
26.6733284353239));
#56583=CARTESIAN_POINT('Ctrl Pts',(29.0326342692594,-1.16351957915387,26.6941109162225));
#56584=CARTESIAN_POINT('Ctrl Pts',(29.1952892767769,-1.28140768888904,26.7052113286353));
#56585=CARTESIAN_POINT('Ctrl Pts',(29.5502593863542,-1.44373597574174,26.7267989550745));
#56586=CARTESIAN_POINT('Ctrl Pts',(29.7380028348229,-1.48930167419739,26.7370974797965));
#56587=CARTESIAN_POINT('Ctrl Pts',(29.9528487018704,-1.49944465692866,26.7477160059146));
#56588=CARTESIAN_POINT('Ctrl Pts',(29.9764341399413,-1.50000000000001,26.7488661870293));
#56589=CARTESIAN_POINT('Ctrl Pts',(29.9999999999999,-1.50000000000001,26.75));
#56590=CARTESIAN_POINT('Ctrl Pts',(30.0000000000001,-1.50000000000001,26.8125));
#56591=CARTESIAN_POINT('Ctrl Pts',(29.8395800016776,-1.50000000000002,26.8047817892321));
#56592=CARTESIAN_POINT('Ctrl Pts',(29.6800130120943,-1.4742710204936,26.7963899249912));
#56593=CARTESIAN_POINT('Ctrl Pts',(29.3406580591605,-1.36160698346738,26.7769331456215));
#56594=CARTESIAN_POINT('Ctrl Pts',(29.1679496395237,-1.26348603655748,26.7658981260489));
#56595=CARTESIAN_POINT('Ctrl Pts',(28.8688888773426,-1.00499369846698,26.744329215695));
#56596=CARTESIAN_POINT('Ctrl Pts',(28.7459708502921,-0.846646295408431,
26.7345359053005));
#56597=CARTESIAN_POINT('Ctrl Pts',(28.5719299961441,-0.497373685523865,
26.7151318714181));
#56598=CARTESIAN_POINT('Ctrl Pts',(28.5201211210885,-0.310969647956289,
26.7047760915532));
#56599=CARTESIAN_POINT('Ctrl Pts',(28.4888763927518,0.078675171393689,26.6831291571448));
#56600=CARTESIAN_POINT('Ctrl Pts',(28.5126680280148,0.27845746343119,26.6720301409206));
#56601=CARTESIAN_POINT('Ctrl Pts',(28.6347687943924,0.650483449918004,26.6513620305602));
#56602=CARTESIAN_POINT('Ctrl Pts',(28.7293030467267,0.819946999855557,26.6425267967844));
#56603=CARTESIAN_POINT('Ctrl Pts',(28.9783004894773,1.11523286685495,26.62234451654));
#56604=CARTESIAN_POINT('Ctrl Pts',(29.1308905878018,1.23784103842587,26.6115972394678));
#56605=CARTESIAN_POINT('Ctrl Pts',(29.4786064716065,1.42045274911996,26.5897952036888));
#56606=CARTESIAN_POINT('Ctrl Pts',(29.671307799161,1.47699671076135,26.5789531911429));
#56607=CARTESIAN_POINT('Ctrl Pts',(30.058657983757,1.51083891985875,26.5593767353335));
#56608=CARTESIAN_POINT('Ctrl Pts',(30.2492918070221,1.49128918840572,26.5502639753537));
#56609=CARTESIAN_POINT('Ctrl Pts',(30.6191301716824,1.38027512961514,26.5293863948823));
#56610=CARTESIAN_POINT('Ctrl Pts',(30.7941362196709,1.2875659668366,26.518391157951));
#56611=CARTESIAN_POINT('Ctrl Pts',(31.1019229551517,1.03729505553015,26.4966307919773));
#56612=CARTESIAN_POINT('Ctrl Pts',(31.2305302882388,0.880892156398053,26.4864384531331));
#56613=CARTESIAN_POINT('Ctrl Pts',(31.4143329938993,0.535011347738905,26.467222852652));
#56614=CARTESIAN_POINT('Ctrl Pts',(31.4709425533457,0.350543024469619,26.4569746124704));
#56615=CARTESIAN_POINT('Ctrl Pts',(31.5126435249117,-0.0370627264893054,
26.4354409596394));
#56616=CARTESIAN_POINT('Ctrl Pts',(31.4944467514533,-0.236856679751601,
26.4243412955692));
#56617=CARTESIAN_POINT('Ctrl Pts',(31.382763240843,-0.612667143007661,26.4034629364995));
#56618=CARTESIAN_POINT('Ctrl Pts',(31.2923692914564,-0.785603738087747,
26.3945234871348));
#56619=CARTESIAN_POINT('Ctrl Pts',(31.0508333839059,-1.08773585408316,26.3745100265869));
#56620=CARTESIAN_POINT('Ctrl Pts',(30.9019600520426,-1.21403192877114,26.3638391307711));
#56621=CARTESIAN_POINT('Ctrl Pts',(30.559750929656,-1.4057831061822,26.3420481650989));
#56622=CARTESIAN_POINT('Ctrl Pts',(30.3686322762759,-1.46754077280931,26.3311374738613));
#56623=CARTESIAN_POINT('Ctrl Pts',(30.1141378164167,-1.49674664949133,26.3180818291001));
#56624=CARTESIAN_POINT('Ctrl Pts',(30.0570405412872,-1.50000000000001,26.3152443643222));
#56625=CARTESIAN_POINT('Ctrl Pts',(30.0000000000002,-1.50000000000001,26.3125));
#56626=CARTESIAN_POINT('Origin',(30.,-1.32966554433622E-14,16.));
#56627=CARTESIAN_POINT('',(30.0000000000001,-1.50000000000001,25.75));
#56628=CARTESIAN_POINT('',(30.,-1.50000000000001,25.8125));
#56629=CARTESIAN_POINT('',(30.,-1.50000000000001,16.));
#56630=CARTESIAN_POINT('Ctrl Pts',(30.0000000000002,-1.50000000000001,25.75));
#56631=CARTESIAN_POINT('Ctrl Pts',(30.0350308469701,-1.50000000000001,25.7516854224107));
#56632=CARTESIAN_POINT('Ctrl Pts',(30.0700958017757,-1.49877287551864,25.7534065726266));
#56633=CARTESIAN_POINT('Ctrl Pts',(30.3035194655511,-1.48237243734734,25.7650927416133));
#56634=CARTESIAN_POINT('Ctrl Pts',(30.4971388675202,-1.42911969045028,25.7758875024032));
#56635=CARTESIAN_POINT('Ctrl Pts',(30.848183508266,-1.2523218603483,25.7976881963921));
#56636=CARTESIAN_POINT('Ctrl Pts',(31.0030592952475,-1.13208157746957,25.8084796690252));
#56637=CARTESIAN_POINT('Ctrl Pts',(31.2567047166631,-0.841106936698577,
25.8287658189633));
#56638=CARTESIAN_POINT('Ctrl Pts',(31.3538096540821,-0.673770640691784,
25.8375682977395));
#56639=CARTESIAN_POINT('Ctrl Pts',(31.4823392304013,-0.304145984064151,
25.8581030008855));
#56640=CARTESIAN_POINT('Ctrl Pts',(31.5096068971125,-0.104447172132542,
25.8691973793261));
#56641=CARTESIAN_POINT('Ctrl Pts',(31.4848844296652,0.286323023183646,25.8909068346215));
#56642=CARTESIAN_POINT('Ctrl Pts',(31.4360830652788,0.473864860798067,25.9013258256));
#56643=CARTESIAN_POINT('Ctrl Pts',(31.2680746858178,0.825196096656156,25.9208442275921));
#56644=CARTESIAN_POINT('Ctrl Pts',(31.1486056539627,0.984726473310249,25.9304245311885));
#56645=CARTESIAN_POINT('Ctrl Pts',(30.8549287066094,1.24817526789042,25.9518720919776));
#56646=CARTESIAN_POINT('Ctrl Pts',(30.6837094772403,1.34958696185865,25.9629268724906));
#56647=CARTESIAN_POINT('Ctrl Pts',(30.3185036845909,1.47806545582453,25.9840666914365));
#56648=CARTESIAN_POINT('Ctrl Pts',(30.1289070957048,1.50647679352315,25.993618043535));
#56649=CARTESIAN_POINT('Ctrl Pts',(29.7404075656125,1.49068855536224,26.0127482980627));
#56650=CARTESIAN_POINT('Ctrl Pts',(29.545331017818,1.44318830470102,26.0234533742517));
#56651=CARTESIAN_POINT('Ctrl Pts',(29.188736991222,1.27663378618483,26.0452365267588));
#56652=CARTESIAN_POINT('Ctrl Pts',(29.0299764729631,1.16060540084053,26.056097906459));
#56653=CARTESIAN_POINT('Ctrl Pts',(28.7683079019703,0.877153943717209,26.0765610930375));
#56654=CARTESIAN_POINT('Ctrl Pts',(28.6667786145465,0.713430148276809,26.0853649917623));
#56655=CARTESIAN_POINT('Ctrl Pts',(28.5272614190292,0.348018884480366,26.1056656175288));
#56656=CARTESIAN_POINT('Ctrl Pts',(28.4940188142116,0.14859972255689,26.1167444598579));
#56657=CARTESIAN_POINT('Ctrl Pts',(28.5074840531687,-0.243852309362615,
26.1385473505201));
#56658=CARTESIAN_POINT('Ctrl Pts',(28.5510714566589,-0.433234122923729,
26.1490685623846));
#56659=CARTESIAN_POINT('Ctrl Pts',(28.7087569062828,-0.788023018123922,
26.1687790565624));
#56660=CARTESIAN_POINT('Ctrl Pts',(28.8224400778707,-0.949553940205162,
26.1780544535033));
#56661=CARTESIAN_POINT('Ctrl Pts',(29.1069273076436,-1.22127183449108,26.1992895710132));
#56662=CARTESIAN_POINT('Ctrl Pts',(29.2754819087647,-1.32821443027861,26.2103697857015));
#56663=CARTESIAN_POINT('Ctrl Pts',(29.6323103908041,-1.46593097223903,26.2313631635471));
#56664=CARTESIAN_POINT('Ctrl Pts',(29.8154198943914,-1.50000000000001,26.2411193855283));
#56665=CARTESIAN_POINT('Ctrl Pts',(30.,-1.50000000000001,26.25));
#56666=CARTESIAN_POINT('Ctrl Pts',(30.0000000000002,-1.50000000000001,26.3125));
#56667=CARTESIAN_POINT('Ctrl Pts',(29.867580258195,-1.50000000000001,26.3061289522019));
#56668=CARTESIAN_POINT('Ctrl Pts',(29.7355134428156,-1.48246999719879,26.299287940062));
#56669=CARTESIAN_POINT('Ctrl Pts',(29.4184023489971,-1.39643165750255,26.2816409715667));
#56670=CARTESIAN_POINT('Ctrl Pts',(29.2414246745114,-1.30875331188796,26.2706906196325));
#56671=CARTESIAN_POINT('Ctrl Pts',(28.9285790709285,-1.068455989113,26.2489639028796));
#56672=CARTESIAN_POINT('Ctrl Pts',(28.7965902868422,-0.917216536990246,
26.2384564742772));
#56673=CARTESIAN_POINT('Ctrl Pts',(28.6032774267936,-0.57923818308581,26.2196798990602));
#56674=CARTESIAN_POINT('Ctrl Pts',(28.5410496718181,-0.397228347537677,
26.2095682415298));
#56675=CARTESIAN_POINT('Ctrl Pts',(28.4870387262231,-0.0124011503103316,
26.1881889527949));
#56676=CARTESIAN_POINT('Ctrl Pts',(28.4986129287161,0.187210043596071,26.1770994420224));
#56677=CARTESIAN_POINT('Ctrl Pts',(28.5978341126594,0.567369358609899,26.1559794800772));
#56678=CARTESIAN_POINT('Ctrl Pts',(28.6833047820777,0.744501773375072,26.1468355900596));
#56679=CARTESIAN_POINT('Ctrl Pts',(28.9160253075989,1.05460577600707,26.1270248184819));
#56680=CARTESIAN_POINT('Ctrl Pts',(29.060441358732,1.18507685788338,26.1164524012633));
#56681=CARTESIAN_POINT('Ctrl Pts',(29.3972605323865,1.3881264388998,26.0946069150758));
#56682=CARTESIAN_POINT('Ctrl Pts',(29.5879874006837,1.45617711323181,26.0835402678372));
#56683=CARTESIAN_POINT('Ctrl Pts',(29.9751313819113,1.51185807000195,26.0633671011121));
#56684=CARTESIAN_POINT('Ctrl Pts',(30.1672228871666,1.50278877622694,26.0545319510962));
#56685=CARTESIAN_POINT('Ctrl Pts',(30.5421508905102,1.41213985662164,26.0339751935801));
#56686=CARTESIAN_POINT('Ctrl Pts',(30.7210278648892,1.32972839399854,26.0230797638426));
#56687=CARTESIAN_POINT('Ctrl Pts',(31.0401525812529,1.09890434445495,26.0013140896138));
#56688=CARTESIAN_POINT('Ctrl Pts',(31.1764827770535,0.951536572108244,25.9906613507783));
#56689=CARTESIAN_POINT('Ctrl Pts',(31.3792148041551,0.619604996410003,25.9716870800294));
#56690=CARTESIAN_POINT('Ctrl Pts',(31.4465937278795,0.439945368358781,25.9619414093531));
#56691=CARTESIAN_POINT('Ctrl Pts',(31.5118285637272,0.0578389075257285,
25.9407132726402));
#56692=CARTESIAN_POINT('Ctrl Pts',(31.5063115855957,-0.141417075009879,
25.9296434958327));
#56693=CARTESIAN_POINT('Ctrl Pts',(31.4186362556573,-0.525426994647723,
25.9083096114084));
#56694=CARTESIAN_POINT('Ctrl Pts',(31.3377111820022,-0.706481965554299,
25.8989028268757));
#56695=CARTESIAN_POINT('Ctrl Pts',(31.1130533652913,-1.0237694591265,25.8792804311414));
#56696=CARTESIAN_POINT('Ctrl Pts',(30.972766729538,-1.15788504149396,25.8688054543882));
#56697=CARTESIAN_POINT('Ctrl Pts',(30.6428698469895,-1.36991560346518,25.8470435453937));
#56698=CARTESIAN_POINT('Ctrl Pts',(30.4547968017865,-1.44330311864552,25.835956334699));
#56699=CARTESIAN_POINT('Ctrl Pts',(30.1725168697432,-1.4925627888959,25.8210068109627));
#56700=CARTESIAN_POINT('Ctrl Pts',(30.0862466800351,-1.50000000000001,25.8166495453279));
#56701=CARTESIAN_POINT('Ctrl Pts',(30.,-1.50000000000001,25.8125));
#56702=CARTESIAN_POINT('Origin',(30.,-1.32966554433622E-14,16.));
#56703=CARTESIAN_POINT('',(30.0000000000001,-1.50000000000001,25.25));
#56704=CARTESIAN_POINT('',(30.,-1.50000000000001,25.3125));
#56705=CARTESIAN_POINT('',(30.,-1.50000000000001,16.));
#56706=CARTESIAN_POINT('Ctrl Pts',(30.0000000000001,-1.50000000000001,25.25));
#56707=CARTESIAN_POINT('Ctrl Pts',(30.0627700539087,-1.50000000000001,25.2530200256268));
#56708=CARTESIAN_POINT('Ctrl Pts',(30.1255978857231,-1.49606031931736,25.2561522666689));
#56709=CARTESIAN_POINT('Ctrl Pts',(30.387395972516,-1.46296629655124,25.2696673114027));
#56710=CARTESIAN_POINT('Ctrl Pts',(30.5795743359629,-1.39800636679879,25.2807179397182));
#56711=CARTESIAN_POINT('Ctrl Pts',(30.9202426421314,-1.20018691165606,25.3026033361058));
#56712=CARTESIAN_POINT('Ctrl Pts',(31.0669765445057,-1.07185443274338,25.3132278653563));
#56713=CARTESIAN_POINT('Ctrl Pts',(31.3042648643842,-0.765865616588927,
25.3331440943071));
#56714=CARTESIAN_POINT('Ctrl Pts',(31.3922917557281,-0.59091969078094,25.3421711282901));
#56715=CARTESIAN_POINT('Ctrl Pts',(31.4979914701149,-0.212996523390812,
25.3631668598117));
#56716=CARTESIAN_POINT('Ctrl Pts',(31.5129981369395,-0.0132639168507718,
25.3742631157306));
#56717=CARTESIAN_POINT('Ctrl Pts',(31.4653583210385,0.373052959697002,25.3957251644277));
#56718=CARTESIAN_POINT('Ctrl Pts',(31.4060337226141,0.556359728684241,25.4059088738159));
#56719=CARTESIAN_POINT('Ctrl Pts',(31.2180258231604,0.89772836856045,25.4248737982534));
#56720=CARTESIAN_POINT('Ctrl Pts',(31.088460968798,1.05109657163312,25.4351618575451));
#56721=CARTESIAN_POINT('Ctrl Pts',(30.7792551558925,1.29659274113508,25.4568578671965));
#56722=CARTESIAN_POINT('Ctrl Pts',(30.6034030192283,1.3871914976091,25.4678351891908));
#56723=CARTESIAN_POINT('Ctrl Pts',(30.2324892526205,1.49400946706811,25.4886479519256));
#56724=CARTESIAN_POINT('Ctrl Pts',(30.0415773273281,1.51141487828139,25.4976825299541));
#56725=CARTESIAN_POINT('Ctrl Pts',(29.6545526771042,1.47316919187237,25.5173656422979));
#56726=CARTESIAN_POINT('Ctrl Pts',(29.4624963512885,1.41443679130397,25.5282374121534));
#56727=CARTESIAN_POINT('Ctrl Pts',(29.1170567587378,1.22797823527613,25.5500367866331));
#56728=CARTESIAN_POINT('Ctrl Pts',(28.9660123174462,1.10381260264269,25.560752961054));
#56729=CARTESIAN_POINT('Ctrl Pts',(28.7201314342041,0.805655980053721,25.5808650389699));
#56730=CARTESIAN_POINT('Ctrl Pts',(28.627324212077,0.634750626561539,25.5897360763022));
#56731=CARTESIAN_POINT('Ctrl Pts',(28.5095600205757,0.261132939276874,25.6104926144847));
#56732=CARTESIAN_POINT('Ctrl Pts',(28.4881034640454,0.0613273497745445,
25.6215929250126));
#56733=CARTESIAN_POINT('Ctrl Pts',(28.5237184917358,-0.327500650137204,
25.6431944805633));
#56734=CARTESIAN_POINT('Ctrl Pts',(28.57753700972,-0.513112472024964,25.6535062484459));
#56735=CARTESIAN_POINT('Ctrl Pts',(28.7556436240904,-0.860981573894074,
25.6728323096608));
#56736=CARTESIAN_POINT('Ctrl Pts',(28.8809148866478,-1.0185241445112,25.6827836630609));
#56737=CARTESIAN_POINT('Ctrl Pts',(29.1836083572217,-1.27362286430434,25.7044330850039));
#56738=CARTESIAN_POINT('Ctrl Pts',(29.357290902101,-1.3695025366285,25.7154527145718));
#56739=CARTESIAN_POINT('Ctrl Pts',(29.6920067607584,-1.47617903100382,25.7345199747848));
#56740=CARTESIAN_POINT('Ctrl Pts',(29.8456406050883,-1.50000000000001,25.7425733801496));
#56741=CARTESIAN_POINT('Ctrl Pts',(30.0000000000002,-1.50000000000001,25.75));
#56742=CARTESIAN_POINT('Ctrl Pts',(30.,-1.50000000000001,25.8125));
#56743=CARTESIAN_POINT('Ctrl Pts',(29.8958136711151,-1.50000000000001,25.8074873329144));
#56744=CARTESIAN_POINT('Ctrl Pts',(29.7916909834384,-1.4891476478018,25.80217627354));
#56745=CARTESIAN_POINT('Ctrl Pts',(29.4989680289332,-1.42717135574301,25.7863710701566));
#56746=CARTESIAN_POINT('Ctrl Pts',(29.3182929815531,-1.3502283271827,25.7755410315376));
#56747=CARTESIAN_POINT('Ctrl Pts',(28.9928896773701,-1.12927046795383,25.7537473394536));
#56748=CARTESIAN_POINT('Ctrl Pts',(28.8522264483536,-0.985982788210688,
25.7429994633659));
#56749=CARTESIAN_POINT('Ctrl Pts',(28.639853465626,-0.660351661724937,25.7237363544014));
#56750=CARTESIAN_POINT('Ctrl Pts',(28.5672444995779,-0.483012345456745,
25.714334019192));
#56751=CARTESIAN_POINT('Ctrl Pts',(28.4907135279836,-0.103874220197911,
25.6932707900109));
#56752=CARTESIAN_POINT('Ctrl Pts',(28.4901189594842,0.0948392876888842,
25.6822311506839));
#56753=CARTESIAN_POINT('Ctrl Pts',(28.5659791907661,0.482606924381713,25.660688504201));
#56754=CARTESIAN_POINT('Ctrl Pts',(28.6422553573453,0.667705397375409,25.6509438140946));
#56755=CARTESIAN_POINT('Ctrl Pts',(28.8587620723286,0.992152292410515,25.6315147161622));
#56756=CARTESIAN_POINT('Ctrl Pts',(28.9948328944551,1.12978254443193,25.6211449431241));
#56757=CARTESIAN_POINT('Ctrl Pts',(29.3175819275344,1.35056278988812,25.599483888434));
#56758=CARTESIAN_POINT('Ctrl Pts',(29.5028611462505,1.42918794783786,25.5883856057019));
#56759=CARTESIAN_POINT('Ctrl Pts',(29.8863465577115,1.507984767606,25.5677463546914));
#56760=CARTESIAN_POINT('Ctrl Pts',(30.0802506039983,1.51013051078303,25.5589203440921));
#56761=CARTESIAN_POINT('Ctrl Pts',(30.4601704571654,1.44079280620514,25.5387153942847));
#56762=CARTESIAN_POINT('Ctrl Pts',(30.6424548754516,1.36926262641685,25.5279582816823));
#56763=CARTESIAN_POINT('Ctrl Pts',(30.9737363815272,1.15817666999724,25.5061559940003));
#56764=CARTESIAN_POINT('Ctrl Pts',(31.118540202541,1.01903114337744,25.4953239633962));
#56765=CARTESIAN_POINT('Ctrl Pts',(31.3403349350297,0.699693252907024,25.4757823623965));
#56766=CARTESIAN_POINT('Ctrl Pts',(31.418072458882,0.524551989157358,25.4666417771753));
#56767=CARTESIAN_POINT('Ctrl Pts',(31.5054879258866,0.148377517280613,25.4457431954044));
#56768=CARTESIAN_POINT('Ctrl Pts',(31.5119666548414,-0.0496365545101339,
25.4347424136382));
#56769=CARTESIAN_POINT('Ctrl Pts',(31.4476607795272,-0.440895614279282,
25.4130057992066));
#56770=CARTESIAN_POINT('Ctrl Pts',(31.3759395541655,-0.629971074835861,
25.4028673928089));
#56771=CARTESIAN_POINT('Ctrl Pts',(31.1673112734267,-0.961240411187918,
25.383627833962));
#56772=CARTESIAN_POINT('Ctrl Pts',(31.0353453440586,-1.10210544227651,25.3733657026948));
#56773=CARTESIAN_POINT('Ctrl Pts',(30.7196295943324,-1.33102399282861,25.3518169729773));
#56774=CARTESIAN_POINT('Ctrl Pts',(30.5371475111052,-1.41455738295539,25.3407169277066));
#56775=CARTESIAN_POINT('Ctrl Pts',(30.2307882933611,-1.48667060842925,25.3239740678184));
#56776=CARTESIAN_POINT('Ctrl Pts',(30.1154677152456,-1.50000000000002,25.31805544304));
#56777=CARTESIAN_POINT('Ctrl Pts',(29.9999999999999,-1.50000000000001,25.3125));
#56778=CARTESIAN_POINT('Origin',(30.,-1.32966554433622E-14,16.));
#56779=CARTESIAN_POINT('',(30.,-1.50000000000001,24.75));
#56780=CARTESIAN_POINT('',(29.9999999999999,-1.50000000000001,24.8125));
#56781=CARTESIAN_POINT('',(30.,-1.50000000000001,16.));
#56782=CARTESIAN_POINT('Ctrl Pts',(30.,-1.50000000000001,24.75));
#56783=CARTESIAN_POINT('Ctrl Pts',(30.0924202028298,-1.50000000000002,24.7544465690819));
#56784=CARTESIAN_POINT('Ctrl Pts',(30.1848415762481,-1.49146009950343,24.759130413942));
#56785=CARTESIAN_POINT('Ctrl Pts',(30.4723479931102,-1.43762037173554,24.7744586208663));
#56786=CARTESIAN_POINT('Ctrl Pts',(30.6592834359903,-1.36205645668747,24.7855515541955));
#56787=CARTESIAN_POINT('Ctrl Pts',(30.9862537983022,-1.14638219357722,24.80727387484));
#56788=CARTESIAN_POINT('Ctrl Pts',(31.1248087259681,-1.01079850350159,24.8177063155187));
#56789=CARTESIAN_POINT('Ctrl Pts',(31.346109752526,-0.69055016576277,24.8372494532827));
#56790=CARTESIAN_POINT('Ctrl Pts',(31.4251274703691,-0.50783917665878,24.8467867124079));
#56791=CARTESIAN_POINT('Ctrl Pts',(31.5079543915197,-0.122264618516638,
24.8682075211936));
#56792=CARTESIAN_POINT('Ctrl Pts',(31.5109523526148,0.0767903025210503,
24.8792661279179));
#56793=CARTESIAN_POINT('Ctrl Pts',(31.441061251381,0.457686740875712,24.9004270411598));
#56794=CARTESIAN_POINT('Ctrl Pts',(31.3715371249325,0.636385044039808,24.9100225849775));
#56795=CARTESIAN_POINT('Ctrl Pts',(31.1648481820269,0.965747220324715,24.9291158607209));
#56796=CARTESIAN_POINT('Ctrl Pts',(31.0267283705006,1.11145999209774,24.939808730245));
#56797=CARTESIAN_POINT('Ctrl Pts',(30.7049953637051,1.33826413832451,24.9615882319247));
#56798=CARTESIAN_POINT('Ctrl Pts',(30.525362209954,1.41844022126688,24.9724579494792));
#56799=CARTESIAN_POINT('Ctrl Pts',(30.1493787440764,1.50469862427576,24.9929435291658));
#56800=CARTESIAN_POINT('Ctrl Pts',(29.9569371691124,1.5114809139774,25.00175294714));
#56801=CARTESIAN_POINT('Ctrl Pts',(29.5704977811955,1.45108059660786,25.0220233074535));
#56802=CARTESIAN_POINT('Ctrl Pts',(29.3808354910635,1.38084291684638,25.0330994853021));
#56803=CARTESIAN_POINT('Ctrl Pts',(29.0468101101847,1.17410520091496,25.0549130032641));
#56804=CARTESIAN_POINT('Ctrl Pts',(28.9040664949486,1.04213311105638,25.0654466500392));
#56805=CARTESIAN_POINT('Ctrl Pts',(28.6746221434491,0.72909790198446,25.0851812190219));
#56806=CARTESIAN_POINT('Ctrl Pts',(28.5909928953227,0.55038117737188,25.0944232679238));
#56807=CARTESIAN_POINT('Ctrl Pts',(28.496446216206,0.168641933616187,25.115631003688));
#56808=CARTESIAN_POINT('Ctrl Pts',(28.4873339658181,-0.0308466586561953,
25.1267137032587));
#56809=CARTESIAN_POINT('Ctrl Pts',(28.5459190178277,-0.414647584032544,
25.1480359768907));
#56810=CARTESIAN_POINT('Ctrl Pts',(28.6102581790788,-0.595692019972521,
25.1580163493537));
#56811=CARTESIAN_POINT('Ctrl Pts',(28.8073809961852,-0.931227827424643,
25.1768208644096));
#56812=CARTESIAN_POINT('Ctrl Pts',(28.9411488677475,-1.08089452062442,25.1874141822753));
#56813=CARTESIAN_POINT('Ctrl Pts',(29.2565034825196,-1.31734526046784,25.2091547643595));
#56814=CARTESIAN_POINT('Ctrl Pts',(29.4342658933141,-1.40290303357365,25.220083967145));
#56815=CARTESIAN_POINT('Ctrl Pts',(29.7466738861071,-1.48392560477994,25.2373653306843));
#56816=CARTESIAN_POINT('Ctrl Pts',(29.8731973879732,-1.50000000000001,25.2438992064844));
#56817=CARTESIAN_POINT('Ctrl Pts',(30.0000000000001,-1.50000000000001,25.25));
#56818=CARTESIAN_POINT('Ctrl Pts',(29.9999999999999,-1.50000000000001,25.3125));
#56819=CARTESIAN_POINT('Ctrl Pts',(29.9230963675565,-1.50000000000001,25.3087999722589));
#56820=CARTESIAN_POINT('Ctrl Pts',(29.8461434428577,-1.49408668250554,25.3049333141238));
#56821=CARTESIAN_POINT('Ctrl Pts',(29.5785997947569,-1.4525378268213,25.2909069794727));
#56822=CARTESIAN_POINT('Ctrl Pts',(29.394946779968,-1.38612426885289,25.2802261486243));
#56823=CARTESIAN_POINT('Ctrl Pts',(29.0584111434883,-1.1844646483524,25.2584329141398));
#56824=CARTESIAN_POINT('Ctrl Pts',(28.9098271705268,-1.04932739740415,25.2475303518813));
#56825=CARTESIAN_POINT('Ctrl Pts',(28.679224033866,-0.736002543967933,25.2277319851447));
#56826=CARTESIAN_POINT('Ctrl Pts',(28.5966653608253,-0.562858820299269,
25.218769934461));
#56827=CARTESIAN_POINT('Ctrl Pts',(28.4992036771274,-0.189506940379824,
25.1980281633544));
#56828=CARTESIAN_POINT('Ctrl Pts',(28.4873077258157,0.00770736323463039,
25.1870718131536));
#56829=CARTESIAN_POINT('Ctrl Pts',(28.5403428741226,0.398677937032776,25.1653512257204));
#56830=CARTESIAN_POINT('Ctrl Pts',(28.6059812891417,0.588385613614782,25.1548923783415));
#56831=CARTESIAN_POINT('Ctrl Pts',(28.8032229731553,0.924175534219124,25.1360750856002));
#56832=CARTESIAN_POINT('Ctrl Pts',(28.9302878616598,1.06867554049118,25.1259477842385));
#56833=CARTESIAN_POINT('Ctrl Pts',(29.2375170160562,1.30684882772379,25.1045502900104));
#56834=CARTESIAN_POINT('Ctrl Pts',(29.416566346389,1.39601031268743,25.0934590671725));
#56835=CARTESIAN_POINT('Ctrl Pts',(29.7956879290814,1.49872079338579,25.0723655026123));
#56836=CARTESIAN_POINT('Ctrl Pts',(29.9916913791595,1.51255777708596,25.0632485758478));
#56837=CARTESIAN_POINT('Ctrl Pts',(30.376338186137,1.46478286918679,25.0434151669436));
#56838=CARTESIAN_POINT('Ctrl Pts',(30.5613937867408,1.40429329778983,25.0328314093361));
#56839=CARTESIAN_POINT('Ctrl Pts',(30.9051019650582,1.2128519030953,25.0109769253773));
#56840=CARTESIAN_POINT('Ctrl Pts',(31.0589867932662,1.08110262857348,24.9999134360581));
#56841=CARTESIAN_POINT('Ctrl Pts',(31.2996601001576,0.7727813254929,24.9797695555402));
#56842=CARTESIAN_POINT('Ctrl Pts',(31.3872075591177,0.601637196257516,24.9709242886809));
#56843=CARTESIAN_POINT('Ctrl Pts',(31.4948659823167,0.231233394936456,24.9503462997187));
#56844=CARTESIAN_POINT('Ctrl Pts',(31.5122374051454,0.0349818838105959,
24.9394434379894));
#56845=CARTESIAN_POINT('Ctrl Pts',(31.4704629549247,-0.356714017311379,
24.9176825545938));
#56846=CARTESIAN_POINT('Ctrl Pts',(31.410306361987,-0.548240683911054,24.9070421842271));
#56847=CARTESIAN_POINT('Ctrl Pts',(31.2229499202263,-0.889130700933294,
24.8881038499482));
#56848=CARTESIAN_POINT('Ctrl Pts',(31.1004741653132,-1.03689935475768,24.8783104947773));
#56849=CARTESIAN_POINT('Ctrl Pts',(30.8011609016804,-1.28341012707365,24.8570622572132));
#56850=CARTESIAN_POINT('Ctrl Pts',(30.6254139659021,-1.37762857486559,24.8459894497178));
#56851=CARTESIAN_POINT('Ctrl Pts',(30.2947063232275,-1.4782094919839,24.8272843564766));
#56852=CARTESIAN_POINT('Ctrl Pts',(30.1476360382517,-1.50000000000004,24.8196031422022));
#56853=CARTESIAN_POINT('Ctrl Pts',(29.9999999999998,-1.50000000000001,24.8125));
#56854=CARTESIAN_POINT('Origin',(30.,-1.32966554433622E-14,16.));
#56855=CARTESIAN_POINT('',(30.,-1.50000000000001,24.25));
#56856=CARTESIAN_POINT('',(30.,-1.50000000000001,24.3125));
#56857=CARTESIAN_POINT('',(30.,-1.50000000000001,16.));
#56858=CARTESIAN_POINT('Ctrl Pts',(29.9999999999999,-1.50000000000001,24.25));
#56859=CARTESIAN_POINT('Ctrl Pts',(30.1233865336442,-1.50000000000002,24.2559364373678));
#56860=CARTESIAN_POINT('Ctrl Pts',(30.2465476489323,-1.48477988594364,24.2622848102359));
#56861=CARTESIAN_POINT('Ctrl Pts',(30.5591244259704,-1.40597165010196,24.2795127850953));
#56862=CARTESIAN_POINT('Ctrl Pts',(30.7400033595231,-1.31975922707827,24.2906101163719));
#56863=CARTESIAN_POINT('Ctrl Pts',(31.0517371878966,-1.08642473531537,24.3120899308425));
#56864=CARTESIAN_POINT('Ctrl Pts',(31.181396759577,-0.943819238764671,24.3222894436867));
#56865=CARTESIAN_POINT('Ctrl Pts',(31.3842738432636,-0.610977913754327,
24.341295964288));
#56866=CARTESIAN_POINT('Ctrl Pts',(31.4529950991553,-0.422325812949031,
24.3515374548362));
#56867=CARTESIAN_POINT('Ctrl Pts',(31.5124147536636,-0.0319347678693356,
24.3732258462295));
#56868=CARTESIAN_POINT('Ctrl Pts',(31.5036442008573,0.165759327603677,24.3842088515336));
#56869=CARTESIAN_POINT('Ctrl Pts',(31.4119825510711,0.540750850840327,24.4050417139356));
#56870=CARTESIAN_POINT('Ctrl Pts',(31.3322181025457,0.715044299742208,24.4140993016492));
#56871=CARTESIAN_POINT('Ctrl Pts',(31.106713322535,1.03186525150623,24.4337494874295));
#56872=CARTESIAN_POINT('Ctrl Pts',(30.9603062459911,1.1693383575936,24.4446121985753));
#56873=CARTESIAN_POINT('Ctrl Pts',(30.6267827077052,1.37647673516795,24.4664127011144));
#56874=CARTESIAN_POINT('Ctrl Pts',(30.4439056234701,1.4458581458551,24.47713864034));
#56875=CARTESIAN_POINT('Ctrl Pts',(30.0630400763872,1.51099956140736,24.4972725262831));
#56876=CARTESIAN_POINT('Ctrl Pts',(29.8687484810349,1.50660828894347,24.5061312780688));
#56877=CARTESIAN_POINT('Ctrl Pts',(29.4860566158504,1.4231980920111,24.526860498932));
#56878=CARTESIAN_POINT('Ctrl Pts',(29.3019333862064,1.34250650777999,24.5379605648438));
#56879=CARTESIAN_POINT('Ctrl Pts',(28.9821049580114,1.11829253966791,24.5595764830508));
#56880=CARTESIAN_POINT('Ctrl Pts',(28.8477437066725,0.979293286040407,24.5699020321484));
#56881=CARTESIAN_POINT('Ctrl Pts',(28.6345240475922,0.651988290747904,24.5892523732038));
#56882=CARTESIAN_POINT('Ctrl Pts',(28.5601403785395,0.465238374198666,24.5991534236556));
#56883=CARTESIAN_POINT('Ctrl Pts',(28.489084947481,0.0759965520384366,24.6207779693312));
#56884=CARTESIAN_POINT('Ctrl Pts',(28.4921379080883,-0.122445995567395,
24.6318025553093));
#56885=CARTESIAN_POINT('Ctrl Pts',(28.5732141775453,-0.500358663169468,
24.6527977035094));
#56886=CARTESIAN_POINT('Ctrl Pts',(28.6479534934179,-0.676775662247645,
24.662082289407));
#56887=CARTESIAN_POINT('Ctrl Pts',(28.8642453292122,-0.999806026462223,
24.6814617008812));
#56888=CARTESIAN_POINT('Ctrl Pts',(29.0066425215227,-1.1413892524153,24.6922456563782));
#56889=CARTESIAN_POINT('Ctrl Pts',(29.3345224631394,-1.35826808429126,24.7140451994209));
#56890=CARTESIAN_POINT('Ctrl Pts',(29.515884916708,-1.43296761407463,24.7248459914751));
#56891=CARTESIAN_POINT('Ctrl Pts',(29.8033393621129,-1.4903304156034,24.7402695610815));
#56892=CARTESIAN_POINT('Ctrl Pts',(29.901655948172,-1.50000000000001,24.7452684196003));
#56893=CARTESIAN_POINT('Ctrl Pts',(30.,-1.50000000000001,24.75));
#56894=CARTESIAN_POINT('Ctrl Pts',(29.9999999999998,-1.50000000000001,24.8125));
#56895=CARTESIAN_POINT('Ctrl Pts',(29.9520844763832,-1.50000000000001,24.8101946632951));
#56896=CARTESIAN_POINT('Ctrl Pts',(29.9041155058213,-1.49770423456202,24.8078229838607));
#56897=CARTESIAN_POINT('Ctrl Pts',(29.6647429412583,-1.47465918202179,24.7956660256301));
#56898=CARTESIAN_POINT('Ctrl Pts',(29.4785801635781,-1.4195491435244,24.7851784304102));
#56899=CARTESIAN_POINT('Ctrl Pts',(29.1305308217309,-1.23854895841351,24.7634051157232));
#56900=CARTESIAN_POINT('Ctrl Pts',(28.9733425780824,-1.11174127780071,24.752319957252));
#56901=CARTESIAN_POINT('Ctrl Pts',(28.7235507953419,-0.81069913235786,24.7319395626836));
#56902=CARTESIAN_POINT('Ctrl Pts',(28.6307275649839,-0.641599855569549,
24.7231444364205));
#56903=CARTESIAN_POINT('Ctrl Pts',(28.5125127288929,-0.274334472746556,
24.7027408040415));
#56904=CARTESIAN_POINT('Ctrl Pts',(28.4895069858667,-0.0792389156648355,
24.6919021619814));
#56905=CARTESIAN_POINT('Ctrl Pts',(28.5196116095794,0.313003938746328,24.6701108922919));
#56906=CARTESIAN_POINT('Ctrl Pts',(28.5740816740222,0.506262436197778,24.6593743091001));
#56907=CARTESIAN_POINT('Ctrl Pts',(28.7511791399573,0.852358280491469,24.640146762195));
#56908=CARTESIAN_POINT('Ctrl Pts',(28.8690245914396,1.00348928998653,24.630706043882));
#56909=CARTESIAN_POINT('Ctrl Pts',(29.1601188576535,1.25831795738381,24.6096221903744));
#56910=CARTESIAN_POINT('Ctrl Pts',(29.3323550489326,1.35757677634782,24.5985782833421));
#56911=CARTESIAN_POINT('Ctrl Pts',(29.7064392762191,1.4842685830248,24.577060930713));
#56912=CARTESIAN_POINT('Ctrl Pts',(29.9047304118308,1.51001063736079,24.5673617334579));
#56913=CARTESIAN_POINT('Ctrl Pts',(30.2937060245362,1.48342562743484,24.547908663068));
#56914=CARTESIAN_POINT('Ctrl Pts',(30.4808263548115,1.43373651283452,24.5375255787967));
#56915=CARTESIAN_POINT('Ctrl Pts',(30.8329282215013,1.26331849859809,24.5158512361083));
#56916=CARTESIAN_POINT('Ctrl Pts',(30.9932828024692,1.14155315563778,24.5047538020966));
#56917=CARTESIAN_POINT('Ctrl Pts',(31.2521599269974,0.847929325410954,24.4841423531291));
#56918=CARTESIAN_POINT('Ctrl Pts',(31.3503160471837,0.680833771104865,24.4753240983947));
#56919=CARTESIAN_POINT('Ctrl Pts',(31.4789636487266,0.316753550496772,24.455097419472));
#56920=CARTESIAN_POINT('Ctrl Pts',(31.5074931621648,0.122957581810777,24.4443309767673));
#56921=CARTESIAN_POINT('Ctrl Pts',(31.4889302469637,-0.269482846800126,
24.4225287307333));
#56922=CARTESIAN_POINT('Ctrl Pts',(31.4401374224707,-0.464284058469581,
24.4117064411961));
#56923=CARTESIAN_POINT('Ctrl Pts',(31.2732400969951,-0.815428064678723,
24.3921984408512));
#56924=CARTESIAN_POINT('Ctrl Pts',(31.1598920572171,-0.96991270557316,24.3830299796895));
#56925=CARTESIAN_POINT('Ctrl Pts',(30.8768520990815,-1.23274788918355,24.3621112360319));
#56926=CARTESIAN_POINT('Ctrl Pts',(30.7081704356177,-1.33679806788068,24.351105252973));
#56927=CARTESIAN_POINT('Ctrl Pts',(30.3563528915165,-1.46803396077468,24.330532982021));
#56928=CARTESIAN_POINT('Ctrl Pts',(30.1788031709794,-1.50000000000002,24.3211026715747));
#56929=CARTESIAN_POINT('Ctrl Pts',(29.9999999999999,-1.50000000000001,24.3125));
#56930=CARTESIAN_POINT('Origin',(30.,-1.32966554433622E-14,16.));
#56931=CARTESIAN_POINT('',(29.9999999999999,-1.50000000000001,23.75));
#56932=CARTESIAN_POINT('',(30.,-1.50000000000001,23.8125));
#56933=CARTESIAN_POINT('',(30.,-1.50000000000001,16.));
#56934=CARTESIAN_POINT('Ctrl Pts',(29.9999999999998,-1.50000000000001,23.75));
#56935=CARTESIAN_POINT('Ctrl Pts',(30.1539214445734,-1.50000000000004,23.7574055489549));
#56936=CARTESIAN_POINT('Ctrl Pts',(30.3071622224275,-1.47631426128188,23.7654362865035));
#56937=CARTESIAN_POINT('Ctrl Pts',(30.6423330661034,-1.36978679250727,23.7845212975935));
#56938=CARTESIAN_POINT('Ctrl Pts',(30.8166966283757,-1.27354330571266,23.7955837985834));
#56939=CARTESIAN_POINT('Ctrl Pts',(31.1127372375018,-1.02370190976136,23.8167670978074));
#56940=CARTESIAN_POINT('Ctrl Pts',(31.2333636655921,-0.874601042154043,
23.8264110532137));
#56941=CARTESIAN_POINT('Ctrl Pts',(31.4166526755054,-0.531631844802988,
23.8454648975109));
#56942=CARTESIAN_POINT('Ctrl Pts',(31.4745582697856,-0.339396978512901,
23.8561446123048));
#56943=CARTESIAN_POINT('Ctrl Pts',(31.511699941184,0.0525578729813968,23.8779198818323));
#56944=CARTESIAN_POINT('Ctrl Pts',(31.4920858025539,0.248369535334408,23.8887983075186));
#56945=CARTESIAN_POINT('Ctrl Pts',(31.3802343334373,0.617537171179423,23.909307620621));
#56946=CARTESIAN_POINT('Ctrl Pts',(31.2906053859832,0.78786629286171,23.9181242275504));
#56947=CARTESIAN_POINT('Ctrl Pts',(31.0463195284336,1.0933231170364,23.9383623481344));
#56948=CARTESIAN_POINT('Ctrl Pts',(30.8911113639651,1.22312916938911,23.9494355281055));
#56949=CARTESIAN_POINT('Ctrl Pts',(30.5456512461468,1.41045613992281,23.9712600127329));
#56950=CARTESIAN_POINT('Ctrl Pts',(30.3601397930707,1.4688221637187,23.9818067151192));
#56951=CARTESIAN_POINT('Ctrl Pts',(29.9746198000426,1.51244309002935,24.0015667468295));
#56952=CARTESIAN_POINT('Ctrl Pts',(29.7781833324316,1.4963071428617,24.0107747387592));
#56953=CARTESIAN_POINT('Ctrl Pts',(29.3999877237922,1.38893180194388,24.0319533318226));
#56954=CARTESIAN_POINT('Ctrl Pts',(29.222220687541,1.29776778429998,24.0430384861654));
#56955=CARTESIAN_POINT('Ctrl Pts',(28.9180417312452,1.05625627096343,24.0643819561719));
#56956=CARTESIAN_POINT('Ctrl Pts',(28.7928010889864,0.910453809129913,24.0744192328261));
#56957=CARTESIAN_POINT('Ctrl Pts',(28.5994385143727,0.572669994103534,24.0931850003275));
#56958=CARTESIAN_POINT('Ctrl Pts',(28.5359684061524,0.382240685005912,24.1037644063885));
#56959=CARTESIAN_POINT('Ctrl Pts',(28.4873420883061,-0.00897112678811804,
24.1254983959326));
#56960=CARTESIAN_POINT('Ctrl Pts',(28.5013820601517,-0.205827079960202,
24.1364348377755));
#56961=CARTESIAN_POINT('Ctrl Pts',(28.6028303892674,-0.578036208077185,
24.1571131226709));
#56962=CARTESIAN_POINT('Ctrl Pts',(28.6873275910153,-0.750394994115161,
24.1660216580016));
#56963=CARTESIAN_POINT('Ctrl Pts',(28.922674074919,-1.0628953635868,24.1860253368065));
#56964=CARTESIAN_POINT('Ctrl Pts',(29.0745736829203,-1.19747470970914,24.197071925274));
#56965=CARTESIAN_POINT('Ctrl Pts',(29.4156235588556,-1.39492862582615,24.2189655260838));
#56966=CARTESIAN_POINT('Ctrl Pts',(29.5999664963488,-1.45853020454807,24.2296014403193));
#56967=CARTESIAN_POINT('Ctrl Pts',(29.8606029709014,-1.49514680076604,24.2431584462207));
#56968=CARTESIAN_POINT('Ctrl Pts',(29.9303308703141,-1.50000000000001,24.2466480424351));
#56969=CARTESIAN_POINT('Ctrl Pts',(29.9999999999999,-1.50000000000001,24.25));
#56970=CARTESIAN_POINT('Ctrl Pts',(29.9999999999999,-1.50000000000001,24.3125));
#56971=CARTESIAN_POINT('Ctrl Pts',(29.9792133017942,-1.50000000000001,24.3114998995163));
#56972=CARTESIAN_POINT('Ctrl Pts',(29.9584107993835,-1.49956791710601,24.3104870363498));
#56973=CARTESIAN_POINT('Ctrl Pts',(29.7464034347025,-1.4907415866322,24.3000416514142));
#56974=CARTESIAN_POINT('Ctrl Pts',(29.5585103106211,-1.44626636462019,24.2897662164333));
#56975=CARTESIAN_POINT('Ctrl Pts',(29.2028124426411,-1.28608329400307,24.2682031650416));
#56976=CARTESIAN_POINT('Ctrl Pts',(29.0395645726164,-1.16922656097766,24.2571028778712));
#56977=CARTESIAN_POINT('Ctrl Pts',(28.7720346147835,-0.882829614311603,
24.2362758660328));
#56978=CARTESIAN_POINT('Ctrl Pts',(28.6687223598358,-0.717623891574991,
24.2273679939764));
#56979=CARTESIAN_POINT('Ctrl Pts',(28.5302095932634,-0.356628416668571,
24.2073126898149));
#56980=CARTESIAN_POINT('Ctrl Pts',(28.4965070465723,-0.164202501526158,
24.1966223611959));
#56981=CARTESIAN_POINT('Ctrl Pts',(28.504169008249,0.22811087427228,24.1748271736516));
#56982=CARTESIAN_POINT('Ctrl Pts',(28.547551398078,0.424213342298486,24.1639325920946));
#56983=CARTESIAN_POINT('Ctrl Pts',(28.7047478969298,0.780036844220854,24.1441646197656));
#56984=CARTESIAN_POINT('Ctrl Pts',(28.8139070776359,0.937725434330763,24.1351846602695));
#56985=CARTESIAN_POINT('Ctrl Pts',(29.089396967151,1.20794416549895,24.1144240709145));
#56986=CARTESIAN_POINT('Ctrl Pts',(29.2546507832928,1.31634974323744,24.10346202693));
#56987=CARTESIAN_POINT('Ctrl Pts',(29.6203184116569,1.46471395475137,24.0817476068599));
#56988=CARTESIAN_POINT('Ctrl Pts',(29.817562104219,1.50206749812624,24.0713349778568));
#56989=CARTESIAN_POINT('Ctrl Pts',(30.2070481745296,1.49784204922514,24.0524784469813));
#56990=CARTESIAN_POINT('Ctrl Pts',(30.3956551706626,1.45939464529562,24.0423361052064));
#56991=CARTESIAN_POINT('Ctrl Pts',(30.7551447714595,1.31111335433136,24.0209212289748));
#56992=CARTESIAN_POINT('Ctrl Pts',(30.9215534250012,1.20000288285394,24.0098284869129));
#56993=CARTESIAN_POINT('Ctrl Pts',(31.1989915137811,0.922095691461922,23.9887605964375));
#56994=CARTESIAN_POINT('Ctrl Pts',(31.3083178283937,0.759038041694919,23.9796687800942));
#56995=CARTESIAN_POINT('Ctrl Pts',(31.4580557742773,0.401642541393168,23.9598134745218));
#56996=CARTESIAN_POINT('Ctrl Pts',(31.4975752946798,0.210938880716583,23.9492188267065));
#56997=CARTESIAN_POINT('Ctrl Pts',(31.5023006219625,-0.182594498957542,
23.927355861169));
#56998=CARTESIAN_POINT('Ctrl Pts',(31.4644403140633,-0.381679718202,23.916295571211));
#56999=CARTESIAN_POINT('Ctrl Pts',(31.3164762945118,-0.74375638752885,23.8961802006929));
#57000=CARTESIAN_POINT('Ctrl Pts',(31.2115088567194,-0.904729197971778,
23.8873240471024));
#57001=CARTESIAN_POINT('Ctrl Pts',(30.9436055459159,-1.18225533242814,23.8667254837612));
#57002=CARTESIAN_POINT('Ctrl Pts',(30.7818828902994,-1.29490194314203,23.8558155263452));
#57003=CARTESIAN_POINT('Ctrl Pts',(30.4211554702292,-1.45331769745592,23.8340595826352));
#57004=CARTESIAN_POINT('Ctrl Pts',(30.225061216149,-1.49628795964726,23.8234313750427));
#57005=CARTESIAN_POINT('Ctrl Pts',(30.01751075903,-1.49992336974507,23.8133446154048));
#57006=CARTESIAN_POINT('Ctrl Pts',(30.0087538759465,-1.50000000000001,23.8129211710528));
#57007=CARTESIAN_POINT('Ctrl Pts',(30.,-1.50000000000001,23.8125));
#57008=CARTESIAN_POINT('Origin',(30.,-1.32966554433622E-14,16.));
#57009=CARTESIAN_POINT('',(30.,-1.50000000000001,23.25));
#57010=CARTESIAN_POINT('',(30.0000000000001,-1.50000000000001,23.3125));
#57011=CARTESIAN_POINT('',(30.,-1.50000000000001,16.));
#57012=CARTESIAN_POINT('Ctrl Pts',(30.,-1.50000000000001,23.25));
#57013=CARTESIAN_POINT('Ctrl Pts',(30.1848807806478,-1.50000000000001,23.2588950807062));
#57014=CARTESIAN_POINT('Ctrl Pts',(30.3682821495602,-1.46581977714696,23.268668433817));
#57015=CARTESIAN_POINT('Ctrl Pts',(30.7253175152828,-1.32777981441322,23.2896807492688));
#57016=CARTESIAN_POINT('Ctrl Pts',(30.8938177244611,-1.22072861570022,23.3007613637715));
#57017=CARTESIAN_POINT('Ctrl Pts',(31.17812266521,-0.948849031570725,23.3219922022812));
#57018=CARTESIAN_POINT('Ctrl Pts',(31.2916923057403,-0.787278580688064,
23.3312623010729));
#57019=CARTESIAN_POINT('Ctrl Pts',(31.4491725851422,-0.432421790169133,
23.3509765672128));
#57020=CARTESIAN_POINT('Ctrl Pts',(31.4926555401856,-0.243004803835009,
23.3614997331203));
#57021=CARTESIAN_POINT('Ctrl Pts',(31.5058959055076,0.149477495401521,23.3833043053001));
#57022=CARTESIAN_POINT('Ctrl Pts',(31.4725342594551,0.348889338242185,23.3943827410135));
#57023=CARTESIAN_POINT('Ctrl Pts',(31.3327988700423,0.714215497781599,23.4146786387656));
#57024=CARTESIAN_POINT('Ctrl Pts',(31.2311812032015,0.877867947558743,23.4234833208414));
#57025=CARTESIAN_POINT('Ctrl Pts',(30.9693523131294,1.16116792111582,23.4439500128983));
#57026=CARTESIAN_POINT('Ctrl Pts',(30.8105149834806,1.27711053175663,23.4548127055575));
#57027=CARTESIAN_POINT('Ctrl Pts',(30.4538126686857,1.44345770015622,23.4765953083576));
#57028=CARTESIAN_POINT('Ctrl Pts',(30.2587086794859,1.49084210066152,23.487298486762));
#57029=CARTESIAN_POINT('Ctrl Pts',(29.8701963712835,1.50640033026212,23.5064229669502));
#57030=CARTESIAN_POINT('Ctrl Pts',(29.6806119299331,1.47787523708767,23.5159811423084));
#57031=CARTESIAN_POINT('Ctrl Pts',(29.3158918902727,1.34932104216597,23.5370996932649));
#57032=CARTESIAN_POINT('Ctrl Pts',(29.1450773397405,1.24811033609704,23.5481294207781));
#57033=CARTESIAN_POINT('Ctrl Pts',(28.8572342555358,0.990033097118328,23.5691470898178));
#57034=CARTESIAN_POINT('Ctrl Pts',(28.741208429162,0.837555866674711,23.578469118518));
#57035=CARTESIAN_POINT('Ctrl Pts',(28.5682103547001,0.489415671302002,23.5978102404832));
#57036=CARTESIAN_POINT('Ctrl Pts',(28.5160198061383,0.295515658346084,23.6085824634252));
#57037=CARTESIAN_POINT('Ctrl Pts',(28.4905622848027,-0.0968477988030621,
23.6303804332668));
#57038=CARTESIAN_POINT('Ctrl Pts',(28.5157978904665,-0.291438773395986,
23.6411910429664));
#57039=CARTESIAN_POINT('Ctrl Pts',(28.6382130227664,-0.657431308298791,
23.6615239615721));
#57040=CARTESIAN_POINT('Ctrl Pts',(28.733169022031,-0.825722839750627,23.6703196450362));
#57041=CARTESIAN_POINT('Ctrl Pts',(28.9866100524997,-1.12380536152502,23.6907934023492));
#57042=CARTESIAN_POINT('Ctrl Pts',(29.1450855427347,-1.24860164286396,23.7018846212987));
#57043=CARTESIAN_POINT('Ctrl Pts',(29.4947960835532,-1.42537206508902,23.723620367045));
#57044=CARTESIAN_POINT('Ctrl Pts',(29.6813612118254,-1.47831159941945,23.7340670285844));
#57045=CARTESIAN_POINT('Ctrl Pts',(29.9152096611065,-1.49820471212254,23.7458706538102));
#57046=CARTESIAN_POINT('Ctrl Pts',(29.957628226374,-1.50000000000001,23.7479613870909));
#57047=CARTESIAN_POINT('Ctrl Pts',(29.9999999999998,-1.50000000000001,23.75));
#57048=CARTESIAN_POINT('Ctrl Pts',(30.,-1.50000000000001,23.8125));
#57049=CARTESIAN_POINT('Ctrl Pts',(29.8186899108673,-1.50000000000001,23.8037767142694));
#57050=CARTESIAN_POINT('Ctrl Pts',(29.6387564217711,-1.46712852254306,23.7942065636429));
#57051=CARTESIAN_POINT('Ctrl Pts',(29.284195027604,-1.33291119731626,23.7734194615783));
#57052=CARTESIAN_POINT('Ctrl Pts',(29.1150531352934,-1.22715164870581,23.762343853251));
#57053=CARTESIAN_POINT('Ctrl Pts',(28.8285848658366,-0.957196675383623,
23.7410623929517));
#57054=CARTESIAN_POINT('Ctrl Pts',(28.713664846415,-0.796095622176884,23.7317275345654));
#57055=CARTESIAN_POINT('Ctrl Pts',(28.5537507892143,-0.442046290271719,
23.7120581272374));
#57056=CARTESIAN_POINT('Ctrl Pts',(28.50903084701,-0.253050072432249,23.7015583373574));
#57057=CARTESIAN_POINT('Ctrl Pts',(28.493125704307,0.139065210502765,23.6797741549721));
#57058=CARTESIAN_POINT('Ctrl Pts',(28.5250759127101,0.338559440554235,23.6686911421915));
#57059=CARTESIAN_POINT('Ctrl Pts',(28.6622225705316,0.704891738980156,23.6483393478345));
#57060=CARTESIAN_POINT('Ctrl Pts',(28.7627930544851,0.869391639366899,23.6395420458263));
#57061=CARTESIAN_POINT('Ctrl Pts',(29.0227223626785,1.15448356589741,23.6191169709735));
#57062=CARTESIAN_POINT('Ctrl Pts',(29.1806474642266,1.27143845898823,23.6082700489523));
#57063=CARTESIAN_POINT('Ctrl Pts',(29.5360600403599,1.4402358268239,23.5864814376371));
#57064=CARTESIAN_POINT('Ctrl Pts',(29.7308346201,1.48899068833401,23.5757560395914));
#57065=CARTESIAN_POINT('Ctrl Pts',(30.1191927262396,1.50727161649964,23.5565633479378));
#57066=CARTESIAN_POINT('Ctrl Pts',(30.3089226794933,1.48009155403507,23.5470839383266));
#57067=CARTESIAN_POINT('Ctrl Pts',(30.6746275130695,1.35410584970156,23.5259893534154));
#57068=CARTESIAN_POINT('Ctrl Pts',(30.8462644331352,1.25401826984556,23.5149512576394));
#57069=CARTESIAN_POINT('Ctrl Pts',(31.1359831388577,0.997812339501797,23.4938953285128));
#57070=CARTESIAN_POINT('Ctrl Pts',(31.2530579642409,0.846112941875841,23.4845062745487));
#57071=CARTESIAN_POINT('Ctrl Pts',(31.4284239202414,0.499151075957345,23.465230615331));
#57072=CARTESIAN_POINT('Ctrl Pts',(31.4819315716114,0.305618089705,23.4544787827614));
#57073=CARTESIAN_POINT('Ctrl Pts',(31.5100720569101,-0.086682490418841,
23.4326843060879));
#57074=CARTESIAN_POINT('Ctrl Pts',(31.4861228872238,-0.281567854400411,
23.4218573414222));
#57075=CARTESIAN_POINT('Ctrl Pts',(31.3661326726942,-0.648296896097567,
23.4014835057724));
#57076=CARTESIAN_POINT('Ctrl Pts',(31.2724103712455,-0.817054396960877,
23.3926895837254));
#57077=CARTESIAN_POINT('Ctrl Pts',(31.0210775409326,-1.11685004948265,23.3722696702745));
#57078=CARTESIAN_POINT('Ctrl Pts',(30.8633432283804,-1.24281066274781,23.3611817686994));
#57079=CARTESIAN_POINT('Ctrl Pts',(30.5145869816219,-1.42202815813894,23.3394239621929));
#57080=CARTESIAN_POINT('Ctrl Pts',(30.3282514191413,-1.47622279958149,23.3289534815563));
#57081=CARTESIAN_POINT('Ctrl Pts',(30.0912045055574,-1.4979228580024,23.3169457772084));
#57082=CARTESIAN_POINT('Ctrl Pts',(30.0455768509778,-1.50000000000001,23.3146928172651));
#57083=CARTESIAN_POINT('Ctrl Pts',(30.0000000000002,-1.50000000000001,23.3125));
#57084=CARTESIAN_POINT('Origin',(30.,-1.32966554433622E-14,16.));
#57085=CARTESIAN_POINT('',(30.0000000000001,-1.50000000000001,22.75));
#57086=CARTESIAN_POINT('',(30.,-1.50000000000001,22.8125));
#57087=CARTESIAN_POINT('',(30.,-1.50000000000001,16.));
#57088=CARTESIAN_POINT('Ctrl Pts',(30.0000000000001,-1.50000000000001,22.75));
#57089=CARTESIAN_POINT('Ctrl Pts',(30.0238190927805,-1.50000000000001,22.7511459966357));
#57090=CARTESIAN_POINT('Ctrl Pts',(30.0476581179369,-1.49943265781826,22.7523087117734));
#57091=CARTESIAN_POINT('Ctrl Pts',(30.2627622738244,-1.48916810759789,22.7629430416939));
#57092=CARTESIAN_POINT('Ctrl Pts',(30.4504917710081,-1.44350305068679,22.7732436551414));
#57093=CARTESIAN_POINT('Ctrl Pts',(30.8053949324493,-1.28097942369943,22.7948334866517));
#57094=CARTESIAN_POINT('Ctrl Pts',(30.9679955997388,-1.16299746502374,22.8059338915341));
#57095=CARTESIAN_POINT('Ctrl Pts',(31.2335580340327,-0.874942371993705,
22.8267123004732));
#57096=CARTESIAN_POINT('Ctrl Pts',(31.3356903480274,-0.709308500806453,
22.8355939721774));
#57097=CARTESIAN_POINT('Ctrl Pts',(31.4719653898389,-0.347606806174152,
22.8556885107681));
#57098=CARTESIAN_POINT('Ctrl Pts',(31.5044992018676,-0.154858219876142,
22.8663967655625));
#57099=CARTESIAN_POINT('Ctrl Pts',(31.4943665307067,0.237510688978279,22.8881950382766));
#57100=CARTESIAN_POINT('Ctrl Pts',(31.4497537465181,0.433331528903234,22.899073973828));
#57101=CARTESIAN_POINT('Ctrl Pts',(31.2903519524536,0.78810181728577,22.9187834342937));
#57102=CARTESIAN_POINT('Ctrl Pts',(31.1802475750943,0.945060620681391,22.9278003293086));
#57103=CARTESIAN_POINT('Ctrl Pts',(30.9030507590494,1.21362000516214,22.948596950241));
#57104=CARTESIAN_POINT('Ctrl Pts',(30.7370141991215,1.32105257322674,22.9595696259569));
#57105=CARTESIAN_POINT('Ctrl Pts',(30.3702805499944,1.46712017353723,22.9812715402192));
#57106=CARTESIAN_POINT('Ctrl Pts',(30.1727871861063,1.50321114583692,22.991597574137));
#57107=CARTESIAN_POINT('Ctrl Pts',(29.7831928098337,1.49647610979574,23.0105290266394));
#57108=CARTESIAN_POINT('Ctrl Pts',(29.5947193673977,1.45676699750561,23.0206999902635));
#57109=CARTESIAN_POINT('Ctrl Pts',(29.2359911149794,1.30598838211349,23.0421476062271));
#57110=CARTESIAN_POINT('Ctrl Pts',(29.0702277888966,1.19366882317697,23.05324288572));
#57111=CARTESIAN_POINT('Ctrl Pts',(28.7948557226535,0.913971635465609,23.0742610967597));
#57112=CARTESIAN_POINT('Ctrl Pts',(28.686793719435,0.750466721324838,23.0833074043708));
#57113=CARTESIAN_POINT('Ctrl Pts',(28.5393908078851,0.39231449396832,23.1032047503351));
#57114=CARTESIAN_POINT('Ctrl Pts',(28.50107471408,0.201238476218244,23.1138200846545));
#57115=CARTESIAN_POINT('Ctrl Pts',(28.4989279287216,-0.192576857122968,
23.1356987142846));
#57116=CARTESIAN_POINT('Ctrl Pts',(28.5381471159066,-0.391544240809387,
23.1467524578227));
#57117=CARTESIAN_POINT('Ctrl Pts',(28.6885908974138,-0.752626531003943,
23.1668125850557));
#57118=CARTESIAN_POINT('Ctrl Pts',(28.7945746463293,-0.912795946069086,
23.1756927219105));
#57119=CARTESIAN_POINT('Ctrl Pts',(29.0643193882896,-1.1885583990927,23.1963308899987));
#57120=CARTESIAN_POINT('Ctrl Pts',(29.2269067570048,-1.30018824275338,23.2072542074138));
#57121=CARTESIAN_POINT('Ctrl Pts',(29.5888237919401,-1.45617120236401,23.228999808865));
#57122=CARTESIAN_POINT('Ctrl Pts',(29.7851989650319,-1.49779418034797,23.2396041076185));
#57123=CARTESIAN_POINT('Ctrl Pts',(29.9893352495882,-1.49997157194577,23.2494861022884));
#57124=CARTESIAN_POINT('Ctrl Pts',(29.9946682024469,-1.50000000000001,23.2497434737706));
#57125=CARTESIAN_POINT('Ctrl Pts',(30.,-1.50000000000001,23.25));
#57126=CARTESIAN_POINT('Ctrl Pts',(30.0000000000003,-1.50000000000001,23.3125));
#57127=CARTESIAN_POINT('Ctrl Pts',(29.8497176527518,-1.50000000000002,23.3052695371968));
#57128=CARTESIAN_POINT('Ctrl Pts',(29.7000480379928,-1.47742120454004,23.2974413657365));
#57129=CARTESIAN_POINT('Ctrl Pts',(29.3674490033452,-1.37435151569836,23.2785761403087));
#57130=CARTESIAN_POINT('Ctrl Pts',(29.1922818901849,-1.27927791742795,23.2675074753621));
#57131=CARTESIAN_POINT('Ctrl Pts',(28.8943459539799,-1.03136235914611,23.2462864826624));
#57132=CARTESIAN_POINT('Ctrl Pts',(28.7726494682524,-0.883034040962408,
23.2365574467202));
#57133=CARTESIAN_POINT('Ctrl Pts',(28.5870020748245,-0.541267982453404,
23.2175704434697));
#57134=CARTESIAN_POINT('Ctrl Pts',(28.5277906685824,-0.349440299767995,
23.2069133499871));
#57135=CARTESIAN_POINT('Ctrl Pts',(28.487963650694,0.0423711662580389,23.185146046319));
#57136=CARTESIAN_POINT('Ctrl Pts',(28.5062787794266,0.238440842104816,23.1742532865498));
#57137=CARTESIAN_POINT('Ctrl Pts',(28.6157002622386,0.608326552071247,23.1537040804405));
#57138=CARTESIAN_POINT('Ctrl Pts',(28.704120723826,0.779127514930934,23.1448722564411));
#57139=CARTESIAN_POINT('Ctrl Pts',(28.9463114752997,1.08624863564316,23.1246887062359));
#57140=CARTESIAN_POINT('Ctrl Pts',(29.100754465216,1.21718400346422,23.1136209708684));
#57141=CARTESIAN_POINT('Ctrl Pts',(29.4452036060534,1.40690072974557,23.0917787447896));
#57142=CARTESIAN_POINT('Ctrl Pts',(29.630453412942,1.46649956876065,23.0812103859941));
#57143=CARTESIAN_POINT('Ctrl Pts',(30.0154678344856,1.51253258675255,23.0614076760565));
#57144=CARTESIAN_POINT('Ctrl Pts',(30.2116518417758,1.49773354664468,23.052253938977));
#57145=CARTESIAN_POINT('Ctrl Pts',(30.5903886500576,1.39306917025536,23.031124612004));
#57146=CARTESIAN_POINT('Ctrl Pts',(30.7689034771477,1.3030667277533,23.0200357455338));
#57147=CARTESIAN_POINT('Ctrl Pts',(31.0748241700176,1.06351798971685,22.9986629977234));
#57148=CARTESIAN_POINT('Ctrl Pts',(31.2011381587389,0.918481956232081,22.9885569343996));
#57149=CARTESIAN_POINT('Ctrl Pts',(31.3967520547264,0.581861797904625,22.9697948964873));
#57150=CARTESIAN_POINT('Ctrl Pts',(31.4615014415134,0.391859484339943,22.9592699713522));
#57151=CARTESIAN_POINT('Ctrl Pts',(31.5127002734739,0.000740375396987882,
22.9375411319665));
#57152=CARTESIAN_POINT('Ctrl Pts',(31.4999079686113,-0.196327016676456,
22.9265929435179));
#57153=CARTESIAN_POINT('Ctrl Pts',(31.4007804390091,-0.569202940848263,
22.9058776143973));
#57154=CARTESIAN_POINT('Ctrl Pts',(31.3174135571943,-0.742018160934012,
22.8969391404085));
#57155=CARTESIAN_POINT('Ctrl Pts',(31.0853396535684,-1.05432624095891,22.8770982550692));
#57156=CARTESIAN_POINT('Ctrl Pts',(30.9361334950341,-1.18878161757634,22.8661846988469));
#57157=CARTESIAN_POINT('Ctrl Pts',(30.5987439832112,-1.38884930936682,22.8443946025078));
#57158=CARTESIAN_POINT('Ctrl Pts',(30.4148754905707,-1.45440359104526,22.8337272732621));
#57159=CARTESIAN_POINT('Ctrl Pts',(30.1494349053273,-1.49442202191131,22.8198446340705));
#57160=CARTESIAN_POINT('Ctrl Pts',(30.0746909808563,-1.50000000000001,22.816093571492));
#57161=CARTESIAN_POINT('Ctrl Pts',(30.0000000000001,-1.50000000000001,22.8125));
#57162=CARTESIAN_POINT('Origin',(30.,-1.32966554433622E-14,16.));
#57163=CARTESIAN_POINT('',(30.0000000000001,-1.50000000000001,22.25));
#57164=CARTESIAN_POINT('',(30.,-1.50000000000001,22.3125));
#57165=CARTESIAN_POINT('',(30.,-1.50000000000001,16.));
#57166=CARTESIAN_POINT('Ctrl Pts',(30.0000000000002,-1.50000000000001,22.25));
#57167=CARTESIAN_POINT('Ctrl Pts',(30.0511677444063,-1.50000000000001,22.2524618092506));
#57168=CARTESIAN_POINT('Ctrl Pts',(30.1023921263505,-1.49738203467576,22.254999064735));
#57169=CARTESIAN_POINT('Ctrl Pts',(30.3449868915282,-1.47242953219059,22.2673640358856));
#57170=CARTESIAN_POINT('Ctrl Pts',(30.5309019965201,-1.41604718249647,22.2778750569255));
#57171=CARTESIAN_POINT('Ctrl Pts',(30.8779534991821,-1.23257211766357,22.2996691097112));
#57172=CARTESIAN_POINT('Ctrl Pts',(31.0343750352224,-1.10459007945506,22.3107500009898));
#57173=CARTESIAN_POINT('Ctrl Pts',(31.2820199524192,-0.801819415517196,
22.3310751188442));
#57174=CARTESIAN_POINT('Ctrl Pts',(31.3735944009353,-0.632242273686504,
22.3398754292397));
#57175=CARTESIAN_POINT('Ctrl Pts',(31.4893318529591,-0.264232559817084,
22.3603204133435));
#57176=CARTESIAN_POINT('Ctrl Pts',(31.511019003439,-0.0688512669519718,
22.3711749296138));
#57177=CARTESIAN_POINT('Ctrl Pts',(31.4781740542578,0.32329452926424,22.3929608071814));
#57178=CARTESIAN_POINT('Ctrl Pts',(31.422363807823,0.516161881943181,22.403675660108));
#57179=CARTESIAN_POINT('Ctrl Pts',(31.2428531453717,0.861044634974944,22.4228358130542));
#57180=CARTESIAN_POINT('Ctrl Pts',(31.1239285676202,1.01138399102137,22.4323522946618));
#57181=CARTESIAN_POINT('Ctrl Pts',(30.8309115401787,1.26428053578999,22.4534749869891));
#57182=CARTESIAN_POINT('Ctrl Pts',(30.6578432463629,1.3623737449238,22.4645265505225));
#57183=CARTESIAN_POINT('Ctrl Pts',(30.2831279004866,1.48623532989505,22.4859956505893));
#57184=CARTESIAN_POINT('Ctrl Pts',(30.0851137662052,1.5105602610331,22.49561162143));
#57185=CARTESIAN_POINT('Ctrl Pts',(29.6966286981958,1.48149502237994,22.5151099857196));
#57186=CARTESIAN_POINT('Ctrl Pts',(29.5097167303907,1.43054672747056,22.5255180223776));
#57187=CARTESIAN_POINT('Ctrl Pts',(29.1585275612845,1.25766527467259,22.547216881732));
#57188=CARTESIAN_POINT('Ctrl Pts',(28.9988940242273,1.13472310971196,22.5583123140024));
#57189=CARTESIAN_POINT('Ctrl Pts',(28.7421191463059,0.839368453848379,22.5788706970727));
#57190=CARTESIAN_POINT('Ctrl Pts',(28.6452032661271,0.671810533827306,22.5876771925652));
#57191=CARTESIAN_POINT('Ctrl Pts',(28.5189623058816,0.306989072921277,22.6079450515044));
#57192=CARTESIAN_POINT('Ctrl Pts',(28.4917024287485,0.112879611784448,22.6187289104564));
#57193=CARTESIAN_POINT('Ctrl Pts',(28.5129271256702,-0.27954553838217,22.6405303076879));
#57194=CARTESIAN_POINT('Ctrl Pts',(28.5630339289139,-0.474005993650327,
22.6513336663139));
#57195=CARTESIAN_POINT('Ctrl Pts',(28.7322894218787,-0.823994430176359,
22.6707774683431));
#57196=CARTESIAN_POINT('Ctrl Pts',(28.8466683628132,-0.977702516203741,
22.680002042295));
#57197=CARTESIAN_POINT('Ctrl Pts',(29.1315598866997,-1.23870928805523,22.7009590802358));
#57198=CARTESIAN_POINT('Ctrl Pts',(29.301068288962,-1.34167114530826,22.7119746086325));
#57199=CARTESIAN_POINT('Ctrl Pts',(29.6506233621551,-1.46928601783117,22.732337442503));
#57200=CARTESIAN_POINT('Ctrl Pts',(29.8247316115896,-1.50000000000001,22.7415673957309));
#57201=CARTESIAN_POINT('Ctrl Pts',(30.0000000000001,-1.50000000000001,22.75));
#57202=CARTESIAN_POINT('Ctrl Pts',(30.0000000000001,-1.50000000000001,22.8125));
#57203=CARTESIAN_POINT('Ctrl Pts',(29.8821180181442,-1.50000000000001,22.8068284005036));
#57204=CARTESIAN_POINT('Ctrl Pts',(29.7644054408515,-1.48610745961779,22.8007790475884));
#57205=CARTESIAN_POINT('Ctrl Pts',(29.4561358619788,-1.41197523055228,22.7838881919746));
#57206=CARTESIAN_POINT('Ctrl Pts',(29.2741386603191,-1.32762177587115,22.7727886960081));
#57207=CARTESIAN_POINT('Ctrl Pts',(28.9596308471203,-1.09734948081223,22.7512604791499));
#57208=CARTESIAN_POINT('Ctrl Pts',(28.8283658665089,-0.955949757636784,
22.7410172197375));
#57209=CARTESIAN_POINT('Ctrl Pts',(28.6210784753189,-0.623528783846783,
22.7218101845402));
#57210=CARTESIAN_POINT('Ctrl Pts',(28.550139211662,-0.43377020073728,22.7115983444854));
#57211=CARTESIAN_POINT('Ctrl Pts',(28.4878128315539,-0.0419315259951405,
22.6898295292219));
#57212=CARTESIAN_POINT('Ctrl Pts',(28.4952899772074,0.155946448584049,22.678836308412));
#57213=CARTESIAN_POINT('Ctrl Pts',(28.5845546436209,0.531607574681399,22.657966245851));
#57214=CARTESIAN_POINT('Ctrl Pts',(28.6631729955745,0.706378968214403,22.6488631478995));
#57215=CARTESIAN_POINT('Ctrl Pts',(28.886581089556,1.02462509962909,22.6292742506491));
#57216=CARTESIAN_POINT('Ctrl Pts',(29.0320840520478,1.16304620087307,22.6184287055121));
#57217=CARTESIAN_POINT('Ctrl Pts',(29.3643456686259,1.37241961531272,22.5966268328521));
#57218=CARTESIAN_POINT('Ctrl Pts',(29.5468906971467,1.44301653433814,22.585883105544));
#57219=CARTESIAN_POINT('Ctrl Pts',(29.9272228832809,1.51053148619831,22.5657089493774));
#57220=CARTESIAN_POINT('Ctrl Pts',(30.1212939503538,1.50741198602448,22.5568701305933));
#57221=CARTESIAN_POINT('Ctrl Pts',(30.5044378408363,1.42661367919911,22.5361917141558));
#57222=CARTESIAN_POINT('Ctrl Pts',(30.6892182911204,1.34709011542225,22.5250924727137));
#57223=CARTESIAN_POINT('Ctrl Pts',(31.0107046879826,1.12481571216727,22.5034506622537));
#57224=CARTESIAN_POINT('Ctrl Pts',(31.1460355364563,0.986589014961116,22.4930999232927));
#57225=CARTESIAN_POINT('Ctrl Pts',(31.3611183370781,0.66090197936205,22.473704885123));
#57226=CARTESIAN_POINT('Ctrl Pts',(31.4365760335144,0.475089538086611,22.463893863227));
#57227=CARTESIAN_POINT('Ctrl Pts',(31.5103576978905,0.0866802952431828,
22.4423155719579));
#57228=CARTESIAN_POINT('Ctrl Pts',(31.5086976507443,-0.111919508747406,
22.431282249514));
#57229=CARTESIAN_POINT('Ctrl Pts',(31.4301969979147,-0.490528747223499,
22.410248402932));
#57230=CARTESIAN_POINT('Ctrl Pts',(31.3566667795852,-0.667467593155736,
22.4008985610562));
#57231=CARTESIAN_POINT('Ctrl Pts',(31.1425983489439,-0.991976419659515,
22.3815850548154));
#57232=CARTESIAN_POINT('Ctrl Pts',(31.0011829334274,-1.13452992378446,22.370821382905));
#57233=CARTESIAN_POINT('Ctrl Pts',(30.6747026750166,-1.35372782384191,22.3490247635913));
#57234=CARTESIAN_POINT('Ctrl Pts',(30.4937271061129,-1.42970164427305,22.3382071885718));
#57235=CARTESIAN_POINT('Ctrl Pts',(30.2032733713701,-1.48966742655325,22.322567010569));
#57236=CARTESIAN_POINT('Ctrl Pts',(30.1016602333963,-1.50000000000001,22.3173911302598));
#57237=CARTESIAN_POINT('Ctrl Pts',(30.,-1.50000000000001,22.3125));
#57238=CARTESIAN_POINT('Origin',(30.,-1.32966554433622E-14,16.));
#57239=CARTESIAN_POINT('',(30.,-1.50000000000001,21.75));
#57240=CARTESIAN_POINT('',(29.9999999999999,-1.50000000000001,21.8125));
#57241=CARTESIAN_POINT('',(30.,-1.50000000000001,16.));
#57242=CARTESIAN_POINT('Ctrl Pts',(30.,-1.50000000000001,21.75));
#57243=CARTESIAN_POINT('Ctrl Pts',(30.0799345840677,-1.50000000000001,21.7538458544691));
#57244=CARTESIAN_POINT('Ctrl Pts',(30.1599122998412,-1.4936114408734,21.7578712440892));
#57245=CARTESIAN_POINT('Ctrl Pts',(30.4303228176761,-1.44993500309235,21.7720946105773));
#57246=CARTESIAN_POINT('Ctrl Pts',(30.6136742893428,-1.38234553687229,21.7827935975436));
#57247=CARTESIAN_POINT('Ctrl Pts',(30.9490281775211,-1.17851150378185,21.8045903754862));
#57248=CARTESIAN_POINT('Ctrl Pts',(31.096754819913,-1.04244516916321,21.8154774972882));
#57249=CARTESIAN_POINT('Ctrl Pts',(31.3253413942278,-0.727732251316939,
21.8352173994684));
#57250=CARTESIAN_POINT('Ctrl Pts',(31.4067935410376,-0.554135842314364,
21.8442146754271));
#57251=CARTESIAN_POINT('Ctrl Pts',(31.5019658936778,-0.180133518226551,
21.8649925823208));
#57252=CARTESIAN_POINT('Ctrl Pts',(31.5126290136531,0.0172760533687308,
21.8759597807428));
#57253=CARTESIAN_POINT('Ctrl Pts',(31.457072059222,0.408029499969523,21.8976683055539));
#57254=CARTESIAN_POINT('Ctrl Pts',(31.3902144216195,0.597326073407902,21.9080390017153));
#57255=CARTESIAN_POINT('Ctrl Pts',(31.1907422817111,0.931962878929858,21.9269315763413));
#57256=CARTESIAN_POINT('Ctrl Pts',(31.0626495240423,1.07572029471252,21.9370877035676));
#57257=CARTESIAN_POINT('Ctrl Pts',(30.7536327605205,1.31199280194067,21.9585184047354));
#57258=CARTESIAN_POINT('Ctrl Pts',(30.5738554020277,1.39999410781883,21.9696124276475));
#57259=CARTESIAN_POINT('Ctrl Pts',(30.1942124641512,1.50002082255712,21.9906565268663));
#57260=CARTESIAN_POINT('Ctrl Pts',(29.9984550225415,1.51253833676667,21.9997260456303));
#57261=CARTESIAN_POINT('Ctrl Pts',(29.6143176021754,1.46236614670513,22.0196015378309));
#57262=CARTESIAN_POINT('Ctrl Pts',(29.4295365026789,1.40065016331119,22.0302061554976));
#57263=CARTESIAN_POINT('Ctrl Pts',(29.0868629977602,1.20683686352092,22.052076744962));
#57264=CARTESIAN_POINT('Ctrl Pts',(28.9337539891966,1.07396976987892,22.0631339581722));
#57265=CARTESIAN_POINT('Ctrl Pts',(28.6951751765203,0.763999003449345,22.0832228857165));
#57266=CARTESIAN_POINT('Ctrl Pts',(28.60882966791,0.592379173375639,22.0920900459236));
#57267=CARTESIAN_POINT('Ctrl Pts',(28.5036090779159,0.221263029136351,22.1127076094925));
#57268=CARTESIAN_POINT('Ctrl Pts',(28.4875441317865,0.0247675363524192,
22.1236240257582));
#57269=CARTESIAN_POINT('Ctrl Pts',(28.5320098906898,-0.36675262012417,22.1453751455625));
#57270=CARTESIAN_POINT('Ctrl Pts',(28.593470220051,-0.557855368091198,22.155991964894));
#57271=CARTESIAN_POINT('Ctrl Pts',(28.7831869687067,-0.897529793649072,
22.1748627663138));
#57272=CARTESIAN_POINT('Ctrl Pts',(28.9067443386156,-1.04452569047662,22.1847486483138));
#57273=CARTESIAN_POINT('Ctrl Pts',(29.2079650540828,-1.28908351396432,22.2060344096185));
#57274=CARTESIAN_POINT('Ctrl Pts',(29.3845091949262,-1.38211075548827,22.2171124835975));
#57275=CARTESIAN_POINT('Ctrl Pts',(29.7125665428598,-1.47927872450056,22.2355952603595));
#57276=CARTESIAN_POINT('Ctrl Pts',(29.8560312883098,-1.50000000000001,22.2430733021292));
#57277=CARTESIAN_POINT('Ctrl Pts',(30.0000000000002,-1.50000000000001,22.25));
#57278=CARTESIAN_POINT('Ctrl Pts',(30.,-1.50000000000001,22.3125));
#57279=CARTESIAN_POINT('Ctrl Pts',(29.9110895843884,-1.50000000000001,22.3082222956344));
#57280=CARTESIAN_POINT('Ctrl Pts',(29.8221645100457,-1.49209634975764,22.3037243401601));
#57281=CARTESIAN_POINT('Ctrl Pts',(29.5376207680931,-1.44087704391974,22.288611464497));
#57282=CARTESIAN_POINT('Ctrl Pts',(29.3500356587678,-1.36654835932947,22.2775215860335));
#57283=CARTESIAN_POINT('Ctrl Pts',(29.0213968226607,-1.15294073825471,22.2557763976293));
#57284=CARTESIAN_POINT('Ctrl Pts',(28.8818555948118,-1.01818896609304,22.2453196123919));
#57285=CARTESIAN_POINT('Ctrl Pts',(28.6586442869874,-0.699623440719697,
22.2257313109655));
#57286=CARTESIAN_POINT('Ctrl Pts',(28.5785399664869,-0.517856468116547,
22.2162698037842));
#57287=CARTESIAN_POINT('Ctrl Pts',(28.4929509348882,-0.133169441708886,
22.1948983023171));
#57288=CARTESIAN_POINT('Ctrl Pts',(28.4885197532221,0.0660037349236151,
22.1838331258375));
#57289=CARTESIAN_POINT('Ctrl Pts',(28.555761801385,0.44759093437612,22.1626338369791));
#57290=CARTESIAN_POINT('Ctrl Pts',(28.6240637192867,0.626835313372202,22.1529543398));
#57291=CARTESIAN_POINT('Ctrl Pts',(28.8284985352011,0.957663958533704,22.1339287805455));
#57292=CARTESIAN_POINT('Ctrl Pts',(28.9656007252824,1.10432288929781,22.1232585891618));
#57293=CARTESIAN_POINT('Ctrl Pts',(29.2858531479679,1.33342212875051,22.1014865695287));
#57294=CARTESIAN_POINT('Ctrl Pts',(29.4650586076933,1.41487321083335,22.0906020127698));
#57295=CARTESIAN_POINT('Ctrl Pts',(29.8404420905807,1.50363480947233,22.0700757665663));
#57296=CARTESIAN_POINT('Ctrl Pts',(30.0326825220108,1.51172235919918,22.0612531825154));
#57297=CARTESIAN_POINT('Ctrl Pts',(30.4195266402016,1.45401546056375,22.0410381667945));
#57298=CARTESIAN_POINT('Ctrl Pts',(30.6097995465824,1.38502427774371,22.029967235573));
#57299=CARTESIAN_POINT('Ctrl Pts',(30.9454244752463,1.18038733089544,22.0081351140291));
#57300=CARTESIAN_POINT('Ctrl Pts',(31.0891246269642,1.04926948856203,21.997579174969));
#57301=CARTESIAN_POINT('Ctrl Pts',(31.3204408508467,0.737906981306312,21.9778010094235));
#57302=CARTESIAN_POINT('Ctrl Pts',(31.4051230902783,0.560097094369773,21.9686165052427));
#57303=CARTESIAN_POINT('Ctrl Pts',(31.5023434434385,0.179258057369552,21.9474587809649));
#57304=CARTESIAN_POINT('Ctrl Pts',(31.5128623034415,-0.0203042234475934,
21.9363719875862));
#57305=CARTESIAN_POINT('Ctrl Pts',(31.4568810475112,-0.404757677376984,
21.9150134623679));
#57306=CARTESIAN_POINT('Ctrl Pts',(31.3937249627295,-0.586348141727015,
21.9049348418193));
#57307=CARTESIAN_POINT('Ctrl Pts',(31.1987850558466,-0.923274808506461,
21.8861967170992));
#57308=CARTESIAN_POINT('Ctrl Pts',(31.0660220732146,-1.07382111006007,21.8756273134093));
#57309=CARTESIAN_POINT('Ctrl Pts',(30.7521571303647,-1.31243843036869,21.8538982204082));
#57310=CARTESIAN_POINT('Ctrl Pts',(30.5748417786265,-1.39921326582906,21.8429567194739));
#57311=CARTESIAN_POINT('Ctrl Pts',(30.2597272838717,-1.48309858829145,21.8254656184301));
#57312=CARTESIAN_POINT('Ctrl Pts',(30.1300238421579,-1.50000000000003,21.8187557750226));
#57313=CARTESIAN_POINT('Ctrl Pts',(29.9999999999998,-1.50000000000001,21.8125));
#57314=CARTESIAN_POINT('Origin',(30.,-1.32966554433622E-14,16.));
#57315=CARTESIAN_POINT('',(30.,-1.50000000000001,21.25));
#57316=CARTESIAN_POINT('',(29.9999999999999,-1.50000000000001,21.3125));
#57317=CARTESIAN_POINT('',(30.,-1.50000000000001,16.));
#57318=CARTESIAN_POINT('Ctrl Pts',(30.,-1.50000000000001,21.25));
#57319=CARTESIAN_POINT('Ctrl Pts',(30.1075848726609,-1.50000000000001,21.2551761795993));
#57320=CARTESIAN_POINT('Ctrl Pts',(30.2150815962025,-1.48842822791985,21.2606695562356));
#57321=CARTESIAN_POINT('Ctrl Pts',(30.5108359622909,-1.42370950162225,21.2766967872056));
#57322=CARTESIAN_POINT('Ctrl Pts',(30.6910987866292,-1.34546461195666,21.2875431555427));
#57323=CARTESIAN_POINT('Ctrl Pts',(31.0150386063333,-1.12214805976604,21.3093319549459));
#57324=CARTESIAN_POINT('Ctrl Pts',(31.1546840327806,-0.977879417444189,
21.3200581109451));
#57325=CARTESIAN_POINT('Ctrl Pts',(31.3647735631693,-0.650743634461253,
21.3392531532717));
#57326=CARTESIAN_POINT('Ctrl Pts',(31.4361426481554,-0.472861434650035,
21.3487299202974));
#57327=CARTESIAN_POINT('Ctrl Pts',(31.5100129878737,-0.0930141634261118,
21.3698325464765));
#57328=CARTESIAN_POINT('Ctrl Pts',(31.5091680819865,0.105843895299734,21.3808802164057));
#57329=CARTESIAN_POINT('Ctrl Pts',(31.4305088048906,0.492738271362424,21.4023743484091));
#57330=CARTESIAN_POINT('Ctrl Pts',(31.3531309016418,0.676876453829759,21.4120329161916));
#57331=CARTESIAN_POINT('Ctrl Pts',(31.1347020158755,0.999644296815675,21.4315078542742));
#57332=CARTESIAN_POINT('Ctrl Pts',(30.9976338252526,1.13646112591015,21.4419030181452));
#57333=CARTESIAN_POINT('Ctrl Pts',(30.6731866853066,1.35520814296552,21.4635892944733));
#57334=CARTESIAN_POINT('Ctrl Pts',(30.4872391020676,1.43261266999426,21.474685827494));
#57335=CARTESIAN_POINT('Ctrl Pts',(30.1032980730075,1.50870030742653,21.4952717443516));
#57336=CARTESIAN_POINT('Ctrl Pts',(29.9096173130592,1.50952898426713,21.5040838450456));
#57337=CARTESIAN_POINT('Ctrl Pts',(29.5302606487566,1.43771855687004,21.5243303851611));
#57338=CARTESIAN_POINT('Ctrl Pts',(29.3483375586665,1.36492268311026,21.5351052715185));
#57339=CARTESIAN_POINT('Ctrl Pts',(29.0184009025148,1.15151905747937,21.5569072347786));
#57340=CARTESIAN_POINT('Ctrl Pts',(28.8745521744234,1.01139585435745,21.5677204711336));
#57341=CARTESIAN_POINT('Ctrl Pts',(28.6549505368779,0.690580628714703,21.5871975938919));
#57342=CARTESIAN_POINT('Ctrl Pts',(28.5784089748082,0.514933598952509,21.596392577836));
#57343=CARTESIAN_POINT('Ctrl Pts',(28.4935139297613,0.138064010695691,21.6173297771836));
#57344=CARTESIAN_POINT('Ctrl Pts',(28.4883967455728,-0.0601274794615553,
21.6283404155257));
#57345=CARTESIAN_POINT('Ctrl Pts',(28.5553929405263,-0.450590041266374,
21.6500327800704));
#57346=CARTESIAN_POINT('Ctrl Pts',(28.6281760530356,-0.63873783180513,21.6600741404618));
#57347=CARTESIAN_POINT('Ctrl Pts',(28.8386308155265,-0.968434016466414,
21.6793578772949));
#57348=CARTESIAN_POINT('Ctrl Pts',(28.9715505605447,-1.10856330761102,21.6896454618184));
#57349=CARTESIAN_POINT('Ctrl Pts',(29.2889068065357,-1.33562316156644,21.7112214894881));
#57350=CARTESIAN_POINT('Ctrl Pts',(29.4720453487169,-1.41803231498314,21.7223218898575));
#57351=CARTESIAN_POINT('Ctrl Pts',(29.7757758521236,-1.48742065117207,21.7388625842992));
#57352=CARTESIAN_POINT('Ctrl Pts',(29.8878284604463,-1.50000000000001,21.7446031442869));
#57353=CARTESIAN_POINT('Ctrl Pts',(30.,-1.50000000000001,21.75));
#57354=CARTESIAN_POINT('Ctrl Pts',(29.9999999999998,-1.50000000000001,21.8125));
#57355=CARTESIAN_POINT('Ctrl Pts',(29.9405204451645,-1.50000000000001,21.8096382885837));
#57356=CARTESIAN_POINT('Ctrl Pts',(29.8809833669271,-1.49646250510709,21.8066755458243));
#57357=CARTESIAN_POINT('Ctrl Pts',(29.6241950912386,-1.46572084178495,21.7934668790576));
#57358=CARTESIAN_POINT('Ctrl Pts',(29.4333772164259,-1.40302797833686,21.782544681346));
#57359=CARTESIAN_POINT('Ctrl Pts',(29.0921865820648,-1.20964665656295,21.760757435914));
#57360=CARTESIAN_POINT('Ctrl Pts',(28.9439925649252,-1.08269733302756,21.7501010778418));
#57361=CARTESIAN_POINT('Ctrl Pts',(28.7038088414644,-0.77933430694382,21.7301184823344));
#57362=CARTESIAN_POINT('Ctrl Pts',(28.6141674942217,-0.605760578772268,
21.7211533654873));
#57363=CARTESIAN_POINT('Ctrl Pts',(28.5043846389733,-0.22927416638246,21.7002374536878));
#57364=CARTESIAN_POINT('Ctrl Pts',(28.4872031236976,-0.0294943674923172,
21.6891385759717));
#57365=CARTESIAN_POINT('Ctrl Pts',(28.5307959749546,0.357711165892058,21.6676271574504));
#57366=CARTESIAN_POINT('Ctrl Pts',(28.588271358922,0.541814389624386,21.6573992005764));
#57367=CARTESIAN_POINT('Ctrl Pts',(28.7738533380075,0.887068805374046,21.6382183997014));
#57368=CARTESIAN_POINT('Ctrl Pts',(28.903512180976,1.043112470525,21.6279461150529));
#57369=CARTESIAN_POINT('Ctrl Pts',(29.2128905056455,1.29185751769652,21.6061515588234));
#57370=CARTESIAN_POINT('Ctrl Pts',(29.3882998946744,1.38356922217579,21.5951646233122));
#57371=CARTESIAN_POINT('Ctrl Pts',(29.7586487303438,1.49259838475184,21.5743176187989));
#57372=CARTESIAN_POINT('Ctrl Pts',(29.9494126813103,1.51113463524617,21.5652431789286));
#57373=CARTESIAN_POINT('Ctrl Pts',(30.3366113826679,1.4752126287187,21.5456162392091));
#57374=CARTESIAN_POINT('Ctrl Pts',(30.5290112502297,1.41763409463152,21.5347599925404));
#57375=CARTESIAN_POINT('Ctrl Pts',(30.8756573292315,1.23320190987312,21.512958859045));
#57376=CARTESIAN_POINT('Ctrl Pts',(31.0275193143428,1.10985575574539,21.5022261138206));
#57377=CARTESIAN_POINT('Ctrl Pts',(31.2750461098143,0.813213213668382,21.4820769047076));
#57378=CARTESIAN_POINT('Ctrl Pts',(31.3687657636095,0.643070885011216,21.4732261602783));
#57379=CARTESIAN_POINT('Ctrl Pts',(31.4888227697242,0.270291882918073,21.4525162157176));
#57380=CARTESIAN_POINT('Ctrl Pts',(31.5115128952941,0.0704953149593227,
21.4414164063865));
#57381=CARTESIAN_POINT('Ctrl Pts',(31.4782054807328,-0.318770290439176,
21.4197905394199));
#57382=CARTESIAN_POINT('Ctrl Pts',(31.4254475382382,-0.504803416717179,
21.4094553657378));
#57383=CARTESIAN_POINT('Ctrl Pts',(31.2494901966584,-0.853416070021567,
21.3900879961098));
#57384=CARTESIAN_POINT('Ctrl Pts',(31.1254658116588,-1.01138492328729,21.3802216401301));
#57385=CARTESIAN_POINT('Ctrl Pts',(30.8246930412984,-1.26828298434064,21.3586146462176));
#57386=CARTESIAN_POINT('Ctrl Pts',(30.6515224369356,-1.36534975789868,21.347586672365));
#57387=CARTESIAN_POINT('Ctrl Pts',(30.3143398429227,-1.47517879246933,21.3283131607309));
#57388=CARTESIAN_POINT('Ctrl Pts',(30.1575657374829,-1.50000000000003,21.3200808850792));
#57389=CARTESIAN_POINT('Ctrl Pts',(29.9999999999998,-1.50000000000001,21.3125));
#57390=CARTESIAN_POINT('Origin',(30.,-1.32966554433622E-14,16.));
#57391=CARTESIAN_POINT('',(29.9999999999999,-1.50000000000001,20.75));
#57392=CARTESIAN_POINT('',(30.0000000238974,-1.50000000000001,20.8125000022995));
#57393=CARTESIAN_POINT('',(30.,-1.50000000000001,16.));
#57394=CARTESIAN_POINT('Ctrl Pts',(29.9999999999998,-1.50000000000001,20.75));
#57395=CARTESIAN_POINT('Ctrl Pts',(30.1355873378723,-1.50000000000003,20.7565234488349));
#57396=CARTESIAN_POINT('Ctrl Pts',(30.2707763371628,-1.48162130053548,20.7635382520255));
#57397=CARTESIAN_POINT('Ctrl Pts',(30.5905052894202,-1.39270558594719,20.7813910993741));
#57398=CARTESIAN_POINT('Ctrl Pts',(30.767029784006,-1.30383501600373,20.7923527650226));
#57399=CARTESIAN_POINT('Ctrl Pts',(31.0784013127494,-1.06141205266722,20.8140676058879));
#57400=CARTESIAN_POINT('Ctrl Pts',(31.2094059572181,-0.909300433903993,
20.8244833092276));
#57401=CARTESIAN_POINT('Ctrl Pts',(31.4005633760122,-0.569930140644686,
20.8433372144086));
#57402=CARTESIAN_POINT('Ctrl Pts',(31.4616108021312,-0.387386085525011,
20.8534785508042));
#57403=CARTESIAN_POINT('Ctrl Pts',(31.5130288281118,-0.00193915990322278,
20.8748922688942));
#57404=CARTESIAN_POINT('Ctrl Pts',(31.5000564049022,0.197728440072968,20.8859849133374));
#57405=CARTESIAN_POINT('Ctrl Pts',(31.3981909189968,0.576981524645895,20.907054529147));
#57406=CARTESIAN_POINT('Ctrl Pts',(31.3116775745975,0.753220156722293,20.9161479987326));
#57407=CARTESIAN_POINT('Ctrl Pts',(31.0770964939546,1.06165196611475,20.9360018364982));
#57408=CARTESIAN_POINT('Ctrl Pts',(30.9317342971964,1.19125838532521,20.946595756762));
#57409=CARTESIAN_POINT('Ctrl Pts',(30.5933406580028,1.39218994814601,20.9684581606193));
#57410=CARTESIAN_POINT('Ctrl Pts',(30.4020178812766,1.458987498605,20.9795186695191));
#57411=CARTESIAN_POINT('Ctrl Pts',(30.0144815741343,1.51197726610397,20.999635956776));
#57412=CARTESIAN_POINT('Ctrl Pts',(29.8225847199203,1.50160380579917,21.0084913464817));
#57413=CARTESIAN_POINT('Ctrl Pts',(29.4482673839794,1.40844186112423,21.0290885295006));
#57414=CARTESIAN_POINT('Ctrl Pts',(29.2698358143887,1.32475295725216,21.0399980141694));
#57415=CARTESIAN_POINT('Ctrl Pts',(28.9522277915389,1.09163995424434,21.0617542984881));
#57416=CARTESIAN_POINT('Ctrl Pts',(28.8169317835683,0.943334467611102,21.0723833275575));
#57417=CARTESIAN_POINT('Ctrl Pts',(28.6164713965323,0.609937924996611,21.0912889974983));
#57418=CARTESIAN_POINT('Ctrl Pts',(28.5503235834348,0.429720618453307,21.1011266323083));
#57419=CARTESIAN_POINT('Ctrl Pts',(28.4877747716401,0.0469249157698905,
21.1223930602351));
#57420=CARTESIAN_POINT('Ctrl Pts',(28.4947443957624,-0.152432728065059,
21.1334684848926));
#57421=CARTESIAN_POINT('Ctrl Pts',(28.585202717896,-0.535530466260377,21.1547516925701));
#57422=CARTESIAN_POINT('Ctrl Pts',(28.6672227696192,-0.715637129073743,
21.1640888680802));
#57423=CARTESIAN_POINT('Ctrl Pts',(28.8938150388557,-1.03121039122832,21.1837567176656));
#57424=CARTESIAN_POINT('Ctrl Pts',(29.0350964807726,-1.16446677665445,21.1942556904709));
#57425=CARTESIAN_POINT('Ctrl Pts',(29.3666683501557,-1.37437197910307,21.2160391495426));
#57426=CARTESIAN_POINT('Ctrl Pts',(29.5553884234738,-1.44649304249621,21.2271223111757));
#57427=CARTESIAN_POINT('Ctrl Pts',(29.8346137979128,-1.49316573714005,21.2418530120072));
#57428=CARTESIAN_POINT('Ctrl Pts',(29.917323692752,-1.50000000000001,21.2460222343129));
#57429=CARTESIAN_POINT('Ctrl Pts',(30.,-1.50000000000001,21.25));
#57430=CARTESIAN_POINT('Ctrl Pts',(29.9999999999998,-1.50000000000001,21.3125));
#57431=CARTESIAN_POINT('Ctrl Pts',(29.9681380540405,-1.50000000000001,21.3109670414103));
#57432=CARTESIAN_POINT('Ctrl Pts',(29.9362464291016,-1.4989848402199,21.3094044560071));
#57433=CARTESIAN_POINT('Ctrl Pts',(29.7059061051266,-1.48427038685078,21.2979134671869));
#57434=CARTESIAN_POINT('Ctrl Pts',(29.5119585810338,-1.43225099507769,21.2871371794785));
#57435=CARTESIAN_POINT('Ctrl Pts',(29.1596955105172,-1.25764065487782,21.2653386273684));
#57436=CARTESIAN_POINT('Ctrl Pts',(29.0039750821709,-1.13829559847059,21.2545313843106));
#57437=CARTESIAN_POINT('Ctrl Pts',(28.7485987477413,-0.848934521932683,
21.2342067770101));
#57438=CARTESIAN_POINT('Ctrl Pts',(28.6505388148689,-0.682384621723858,
21.2254102567623));
#57439=CARTESIAN_POINT('Ctrl Pts',(28.5196273945211,-0.313661198442873,
21.2049256221356));
#57440=CARTESIAN_POINT('Ctrl Pts',(28.4910680085409,-0.114008266472331,
21.1938337925817));
#57441=CARTESIAN_POINT('Ctrl Pts',(28.5133617159534,0.277152561451723,21.1721026354748));
#57442=CARTESIAN_POINT('Ctrl Pts',(28.5610406223868,0.465104578293146,21.1616608567614));
#57443=CARTESIAN_POINT('Ctrl Pts',(28.7268127368948,0.817191792877632,21.1421004559512));
#57444=CARTESIAN_POINT('Ctrl Pts',(28.8450160186508,0.977157792197407,21.1325925873729));
#57445=CARTESIAN_POINT('Ctrl Pts',(29.1366994431696,1.24242044599111,21.1111905550177));
#57446=CARTESIAN_POINT('Ctrl Pts',(29.3073536529405,1.34504122266248,21.1001293733922));
#57447=CARTESIAN_POINT('Ctrl Pts',(29.6718885684984,1.47596994041667,21.0789537702634));
#57448=CARTESIAN_POINT('Ctrl Pts',(29.8613546451375,1.5056180641301,21.0693266350828));
#57449=CARTESIAN_POINT('Ctrl Pts',(30.2499905035945,1.49232790599687,21.0502592125655));
#57450=CARTESIAN_POINT('Ctrl Pts',(30.4453612619354,1.44608660162569,21.0395749518952));
#57451=CARTESIAN_POINT('Ctrl Pts',(30.8031247707546,1.28178759217525,21.017798185678));
#57452=CARTESIAN_POINT('Ctrl Pts',(30.9627170127615,1.16669332668992,21.0069227374242));
#57453=CARTESIAN_POINT('Ctrl Pts',(31.2261252563514,0.884888124749317,20.9864215801195));
#57454=CARTESIAN_POINT('Ctrl Pts',(31.3286136134484,0.721936793997485,20.9776075996665));
#57455=CARTESIAN_POINT('Ctrl Pts',(31.4704956794702,0.357450862099888,20.9573583812278));
#57456=CARTESIAN_POINT('Ctrl Pts',(31.5050292215643,0.158114714869949,20.9462841508261));
#57457=CARTESIAN_POINT('Ctrl Pts',(31.4940038450927,-0.234658795010768,
20.9244634002772));
#57458=CARTESIAN_POINT('Ctrl Pts',(31.4515503117875,-0.4244189406881,20.9139211699618));
#57459=CARTESIAN_POINT('Ctrl Pts',(31.2960889353342,-0.779942120592769,
20.8941698821893));
#57460=CARTESIAN_POINT('Ctrl Pts',(31.1836334516182,-0.941901166431575,
20.8849503363697));
#57461=CARTESIAN_POINT('Ctrl Pts',(30.9011214218994,-1.21536636315781,20.8637617145378));
#57462=CARTESIAN_POINT('Ctrl Pts',(30.7331593249481,-1.323483412269,20.8526773830162));
#57463=CARTESIAN_POINT('Ctrl Pts',(30.374104697925,-1.46471715060753,20.8314791998208));
#57464=CARTESIAN_POINT('Ctrl Pts',(30.1878361111775,-1.49999999700053,20.821537269196));
#57465=CARTESIAN_POINT('Ctrl Pts',(30.0000000239529,-1.50000000000001,20.8125000011524));
#57466=CARTESIAN_POINT('Origin',(30.,-1.32966554433622E-14,16.));
#57467=CARTESIAN_POINT('',(29.9999999999999,-1.50000000000001,20.25));
#57468=CARTESIAN_POINT('',(30.0000000000001,-1.50000000000001,20.3125));
#57469=CARTESIAN_POINT('',(30.,-1.50000000000001,16.));
#57470=CARTESIAN_POINT('Ctrl Pts',(29.9999999999999,-1.50000000000001,20.25));
#57471=CARTESIAN_POINT('Ctrl Pts',(30.1641246040904,-1.50000000000003,20.257896448696));
#57472=CARTESIAN_POINT('Ctrl Pts',(30.3273129308388,-1.47306839847894,20.2664959507697));
#57473=CARTESIAN_POINT('Ctrl Pts',(30.6694540696788,-1.35668483193177,20.2861901008358));
#57474=CARTESIAN_POINT('Ctrl Pts',(30.8415535621189,-1.25719932144175,20.2972337279289));
#57475=CARTESIAN_POINT('Ctrl Pts',(31.1383891848058,-0.996648092240175,
20.3187527726287));
#57476=CARTESIAN_POINT('Ctrl Pts',(31.2598762410215,-0.837810488997904,
20.3284549728335));
#57477=CARTESIAN_POINT('Ctrl Pts',(31.4314249865634,-0.487683998530185,
20.3479064445261));
#57478=CARTESIAN_POINT('Ctrl Pts',(31.4819950779928,-0.300804420279551,
20.3582886433178));
#57479=CARTESIAN_POINT('Ctrl Pts',(31.5105507066295,0.0893179172321859,
20.3799621065129));
#57480=CARTESIAN_POINT('Ctrl Pts',(31.4853246402279,0.289072829407564,20.3910596016338));
#57481=CARTESIAN_POINT('Ctrl Pts',(31.3605672791737,0.660112394093701,20.411672910783));
#57482=CARTESIAN_POINT('Ctrl Pts',(31.2649722312571,0.828695575895264,20.4204916500332));
#57483=CARTESIAN_POINT('Ctrl Pts',(31.0140581775355,1.12220790918685,20.4407168784407));
#57484=CARTESIAN_POINT('Ctrl Pts',(30.8605226301063,1.24384616367647,20.4514827013131));
#57485=CARTESIAN_POINT('Ctrl Pts',(30.5114243415045,1.42407146100134,20.4732849588136));
#57486=CARTESIAN_POINT('Ctrl Pts',(30.3183380047095,1.47926213924964,20.4841079039198));
#57487=CARTESIAN_POINT('Ctrl Pts',(29.9307960888716,1.51038882263748,20.5036181531332));
#57488=CARTESIAN_POINT('Ctrl Pts',(29.7403288665302,1.48951380456358,20.5127847164407));
#57489=CARTESIAN_POINT('Ctrl Pts',(29.3711639835748,1.37589985350485,20.5337021132381));
#57490=CARTESIAN_POINT('Ctrl Pts',(29.1966946677341,1.28188655628153,20.5447077525887));
#57491=CARTESIAN_POINT('Ctrl Pts',(28.8909965958092,1.02962579258236,20.5664229013678));
#57492=CARTESIAN_POINT('Ctrl Pts',(28.7637626025144,0.872753791453066,20.5765136782526));
#57493=CARTESIAN_POINT('Ctrl Pts',(28.582295287402,0.526054660802727,20.5957747410665));
#57494=CARTESIAN_POINT('Ctrl Pts',(28.5268265400693,0.341112810094873,20.6060492883281));
#57495=CARTESIAN_POINT('Ctrl Pts',(28.4876154625531,-0.0470049788678421,
20.6276113877149));
#57496=CARTESIAN_POINT('Ctrl Pts',(28.5071470207889,-0.246809925970759,
20.6387116625539));
#57497=CARTESIAN_POINT('Ctrl Pts',(28.6213243381125,-0.621726643029005,
20.6595403690571));
#57498=CARTESIAN_POINT('Ctrl Pts',(28.7127069454602,-0.793828860292424,
20.6684492190444));
#57499=CARTESIAN_POINT('Ctrl Pts',(28.9560213000323,-1.09433750409046,20.6885031487146));
#57500=CARTESIAN_POINT('Ctrl Pts',(29.1057854975977,-1.21976733917156,20.6991928441151));
#57501=CARTESIAN_POINT('Ctrl Pts',(29.4493247586543,-1.40936219023255,20.7209879081598));
#57502=CARTESIAN_POINT('Ctrl Pts',(29.6408325610402,-1.46988527163767,20.7318830283038));
#57503=CARTESIAN_POINT('Ctrl Pts',(29.8922912775479,-1.4971028845898,20.7447373862468));
#57504=CARTESIAN_POINT('Ctrl Pts',(29.9461731363168,-1.50000000000001,20.7474102538136));
#57505=CARTESIAN_POINT('Ctrl Pts',(29.9999999999998,-1.50000000000001,20.75));
#57506=CARTESIAN_POINT('Ctrl Pts',(30.0000000239529,-1.50000000000001,20.8125000011524));
#57507=CARTESIAN_POINT('Ctrl Pts',(29.9974904007656,-1.50000000004009,20.8123792568517));
#57508=CARTESIAN_POINT('Ctrl Pts',(29.994980514477,-1.49999370187214,20.8122583249421));
#57509=CARTESIAN_POINT('Ctrl Pts',(29.7936662704942,-1.49898314378545,20.8025445178046));
#57510=CARTESIAN_POINT('Ctrl Pts',(29.5970666373285,-1.45847246315053,20.7919603168594));
#57511=CARTESIAN_POINT('Ctrl Pts',(29.2341811004286,-1.30450218441903,20.7702240261379));
#57512=CARTESIAN_POINT('Ctrl Pts',(29.0708854167951,-1.19371554978206,20.7592900523783));
#57513=CARTESIAN_POINT('Ctrl Pts',(28.7996246113049,-0.919409908918738,
20.738619409654));
#57514=CARTESIAN_POINT('Ctrl Pts',(28.6928036628702,-0.759898893507146,
20.7297166051949));
#57515=CARTESIAN_POINT('Ctrl Pts',(28.540323338491,-0.399638425423168,20.7097021347457));
#57516=CARTESIAN_POINT('Ctrl Pts',(28.4999872115666,-0.200774562873281,
20.6986541423819));
#57517=CARTESIAN_POINT('Ctrl Pts',(28.5000123038317,0.193260173251348,20.6767633237083));
#57518=CARTESIAN_POINT('Ctrl Pts',(28.5373370740434,0.384636586987589,20.6661313007229));
#57519=CARTESIAN_POINT('Ctrl Pts',(28.6828216865171,0.743407395273799,20.6461995891515));
#57520=CARTESIAN_POINT('Ctrl Pts',(28.7898502936129,0.90727948583588,20.637187813622));
#57521=CARTESIAN_POINT('Ctrl Pts',(29.0635269308615,1.18843769395866,20.6162105900475));
#57522=CARTESIAN_POINT('Ctrl Pts',(29.228755223573,1.30174519776628,20.6051136094466));
#57523=CARTESIAN_POINT('Ctrl Pts',(29.5868470804747,1.45456710532649,20.5836398539607));
#57524=CARTESIAN_POINT('Ctrl Pts',(29.7752048690842,1.49530975495507,20.5734457453635));
#57525=CARTESIAN_POINT('Ctrl Pts',(30.1648759814307,1.50410182396658,20.5544534610902));
#57526=CARTESIAN_POINT('Ctrl Pts',(30.3625681263815,1.46904639647318,20.544196110566));
#57527=CARTESIAN_POINT('Ctrl Pts',(30.7301648562918,1.32486538129436,20.5225050764527));
#57528=CARTESIAN_POINT('Ctrl Pts',(30.8968384149473,1.21823387618242,20.5115240048699));
#57529=CARTESIAN_POINT('Ctrl Pts',(31.1754315899033,0.951036194862134,20.4906980266758));
#57530=CARTESIAN_POINT('Ctrl Pts',(31.2863099173977,0.794671992670377,20.4816484440372));
#57531=CARTESIAN_POINT('Ctrl Pts',(31.4475104523221,0.440765387920731,20.4619869659956));
#57532=CARTESIAN_POINT('Ctrl Pts',(31.4931266838049,0.245180433281527,20.4511211351823));
#57533=CARTESIAN_POINT('Ctrl Pts',(31.505277935416,-0.147222207316758,20.4293209884824));
#57534=CARTESIAN_POINT('Ctrl Pts',(31.4737006088925,-0.340229130529765,
20.4185983816372));
#57535=CARTESIAN_POINT('Ctrl Pts',(31.339252899941,-0.702504700740186,20.39847196107));
#57536=CARTESIAN_POINT('Ctrl Pts',(31.2380795698328,-0.868488363198902,
20.3896091209879));
#57537=CARTESIAN_POINT('Ctrl Pts',(30.9741217873874,-1.15788922779948,20.3688705333532));
#57538=CARTESIAN_POINT('Ctrl Pts',(30.8120536546578,-1.27678494801521,20.3577703677868));
#57539=CARTESIAN_POINT('Ctrl Pts',(30.4578087067642,-1.44121172280179,20.3361593393739));
#57540=CARTESIAN_POINT('Ctrl Pts',(30.2702179556352,-1.48784534045563,20.3258384968839));
#57541=CARTESIAN_POINT('Ctrl Pts',(30.052598998323,-1.49930896382792,20.3150498659359));
#57542=CARTESIAN_POINT('Ctrl Pts',(30.0262877690999,-1.50000000000001,20.3137647708805));
#57543=CARTESIAN_POINT('Ctrl Pts',(30.0000000000001,-1.50000000000001,20.3125));
#57544=CARTESIAN_POINT('Origin',(30.,-1.32966554433622E-14,16.));
#57545=CARTESIAN_POINT('',(29.9999999508795,-1.50000000000001,19.7499999952734));
#57546=CARTESIAN_POINT('',(30.0000000000001,-1.50000000000001,19.8125));
#57547=CARTESIAN_POINT('',(30.,-1.50000000000001,16.));
#57548=CARTESIAN_POINT('Ctrl Pts',(29.9999999507652,-1.50000000000001,19.7499999976312));
#57549=CARTESIAN_POINT('Ctrl Pts',(30.0036354883629,-1.50000000011934,19.7501749125187));
#57550=CARTESIAN_POINT('Ctrl Pts',(30.007271600744,-1.4999867831078,19.7503502221899));
#57551=CARTESIAN_POINT('Ctrl Pts',(30.201622915749,-1.49857339489822,19.7597402149765));
#57552=CARTESIAN_POINT('Ctrl Pts',(30.3903004853368,-1.46082693625102,19.769866481516));
#57553=CARTESIAN_POINT('Ctrl Pts',(30.7502056783764,-1.31393443624912,19.7912627754119));
#57554=CARTESIAN_POINT('Ctrl Pts',(30.9169691324023,-1.2034971179945,19.8023538891195));
#57555=CARTESIAN_POINT('Ctrl Pts',(31.1955532827852,-0.926587489668503,
19.8234492094243));
#57556=CARTESIAN_POINT('Ctrl Pts',(31.305583357368,-0.763777918932018,19.8325678933928));
#57557=CARTESIAN_POINT('Ctrl Pts',(31.4566154175894,-0.406803589900389,
19.8523998005612));
#57558=CARTESIAN_POINT('Ctrl Pts',(31.4968003232487,-0.216309448389897,
19.8629828084229));
#57559=CARTESIAN_POINT('Ctrl Pts',(31.5029527191874,0.177060648076386,19.884836702671));
#57560=CARTESIAN_POINT('Ctrl Pts',(31.4658451495388,0.376207311237188,19.8959004061799));
#57561=CARTESIAN_POINT('Ctrl Pts',(31.3192558360179,0.738832237635632,19.9160462354243));
#57562=CARTESIAN_POINT('Ctrl Pts',(31.2148503942445,0.900251242918639,19.9248907954582));
#57563=CARTESIAN_POINT('Ctrl Pts',(30.9479657510409,1.17875033469753,19.9454673747239));
#57564=CARTESIAN_POINT('Ctrl Pts',(30.7867234803792,1.29195591113542,19.9563697464337));
#57565=CARTESIAN_POINT('Ctrl Pts',(30.4266603329508,1.45171184585212,19.9781309575447));
#57566=CARTESIAN_POINT('Ctrl Pts',(30.2307253625385,1.49542562590392,19.9887721548721));
#57567=CARTESIAN_POINT('Ctrl Pts',(29.8418323593176,1.50370934578551,20.0077128815434));
#57568=CARTESIAN_POINT('Ctrl Pts',(29.6526184508184,1.47157346290215,20.0175030286082));
#57569=CARTESIAN_POINT('Ctrl Pts',(29.2894512067405,1.33570909972092,20.038749930874));
#57570=CARTESIAN_POINT('Ctrl Pts',(29.1199599079427,1.2306626568369,20.0498225415362));
#57571=CARTESIAN_POINT('Ctrl Pts',(28.8323016398048,0.961771765690436,20.0711316978356));
#57572=CARTESIAN_POINT('Ctrl Pts',(28.7166359490173,0.80092922531751,20.0805039319268));
#57573=CARTESIAN_POINT('Ctrl Pts',(28.5553841103709,0.447325657819572,20.1001485745656));
#57574=CARTESIAN_POINT('Ctrl Pts',(28.5099861175222,0.258564005548656,20.1106353330251));
#57575=CARTESIAN_POINT('Ctrl Pts',(28.4926188058233,-0.133342134639988,
20.1324078963689));
#57576=CARTESIAN_POINT('Ctrl Pts',(28.5237938243712,-0.332877530953282,
20.1434931961641));
#57577=CARTESIAN_POINT('Ctrl Pts',(28.6595170927538,-0.699759711689848,
20.1638755395383));
#57578=CARTESIAN_POINT('Ctrl Pts',(28.759513047986,-0.864726488741114,20.1726705572702));
#57579=CARTESIAN_POINT('Ctrl Pts',(29.0184002150316,-1.15079879551533,20.1930727248681));
#57580=CARTESIAN_POINT('Ctrl Pts',(29.1758229214277,-1.26830528519454,20.2039107975187));
#57581=CARTESIAN_POINT('Ctrl Pts',(29.5305217931358,-1.4384406773805,20.2257022380569));
#57582=CARTESIAN_POINT('Ctrl Pts',(29.7251117157194,-1.4879453135066,20.2364395788536));
#57583=CARTESIAN_POINT('Ctrl Pts',(29.9491466954872,-1.49935402178859,20.2475353754067));
#57584=CARTESIAN_POINT('Ctrl Pts',(29.9745837219083,-1.50000000000001,20.2487771587502));
#57585=CARTESIAN_POINT('Ctrl Pts',(29.9999999999999,-1.50000000000001,20.25));
#57586=CARTESIAN_POINT('Ctrl Pts',(30.0000000000001,-1.50000000000001,20.3125));
#57587=CARTESIAN_POINT('Ctrl Pts',(29.8275998140085,-1.50000000000001,20.3042053921841));
#57588=CARTESIAN_POINT('Ctrl Pts',(29.6562870357889,-1.47028352574469,20.2951376446808));
#57589=CARTESIAN_POINT('Ctrl Pts',(29.3085931862514,-1.34558031058123,20.2749452383464));
#57590=CARTESIAN_POINT('Ctrl Pts',(29.1384186293223,-1.24350663328035,20.2639223312337));
#57591=CARTESIAN_POINT('Ctrl Pts',(28.8520258822514,-0.983987574399218,
20.242934391019));
#57592=CARTESIAN_POINT('Ctrl Pts',(28.7368098691781,-0.830906588856551,
20.2336614771587));
#57593=CARTESIAN_POINT('Ctrl Pts',(28.5656483010559,-0.481857271883387,
20.214269848438));
#57594=CARTESIAN_POINT('Ctrl Pts',(28.5144799811963,-0.287679235979695,
20.2034821797766));
#57595=CARTESIAN_POINT('Ctrl Pts',(28.4911007681834,0.104720249591022,20.181682208356));
#57596=CARTESIAN_POINT('Ctrl Pts',(28.5173310962609,0.299077411990059,20.1708845882228));
#57597=CARTESIAN_POINT('Ctrl Pts',(28.6416246239434,0.664496311411631,20.1505835382549));
#57598=CARTESIAN_POINT('Ctrl Pts',(28.7375408574377,0.832427515421977,20.1417837739438));
#57599=CARTESIAN_POINT('Ctrl Pts',(28.9926175512114,1.12917452204563,20.1212684183864));
#57600=CARTESIAN_POINT('Ctrl Pts',(29.1516633795811,1.2530630770023,20.1101749736523));
#57601=CARTESIAN_POINT('Ctrl Pts',(29.5021040725661,1.42792836972927,20.0884570187074));
#57602=CARTESIAN_POINT('Ctrl Pts',(29.6888418601191,1.47989191267207,20.0780291609664));
#57603=CARTESIAN_POINT('Ctrl Pts',(30.0769287467939,1.5109546306831,20.0584944686474));
#57604=CARTESIAN_POINT('Ctrl Pts',(30.2747213678695,1.48776626200004,20.0489426359701));
#57605=CARTESIAN_POINT('Ctrl Pts',(30.6499367323256,1.36617967610523,20.027512673167));
#57606=CARTESIAN_POINT('Ctrl Pts',(30.8236685705517,1.26902858360925,20.0164553547449));
#57607=CARTESIAN_POINT('Ctrl Pts',(31.1182297704941,1.01768973269335,19.9953016376572));
#57608=CARTESIAN_POINT('Ctrl Pts',(31.2380227260335,0.867983838688731,19.9857213243715));
#57609=CARTESIAN_POINT('Ctrl Pts',(31.4194655172301,0.52407745893419,19.9666154143852));
#57610=CARTESIAN_POINT('Ctrl Pts',(31.4763477416476,0.331530482038543,19.9559183601132));
#57611=CARTESIAN_POINT('Ctrl Pts',(31.5113890098208,-0.0605236259430762,
19.9341375763365));
#57612=CARTESIAN_POINT('Ctrl Pts',(31.4907606610887,-0.256127601642152,
19.9232706887976));
#57613=CARTESIAN_POINT('Ctrl Pts',(31.3770092904839,-0.62473058770716,19.9027927451274));
#57614=CARTESIAN_POINT('Ctrl Pts',(31.2864311739689,-0.794691675228615,
19.8939853466257));
#57615=CARTESIAN_POINT('Ctrl Pts',(31.0405043429371,-1.09883901947073,19.8737046491109));
#57616=CARTESIAN_POINT('Ctrl Pts',(30.8847013390568,-1.22775605549742,19.8626275448131));
#57617=CARTESIAN_POINT('Ctrl Pts',(30.5384592288504,-1.41320441242881,19.8408176202706));
#57618=CARTESIAN_POINT('Ctrl Pts',(30.3527481344157,-1.47060245170435,19.8302882010938));
#57619=CARTESIAN_POINT('Ctrl Pts',(30.1075898199807,-1.49710947656403,19.8177567099449));
#57620=CARTESIAN_POINT('Ctrl Pts',(30.0537655536404,-1.50000000000001,19.8150867964056));
#57621=CARTESIAN_POINT('Ctrl Pts',(30.0000000000003,-1.50000000000001,19.8125));
#57622=CARTESIAN_POINT('Origin',(30.,-1.32966554433622E-14,16.));
#57623=CARTESIAN_POINT('',(30.0000000000001,-1.50000000000001,19.25));
#57624=CARTESIAN_POINT('',(30.,-1.50000000000001,19.3125));
#57625=CARTESIAN_POINT('',(30.,-1.50000000000001,16.));
#57626=CARTESIAN_POINT('Ctrl Pts',(30.0000000000001,-1.50000000000001,19.25));
#57627=CARTESIAN_POINT('Ctrl Pts',(30.0322695745912,-1.50000000000001,19.2515525706314));
#57628=CARTESIAN_POINT('Ctrl Pts',(30.0645714825038,-1.49895869986435,19.2531356219044));
#57629=CARTESIAN_POINT('Ctrl Pts',(30.2882590679586,-1.48448482383795,19.2642998479893));
#57630=CARTESIAN_POINT('Ctrl Pts',(30.4754930135539,-1.43550485550641,19.2746687000727));
#57631=CARTESIAN_POINT('Ctrl Pts',(30.8281012978914,-1.26647563555772,19.2963288301724));
#57632=CARTESIAN_POINT('Ctrl Pts',(30.9888581275123,-1.14537453755813,19.3074271661326));
#57633=CARTESIAN_POINT('Ctrl Pts',(31.2489169787693,-0.852727854965852,
19.328068327964));
#57634=CARTESIAN_POINT('Ctrl Pts',(31.3477723438117,-0.685891580063111,
19.3368949122188));
#57635=CARTESIAN_POINT('Ctrl Pts',(31.4777710225729,-0.322229436301838,
19.35709836465));
#57636=CARTESIAN_POINT('Ctrl Pts',(31.5070120496637,-0.128613045958812,
19.3678548307802));
#57637=CARTESIAN_POINT('Ctrl Pts',(31.4899431617665,0.263827999699887,19.3896571110945));
#57638=CARTESIAN_POINT('Ctrl Pts',(31.4418890858574,0.458816520684437,19.4004898067048));
#57639=CARTESIAN_POINT('Ctrl Pts',(31.2763170645903,0.810606892156535,19.420033716231));
#57640=CARTESIAN_POINT('Ctrl Pts',(31.1635461572557,0.965528328551652,19.4291724240899));
#57641=CARTESIAN_POINT('Ctrl Pts',(30.8815440072885,1.22938524433353,19.4500696176279));
#57642=CARTESIAN_POINT('Ctrl Pts',(30.713328176096,1.33404197013925,19.4610700368521));
#57643=CARTESIAN_POINT('Ctrl Pts',(30.3423586225268,1.47407873960012,19.4828082280827));
#57644=CARTESIAN_POINT('Ctrl Pts',(30.1427440803289,1.50655371354715,19.4929501746347));
#57645=CARTESIAN_POINT('Ctrl Pts',(29.7515262729803,1.4915957790601,19.5121881483469));
#57646=CARTESIAN_POINT('Ctrl Pts',(29.563545020268,1.44778515274356,19.522449362427));
#57647=CARTESIAN_POINT('Ctrl Pts',(29.2074099124303,1.28891068317319,19.5439971005021));
#57648=CARTESIAN_POINT('Ctrl Pts',(29.0438038910602,1.17268375630169,19.5550971246218));
#57649=CARTESIAN_POINT('Ctrl Pts',(28.7751767012687,0.88721540741588,19.5759511326745));
#57650=CARTESIAN_POINT('Ctrl Pts',(28.6712044325382,0.722248138115754,19.5848751034381));
#57651=CARTESIAN_POINT('Ctrl Pts',(28.5314450700553,0.361647735614998,19.6049084591326));
#57652=CARTESIAN_POINT('Ctrl Pts',(28.4970926988021,0.169404578017586,19.6155886345547));
#57653=CARTESIAN_POINT('Ctrl Pts',(28.5033789257342,-0.222871075081128,
19.6373817263935));
#57654=CARTESIAN_POINT('Ctrl Pts',(28.5460751647458,-0.419126971559099,
19.6482848317533));
#57655=CARTESIAN_POINT('Ctrl Pts',(28.7020419000445,-0.77553505760853,19.6680852809783));
#57656=CARTESIAN_POINT('Ctrl Pts',(28.8106757232385,-0.933630997355151,
19.6770461367592));
#57657=CARTESIAN_POINT('Ctrl Pts',(29.0852161697017,-1.20477024704427,19.697786615973));
#57658=CARTESIAN_POINT('Ctrl Pts',(29.2500326897204,-1.31371406923191,19.7087425717726));
#57659=CARTESIAN_POINT('Ctrl Pts',(29.611734771314,-1.46197087611401,19.7302632159228));
#57660=CARTESIAN_POINT('Ctrl Pts',(29.8049901134984,-1.49999999359916,19.7406175822833));
#57661=CARTESIAN_POINT('Ctrl Pts',(29.9999999507652,-1.50000000000001,19.7499999976312));
#57662=CARTESIAN_POINT('Ctrl Pts',(30.0000000000003,-1.50000000000001,19.8125));
#57663=CARTESIAN_POINT('Ctrl Pts',(29.8589500630315,-1.50000000000001,19.8057137317435));
#57664=CARTESIAN_POINT('Ctrl Pts',(29.7183576297039,-1.48011045726929,19.7983969878431));
#57665=CARTESIAN_POINT('Ctrl Pts',(29.392433533781,-1.38562863633522,19.7800914624408));
#57666=CARTESIAN_POINT('Ctrl Pts',(29.2152602016442,-1.29355450601908,19.7690095917929));
#57667=CARTESIAN_POINT('Ctrl Pts',(28.9125224323809,-1.05055621120639,19.7476941614444));
#57668=CARTESIAN_POINT('Ctrl Pts',(28.7881027470448,-0.904173072558181,
19.7377318373643));
#57669=CARTESIAN_POINT('Ctrl Pts',(28.5965141205021,-0.565467385757126,
19.7189148547643));
#57670=CARTESIAN_POINT('Ctrl Pts',(28.5340212729776,-0.374707579896709,
19.708317087772));
#57671=CARTESIAN_POINT('Ctrl Pts',(28.4874198303467,0.0166598622973653,
19.6865744520946));
#57672=CARTESIAN_POINT('Ctrl Pts',(28.5024461232084,0.213342923270549,19.6756476153738));
#57673=CARTESIAN_POINT('Ctrl Pts',(28.605730933148,0.585021358101511,19.6549988134388));
#57674=CARTESIAN_POINT('Ctrl Pts',(28.6911262279336,0.757019946925095,19.6461115535275));
#57675=CARTESIAN_POINT('Ctrl Pts',(28.9280450078188,1.06829223859541,19.6260663408692));
#57676=CARTESIAN_POINT('Ctrl Pts',(29.0805347242822,1.20204064727676,19.6150144423906));
#57677=CARTESIAN_POINT('Ctrl Pts',(29.4223784266326,1.3977266885599,19.5931317562239));
#57678=CARTESIAN_POINT('Ctrl Pts',(29.6069366918152,1.46041214264913,19.5825109299366));
#57679=CARTESIAN_POINT('Ctrl Pts',(29.9906687655378,1.51247863508202,19.562602320475));
#57680=CARTESIAN_POINT('Ctrl Pts',(30.1862339040192,1.50100007477566,19.55356759697));
#57681=CARTESIAN_POINT('Ctrl Pts',(30.5662821795392,1.40308967236277,19.5325627823883));
#57682=CARTESIAN_POINT('Ctrl Pts',(30.7466285872712,1.31600734425417,19.5214669082421));
#57683=CARTESIAN_POINT('Ctrl Pts',(31.0570470506688,1.08124306107491,19.5000106628701));
#57684=CARTESIAN_POINT('Ctrl Pts',(31.185947420448,0.938076365153711,19.4898320882731));
#57685=CARTESIAN_POINT('Ctrl Pts',(31.387173884418,0.604359282145194,19.4708806565388));
#57686=CARTESIAN_POINT('Ctrl Pts',(31.4549913450499,0.415392173173207,19.460577342954));
#57687=CARTESIAN_POINT('Ctrl Pts',(31.5125364736871,0.0248207245632997,
19.4388789291423));
#57688=CARTESIAN_POINT('Ctrl Pts',(31.5028468405333,-0.172737498474235,
19.4279034723069));
#57689=CARTESIAN_POINT('Ctrl Pts',(31.4094808313587,-0.547250043493136,
19.4070972198059));
#57690=CARTESIAN_POINT('Ctrl Pts',(31.3288984144444,-0.721204660777261,
19.3980698586427));
#57691=CARTESIAN_POINT('Ctrl Pts',(31.1018991125715,-1.03700530321776,19.3783761095713));
#57692=CARTESIAN_POINT('Ctrl Pts',(30.9548507096631,-1.17379817492847,19.3675014379958));
#57693=CARTESIAN_POINT('Ctrl Pts',(30.6204358823266,-1.37933694163779,19.3457024869274));
#57694=CARTESIAN_POINT('Ctrl Pts',(30.4373267027344,-1.44785012953098,19.3349894983086));
#57695=CARTESIAN_POINT('Ctrl Pts',(30.1646733538461,-1.49322482781476,19.3206110496582));
#57696=CARTESIAN_POINT('Ctrl Pts',(30.0823180279059,-1.50000000000001,19.3164605279642));
#57697=CARTESIAN_POINT('Ctrl Pts',(30.,-1.50000000000001,19.3125));
#57698=CARTESIAN_POINT('Origin',(30.,-1.32966554433622E-14,16.));
#57699=CARTESIAN_POINT('',(30.0000000000001,-1.50000000000001,18.75));
#57700=CARTESIAN_POINT('',(30.,-1.50000000000001,18.8125));
#57701=CARTESIAN_POINT('',(30.,-1.50000000000001,16.));
#57702=CARTESIAN_POINT('Ctrl Pts',(30.0000000000002,-1.50000000000001,18.75));
#57703=CARTESIAN_POINT('Ctrl Pts',(30.0598815861698,-1.50000000000001,18.7528810541579));
#57704=CARTESIAN_POINT('Ctrl Pts',(30.1198247627216,-1.4964145214846,18.7558646682098));
#57705=CARTESIAN_POINT('Ctrl Pts',(30.3709807388755,-1.46613984657296,18.7687893789386));
#57706=CARTESIAN_POINT('Ctrl Pts',(30.5561899070999,-1.40635296128044,18.7793610060131));
#57707=CARTESIAN_POINT('Ctrl Pts',(30.9004833554958,-1.21627199481911,18.8012058591186));
#57708=CARTESIAN_POINT('Ctrl Pts',(31.054808880873,-1.08516465668695,18.8122727199239));
#57709=CARTESIAN_POINT('Ctrl Pts',(31.2966795386424,-0.777790002612556,
18.832447912207));
#57710=CARTESIAN_POINT('Ctrl Pts',(31.3849156897549,-0.606916752329299,
18.8412824026485));
#57711=CARTESIAN_POINT('Ctrl Pts',(31.4939654845851,-0.236921615045211,
18.8618376880532));
#57712=CARTESIAN_POINT('Ctrl Pts',(31.5120817444602,-0.0408132290769898,
18.8727325983848));
#57713=CARTESIAN_POINT('Ctrl Pts',(31.4718441015158,0.350974679810523,18.8944985933229));
#57714=CARTESIAN_POINT('Ctrl Pts',(31.4124332725198,0.54273929222595,18.9051521829016));
#57715=CARTESIAN_POINT('Ctrl Pts',(31.2264254338517,0.884320880490274,18.9241289378051));
#57716=CARTESIAN_POINT('Ctrl Pts',(31.1045648671413,1.03253115218655,18.9338713522791));
#57717=CARTESIAN_POINT('Ctrl Pts',(30.8063387149155,1.2801510812434,18.9550980960807));
#57718=CARTESIAN_POINT('Ctrl Pts',(30.6310491381331,1.37504484021148,18.9661676575249));
#57719=CARTESIAN_POINT('Ctrl Pts',(30.2546711108962,1.4912245976519,18.9875033692879));
#57720=CARTESIAN_POINT('Ctrl Pts',(30.05740041095,1.51172051693628,18.9969127515258));
#57721=CARTESIAN_POINT('Ctrl Pts',(29.6702738320324,1.47589654334487,19.0165334981157));
#57722=CARTESIAN_POINT('Ctrl Pts',(29.4839742576828,1.42150925053353,19.0270075986994));
#57723=CARTESIAN_POINT('Ctrl Pts',(29.1353660189379,1.24191643228194,19.048768709802));
#57724=CARTESIAN_POINT('Ctrl Pts',(28.9777462443354,1.1157773991078,19.059856056776));
#57725=CARTESIAN_POINT('Ctrl Pts',(28.7267374929236,0.815719209989595,19.0802676706567));
#57726=CARTESIAN_POINT('Ctrl Pts',(28.6332044534767,0.64688991790973,19.0890616712273));
#57727=CARTESIAN_POINT('Ctrl Pts',(28.5135873974093,0.280047942578678,19.109441780968));
#57728=CARTESIAN_POINT('Ctrl Pts',(28.4898364137009,0.0851180238092936,
19.1202712208996));
#57729=CARTESIAN_POINT('Ctrl Pts',(28.5183897482981,-0.307171243363851,
19.1420650690759));
#57730=CARTESIAN_POINT('Ctrl Pts',(28.5720998196786,-0.500646940480604,
19.1528137189157));
#57731=CARTESIAN_POINT('Ctrl Pts',(28.747829861517,-0.847427013151625,19.1720792785085));
#57732=CARTESIAN_POINT('Ctrl Pts',(28.8650664758991,-0.999006868470888,
19.1814790094866));
#57733=CARTESIAN_POINT('Ctrl Pts',(29.1550741400796,-1.25492382568339,19.2025408141021));
#57734=CARTESIAN_POINT('Ctrl Pts',(29.3268372187205,-1.35483766663846,19.2135801535473));
#57735=CARTESIAN_POINT('Ctrl Pts',(29.6699517271029,-1.47262040644266,19.2333600008011));
#57736=CARTESIAN_POINT('Ctrl Pts',(29.8345144389513,-1.50000000000001,19.2420380722318));
#57737=CARTESIAN_POINT('Ctrl Pts',(30.0000000000001,-1.50000000000001,19.25));
#57738=CARTESIAN_POINT('Ctrl Pts',(30.,-1.50000000000001,19.3125));
#57739=CARTESIAN_POINT('Ctrl Pts',(29.8904115959066,-1.50000000000001,19.3072274254497));
#57740=CARTESIAN_POINT('Ctrl Pts',(29.7809217474217,-1.48799325955223,19.3016260720903));
#57741=CARTESIAN_POINT('Ctrl Pts',(29.479267613868,-1.42071467340943,19.2852438812078));
#57742=CARTESIAN_POINT('Ctrl Pts',(29.2956191224553,-1.33919024824593,19.2741435216794));
#57743=CARTESIAN_POINT('Ctrl Pts',(28.9769843310201,-1.11359538988626,19.2525466742853));
#57744=CARTESIAN_POINT('Ctrl Pts',(28.8433197059369,-0.97404728751911,19.2422393958357));
#57745=CARTESIAN_POINT('Ctrl Pts',(28.6314369352188,-0.64558462894177,19.2229212185382));
#57746=CARTESIAN_POINT('Ctrl Pts',(28.5578261508896,-0.458159789494097,
19.2129533216385));
#57747=CARTESIAN_POINT('Ctrl Pts',(28.4887314396478,-0.0683254796838233,
19.1912958599824));
#57748=CARTESIAN_POINT('Ctrl Pts',(28.4927829468086,0.129998312926432,19.180277871504));
#57749=CARTESIAN_POINT('Ctrl Pts',(28.5757061903925,0.507408017565263,19.1593106656908));
#57750=CARTESIAN_POINT('Ctrl Pts',(28.6513157241137,0.683452060166118,19.1500704896955));
#57751=CARTESIAN_POINT('Ctrl Pts',(28.8692063981292,1.00541452618758,19.1306438179201));
#57752=CARTESIAN_POINT('Ctrl Pts',(29.0123062748592,1.14629480240063,19.119845580885));
#57753=CARTESIAN_POINT('Ctrl Pts',(29.3411837772215,1.36149831072911,19.0980445794436));
#57754=CARTESIAN_POINT('Ctrl Pts',(29.5228193452006,1.43527924918368,19.0872561635921));
#57755=CARTESIAN_POINT('Ctrl Pts',(29.9017346505858,1.50901487689319,19.0669773805809));
#57756=CARTESIAN_POINT('Ctrl Pts',(30.095243866884,1.50920856983617,19.0581733709244));
#57757=CARTESIAN_POINT('Ctrl Pts',(30.4795337547919,1.43522535350299,19.0376291257293));
#57758=CARTESIAN_POINT('Ctrl Pts',(30.6659951148259,1.35877256279477,19.0265343107311));
#57759=CARTESIAN_POINT('Ctrl Pts',(30.9917525251624,1.14161337833726,19.0048291004505));
#57760=CARTESIAN_POINT('Ctrl Pts',(31.12959203788,1.00543319777699,18.9944145110095));
#57761=CARTESIAN_POINT('Ctrl Pts',(31.3495099297643,0.683969951441068,18.9749041718824));
#57762=CARTESIAN_POINT('Ctrl Pts',(31.4277388995994,0.500572833869038,18.9653096018815));
#57763=CARTESIAN_POINT('Ctrl Pts',(31.5085610210805,0.114360476914036,18.9438533598284));
#57764=CARTESIAN_POINT('Ctrl Pts',(31.510521839189,-0.0846024989690804,
18.9327998611683));
#57765=CARTESIAN_POINT('Ctrl Pts',(31.4387139095947,-0.464995267712227,
18.9116669295714));
#57766=CARTESIAN_POINT('Ctrl Pts',(31.3683024334794,-0.643299822803022,
18.9021297086694));
#57767=CARTESIAN_POINT('Ctrl Pts',(31.1599775839064,-0.97159308723095,18.8829874173259));
#57768=CARTESIAN_POINT('Ctrl Pts',(31.021122395481,-1.11661364586043,18.8722783951071));
#57769=CARTESIAN_POINT('Ctrl Pts',(30.6983237124874,-1.34174379218127,18.8504941210548));
#57770=CARTESIAN_POINT('Ctrl Pts',(30.5183853004494,-1.42099198981035,18.8396354913461));
#57771=CARTESIAN_POINT('Ctrl Pts',(30.220307982392,-1.48785706899676,18.8234368763837));
#57772=CARTESIAN_POINT('Ctrl Pts',(30.1102084329115,-1.50000000000001,18.8178024057007));
#57773=CARTESIAN_POINT('Ctrl Pts',(30.,-1.50000000000001,18.8125));
#57774=CARTESIAN_POINT('Origin',(30.,-1.32966554433622E-14,16.));
#57775=CARTESIAN_POINT('',(30.,-1.50000000000001,18.25));
#57776=CARTESIAN_POINT('',(29.9999999999999,-1.50000000000001,18.3125));
#57777=CARTESIAN_POINT('',(30.,-1.50000000000001,16.));
#57778=CARTESIAN_POINT('Ctrl Pts',(30.,-1.50000000000001,18.25));
#57779=CARTESIAN_POINT('Ctrl Pts',(30.0882156275205,-1.50000000000001,18.254244276358));
#57780=CARTESIAN_POINT('Ctrl Pts',(30.1764501130872,-1.49221937550789,18.2587055884823));
#57781=CARTESIAN_POINT('Ctrl Pts',(30.4546079281867,-1.44254775409159,18.2734682298626));
#57782=CARTESIAN_POINT('Ctrl Pts',(30.6370980720641,-1.37175281599007,18.2842148170619));
#57783=CARTESIAN_POINT('Ctrl Pts',(30.9691525442989,-1.16201577961996,18.3060168240942));
#57784=CARTESIAN_POINT('Ctrl Pts',(31.1145075241426,-1.02344071977941,18.3168595260404));
#57785=CARTESIAN_POINT('Ctrl Pts',(31.3375735551139,-0.704962761586156,
18.3364384054093));
#57786=CARTESIAN_POINT('Ctrl Pts',(31.4160050795816,-0.530113102524481,
18.345549272082));
#57787=CARTESIAN_POINT('Ctrl Pts',(31.5048780292219,-0.154342998497877,
18.3664253889724));
#57788=CARTESIAN_POINT('Ctrl Pts',(31.5121437205665,0.0435642244476196,
18.3774202346916));
#57789=CARTESIAN_POINT('Ctrl Pts',(31.4493976248982,0.435280459623824,18.3991822477569));
#57790=CARTESIAN_POINT('Ctrl Pts',(31.3782925123276,0.624894161678516,18.4093783750732));
#57791=CARTESIAN_POINT('Ctrl Pts',(31.1707210215853,0.957071364942045,18.428592307613));
#57792=CARTESIAN_POINT('Ctrl Pts',(31.0393074800838,1.09835818528463,18.4388395784748));
#57793=CARTESIAN_POINT('Ctrl Pts',(30.7245434883219,1.32834442072559,18.4603721746294));
#57794=CARTESIAN_POINT('Ctrl Pts',(30.5424433469957,1.41252449906513,18.4714718072734));
#57795=CARTESIAN_POINT('Ctrl Pts',(30.1611576166725,1.50380428740964,18.492351975203));
#57796=CARTESIAN_POINT('Ctrl Pts',(29.9661847612145,1.51203572283979,18.5012926108002));
#57797=CARTESIAN_POINT('Ctrl Pts',(29.583743920727,1.45401144673963,18.5213045897645));
#57798=CARTESIAN_POINT('Ctrl Pts',(29.3999206687447,1.38827539073469,18.5319747916547));
#57799=CARTESIAN_POINT('Ctrl Pts',(29.0627111089636,1.18787072518152,18.5537655904295));
#57800=CARTESIAN_POINT('Ctrl Pts',(28.9136362676481,1.05327089433686,18.5646768412665));
#57801=CARTESIAN_POINT('Ctrl Pts',(28.6818733006966,0.740747545450625,18.5845087463487));
#57802=CARTESIAN_POINT('Ctrl Pts',(28.5986773683508,0.567862991064222,18.593452056052));
#57803=CARTESIAN_POINT('Ctrl Pts',(28.4999017481138,0.194886335563048,18.6141729813576));
#57804=CARTESIAN_POINT('Ctrl Pts',(28.4872987443723,-0.0022124298529334,
18.6251229127696));
#57805=CARTESIAN_POINT('Ctrl Pts',(28.538885584329,-0.393300822235859,18.6468500456797));
#57806=CARTESIAN_POINT('Ctrl Pts',(28.6038229043615,-0.583241208522858,
18.6573608761808));
#57807=CARTESIAN_POINT('Ctrl Pts',(28.7997809979745,-0.919686600601166,
18.6761346196911));
#57808=CARTESIAN_POINT('Ctrl Pts',(28.9262538190534,-1.06460970419426,18.6862451878989));
#57809=CARTESIAN_POINT('Ctrl Pts',(29.2324514589516,-1.30386842227857,18.7076232042196));
#57810=CARTESIAN_POINT('Ctrl Pts',(29.4110795308611,-1.39369344460164,18.7187125908454));
#57811=CARTESIAN_POINT('Ctrl Pts',(29.7319270119205,-1.48199126728517,18.7366020897721));
#57812=CARTESIAN_POINT('Ctrl Pts',(29.8657845574029,-1.50000000000001,18.7435425565073));
#57813=CARTESIAN_POINT('Ctrl Pts',(30.0000000000002,-1.50000000000001,18.75));
#57814=CARTESIAN_POINT('Ctrl Pts',(30.,-1.50000000000001,18.8125));
#57815=CARTESIAN_POINT('Ctrl Pts',(29.9200694828282,-1.50000000000001,18.8086543411995));
#57816=CARTESIAN_POINT('Ctrl Pts',(29.8400989517173,-1.4936120985387,18.8046293155201));
#57817=CARTESIAN_POINT('Ctrl Pts',(29.5632380932733,-1.44889785862683,18.7900667790378));
#57818=CARTESIAN_POINT('Ctrl Pts',(29.3740258977232,-1.377754564609,18.7789871004233));
#57819=CARTESIAN_POINT('Ctrl Pts',(29.041174726881,-1.16949277461302,18.7571877412774));
#57820=CARTESIAN_POINT('Ctrl Pts',(28.8991316339595,-1.03690216726548,18.7466706173565));
#57821=CARTESIAN_POINT('Ctrl Pts',(28.6710550609186,-0.722648191218263,
18.7269680010074));
#57822=CARTESIAN_POINT('Ctrl Pts',(28.5881967902834,-0.543266122771758,
18.717681451265));
#57823=CARTESIAN_POINT('Ctrl Pts',(28.4956085723343,-0.160873384602161,
18.6964374102556));
#57824=CARTESIAN_POINT('Ctrl Pts',(28.4875239735192,0.0385552236194734,
18.6853580431322));
#57825=CARTESIAN_POINT('Ctrl Pts',(28.5480104653806,0.421875716785893,18.6640624601785));
#57826=CARTESIAN_POINT('Ctrl Pts',(28.6132160700899,0.602522755625134,18.6541515963916));
#57827=CARTESIAN_POINT('Ctrl Pts',(28.8119377533085,0.937035677616922,18.635298569339));
#57828=CARTESIAN_POINT('Ctrl Pts',(28.9464389491764,1.08605274148643,18.6246880146503));
#57829=CARTESIAN_POINT('Ctrl Pts',(29.2628767471001,1.32090830831045,18.6029396282541));
#57830=CARTESIAN_POINT('Ctrl Pts',(29.4409618987283,1.40557199772365,18.5920197332512));
#57831=CARTESIAN_POINT('Ctrl Pts',(29.814809484317,1.50065373381321,18.5713918235674));
#57832=CARTESIAN_POINT('Ctrl Pts',(30.0065604479866,1.51202122412194,18.5625182831912));
#57833=CARTESIAN_POINT('Ctrl Pts',(30.3943911928229,1.4610824148403,18.5424438008558));
#57834=CARTESIAN_POINT('Ctrl Pts',(30.58616263238,1.39524271133166,18.5313883125152));
#57835=CARTESIAN_POINT('Ctrl Pts',(30.9257469654151,1.19593240245758,18.5095136562056));
#57836=CARTESIAN_POINT('Ctrl Pts',(31.0718264769195,1.06698913560375,18.4989036450188));
#57837=CARTESIAN_POINT('Ctrl Pts',(31.3078217753803,0.759832047419874,18.4790171745892));
#57838=CARTESIAN_POINT('Ctrl Pts',(31.3951262846915,0.584269865007977,18.4699594369449));
#57839=CARTESIAN_POINT('Ctrl Pts',(31.4989966927882,0.205709858638526,18.4489283254799));
#57840=CARTESIAN_POINT('Ctrl Pts',(31.5130318328004,0.00600577899638372,
18.4378336543887));
#57841=CARTESIAN_POINT('Ctrl Pts',(31.4635867359632,-0.379900299649008,
18.4163944277973));
#57842=CARTESIAN_POINT('Ctrl Pts',(31.4034385131977,-0.562844950250642,
18.4062308360972));
#57843=CARTESIAN_POINT('Ctrl Pts',(31.213924427377,-0.903263174389702,18.387318712534));
#57844=CARTESIAN_POINT('Ctrl Pts',(31.0836707542498,-1.05603307941032,18.3769705479341));
#57845=CARTESIAN_POINT('Ctrl Pts',(30.7734274797909,-1.30006438227702,18.3552653141303));
#57846=CARTESIAN_POINT('Ctrl Pts',(30.5972523067208,-1.389838711312,18.3442953508018));
#57847=CARTESIAN_POINT('Ctrl Pts',(30.27555179434,-1.4809632576453,18.3262862902852));
#57848=CARTESIAN_POINT('Ctrl Pts',(30.1379932399681,-1.50000000000003,18.3191392028535));
#57849=CARTESIAN_POINT('Ctrl Pts',(29.9999999999998,-1.50000000000001,18.3125));
#57850=CARTESIAN_POINT('Origin',(30.,-1.32966554433622E-14,16.));
#57851=CARTESIAN_POINT('',(30.,-1.50000000000001,17.75));
#57852=CARTESIAN_POINT('',(30.,-1.50000000000001,17.8125));
#57853=CARTESIAN_POINT('',(30.,-1.50000000000001,16.));
#57854=CARTESIAN_POINT('Ctrl Pts',(30.,-1.50000000000001,17.75));
#57855=CARTESIAN_POINT('Ctrl Pts',(30.1165214576707,-1.50000000000002,17.755606141246));
#57856=CARTESIAN_POINT('Ctrl Pts',(30.2328774102524,-1.48642630258387,17.7615813667753));
#57857=CARTESIAN_POINT('Ctrl Pts',(30.5364815251301,-1.41429282343802,17.778192234317));
#57858=CARTESIAN_POINT('Ctrl Pts',(30.7156172892318,-1.33263663661631,17.7890791351975));
#57859=CARTESIAN_POINT('Ctrl Pts',(31.0356297737271,-1.1031687507031,17.8108498509785));
#57860=CARTESIAN_POINT('Ctrl Pts',(31.1725674881258,-0.956358157459637,
17.8215163418689));
#57861=CARTESIAN_POINT('Ctrl Pts',(31.376639002963,-0.625293846242278,17.8405309680715));
#57862=CARTESIAN_POINT('Ctrl Pts',(31.4447439774106,-0.445961069817197,
17.8502243850103));
#57863=CARTESIAN_POINT('Ctrl Pts',(31.5115582160321,-0.0642628969545898,
17.8714298390582));
#57864=CARTESIAN_POINT('Ctrl Pts',(31.5068955968845,0.134928419608339,17.8824960233117));
#57865=CARTESIAN_POINT('Ctrl Pts',(31.4208614242251,0.519471460613856,17.9038595255897));
#57866=CARTESIAN_POINT('Ctrl Pts',(31.3405819882652,0.701086441059189,17.9133091757132));
#57867=CARTESIAN_POINT('Ctrl Pts',(31.1170623100669,1.01937978501502,17.9329047530211));
#57868=CARTESIAN_POINT('Ctrl Pts',(30.9773620677606,1.15399638378434,17.9433654340287));
#57869=CARTESIAN_POINT('Ctrl Pts',(30.6484546459992,1.36726868066811,17.9651142302054));
#57870=CARTESIAN_POINT('Ctrl Pts',(30.4607652253454,1.44139714446346,17.9762035656613));
#57871=CARTESIAN_POINT('Ctrl Pts',(30.0756449322311,1.51026934438856,17.9966457910675));
#57872=CARTESIAN_POINT('Ctrl Pts',(29.8825476840369,1.50759466650969,18.005439964228));
#57873=CARTESIAN_POINT('Ctrl Pts',(29.5047175214704,1.42916638864856,18.025796889674));
#57874=CARTESIAN_POINT('Ctrl Pts',(29.323805468645,1.35298625851431,18.0366171395998));
#57875=CARTESIAN_POINT('Ctrl Pts',(28.9975535579724,1.13341344377778,18.0584131868245));
#57876=CARTESIAN_POINT('Ctrl Pts',(28.8562978602342,0.990703384015885,18.0691735230773));
#57877=CARTESIAN_POINT('Ctrl Pts',(28.6425900107442,0.665955504210131,18.088476321219));
#57878=CARTESIAN_POINT('Ctrl Pts',(28.5692557712623,0.488931672930093,18.0978371292817));
#57879=CARTESIAN_POINT('Ctrl Pts',(28.4911736103312,0.110209786397706,18.118877234089));
#57880=CARTESIAN_POINT('Ctrl Pts',(28.4897399259643,-0.0884146511275797,
18.1299119250627));
#57881=CARTESIAN_POINT('Ctrl Pts',(28.563963673652,-0.476687925939349,18.1514826625522));
#57882=CARTESIAN_POINT('Ctrl Pts',(28.6395954743022,-0.662348456736596,
18.1612794083161));
#57883=CARTESIAN_POINT('Ctrl Pts',(28.8549808751967,-0.987772207975308,
18.1806816918938));
#57884=CARTESIAN_POINT('Ctrl Pts',(28.9904690556508,-1.12587258901724,18.1910364917109));
#57885=CARTESIAN_POINT('Ctrl Pts',(29.3122241078786,-1.34783032180127,18.2126824314563));
#57886=CARTESIAN_POINT('Ctrl Pts',(29.4971108100191,-1.42716337813628,18.2237814930698));
#57887=CARTESIAN_POINT('Ctrl Pts',(29.7935943795659,-1.48934588454492,18.2397733573052));
#57888=CARTESIAN_POINT('Ctrl Pts',(29.8967698772032,-1.50000000000001,18.2450333384012));
#57889=CARTESIAN_POINT('Ctrl Pts',(30.,-1.50000000000001,18.25));
#57890=CARTESIAN_POINT('Ctrl Pts',(29.9999999999998,-1.50000000000001,18.3125));
#57891=CARTESIAN_POINT('Ctrl Pts',(29.9486057940186,-1.50000000000001,18.3100272951118));
#57892=CARTESIAN_POINT('Ctrl Pts',(29.8971583803719,-1.4973588143077,18.3074786639994));
#57893=CARTESIAN_POINT('Ctrl Pts',(29.6480074739756,-1.47161947014145,18.294776403644));
#57894=CARTESIAN_POINT('Ctrl Pts',(29.4562105276991,-1.41203266981329,18.2838933798658));
#57895=CARTESIAN_POINT('Ctrl Pts',(29.1116733937691,-1.22407639141983,18.2620958215476));
#57896=CARTESIAN_POINT('Ctrl Pts',(28.9612380534891,-1.09930641465076,18.2513921651757));
#57897=CARTESIAN_POINT('Ctrl Pts',(28.7165798694464,-0.800027931931824,
18.231307751621));
#57898=CARTESIAN_POINT('Ctrl Pts',(28.6244510402799,-0.628553460673264,
18.2224196367041));
#57899=CARTESIAN_POINT('Ctrl Pts',(28.5083938755392,-0.254315567480426,
18.2016286426378));
#57900=CARTESIAN_POINT('Ctrl Pts',(28.4878541874048,-0.054508044740069,
18.1905282247078));
#57901=CARTESIAN_POINT('Ctrl Pts',(28.5251827599344,0.333985841156563,18.1689452310469));
#57902=CARTESIAN_POINT('Ctrl Pts',(28.5797880070138,0.519280463308488,18.1586510853718));
#57903=CARTESIAN_POINT('Ctrl Pts',(28.7594942565881,0.866593796413574,18.1393559001993));
#57904=CARTESIAN_POINT('Ctrl Pts',(28.8856977548396,1.02381782162173,18.1293391744996));
#57905=CARTESIAN_POINT('Ctrl Pts',(29.1898211855382,1.2775694571787,18.1076583725746));
#57906=CARTESIAN_POINT('Ctrl Pts',(29.3638803222543,1.37256230066096,18.096645258358));
#57907=CARTESIAN_POINT('Ctrl Pts',(29.732534735318,1.48813273455022,18.0756980748094));
#57908=CARTESIAN_POINT('Ctrl Pts',(29.9228794435952,1.51000349618475,18.066488339394));
#57909=CARTESIAN_POINT('Ctrl Pts',(30.3105607244676,1.48091384388274,18.0470279691741));
#57910=CARTESIAN_POINT('Ctrl Pts',(30.5039294602603,1.4267400893485,18.0362196850207));
#57911=CARTESIAN_POINT('Ctrl Pts',(30.8540539626656,1.24831186951753,18.0144179726049));
#57912=CARTESIAN_POINT('Ctrl Pts',(31.0082947964679,1.12740587313612,18.0036385571291));
#57913=CARTESIAN_POINT('Ctrl Pts',(31.2606439376435,0.835225571389926,17.9833812839205));
#57914=CARTESIAN_POINT('Ctrl Pts',(31.3570327509323,0.667298431844612,17.9745721351024));
#57915=CARTESIAN_POINT('Ctrl Pts',(31.4837741625619,0.297001147228916,17.9540000637349));
#57916=CARTESIAN_POINT('Ctrl Pts',(31.5100733842477,0.0972732161684081,
17.9429040675649));
#57917=CARTESIAN_POINT('Ctrl Pts',(31.4835317838137,-0.293194316444828,
17.9212114268642));
#57918=CARTESIAN_POINT('Ctrl Pts',(31.4338905957024,-0.480424140062753,
17.9108097699965));
#57919=CARTESIAN_POINT('Ctrl Pts',(31.2642037542022,-0.83118542637216,17.8913230318682));
#57920=CARTESIAN_POINT('Ctrl Pts',(31.14378015867,-0.99038786521744,17.8816860411746));
#57921=CARTESIAN_POINT('Ctrl Pts',(30.8486060826855,-1.25246692848107,17.8602044978428));
#57922=CARTESIAN_POINT('Ctrl Pts',(30.6769673305094,-1.35296725332812,17.8491548488382));
#57923=CARTESIAN_POINT('Ctrl Pts',(30.3327732686651,-1.47215364288648,17.8292840712733));
#57924=CARTESIAN_POINT('Ctrl Pts',(30.1668871533766,-1.50000000000002,17.8205293619105));
#57925=CARTESIAN_POINT('Ctrl Pts',(29.9999999999999,-1.50000000000001,17.8125));
#57926=CARTESIAN_POINT('Origin',(30.,-1.32966554433622E-14,16.));
#57927=CARTESIAN_POINT('',(29.9999999999999,-1.50000000000001,17.25));
#57928=CARTESIAN_POINT('',(30.,-1.50000000000001,17.3125));
#57929=CARTESIAN_POINT('',(30.,-1.50000000000001,16.));
#57930=CARTESIAN_POINT('Ctrl Pts',(29.9999999999998,-1.50000000000001,17.25));
#57931=CARTESIAN_POINT('Ctrl Pts',(30.1437406795734,-1.50000000000003,17.2569157266704));
#57932=CARTESIAN_POINT('Ctrl Pts',(30.2869532673798,-1.47934432155244,17.2643798143597));
#57933=CARTESIAN_POINT('Ctrl Pts',(30.6133040117111,-1.38286217393555,17.2827614315232));
#57934=CARTESIAN_POINT('Ctrl Pts',(30.7886268831202,-1.29093521604786,17.2937501837148));
#57935=CARTESIAN_POINT('Ctrl Pts',(31.0976621700988,-1.04186059007729,17.3155373905022));
#57936=CARTESIAN_POINT('Ctrl Pts',(31.2270940102629,-0.885739363684009,
17.3257922575731));
#57937=CARTESIAN_POINT('Ctrl Pts',(31.4122925189225,-0.540349731904653,
17.3449805704497));
#57938=CARTESIAN_POINT('Ctrl Pts',(31.4695815451721,-0.356167506723217,
17.3552129162933));
#57939=CARTESIAN_POINT('Ctrl Pts',(31.5127670349393,0.0311250181831806,
17.376729167677));
#57940=CARTESIAN_POINT('Ctrl Pts',(31.4953668358477,0.230908289106308,17.3878282382838));
#57941=CARTESIAN_POINT('Ctrl Pts',(31.3851742993692,0.607249385403804,17.408736076967));
#57942=CARTESIAN_POINT('Ctrl Pts',(31.2953707932844,0.78068569360338,17.4176954906944));
#57943=CARTESIAN_POINT('Ctrl Pts',(31.054895847731,1.08378386704463,17.4376847406135));
#57944=CARTESIAN_POINT('Ctrl Pts',(30.9065553840191,1.21059289157644,17.4483442474051));
#57945=CARTESIAN_POINT('Ctrl Pts',(30.5651448786952,1.40362381134034,17.4701323379946));
#57946=CARTESIAN_POINT('Ctrl Pts',(30.3742618691092,1.46611551598061,17.4810520817598));
#57947=CARTESIAN_POINT('Ctrl Pts',(29.9878426931301,1.51196372025337,17.5009172442622));
#57948=CARTESIAN_POINT('Ctrl Pts',(29.7964276873605,1.49824842026232,17.5098430324513));
#57949=CARTESIAN_POINT('Ctrl Pts',(29.423704438961,1.39861791618851,17.5305432021031));
#57950=CARTESIAN_POINT('Ctrl Pts',(29.2464613140656,1.31164870813791,17.5414866272603));
#57951=CARTESIAN_POINT('Ctrl Pts',(28.9327465597656,1.07261781027188,17.5632199825769));
#57952=CARTESIAN_POINT('Ctrl Pts',(28.8001758891987,0.921899105215767,17.5737833830436));
#57953=CARTESIAN_POINT('Ctrl Pts',(28.6055876448106,0.584753731199478,17.5925136816001));
#57954=CARTESIAN_POINT('Ctrl Pts',(28.5426610065469,0.403064732761888,17.6026075148466));
#57955=CARTESIAN_POINT('Ctrl Pts',(28.487113056257,0.0186136653436067,17.623965907481));
#57956=CARTESIAN_POINT('Ctrl Pts',(28.4978576022209,-0.180959534499292,
17.6350533074722));
#57957=CARTESIAN_POINT('Ctrl Pts',(28.5955062015491,-0.561653522812593,
17.6562029734896));
#57958=CARTESIAN_POINT('Ctrl Pts',(28.6803571582567,-0.739318323214391,
17.6653786075964));
#57959=CARTESIAN_POINT('Ctrl Pts',(28.9119736981394,-1.05041195534416,17.6851637533487));
#57960=CARTESIAN_POINT('Ctrl Pts',(29.0558270731865,-1.1813919096406,17.6957232341464));
#57961=CARTESIAN_POINT('Ctrl Pts',(29.3917078154049,-1.38569020760041,17.7175582566121));
#57962=CARTESIAN_POINT('Ctrl Pts',(29.5820781032457,-1.45448064464283,17.7286282968298));
#57963=CARTESIAN_POINT('Ctrl Pts',(29.8532284268276,-1.49461899708891,17.7427889770903));
#57964=CARTESIAN_POINT('Ctrl Pts',(29.9266397495672,-1.50000000000001,17.7464704533054));
#57965=CARTESIAN_POINT('Ctrl Pts',(30.,-1.50000000000001,17.75));
#57966=CARTESIAN_POINT('Ctrl Pts',(29.9999999999999,-1.50000000000001,17.8125));
#57967=CARTESIAN_POINT('Ctrl Pts',(29.9772840745252,-1.50000000000001,17.811407079526));
#57968=CARTESIAN_POINT('Ctrl Pts',(29.9545509622526,-1.49948399224778,17.8102989986031));
#57969=CARTESIAN_POINT('Ctrl Pts',(29.7331702393738,-1.48941079200354,17.7993680024896));
#57970=CARTESIAN_POINT('Ctrl Pts',(29.5383211874472,-1.44096198242896,17.7886475228419));
#57971=CARTESIAN_POINT('Ctrl Pts',(29.1826189299973,-1.27271128807371,17.7668601596023));
#57972=CARTESIAN_POINT('Ctrl Pts',(29.0244894301944,-1.15598200374574,17.7560096703756));
#57973=CARTESIAN_POINT('Ctrl Pts',(28.764135320164,-0.871290254073719,17.7355752732588));
#57974=CARTESIAN_POINT('Ctrl Pts',(28.6633306533142,-0.706980266162622,
17.7267766814534));
#57975=CARTESIAN_POINT('Ctrl Pts',(28.5256044330412,-0.340872542641299,
17.70643736348));
#57976=CARTESIAN_POINT('Ctrl Pts',(28.4933384090279,-0.141395913779689,
17.6953553285433));
#57977=CARTESIAN_POINT('Ctrl Pts',(28.5086475773052,0.250803035896437,17.6735664980057));
#57978=CARTESIAN_POINT('Ctrl Pts',(28.5530910089168,0.439894111123241,17.6630614382709));
#57979=CARTESIAN_POINT('Ctrl Pts',(28.7124602775381,0.794124581104987,17.6433819677164));
#57980=CARTESIAN_POINT('Ctrl Pts',(28.8270773285161,0.955330804312479,17.6340619682235));
#57981=CARTESIAN_POINT('Ctrl Pts',(29.1130611662184,1.22571784831621,17.6127918131944));
#57982=CARTESIAN_POINT('Ctrl Pts',(29.2820600929988,1.33176716482588,17.6017150341911));
#57983=CARTESIAN_POINT('Ctrl Pts',(29.6446531268203,1.46968030941703,17.5804388480344));
#57984=CARTESIAN_POINT('Ctrl Pts',(29.8337664889299,1.50284763615596,17.5705770145346));
#57985=CARTESIAN_POINT('Ctrl Pts',(30.2227595353817,1.49663210693258,17.5516889242716));
#57986=CARTESIAN_POINT('Ctrl Pts',(30.4189176611452,1.45396403183943,17.5410660377374));
#57987=CARTESIAN_POINT('Ctrl Pts',(30.7799134803451,1.29609345193241,17.5193123244018));
#57988=CARTESIAN_POINT('Ctrl Pts',(30.9418307309724,1.18367445855365,17.5083993272327));
#57989=CARTESIAN_POINT('Ctrl Pts',(31.2101475557693,0.906543829758461,17.4877918549585));
#57990=CARTESIAN_POINT('Ctrl Pts',(31.3153431699375,0.745751786456619,17.478930654803));
#57991=CARTESIAN_POINT('Ctrl Pts',(31.463864637894,0.383898047749162,17.4588276693193));
#57992=CARTESIAN_POINT('Ctrl Pts',(31.5020303054666,0.184838532612863,17.4477688073673));
#57993=CARTESIAN_POINT('Ctrl Pts',(31.4978841524782,-0.208759642694536,
17.4259022420724));
#57994=CARTESIAN_POINT('Ctrl Pts',(31.4586348080642,-0.399547636290809,
17.4153029090948));
#57995=CARTESIAN_POINT('Ctrl Pts',(31.3094217036004,-0.757113584921528,
17.3954381341709));
#57996=CARTESIAN_POINT('Ctrl Pts',(31.200380183046,-0.920271802442848,17.3863568795276));
#57997=CARTESIAN_POINT('Ctrl Pts',(30.923406682912,-1.19858244148629,17.3653001347046));
#57998=CARTESIAN_POINT('Ctrl Pts',(30.7571425046312,-1.30996529750999,17.3542067774745));
#57999=CARTESIAN_POINT('Ctrl Pts',(30.3978227489156,-1.45880886920802,17.3327844540089));
#58000=CARTESIAN_POINT('Ctrl Pts',(30.2092450764931,-1.49754020852369,17.3226356359777));
#58001=CARTESIAN_POINT('Ctrl Pts',(30.0122952852091,-1.49996221637769,17.3130926067305));
#58002=CARTESIAN_POINT('Ctrl Pts',(30.0061468402235,-1.50000000000001,17.3127957399881));
#58003=CARTESIAN_POINT('Ctrl Pts',(30.,-1.50000000000001,17.3125));
#58004=CARTESIAN_POINT('Origin',(30.,-1.32966554433622E-14,16.));
#58005=CARTESIAN_POINT('',(30.,-1.50000000000001,16.75));
#58006=CARTESIAN_POINT('',(30.0000000000001,-1.50000000000001,16.8125));
#58007=CARTESIAN_POINT('',(30.,-1.50000000000001,16.));
#58008=CARTESIAN_POINT('Ctrl Pts',(30.,-1.50000000000001,16.75));
#58009=CARTESIAN_POINT('Ctrl Pts',(30.1733135774153,-1.50000000000002,16.7583385533812));
#58010=CARTESIAN_POINT('Ctrl Pts',(30.3454665850143,-1.46996630625128,16.767455538092));
#58011=CARTESIAN_POINT('Ctrl Pts',(30.6943533649566,-1.34416445320596,16.7877358570363));
#58012=CARTESIAN_POINT('Ctrl Pts',(30.8648984846931,-1.24131259552183,16.7987982089822));
#58013=CARTESIAN_POINT('Ctrl Pts',(31.1561999433551,-0.975703692756434,
16.8201914820235));
#58014=CARTESIAN_POINT('Ctrl Pts',(31.2741613882488,-0.815654351280513,
16.8296858693734));
#58015=CARTESIAN_POINT('Ctrl Pts',(31.4395048489934,-0.463422668720622,
16.8492542961822));
#58016=CARTESIAN_POINT('Ctrl Pts',(31.4869681438372,-0.275392752547583,
16.8597004026363));
#58017=CARTESIAN_POINT('Ctrl Pts',(31.5087956503657,0.115841301406496,16.881435627856));
#58018=CARTESIAN_POINT('Ctrl Pts',(31.4799884843839,0.315484512989904,16.8925269173884));
#58019=CARTESIAN_POINT('Ctrl Pts',(31.3486206066034,0.684034451059388,16.9130019139478));
#58020=CARTESIAN_POINT('Ctrl Pts',(31.2503774147184,0.850433854559545,16.9217976845453));
#58021=CARTESIAN_POINT('Ctrl Pts',(30.994668844219,1.13948462780369,16.9421296570253));
#58022=CARTESIAN_POINT('Ctrl Pts',(30.8387866934565,1.25865700214481,16.9529398842324));
#58023=CARTESIAN_POINT('Ctrl Pts',(30.4862910667067,1.43284604521895,16.9747379225116));
#58024=CARTESIAN_POINT('Ctrl Pts',(30.2922814189341,1.48462820882751,16.9855106094757));
#58025=CARTESIAN_POINT('Ctrl Pts',(29.904287970164,1.50893843055208,17.0048532369201));
#58026=CARTESIAN_POINT('Ctrl Pts',(29.714222422622,1.48472560659638,17.014173768808));
#58027=CARTESIAN_POINT('Ctrl Pts',(29.3467837907597,1.36454370703768,17.0351905543248));
#58028=CARTESIAN_POINT('Ctrl Pts',(29.1737126610206,1.26724866527873,17.0462200829857));
#58029=CARTESIAN_POINT('Ctrl Pts',(28.8733100927186,1.01000510192613,17.0678188628294));
#58030=CARTESIAN_POINT('Ctrl Pts',(28.7495253450837,0.851954282658887,17.0776692065189));
#58031=CARTESIAN_POINT('Ctrl Pts',(28.5739823591041,0.503198698880474,17.0970445167289));
#58032=CARTESIAN_POINT('Ctrl Pts',(28.5214293436323,0.317084997718663,17.1073841667934));
#58033=CARTESIAN_POINT('Ctrl Pts',(28.4885674976081,-0.0722634762162506,
17.1290146375676));
#58034=CARTESIAN_POINT('Ctrl Pts',(28.5114956545415,-0.272057456078969,
17.1401143031155));
#58035=CARTESIAN_POINT('Ctrl Pts',(28.6319945909535,-0.644674063533988,
17.1608152257519));
#58036=CARTESIAN_POINT('Ctrl Pts',(28.7258902835189,-0.814669507709904,
17.1696624095652));
#58037=CARTESIAN_POINT('Ctrl Pts',(28.9737348011573,-1.1110192567928,17.1898187719544));
#58038=CARTESIAN_POINT('Ctrl Pts',(29.1257542814876,-1.2342064357884,17.2005546786951));
#58039=CARTESIAN_POINT('Ctrl Pts',(29.4726321438156,-1.41824610841819,17.2223560607564));
#58040=CARTESIAN_POINT('Ctrl Pts',(29.6650975807577,-1.47560141498182,17.2332092613688));
#58041=CARTESIAN_POINT('Ctrl Pts',(29.9087297050291,-1.49791971441829,17.2455509701752));
#58042=CARTESIAN_POINT('Ctrl Pts',(29.9543886563371,-1.50000000000001,17.2478055232048));
#58043=CARTESIAN_POINT('Ctrl Pts',(29.9999999999998,-1.50000000000001,17.25));
#58044=CARTESIAN_POINT('Ctrl Pts',(30.,-1.50000000000001,17.3125));
#58045=CARTESIAN_POINT('Ctrl Pts',(29.8075276745562,-1.50000000000001,17.3032396709245));
#58046=CARTESIAN_POINT('Ctrl Pts',(29.6167265402445,-1.46295509134636,17.2930307218294));
#58047=CARTESIAN_POINT('Ctrl Pts',(29.2565239800332,-1.31741270776536,17.2716576240826));
#58048=CARTESIAN_POINT('Ctrl Pts',(29.0910935230227,-1.20922562866616,17.2606931508671));
#58049=CARTESIAN_POINT('Ctrl Pts',(28.8152192771185,-0.939380042859163,
17.2399244343056));
#58050=CARTESIAN_POINT('Ctrl Pts',(28.7058473428781,-0.781856067083356,
17.2309364481713));
#58051=CARTESIAN_POINT('Ctrl Pts',(28.5481536416827,-0.426269472803969,
17.211181637378));
#58052=CARTESIAN_POINT('Ctrl Pts',(28.5044938401357,-0.230229772369996,
17.2002905429095));
#58053=CARTESIAN_POINT('Ctrl Pts',(28.4962752409133,0.162097483734217,17.178494584237));
#58054=CARTESIAN_POINT('Ctrl Pts',(28.5297146688179,0.3545967167103,17.167800182405));
#58055=CARTESIAN_POINT('Ctrl Pts',(28.6677231734513,0.715751667501951,17.1477360184722));
#58056=CARTESIAN_POINT('Ctrl Pts',(28.7707689938353,0.881053857184024,17.1388343527704));
#58057=CARTESIAN_POINT('Ctrl Pts',(29.0378553430027,1.16782543883526,17.1180182775366));
#58058=CARTESIAN_POINT('Ctrl Pts',(29.2009578477084,1.28493633443696,17.1069179241867));
#58059=CARTESIAN_POINT('Ctrl Pts',(29.5564777297123,1.44564779283652,17.0853487587108));
#58060=CARTESIAN_POINT('Ctrl Pts',(29.7443345881639,1.49039149544099,17.0750676107666));
#58061=CARTESIAN_POINT('Ctrl Pts',(30.1352017346056,1.50720082969336,17.0557950804638));
#58062=CARTESIAN_POINT('Ctrl Pts',(30.3346031531762,1.47580805773789,17.0457293998907));
#58063=CARTESIAN_POINT('Ctrl Pts',(30.7060862860091,1.33790450333634,17.02402575504));
#58064=CARTESIAN_POINT('Ctrl Pts',(30.8749553104054,1.23409963004519,17.0130175716131));
#58065=CARTESIAN_POINT('Ctrl Pts',(31.1584137835032,0.971677105747927,16.9920901549037));
#58066=CARTESIAN_POINT('Ctrl Pts',(31.271994699923,0.817368296550736,16.9829093498084));
#58067=CARTESIAN_POINT('Ctrl Pts',(31.4394257557863,0.466485221859018,16.9634158456588));
#58068=CARTESIAN_POINT('Ctrl Pts',(31.488516036617,0.271760297088586,16.9525977942827));
#58069=CARTESIAN_POINT('Ctrl Pts',(31.5076810248584,-0.120678265071266,
16.9307956519405));
#58070=CARTESIAN_POINT('Ctrl Pts',(31.4794384691607,-0.314545865899112,
16.9200252296723));
#58071=CARTESIAN_POINT('Ctrl Pts',(31.3513352758344,-0.678794152386266,
16.8997892137563));
#58072=CARTESIAN_POINT('Ctrl Pts',(31.2534603041453,-0.845994238167287,
16.890973963719));
#58073=CARTESIAN_POINT('Ctrl Pts',(30.9950590391717,-1.14001068930543,16.8703745034186));
#58074=CARTESIAN_POINT('Ctrl Pts',(30.8348670617779,-1.26204295887652,16.8592774780469));
#58075=CARTESIAN_POINT('Ctrl Pts',(30.4829704713108,-1.43301939771413,16.8375974999208));
#58076=CARTESIAN_POINT('Ctrl Pts',(30.2958966065637,-1.48299380376918,16.8272087264607));
#58077=CARTESIAN_POINT('Ctrl Pts',(30.0696474084832,-1.49878860163674,16.8158845624575));
#58078=CARTESIAN_POINT('Ctrl Pts',(30.0348056486057,-1.50000000000001,16.8141745875493));
#58079=CARTESIAN_POINT('Ctrl Pts',(30.0000000000002,-1.50000000000001,16.8125));
#58080=CARTESIAN_POINT('Origin',(30.,-1.32966554433622E-14,16.));
#58081=CARTESIAN_POINT('',(30.0000000000023,1.33373412263454,16.1584936490537));
#58082=CARTESIAN_POINT('',(30.,1.1752404735808,16.));
#58083=CARTESIAN_POINT('',(30.,1.17524047358083,16.));
#58084=CARTESIAN_POINT('',(30.,-1.17524047358085,16.));
#58085=CARTESIAN_POINT('Ctrl Pts',(30.,-1.17524047358083,16.));
#58086=CARTESIAN_POINT('Ctrl Pts',(30.0938726776238,-1.17889502189498,16.0036545483141));
#58087=CARTESIAN_POINT('Ctrl Pts',(30.2222715669962,-1.17292308708929,16.0088746896198));
#58088=CARTESIAN_POINT('Ctrl Pts',(30.4821758748939,-1.10061359842964,16.0205734257761));
#58089=CARTESIAN_POINT('Ctrl Pts',(30.5904809486724,-1.05245648363552,16.0257840816621));
#58090=CARTESIAN_POINT('Ctrl Pts',(30.8133642274912,-0.91102859460423,16.0372929849601));
#58091=CARTESIAN_POINT('Ctrl Pts',(30.9213977318432,-0.810903247446717,
16.0434573291476));
#58092=CARTESIAN_POINT('Ctrl Pts',(31.1067869536601,-0.562636269482013,
16.0555173993883));
#58093=CARTESIAN_POINT('Ctrl Pts',(31.1779495349821,-0.411557996758087,
16.0617064115579));
#58094=CARTESIAN_POINT('Ctrl Pts',(31.2569648094213,-0.0966670523057213,
16.075198195417));
#58095=CARTESIAN_POINT('Ctrl Pts',(31.2657685184509,0.0650399419384585,
16.0820144838088));
#58096=CARTESIAN_POINT('Ctrl Pts',(31.2286447980599,0.334175553677255,16.0931820826379));
#58097=CARTESIAN_POINT('Ctrl Pts',(31.1927617340632,0.495209878479218,16.0995752755442));
#58098=CARTESIAN_POINT('Ctrl Pts',(31.0046982036223,0.825162649859306,16.1133508913014));
#58099=CARTESIAN_POINT('Ctrl Pts',(30.8901527526008,0.956864086379422,16.1201881413696));
#58100=CARTESIAN_POINT('Ctrl Pts',(30.6234294043457,1.16264469041258,16.1337830625282));
#58101=CARTESIAN_POINT('Ctrl Pts',(30.4758334589096,1.2374906559331,16.1404068749596));
#58102=CARTESIAN_POINT('Ctrl Pts',(30.2026344427889,1.31649705751482,16.1513204506313));
#58103=CARTESIAN_POINT('Ctrl Pts',(30.094862299376,1.33047991225226,16.1552394386714));
#58104=CARTESIAN_POINT('Ctrl Pts',(30.0000000000046,1.33373412263454,16.1584936490537));
#58105=CARTESIAN_POINT('Origin',(30.,-1.32966554433622E-14,16.));
#58106=CARTESIAN_POINT('Origin',(30.,-1.21864324187371E-14,15.78125));
#58107=CARTESIAN_POINT('',(30.0000000000002,-1.17524047358085,16.0625));
#58108=CARTESIAN_POINT('',(30.,-1.17524047358085,15.78125));
#58109=CARTESIAN_POINT('',(29.1765921258349,-0.838564036615843,16.));
#58110=CARTESIAN_POINT('Ctrl Pts',(30.0000000000004,-1.17524047358085,16.0625));
#58111=CARTESIAN_POINT('Ctrl Pts',(29.8936372832897,-1.17524047358089,16.0559685129868));
#58112=CARTESIAN_POINT('Ctrl Pts',(29.7875857388152,-1.16080842474563,16.0489444642731));
#58113=CARTESIAN_POINT('Ctrl Pts',(29.5893382840682,-1.10559796441283,16.034813132098));
#58114=CARTESIAN_POINT('Ctrl Pts',(29.4977179176601,-1.06709869274158,16.0278219954706));
#58115=CARTESIAN_POINT('Ctrl Pts',(29.3263212626278,-0.968061456605931,
16.0137856854629));
#58116=CARTESIAN_POINT('Ctrl Pts',(29.2472234502441,-0.90791877416947,16.0067961899552));
#58117=CARTESIAN_POINT('Ctrl Pts',(29.176592125834,-0.838564036614912,15.9999999999999));
#58118=CARTESIAN_POINT('Origin',(30.,-1.32966554433622E-14,16.));
#58119=CARTESIAN_POINT('Origin',(30.,-1.21864324187371E-14,15.78125));
#58120=CARTESIAN_POINT('',(30.0000000000002,-1.17524047358085,16.5625));
#58121=CARTESIAN_POINT('',(30.,-1.17524047358085,16.5));
#58122=CARTESIAN_POINT('',(30.,-1.17524047358085,15.78125));
#58123=CARTESIAN_POINT('Ctrl Pts',(30.0000000000004,-1.17524047358085,16.5625));
#58124=CARTESIAN_POINT('Ctrl Pts',(29.8712710011335,-1.17524047358089,16.5545950516279));
#58125=CARTESIAN_POINT('Ctrl Pts',(29.7432544697015,-1.15409887958747,16.5459843057103));
#58126=CARTESIAN_POINT('Ctrl Pts',(29.4749058017838,-1.06268366571272,16.5262646272929));
#58127=CARTESIAN_POINT('Ctrl Pts',(29.3400104190766,-0.984598569044377,
16.515212607152));
#58128=CARTESIAN_POINT('Ctrl Pts',(29.1121607207208,-0.784303734398693,
16.4941196868072));
#58129=CARTESIAN_POINT('Ctrl Pts',(29.0200231478196,-0.665589512335134,
16.4846952710458));
#58130=CARTESIAN_POINT('Ctrl Pts',(28.8817974975863,-0.393869611486594,
16.465428299239));
#58131=CARTESIAN_POINT('Ctrl Pts',(28.83947486215,-0.242215228858268,16.4546748700446));
#58132=CARTESIAN_POINT('Ctrl Pts',(28.8167032491755,0.0653802904577292,
16.4328640487538));
#58133=CARTESIAN_POINT('Ctrl Pts',(28.8351718353917,0.218291541824621,16.422021498172));
#58134=CARTESIAN_POINT('Ctrl Pts',(28.9287391651494,0.506051914833821,16.4016171370023));
#58135=CARTESIAN_POINT('Ctrl Pts',(29.0019741006921,0.638460005621421,16.3928173224174));
#58136=CARTESIAN_POINT('Ctrl Pts',(29.1986594960153,0.873851822283252,16.3723938102577));
#58137=CARTESIAN_POINT('Ctrl Pts',(29.3222166226463,0.972810188230982,16.3612980106481));
#58138=CARTESIAN_POINT('Ctrl Pts',(29.5955374213776,1.11370354874836,16.3395188200451));
#58139=CARTESIAN_POINT('Ctrl Pts',(29.7416409158841,1.1563714827732,16.3290342066007));
#58140=CARTESIAN_POINT('Ctrl Pts',(30.0452139523297,1.18442751027465,16.309397801581));
#58141=CARTESIAN_POINT('Ctrl Pts',(30.1998697024494,1.16832333055968,16.2999812279383));
#58142=CARTESIAN_POINT('Ctrl Pts',(30.4949641982123,1.07710916023858,16.2786262781941));
#58143=CARTESIAN_POINT('Ctrl Pts',(30.6323783558426,1.00262103976947,16.2675471121926));
#58144=CARTESIAN_POINT('Ctrl Pts',(30.8661146099677,0.80826573510396,16.246303290685));
#58145=CARTESIAN_POINT('Ctrl Pts',(30.9615634972897,0.691955855651338,16.2365648418493));
#58146=CARTESIAN_POINT('Ctrl Pts',(31.1071384709944,0.423965303495795,16.217562308738));
#58147=CARTESIAN_POINT('Ctrl Pts',(31.153539286677,0.273539680121433,16.2068960077584));
#58148=CARTESIAN_POINT('Ctrl Pts',(31.1846742020807,-0.0336925499575308,
16.1851109463897));
#58149=CARTESIAN_POINT('Ctrl Pts',(31.1702391074247,-0.187447361382806,
16.174208581095));
#58150=CARTESIAN_POINT('Ctrl Pts',(31.0842361864784,-0.477469105777865,
16.1536438717926));
#58151=CARTESIAN_POINT('Ctrl Pts',(31.0147909316618,-0.611342914691707,
16.1448082262658));
#58152=CARTESIAN_POINT('Ctrl Pts',(30.8246452237759,-0.851973319529638,
16.1246005735716));
#58153=CARTESIAN_POINT('Ctrl Pts',(30.7034471847234,-0.954486386541281,
16.1135236126058));
#58154=CARTESIAN_POINT('Ctrl Pts',(30.4332129266933,-1.10289061678379,16.0916676708875));
#58155=CARTESIAN_POINT('Ctrl Pts',(30.2878849143487,-1.14942616400118,16.0810935566577));
#58156=CARTESIAN_POINT('Ctrl Pts',(30.0919105154022,-1.17254804866719,16.0682394674743));
#58157=CARTESIAN_POINT('Ctrl Pts',(30.0459321343385,-1.17524047358084,16.0653205855228));
#58158=CARTESIAN_POINT('Ctrl Pts',(30.0000000000004,-1.17524047358085,16.0625));
#58159=CARTESIAN_POINT('Ctrl Pts',(29.9999999999986,-1.17524047358085,15.9999999999999));
#58160=CARTESIAN_POINT('Ctrl Pts',(30.1214028111116,-1.17524047358099,16.0074550642242));
#58161=CARTESIAN_POINT('Ctrl Pts',(30.2421537204218,-1.15643017464734,16.0155369920666));
#58162=CARTESIAN_POINT('Ctrl Pts',(30.4776301337898,-1.08113291233427,16.0326666201836));
#58163=CARTESIAN_POINT('Ctrl Pts',(30.5903997908,-1.02391620718435,16.0416200885134));
#58164=CARTESIAN_POINT('Ctrl Pts',(30.8179173133188,-0.858187726048923,
16.0614671043063));
#58165=CARTESIAN_POINT('Ctrl Pts',(30.9244135286053,-0.742266950950034,
16.0721166138301));
#58166=CARTESIAN_POINT('Ctrl Pts',(31.0824458543846,-0.481384401141323,
16.0910702726526));
#58167=CARTESIAN_POINT('Ctrl Pts',(31.1347636661213,-0.340257482296023,
16.1008732014181));
#58168=CARTESIAN_POINT('Ctrl Pts',(31.1847167047507,-0.0402726429290417,
16.1221443686182));
#58169=CARTESIAN_POINT('Ctrl Pts',(31.1797095913038,0.116033015525934,16.1332276080324));
#58170=CARTESIAN_POINT('Ctrl Pts',(31.1096057651028,0.416692954381308,16.1545466448319));
#58171=CARTESIAN_POINT('Ctrl Pts',(31.0456145958404,0.558153128413804,16.1639131875247));
#58172=CARTESIAN_POINT('Ctrl Pts',(30.868452148125,0.806074678480504,16.1835820667589));
#58173=CARTESIAN_POINT('Ctrl Pts',(30.7578944192075,0.910792535772415,16.1940837990854));
#58174=CARTESIAN_POINT('Ctrl Pts',(30.4982839285527,1.07586594639843,16.2158783446996));
#58175=CARTESIAN_POINT('Ctrl Pts',(30.350445183185,1.13268560339106,16.2269712473271));
#58176=CARTESIAN_POINT('Ctrl Pts',(30.0480054721768,1.18378716120051,16.2473551076386));
#58177=CARTESIAN_POINT('Ctrl Pts',(29.8968386090012,1.18026105605562,16.2561569026374));
#58178=CARTESIAN_POINT('Ctrl Pts',(29.6011798659176,1.11599305250821,16.276591159187));
#58179=CARTESIAN_POINT('Ctrl Pts',(29.4597499374869,1.05480717934155,16.2874453099545));
#58180=CARTESIAN_POINT('Ctrl Pts',(29.2055652972218,0.87997645163687,16.3092526000714));
#58181=CARTESIAN_POINT('Ctrl Pts',(29.0959568884663,0.766951615708884,16.3199905502909));
#58182=CARTESIAN_POINT('Ctrl Pts',(28.9310246543964,0.510549118020342,16.3392090818415));
#58183=CARTESIAN_POINT('Ctrl Pts',(28.8749728808886,0.371095429589151,16.348686560472));
#58184=CARTESIAN_POINT('Ctrl Pts',(28.8169184420094,0.0732292943615943,
16.3698074957134));
#58185=CARTESIAN_POINT('Ctrl Pts',(28.817543647408,-0.0827153411142831,
16.3808651359001));
#58186=CARTESIAN_POINT('Ctrl Pts',(28.8792006517981,-0.386085589929172,
16.4023763539327));
#58187=CARTESIAN_POINT('Ctrl Pts',(28.9398691853048,-0.530428612710414,
16.4120388426041));
#58188=CARTESIAN_POINT('Ctrl Pts',(29.1111806434797,-0.783487027051828,
16.4315305472161));
#58189=CARTESIAN_POINT('Ctrl Pts',(29.2187204550675,-0.890749010718532,
16.441937155047));
#58190=CARTESIAN_POINT('Ctrl Pts',(29.4732317621912,-1.06214794881238,16.4636428352494));
#58191=CARTESIAN_POINT('Ctrl Pts',(29.6190899112583,-1.1227476098516,16.4747481293347));
#58192=CARTESIAN_POINT('Ctrl Pts',(29.8476395120001,-1.16783357420714,16.490381294589));
#58193=CARTESIAN_POINT('Ctrl Pts',(29.9238084968367,-1.17524047358085,16.4953212570267));
#58194=CARTESIAN_POINT('Ctrl Pts',(30.,-1.17524047358085,16.5));
#58195=CARTESIAN_POINT('Origin',(30.,-1.21864324187371E-14,15.78125));
#58196=CARTESIAN_POINT('',(30.,-1.17524047358085,17.0625));
#58197=CARTESIAN_POINT('',(30.0000000000001,-1.17524047358085,17.));
#58198=CARTESIAN_POINT('',(30.,-1.17524047358085,15.78125));
#58199=CARTESIAN_POINT('Ctrl Pts',(30.,-1.17524047358085,17.0625));
#58200=CARTESIAN_POINT('Ctrl Pts',(29.8500434788821,-1.17524047358086,17.0532915188657));
#58201=CARTESIAN_POINT('Ctrl Pts',(29.7013448813168,-1.14654165820119,17.0431428036379));
#58202=CARTESIAN_POINT('Ctrl Pts',(29.4194581258723,-1.03331719487298,17.0218185633632));
#58203=CARTESIAN_POINT('Ctrl Pts',(29.2895397758247,-0.948696042884902,
17.0108404436342));
#58204=CARTESIAN_POINT('Ctrl Pts',(29.0728347660888,-0.737413048700427,
16.9900423213744));
#58205=CARTESIAN_POINT('Ctrl Pts',(28.9869014388118,-0.614031092098323,
16.9810393937031));
#58206=CARTESIAN_POINT('Ctrl Pts',(28.8628735458866,-0.335358890642938,
16.9612794518217));
#58207=CARTESIAN_POINT('Ctrl Pts',(28.82846267168,-0.181667965469806,16.9503816165397));
#58208=CARTESIAN_POINT('Ctrl Pts',(28.8217124648996,0.125982959524893,16.9285668665722));
#58209=CARTESIAN_POINT('Ctrl Pts',(28.8478169965895,0.276986540894418,16.9178595840512));
#58210=CARTESIAN_POINT('Ctrl Pts',(28.9558731518301,0.560261316962501,16.89777328523));
#58211=CARTESIAN_POINT('Ctrl Pts',(29.0365906245512,0.68988311408331,16.8888684608487));
#58212=CARTESIAN_POINT('Ctrl Pts',(29.2459337687842,0.914815990147539,16.868038474302));
#58213=CARTESIAN_POINT('Ctrl Pts',(29.3738173058995,1.00667300394252,16.8569287693601));
#58214=CARTESIAN_POINT('Ctrl Pts',(29.6525904034611,1.13269913332434,16.8353418646716));
#58215=CARTESIAN_POINT('Ctrl Pts',(29.7999172965718,1.16777128086699,16.825051424181));
#58216=CARTESIAN_POINT('Ctrl Pts',(30.1064062467105,1.18085135988937,16.8057669130232));
#58217=CARTESIAN_POINT('Ctrl Pts',(30.2627337376109,1.15617395633467,16.7956901530542));
#58218=CARTESIAN_POINT('Ctrl Pts',(30.5539694020395,1.04785975388265,16.7739659051239));
#58219=CARTESIAN_POINT('Ctrl Pts',(30.6863296582614,0.96635719030164,16.7629483992302));
#58220=CARTESIAN_POINT('Ctrl Pts',(30.9084297587183,0.760352988428474,16.7420061299136));
#58221=CARTESIAN_POINT('Ctrl Pts',(30.9973576321623,0.639251123876904,16.7328276824508));
#58222=CARTESIAN_POINT('Ctrl Pts',(31.1283061935881,0.363925745860841,16.7133050553655));
#58223=CARTESIAN_POINT('Ctrl Pts',(31.1665770325591,0.21117202309341,16.7024736747387));
#58224=CARTESIAN_POINT('Ctrl Pts',(31.1811107740607,-0.0965571386816749,
16.6806533771987));
#58225=CARTESIAN_POINT('Ctrl Pts',(31.1587010998539,-0.248535347285279,
16.6698769863224));
#58226=CARTESIAN_POINT('Ctrl Pts',(31.0576874952353,-0.534014859537023,
16.6496343552276));
#58227=CARTESIAN_POINT('Ctrl Pts',(30.9806443499075,-0.664990212129755,
16.6408093669374));
#58228=CARTESIAN_POINT('Ctrl Pts',(30.7774744062741,-0.895077677115282,
16.6201757128395));
#58229=CARTESIAN_POINT('Ctrl Pts',(30.6516599935628,-0.990433515302137,
16.6090690216144));
#58230=CARTESIAN_POINT('Ctrl Pts',(30.3754577665479,-1.12376244747141,16.5873810764564));
#58231=CARTESIAN_POINT('Ctrl Pts',(30.2286809422177,-1.16255586785604,16.5769924813814));
#58232=CARTESIAN_POINT('Ctrl Pts',(30.0523684587312,-1.17436628643519,16.5657468184328));
#58233=CARTESIAN_POINT('Ctrl Pts',(30.0261713894288,-1.17524047358084,16.5641071241452));
#58234=CARTESIAN_POINT('Ctrl Pts',(30.0000000000004,-1.17524047358085,16.5625));
#58235=CARTESIAN_POINT('Ctrl Pts',(30.,-1.17524047358085,16.5));
#58236=CARTESIAN_POINT('Ctrl Pts',(30.073608323754,-1.17524047358085,16.5045201159347));
#58237=CARTESIAN_POINT('Ctrl Pts',(30.1472072638744,-1.16832718018639,16.5092847577281));
#58238=CARTESIAN_POINT('Ctrl Pts',(30.369441082132,-1.12600740446215,16.5244320137475));
#58239=CARTESIAN_POINT('Ctrl Pts',(30.5120596783037,-1.06872004059094,16.5352209411127));
#58240=CARTESIAN_POINT('Ctrl Pts',(30.770540092832,-0.900978381413799,16.5570406907631));
#58241=CARTESIAN_POINT('Ctrl Pts',(30.8831588051698,-0.790914789141215,
16.5678585095693));
#58242=CARTESIAN_POINT('Ctrl Pts',(31.0548992370084,-0.539025681589464,
16.5873351001607));
#58243=CARTESIAN_POINT('Ctrl Pts',(31.1146464335618,-0.40117702528207,16.5965535505072));
#58244=CARTESIAN_POINT('Ctrl Pts',(31.1805926646682,-0.105443065986663,
16.6175232985392));
#58245=CARTESIAN_POINT('Ctrl Pts',(31.1842348048322,0.0500317177053629,
16.6285476227227));
#58246=CARTESIAN_POINT('Ctrl Pts',(31.1309192517252,0.355959076743607,16.650240158982));
#58247=CARTESIAN_POINT('Ctrl Pts',(31.0735350939833,0.503164977113694,16.6602491192277));
#58248=CARTESIAN_POINT('Ctrl Pts',(30.9079406905516,0.761174069707616,16.6795652728517));
#58249=CARTESIAN_POINT('Ctrl Pts',(30.8033709986449,0.870813111599809,16.6898737681392));
#58250=CARTESIAN_POINT('Ctrl Pts',(30.5539282192807,1.04817985026245,16.7114797826742));
#58251=CARTESIAN_POINT('Ctrl Pts',(30.4100715847777,1.1123704677318,16.7225894812308));
#58252=CARTESIAN_POINT('Ctrl Pts',(30.1103488398163,1.179778360742,16.7433846194973));
#58253=CARTESIAN_POINT('Ctrl Pts',(29.957856215253,1.1841771173115,16.7522711143702));
#58254=CARTESIAN_POINT('Ctrl Pts',(29.6587896018035,1.13483145500942,16.7723855875496));
#58255=CARTESIAN_POINT('Ctrl Pts',(29.5151366653971,1.08127741557342,16.7831056710399));
#58256=CARTESIAN_POINT('Ctrl Pts',(29.252747940286,0.920389087589127,16.80492244475));
#58257=CARTESIAN_POINT('Ctrl Pts',(29.137337166046,0.813224513877345,16.8158089365411));
#58258=CARTESIAN_POINT('Ctrl Pts',(28.9591466935998,0.565701034789473,16.8355268312788));
#58259=CARTESIAN_POINT('Ctrl Pts',(28.8958814901205,0.429333298679841,16.8445570602832));
#58260=CARTESIAN_POINT('Ctrl Pts',(28.8225467136217,0.135655218439199,16.8653810311245));
#58261=CARTESIAN_POINT('Ctrl Pts',(28.8149165149687,-0.0192736957647923,
16.8763666490815));
#58262=CARTESIAN_POINT('Ctrl Pts',(28.8600359901893,-0.325574492875678,
16.8980856648912));
#58263=CARTESIAN_POINT('Ctrl Pts',(28.9132427466147,-0.473736863683124,
16.908393840582));
#58264=CARTESIAN_POINT('Ctrl Pts',(29.0711075417097,-0.735375844223955,
16.9273640300312));
#58265=CARTESIAN_POINT('Ctrl Pts',(29.1722563389189,-0.847605887640186,
16.9375543168196));
#58266=CARTESIAN_POINT('Ctrl Pts',(29.4158032201734,-1.03154789820323,16.9590313959273));
#58267=CARTESIAN_POINT('Ctrl Pts',(29.5572939812199,-1.09972494823153,16.97013714563));
#58268=CARTESIAN_POINT('Ctrl Pts',(29.8035947514828,-1.1629117021743,16.9875021095456));
#58269=CARTESIAN_POINT('Ctrl Pts',(29.9016938547886,-1.17524047358087,16.9939632483014));
#58270=CARTESIAN_POINT('Ctrl Pts',(30.0000000000002,-1.17524047358085,17.));
#58271=CARTESIAN_POINT('Origin',(30.,-1.21864324187371E-14,15.78125));
#58272=CARTESIAN_POINT('',(30.,-1.17524047358085,17.5625));
#58273=CARTESIAN_POINT('',(30.0000000000003,-1.17524047358085,17.5));
#58274=CARTESIAN_POINT('',(30.,-1.17524047358085,15.78125));
#58275=CARTESIAN_POINT('Ctrl Pts',(29.9999999999999,-1.17524047358085,17.5625));
#58276=CARTESIAN_POINT('Ctrl Pts',(29.9853039952848,-1.17524047358085,17.5615975525362));
#58277=CARTESIAN_POINT('Ctrl Pts',(29.9705988101993,-1.17496482223763,17.560684768457));
#58278=CARTESIAN_POINT('Ctrl Pts',(29.8000675583885,-1.16856010727206,17.5499857698916));
#58279=CARTESIAN_POINT('Ctrl Pts',(29.6469974366404,-1.13175546252589,17.53928122759));
#58280=CARTESIAN_POINT('Ctrl Pts',(29.3669883306193,-1.00191414640604,17.51748315987));
#58281=CARTESIAN_POINT('Ctrl Pts',(29.2422159979844,-0.911212372037981,
17.5066054643129));
#58282=CARTESIAN_POINT('Ctrl Pts',(29.0365009193432,-0.689398438610156,
17.4861088470066));
#58283=CARTESIAN_POINT('Ctrl Pts',(28.9566358845376,-0.561238966410083,
17.477296037423));
#58284=CARTESIAN_POINT('Ctrl Pts',(28.8466374529962,-0.274946499836391,
17.4569957617908));
#58285=CARTESIAN_POINT('Ctrl Pts',(28.8202715815142,-0.118602529031394,
17.4459098057446));
#58286=CARTESIAN_POINT('Ctrl Pts',(28.8303001790337,0.189193535952347,17.4240847642671));
#58287=CARTESIAN_POINT('Ctrl Pts',(28.8642598713376,0.337792935402822,17.413547956213));
#58288=CARTESIAN_POINT('Ctrl Pts',(28.9875332190235,0.616132121834573,17.3938116275857));
#58289=CARTESIAN_POINT('Ctrl Pts',(29.0764632180064,0.742831294355827,17.3845427667776));
#58290=CARTESIAN_POINT('Ctrl Pts',(29.2992557500629,0.956131495581886,17.3632993064049));
#58291=CARTESIAN_POINT('Ctrl Pts',(29.431365525465,1.04013508414132,17.3522085112739));
#58292=CARTESIAN_POINT('Ctrl Pts',(29.7152659077079,1.14996876403328,17.3308808348058));
#58293=CARTESIAN_POINT('Ctrl Pts',(29.8634965281812,1.17678287245723,17.3209370444755));
#58294=CARTESIAN_POINT('Ctrl Pts',(30.1685869462377,1.17348866615416,17.3020853596773));
#58295=CARTESIAN_POINT('Ctrl Pts',(30.3225567032231,1.14080144678595,17.291471550985));
#58296=CARTESIAN_POINT('Ctrl Pts',(30.6062809135034,1.01837161133764,17.269708112041));
#58297=CARTESIAN_POINT('Ctrl Pts',(30.7337302229979,0.930754504232001,17.2587753925441));
#58298=CARTESIAN_POINT('Ctrl Pts',(30.9451039338725,0.714326579760782,17.2381222459404));
#58299=CARTESIAN_POINT('Ctrl Pts',(31.0280898505948,0.588650269560749,17.2292397036887));
#58300=CARTESIAN_POINT('Ctrl Pts',(31.1457356989614,0.305390771140385,17.209154488167));
#58301=CARTESIAN_POINT('Ctrl Pts',(31.1762844162632,0.149369866697047,17.1980914399405));
#58302=CARTESIAN_POINT('Ctrl Pts',(31.1741828829317,-0.159374372954329,
17.1761991657924));
#58303=CARTESIAN_POINT('Ctrl Pts',(31.1439148549186,-0.309160960295119,
17.1655781772438));
#58304=CARTESIAN_POINT('Ctrl Pts',(31.0278391895685,-0.589863984020037,
17.1456742348851));
#58305=CARTESIAN_POINT('Ctrl Pts',(30.9428415818715,-0.717947604052165,
17.1366104494432));
#58306=CARTESIAN_POINT('Ctrl Pts',(30.7264277284841,-0.936836489561928,
17.1155605491468));
#58307=CARTESIAN_POINT('Ctrl Pts',(30.5962729133073,-1.02460346942682,17.10445637729));
#58308=CARTESIAN_POINT('Ctrl Pts',(30.3147671476396,-1.1421454095557,17.0830024620243));
#58309=CARTESIAN_POINT('Ctrl Pts',(30.1669216238945,-1.17291749944691,17.0728326267459));
#58310=CARTESIAN_POINT('Ctrl Pts',(30.0114948569556,-1.17519832475422,17.06320736676));
#58311=CARTESIAN_POINT('Ctrl Pts',(30.0057465951805,-1.17524047358085,17.0628528850424));
#58312=CARTESIAN_POINT('Ctrl Pts',(30.,-1.17524047358085,17.0625));
#58313=CARTESIAN_POINT('Ctrl Pts',(30.0000000000002,-1.17524047358085,17.));
#58314=CARTESIAN_POINT('Ctrl Pts',(30.0532026451947,-1.17524047358084,17.0032670506819));
#58315=CARTESIAN_POINT('Ctrl Pts',(30.1064500803375,-1.17162840402792,17.0066649131742));
#58316=CARTESIAN_POINT('Ctrl Pts',(30.3094843531048,-1.14383638948677,17.0201181063427));
#58317=CARTESIAN_POINT('Ctrl Pts',(30.4541770343026,-1.0944632219883,17.0307538106078));
#58318=CARTESIAN_POINT('Ctrl Pts',(30.7220117324143,-0.94057404805184,17.0526568626846));
#58319=CARTESIAN_POINT('Ctrl Pts',(30.8414109395085,-0.835479490322757,
17.0637148850572));
#58320=CARTESIAN_POINT('Ctrl Pts',(31.0267110546809,-0.591037021798696,
17.0837601330781));
#58321=CARTESIAN_POINT('Ctrl Pts',(31.0933788874677,-0.456058910657645,
17.0926620146465));
#58322=CARTESIAN_POINT('Ctrl Pts',(31.1737387540124,-0.16438811954927,17.1133436536858));
#58323=CARTESIAN_POINT('Ctrl Pts',(31.1851490819135,-0.0100732318962758,
17.1242857325711));
#58324=CARTESIAN_POINT('Ctrl Pts',(31.1477867853133,0.296739304676255,17.1460410345334));
#58325=CARTESIAN_POINT('Ctrl Pts',(31.0983725298423,0.446176311422578,17.156637235205));
#58326=CARTESIAN_POINT('Ctrl Pts',(30.9473434585081,0.711342976495719,17.1754395336164));
#58327=CARTESIAN_POINT('Ctrl Pts',(30.8493881217234,0.825870653120103,17.1854545855523));
#58328=CARTESIAN_POINT('Ctrl Pts',(30.6112318646727,1.01569990967513,17.2068093638384));
#58329=CARTESIAN_POINT('Ctrl Pts',(30.4719800604887,1.0874234537732,17.2179033608764));
#58330=CARTESIAN_POINT('Ctrl Pts',(30.1755334231398,1.17210985582506,17.2391099087106));
#58331=CARTESIAN_POINT('Ctrl Pts',(30.0214941231326,1.18498177307235,17.2483347304275));
#58332=CARTESIAN_POINT('Ctrl Pts',(29.7191034448427,1.1511421779865,17.2681035786673));
#58333=CARTESIAN_POINT('Ctrl Pts',(29.5735822533488,1.10552321949792,17.2786570590835));
#58334=CARTESIAN_POINT('Ctrl Pts',(29.3025973986068,0.958895356196027,17.3004961143537));
#58335=CARTESIAN_POINT('Ctrl Pts',(29.1808306521913,0.85722095928387,17.3115782643265));
#58336=CARTESIAN_POINT('Ctrl Pts',(28.9891285746956,0.617827320312939,17.3318376420863));
#58337=CARTESIAN_POINT('Ctrl Pts',(28.918785924397,0.484304768960115,17.3406591721831));
#58338=CARTESIAN_POINT('Ctrl Pts',(28.8309775509286,0.194817478373176,17.361185984716));
#58339=CARTESIAN_POINT('Ctrl Pts',(28.8155773691905,0.0412543792472424,
17.3720747561758));
#58340=CARTESIAN_POINT('Ctrl Pts',(28.8447173912596,-0.266085346871024,
17.3938674398171));
#58341=CARTESIAN_POINT('Ctrl Pts',(28.8901486797617,-0.416814366578493,
17.4045552538642));
#58342=CARTESIAN_POINT('Ctrl Pts',(29.0339735284972,-0.685700945089528,
17.423621321941));
#58343=CARTESIAN_POINT('Ctrl Pts',(29.1286271803726,-0.802582950507819,
17.4332789203108));
#58344=CARTESIAN_POINT('Ctrl Pts',(29.3609543925255,-0.998368963070605,
17.45448693977));
#58345=CARTESIAN_POINT('Ctrl Pts',(29.4977729352126,-1.07372697749091,17.4655603714348));
#58346=CARTESIAN_POINT('Ctrl Pts',(29.7602131749374,-1.15682002764215,17.484622175217));
#58347=CARTESIAN_POINT('Ctrl Pts',(29.879837116137,-1.1752404735809,17.4926210768238));
#58348=CARTESIAN_POINT('Ctrl Pts',(30.0000000000005,-1.17524047358085,17.5));
#58349=CARTESIAN_POINT('Origin',(30.,-1.21864324187371E-14,15.78125));
#58350=CARTESIAN_POINT('',(29.9999999999998,-1.17524047358085,18.0625));
#58351=CARTESIAN_POINT('',(30.,-1.17524047358085,18.));
#58352=CARTESIAN_POINT('',(30.,-1.17524047358085,15.78125));
#58353=CARTESIAN_POINT('Ctrl Pts',(29.9999999999995,-1.17524047358085,18.0625));
#58354=CARTESIAN_POINT('Ctrl Pts',(29.9645254254169,-1.17524047358085,18.0603215888955));
#58355=CARTESIAN_POINT('Ctrl Pts',(29.929015100466,-1.17363438891304,18.0580840407407));
#58356=CARTESIAN_POINT('Ctrl Pts',(29.7382382629168,-1.15628718990462,18.0457538558988));
#58357=CARTESIAN_POINT('Ctrl Pts',(29.5872914572777,-1.11138228831714,18.0348925171245));
#58358=CARTESIAN_POINT('Ctrl Pts',(29.315235711072,-0.96715790012321,18.0130729130751));
#58359=CARTESIAN_POINT('Ctrl Pts',(29.1959940490486,-0.870565282945587,
18.0023259907432));
#58360=CARTESIAN_POINT('Ctrl Pts',(29.0016396885941,-0.638155310236294,
17.9821513395236));
#58361=CARTESIAN_POINT('Ctrl Pts',(28.9280461950896,-0.504858426874225,
17.9732982357813));
#58362=CARTESIAN_POINT('Ctrl Pts',(28.8336569152641,-0.212647772939916,
17.9525783164326));
#58363=CARTESIAN_POINT('Ctrl Pts',(28.8157570812338,-0.0559802507924535,
17.9414694181781));
#58364=CARTESIAN_POINT('Ctrl Pts',(28.841716723376,0.249283949869151,17.9198239048041));
#58365=CARTESIAN_POINT('Ctrl Pts',(28.8830393993721,0.395199804389445,17.9094773801424));
#58366=CARTESIAN_POINT('Ctrl Pts',(29.0209639808548,0.668562290928518,17.8900939367334));
#58367=CARTESIAN_POINT('Ctrl Pts',(29.1181759703235,0.792402282110926,17.8802238069267));
#58368=CARTESIAN_POINT('Ctrl Pts',(29.3540263292146,0.993822233016871,17.8585996950535));
#58369=CARTESIAN_POINT('Ctrl Pts',(29.4898462594122,1.06991069869815,17.8475616886318));
#58370=CARTESIAN_POINT('Ctrl Pts',(29.7781387158762,1.16368326761588,17.8265337315072));
#58371=CARTESIAN_POINT('Ctrl Pts',(29.9272121099849,1.18239624377936,17.817223433802));
#58372=CARTESIAN_POINT('Ctrl Pts',(30.231427568808,1.16273575019751,17.7978452321702));
#58373=CARTESIAN_POINT('Ctrl Pts',(30.3834744853667,1.1218012564522,17.7870571039388));
#58374=CARTESIAN_POINT('Ctrl Pts',(30.6595367886018,0.984593855649311,17.7652402449678));
#58375=CARTESIAN_POINT('Ctrl Pts',(30.78153371397,0.890859052478792,17.7544254485094));
#58376=CARTESIAN_POINT('Ctrl Pts',(30.9814968973686,0.663646825098318,17.7340906520159));
#58377=CARTESIAN_POINT('Ctrl Pts',(31.0581916579204,0.532910080900297,17.7252873077101));
#58378=CARTESIAN_POINT('Ctrl Pts',(31.1603311881744,0.243593094566313,17.7047725710215));
#58379=CARTESIAN_POINT('Ctrl Pts',(31.1824208985569,0.0870303935487086,
17.6936711053685));
#58380=CARTESIAN_POINT('Ctrl Pts',(31.1643265939555,-0.219589452433675,
17.6719294666093));
#58381=CARTESIAN_POINT('Ctrl Pts',(31.126629625228,-0.366880394031282,17.6614854379963));
#58382=CARTESIAN_POINT('Ctrl Pts',(30.9959732548856,-0.642739672382233,
17.6419249533869));
#58383=CARTESIAN_POINT('Ctrl Pts',(30.9029171297163,-0.76800751067264,17.6323839709445));
#58384=CARTESIAN_POINT('Ctrl Pts',(30.6735549835348,-0.97540763183831,17.6109462657373));
#58385=CARTESIAN_POINT('Ctrl Pts',(30.5395284406378,-1.05546393695081,17.5998777123224));
#58386=CARTESIAN_POINT('Ctrl Pts',(30.2672665806154,-1.15230702152505,17.5797252955804));
#58387=CARTESIAN_POINT('Ctrl Pts',(30.1340643685791,-1.17524047358085,17.5707325810151));
#58388=CARTESIAN_POINT('Ctrl Pts',(29.9999999999999,-1.17524047358085,17.5625));
#58389=CARTESIAN_POINT('Ctrl Pts',(30.0000000000005,-1.17524047358085,17.5));
#58390=CARTESIAN_POINT('Ctrl Pts',(30.033668671514,-1.17524047358084,17.5020675147979));
#58391=CARTESIAN_POINT('Ctrl Pts',(30.0673733741507,-1.17379373295066,17.504188534545));
#58392=CARTESIAN_POINT('Ctrl Pts',(30.2512194694897,-1.15793171152857,17.5160404635345));
#58393=CARTESIAN_POINT('Ctrl Pts',(30.3974945854731,-1.11619705184184,17.5265025277916));
#58394=CARTESIAN_POINT('Ctrl Pts',(30.6715286389123,-0.977122112696594,
17.5482610478741));
#58395=CARTESIAN_POINT('Ctrl Pts',(30.7956391457863,-0.8790277241657,17.559360198049));
#58396=CARTESIAN_POINT('Ctrl Pts',(30.9938921656194,-0.644908297614295,
17.579834863399));
#58397=CARTESIAN_POINT('Ctrl Pts',(31.0680432549382,-0.51284781086492,17.5886352571811));
#58398=CARTESIAN_POINT('Ctrl Pts',(31.1634155774875,-0.225635628704456,
17.6090007475224));
#58399=CARTESIAN_POINT('Ctrl Pts',(31.1828424433655,-0.0729412614644995,
17.6198279193986));
#58400=CARTESIAN_POINT('Ctrl Pts',(31.1620678214981,0.234707081573543,17.6416424862861));
#58401=CARTESIAN_POINT('Ctrl Pts',(31.120724241081,0.386638085314584,17.6524155299848));
#58402=CARTESIAN_POINT('Ctrl Pts',(30.9842587758127,0.659238100700609,17.6717449084903));
#58403=CARTESIAN_POINT('Ctrl Pts',(30.8929036275603,0.778529076192667,17.6811039637465));
#58404=CARTESIAN_POINT('Ctrl Pts',(30.6664518626416,0.98022024209091,17.7021605454119));
#58405=CARTESIAN_POINT('Ctrl Pts',(30.5321662358965,1.05914504613978,17.7132048926221));
#58406=CARTESIAN_POINT('Ctrl Pts',(30.2394356343315,1.16107865610412,17.7347947253164));
#58407=CARTESIAN_POINT('Ctrl Pts',(30.0837395746803,1.18253750639866,17.7445990404306));
#58408=CARTESIAN_POINT('Ctrl Pts',(29.7783085058998,1.16389753061854,17.7640157086725));
#58409=CARTESIAN_POINT('Ctrl Pts',(29.6313883618284,1.12601470121935,17.7743808208261));
#58410=CARTESIAN_POINT('Ctrl Pts',(29.3545393068819,0.994469365010162,17.7960452510406));
#58411=CARTESIAN_POINT('Ctrl Pts',(29.2282096618696,0.899966183720928,17.8071533516094));
#58412=CARTESIAN_POINT('Ctrl Pts',(29.0235241701317,0.671134004766118,17.8278355674102));
#58413=CARTESIAN_POINT('Ctrl Pts',(28.9455840780504,0.540492245953914,17.8366750601186));
#58414=CARTESIAN_POINT('Ctrl Pts',(28.8428376707835,0.255550540540784,17.8568795566889));
#58415=CARTESIAN_POINT('Ctrl Pts',(28.819515816648,0.103803872119581,17.8676395296357));
#58416=CARTESIAN_POINT('Ctrl Pts',(28.8321334408652,-0.203924479248023,
17.8894597697118));
#58417=CARTESIAN_POINT('Ctrl Pts',(28.8694569005926,-0.356918085677502,
17.9003081598831));
#58418=CARTESIAN_POINT('Ctrl Pts',(28.9987062002081,-0.633072693900888,
17.9198895855878));
#58419=CARTESIAN_POINT('Ctrl Pts',(29.0868937988439,-0.754733453808526,
17.9290197269592));
#58420=CARTESIAN_POINT('Ctrl Pts',(29.3076626510103,-0.962047131353844,
17.9499266732212));
#58421=CARTESIAN_POINT('Ctrl Pts',(29.439425880769,-1.04432722335896,17.9609350833968));
#58422=CARTESIAN_POINT('Ctrl Pts',(29.7165797609128,-1.14942800619046,17.981680673977));
#58423=CARTESIAN_POINT('Ctrl Pts',(29.857771536572,-1.17524047358086,17.9912660809114));
#58424=CARTESIAN_POINT('Ctrl Pts',(30.0000000000001,-1.17524047358085,18.));
#58425=CARTESIAN_POINT('Origin',(30.,-1.21864324187371E-14,15.78125));
#58426=CARTESIAN_POINT('',(29.9999999999999,-1.17524047358085,18.5625));
#58427=CARTESIAN_POINT('',(30.,-1.17524047358085,18.5));
#58428=CARTESIAN_POINT('',(30.,-1.17524047358085,15.78125));
#58429=CARTESIAN_POINT('Ctrl Pts',(29.9999999999998,-1.17524047358085,18.5625));
#58430=CARTESIAN_POINT('Ctrl Pts',(29.9448799883238,-1.17524047358085,18.5591152083026));
#58431=CARTESIAN_POINT('Ctrl Pts',(29.8897199177939,-1.17136342891428,18.5555905009623));
#58432=CARTESIAN_POINT('Ctrl Pts',(29.6792216999803,-1.14149919812993,18.5416054964814));
#58433=CARTESIAN_POINT('Ctrl Pts',(29.5295600411529,-1.08838822549331,18.5305321396985));
#58434=CARTESIAN_POINT('Ctrl Pts',(29.2651715824486,-0.929562358041593,
18.5086656889335));
#58435=CARTESIAN_POINT('Ctrl Pts',(29.1517563578462,-0.827380506823195,
18.4980783953365));
#58436=CARTESIAN_POINT('Ctrl Pts',(28.9690035888602,-0.584433789122884,
18.4782426038757));
#58437=CARTESIAN_POINT('Ctrl Pts',(28.9018681826973,-0.445680079983302,
18.4691020486872));
#58438=CARTESIAN_POINT('Ctrl Pts',(28.8237798560613,-0.147691887525462,
18.4479724586759));
#58439=CARTESIAN_POINT('Ctrl Pts',(28.8145788645707,0.00884554058040183,
18.4368727850612));
#58440=CARTESIAN_POINT('Ctrl Pts',(28.8567482751501,0.310649796974269,18.4154726075955));
#58441=CARTESIAN_POINT('Ctrl Pts',(28.9054833559201,0.453415390787842,18.4053494599629));
#58442=CARTESIAN_POINT('Ctrl Pts',(29.0569965845258,0.718468314308288,18.3865552266777));
#58443=CARTESIAN_POINT('Ctrl Pts',(29.1604683184012,0.83707730034545,18.3760428358642));
#58444=CARTESIAN_POINT('Ctrl Pts',(29.4058248734932,1.0255154952049,18.3542952223602));
#58445=CARTESIAN_POINT('Ctrl Pts',(29.544631443668,1.0942445155017,18.3433347331662));
#58446=CARTESIAN_POINT('Ctrl Pts',(29.8366929775619,1.17335763361873,18.3225950580774));
#58447=CARTESIAN_POINT('Ctrl Pts',(29.986714530993,1.18458952273488,18.3136472884771));
#58448=CARTESIAN_POINT('Ctrl Pts',(30.2898186404183,1.14957783224746,18.2937930749288));
#58449=CARTESIAN_POINT('Ctrl Pts',(30.4396462258347,1.10100720458506,18.2828705011767));
#58450=CARTESIAN_POINT('Ctrl Pts',(30.7078144176317,0.95036138884417,18.2610619591969));
#58451=CARTESIAN_POINT('Ctrl Pts',(30.8244348872713,0.851181456147988,18.250384268188));
#58452=CARTESIAN_POINT('Ctrl Pts',(31.0135314789776,0.613960284599869,18.2303619093383));
#58453=CARTESIAN_POINT('Ctrl Pts',(31.0842069749077,0.478217809229905,18.2214092168781));
#58454=CARTESIAN_POINT('Ctrl Pts',(31.1712537448649,0.183351777827692,18.2005010114207));
#58455=CARTESIAN_POINT('Ctrl Pts',(31.1852144107931,0.026684835425868,18.1893921542744));
#58456=CARTESIAN_POINT('Ctrl Pts',(31.151894218573,-0.277120859310672,18.1678500598715));
#58457=CARTESIAN_POINT('Ctrl Pts',(31.1071955868466,-0.421659698179358,
18.1576011759113));
#58458=CARTESIAN_POINT('Ctrl Pts',(30.9623980704004,-0.692609521716023,
18.1383888083414));
#58459=CARTESIAN_POINT('Ctrl Pts',(30.8611688824271,-0.815074867780112,
18.1281515944925));
#58460=CARTESIAN_POINT('Ctrl Pts',(30.6191698348665,-1.010677278137,18.1063561595037));
#58461=CARTESIAN_POINT('Ctrl Pts',(30.481744547401,-1.08294295672688,18.0953551039148));
#58462=CARTESIAN_POINT('Ctrl Pts',(30.2255864017037,-1.15894806928573,18.0769303627887));
#58463=CARTESIAN_POINT('Ctrl Pts',(30.1130100641695,-1.17524047358085,18.0694396851576));
#58464=CARTESIAN_POINT('Ctrl Pts',(29.9999999999995,-1.17524047358085,18.0625));
#58465=CARTESIAN_POINT('Ctrl Pts',(30.0000000000001,-1.17524047358085,18.));
#58466=CARTESIAN_POINT('Ctrl Pts',(30.0145244311397,-1.17524047358085,18.0008919115297));
#58467=CARTESIAN_POINT('Ctrl Pts',(30.0290585224951,-1.1749712210064,18.0017939622806));
#58468=CARTESIAN_POINT('Ctrl Pts',(30.1935181174434,-1.16886648233729,18.0121094792412));
#58469=CARTESIAN_POINT('Ctrl Pts',(30.3409577753235,-1.13464684718278,18.022376619604));
#58470=CARTESIAN_POINT('Ctrl Pts',(30.6202928748417,-1.01029888563142,18.0439385382044));
#58471=CARTESIAN_POINT('Ctrl Pts',(30.7486368752819,-0.919248747112441,
18.055047912384));
#58472=CARTESIAN_POINT('Ctrl Pts',(30.9593869332128,-0.695506306327382,
18.0759220888488));
#58473=CARTESIAN_POINT('Ctrl Pts',(31.0409497614259,-0.566191331080132,
18.084852802908));
#58474=CARTESIAN_POINT('Ctrl Pts',(31.1506054030915,-0.283424289026694,
18.1049030995926));
#58475=CARTESIAN_POINT('Ctrl Pts',(31.1775442736485,-0.132654402671248,
18.1155938113905));
#58476=CARTESIAN_POINT('Ctrl Pts',(31.1725598607287,0.174951078257229,18.1374053390341));
#58477=CARTESIAN_POINT('Ctrl Pts',(31.1390289434739,0.328840847644919,18.148317273857));
#58478=CARTESIAN_POINT('Ctrl Pts',(31.0165781905916,0.608264397522364,18.1681304919571));
#58479=CARTESIAN_POINT('Ctrl Pts',(30.9313199722933,0.732167484063905,18.1771012136858));
#58480=CARTESIAN_POINT('Ctrl Pts',(30.7158345492886,0.944633593585631,18.1978663898215));
#58481=CARTESIAN_POINT('Ctrl Pts',(30.5864762504196,1.02994768568734,18.208834685427));
#58482=CARTESIAN_POINT('Ctrl Pts',(30.3000115977578,1.14695518635867,18.2305741665317));
#58483=CARTESIAN_POINT('Ctrl Pts',(30.1454149851266,1.17656763909288,18.2410233510493));
#58484=CARTESIAN_POINT('Ctrl Pts',(29.8400425266379,1.17387642244061,18.2598709770579));
#58485=CARTESIAN_POINT('Ctrl Pts',(29.6921041520777,1.14400535739554,18.2700145693908));
#58486=CARTESIAN_POINT('Ctrl Pts',(29.4100579886469,1.02824734385133,18.2914384223622));
#58487=CARTESIAN_POINT('Ctrl Pts',(29.2794434337127,0.941343746808855,18.3025402156205));
#58488=CARTESIAN_POINT('Ctrl Pts',(29.061555804029,0.723734320476339,18.3236352554819));
#58489=CARTESIAN_POINT('Ctrl Pts',(28.9756558249342,0.595970538008072,18.3327412345668));
#58490=CARTESIAN_POINT('Ctrl Pts',(28.8579142725366,0.315809924655313,18.3526067159761));
#58491=CARTESIAN_POINT('Ctrl Pts',(28.8267878271973,0.166290213657428,18.3632087809973));
#58492=CARTESIAN_POINT('Ctrl Pts',(28.8228465258246,-0.142252171918218,
18.3850867421828));
#58493=CARTESIAN_POINT('Ctrl Pts',(28.8524261916584,-0.298357527348321,
18.3961557786154));
#58494=CARTESIAN_POINT('Ctrl Pts',(28.9683032793772,-0.582326286319503,
18.4162912860112));
#58495=CARTESIAN_POINT('Ctrl Pts',(29.0505638845767,-0.708574806470949,
18.4251522948912));
#58496=CARTESIAN_POINT('Ctrl Pts',(29.2606233813178,-0.926260402003281,
18.4457693278011));
#58497=CARTESIAN_POINT('Ctrl Pts',(29.3874559625716,-1.01460273580079,18.4566898874478));
#58498=CARTESIAN_POINT('Ctrl Pts',(29.670332667393,-1.13876808411125,18.4784628134696));
#58499=CARTESIAN_POINT('Ctrl Pts',(29.8241031351402,-1.17241612945781,18.4890984491449));
#58500=CARTESIAN_POINT('Ctrl Pts',(29.9866645216768,-1.17518374723239,18.4991790881359));
#58501=CARTESIAN_POINT('Ctrl Pts',(29.9933333092278,-1.17524047358085,18.4995906140276));
#58502=CARTESIAN_POINT('Ctrl Pts',(30.,-1.17524047358085,18.5));
#58503=CARTESIAN_POINT('Origin',(30.,-1.21864324187371E-14,15.78125));
#58504=CARTESIAN_POINT('',(30.,-1.17524047358085,19.0625));
#58505=CARTESIAN_POINT('',(29.9999999999998,-1.17524047358085,18.9999999999999));
#58506=CARTESIAN_POINT('',(30.,-1.17524047358085,15.78125));
#58507=CARTESIAN_POINT('Ctrl Pts',(30.,-1.17524047358085,19.0625));
#58508=CARTESIAN_POINT('Ctrl Pts',(29.9235115354988,-1.17524047358085,19.0578030213218));
#58509=CARTESIAN_POINT('Ctrl Pts',(29.84704716558,-1.16777574293408,19.0528428696387));
#58510=CARTESIAN_POINT('Ctrl Pts',(29.6182505756017,-1.12246086107485,19.0371864213689));
#58511=CARTESIAN_POINT('Ctrl Pts',(29.4724485773796,-1.06175746863862,19.0260808977107));
#58512=CARTESIAN_POINT('Ctrl Pts',(29.2180805672544,-0.890185564352666,
19.0043778847458));
#58513=CARTESIAN_POINT('Ctrl Pts',(29.1106251205818,-0.782854361416016,
18.9939740034863));
#58514=CARTESIAN_POINT('Ctrl Pts',(28.9394765622835,-0.529653947083613,
18.9744872677464));
#58515=CARTESIAN_POINT('Ctrl Pts',(28.8789010658566,-0.385229961133875,
18.9648156834562));
#58516=CARTESIAN_POINT('Ctrl Pts',(28.8174805423046,-0.0817855742350542,
18.9432992084794));
#58517=CARTESIAN_POINT('Ctrl Pts',(28.8169771571136,0.0741472763924911,
18.9322424039265));
#58518=CARTESIAN_POINT('Ctrl Pts',(28.8752567923883,0.371953492557534,18.9111257173945));
#58519=CARTESIAN_POINT('Ctrl Pts',(28.9314131886074,0.511361040736907,18.9016564371649));
#58520=CARTESIAN_POINT('Ctrl Pts',(29.0965385184593,0.767636822695621,18.8824305405978));
#58521=CARTESIAN_POINT('Ctrl Pts',(29.2062331582591,0.880579083863968,18.8716902227143));
#58522=CARTESIAN_POINT('Ctrl Pts',(29.4605419802015,1.05521085002794,18.8498823608196));
#58523=CARTESIAN_POINT('Ctrl Pts',(29.6020069692685,1.11628678080371,18.8390299549287));
#58524=CARTESIAN_POINT('Ctrl Pts',(29.8977163387384,1.18033932535056,18.8186002283572));
#58525=CARTESIAN_POINT('Ctrl Pts',(30.0489012110254,1.18375239923791,18.8097988699583));
#58526=CARTESIAN_POINT('Ctrl Pts',(30.351304458352,1.13241772416719,18.7894089839185));
#58527=CARTESIAN_POINT('Ctrl Pts',(30.4990888608278,1.07549105419273,18.7783156243515));
#58528=CARTESIAN_POINT('Ctrl Pts',(30.7585582244441,0.910237971254531,18.7565233749656));
#58529=CARTESIAN_POINT('Ctrl Pts',(30.869032001546,0.80544751578808,18.7460242240482));
#58530=CARTESIAN_POINT('Ctrl Pts',(31.0460310070461,0.557381504027199,18.7263602597134));
#58531=CARTESIAN_POINT('Ctrl Pts',(31.1099298338315,0.41584148204013,18.7169862690792));
#58532=CARTESIAN_POINT('Ctrl Pts',(31.1797989523814,0.115104609901925,18.6956617771348));
#58533=CARTESIAN_POINT('Ctrl Pts',(31.1846835245906,-0.0411926090939851,
18.6845791361414));
#58534=CARTESIAN_POINT('Ctrl Pts',(31.134503841219,-0.341119161052378,18.6633121019541));
#58535=CARTESIAN_POINT('Ctrl Pts',(31.082082323541,-0.482198917475646,18.6535190714213));
#58536=CARTESIAN_POINT('Ctrl Pts',(30.9238582069445,-0.74295817680152,18.6345580062792));
#58537=CARTESIAN_POINT('Ctrl Pts',(30.8172746962663,-0.85879990158245,18.6239059387776));
#58538=CARTESIAN_POINT('Ctrl Pts',(30.5674863902569,-1.04046451233651,18.6021263306283));
#58539=CARTESIAN_POINT('Ctrl Pts',(30.4273223446806,-1.10544579712631,18.5912153532567));
#58540=CARTESIAN_POINT('Ctrl Pts',(30.1872213612661,-1.164041447155,18.5743938756203));
#58541=CARTESIAN_POINT('Ctrl Pts',(30.0936931422672,-1.17524047358085,18.5682534779185));
#58542=CARTESIAN_POINT('Ctrl Pts',(29.9999999999998,-1.17524047358085,18.5625));
#58543=CARTESIAN_POINT('Ctrl Pts',(30.,-1.17524047358085,18.5));
#58544=CARTESIAN_POINT('Ctrl Pts',(30.1423690472132,-1.17524047358085,18.5087425520117));
#58545=CARTESIAN_POINT('Ctrl Pts',(30.2836710124158,-1.14937338085773,18.5183366621019));
#58546=CARTESIAN_POINT('Ctrl Pts',(30.561858730089,-1.04379601878612,18.5391626347549));
#58547=CARTESIAN_POINT('Ctrl Pts',(30.6944274791866,-0.96071277520592,18.550248984724));
#58548=CARTESIAN_POINT('Ctrl Pts',(30.9187624839086,-0.748784365111015,
18.5715385296331));
#58549=CARTESIAN_POINT('Ctrl Pts',(31.0086541273172,-0.622420436396325,
18.5808657390843));
#58550=CARTESIAN_POINT('Ctrl Pts',(31.1336634286392,-0.344659292163419,
18.6005610801994));
#58551=CARTESIAN_POINT('Ctrl Pts',(31.1685065373813,-0.196359387070609,
18.6110766518651));
#58552=CARTESIAN_POINT('Ctrl Pts',(31.1804379609257,0.111178530247992,18.6328833887437));
#58553=CARTESIAN_POINT('Ctrl Pts',(31.1550790566304,0.267584160665563,18.6439737169172));
#58554=CARTESIAN_POINT('Ctrl Pts',(31.0469271232095,0.554595748580105,18.6643249836272));
#58555=CARTESIAN_POINT('Ctrl Pts',(30.9678100781097,0.68335841703765,18.6731299773448));
#58556=CARTESIAN_POINT('Ctrl Pts',(30.763452167876,0.90645295543942,18.6935886563282));
#58557=CARTESIAN_POINT('Ctrl Pts',(30.6393299618342,0.997879761179756,18.7044521341951));
#58558=CARTESIAN_POINT('Ctrl Pts',(30.3602369836734,1.12947461105548,18.7262561139589));
#58559=CARTESIAN_POINT('Ctrl Pts',(30.207398548302,1.16725893034935,18.7369811620628));
#58560=CARTESIAN_POINT('Ctrl Pts',(29.9028111520737,1.18064726329168,18.7561598319717));
#58561=CARTESIAN_POINT('Ctrl Pts',(29.7540809815473,1.15884794274813,18.7656824913455));
#58562=CARTESIAN_POINT('Ctrl Pts',(29.4674235177593,1.05897426017317,18.7868263546523));
#58563=CARTESIAN_POINT('Ctrl Pts',(29.332959967187,0.979858413005439,18.7978884009434));
#58564=CARTESIAN_POINT('Ctrl Pts',(29.1020498086111,0.773870883761844,18.8193710843283));
#58565=CARTESIAN_POINT('Ctrl Pts',(29.0080096312967,0.648942084974305,18.8289851559772));
#58566=CARTESIAN_POINT('Ctrl Pts',(28.8756172989166,0.373674108747255,18.8485037128466));
#58567=CARTESIAN_POINT('Ctrl Pts',(28.8370493704244,0.226703861544607,18.85892500183));
#58568=CARTESIAN_POINT('Ctrl Pts',(28.8170693542027,-0.0796098764074361,
18.8806449352421));
#58569=CARTESIAN_POINT('Ctrl Pts',(28.838156352639,-0.236207536581086,18.8917488797605));
#58570=CARTESIAN_POINT('Ctrl Pts',(28.9384458248014,-0.526222673597261,
18.9123131205504));
#58571=CARTESIAN_POINT('Ctrl Pts',(29.0143989785152,-0.657569956199922,
18.921123179589));
#58572=CARTESIAN_POINT('Ctrl Pts',(29.2130173163762,-0.886033452067211,
18.9414197543903));
#58573=CARTESIAN_POINT('Ctrl Pts',(29.3343580168877,-0.980462303689547,
18.9522188602181));
#58574=CARTESIAN_POINT('Ctrl Pts',(29.609473809437,-1.11936682716347,18.9740377655105));
#58575=CARTESIAN_POINT('Ctrl Pts',(29.7612660994758,-1.16125829944545,18.9848441861849));
#58576=CARTESIAN_POINT('Ctrl Pts',(29.9445511530895,-1.1742603871282,18.9965602675684));
#58577=CARTESIAN_POINT('Ctrl Pts',(29.9722886221142,-1.17524047358085,18.998298308746));
#58578=CARTESIAN_POINT('Ctrl Pts',(29.9999999999996,-1.17524047358085,18.9999999999999));
#58579=CARTESIAN_POINT('Origin',(30.,-1.21864324187371E-14,15.78125));
#58580=CARTESIAN_POINT('',(30.0000000000001,-1.17524047358085,19.5625));
#58581=CARTESIAN_POINT('',(29.9999999999998,-1.17524047358085,19.4999999999999));
#58582=CARTESIAN_POINT('',(30.,-1.17524047358085,15.78125));
#58583=CARTESIAN_POINT('Ctrl Pts',(30.0000000000003,-1.17524047358085,19.5625));
#58584=CARTESIAN_POINT('Ctrl Pts',(29.9013941092948,-1.17524047358088,19.5564448416279));
#58585=CARTESIAN_POINT('Ctrl Pts',(29.8029987638489,-1.16283641906691,19.549962842264));
#58586=CARTESIAN_POINT('Ctrl Pts',(29.5564668004839,-1.09938994466242,19.5325744732568));
#58587=CARTESIAN_POINT('Ctrl Pts',(29.415037771559,-1.03111229808663,19.5214689478566));
#58588=CARTESIAN_POINT('Ctrl Pts',(29.1716434679328,-0.847005065425004,
19.4999953804452));
#58589=CARTESIAN_POINT('Ctrl Pts',(29.0705827398005,-0.734710314058229,
19.4898082076353));
#58590=CARTESIAN_POINT('Ctrl Pts',(28.9129094963582,-0.472970867922037,
19.4708462190468));
#58591=CARTESIAN_POINT('Ctrl Pts',(28.8598073237114,-0.32477237703938,19.4605287888834));
#58592=CARTESIAN_POINT('Ctrl Pts',(28.8149047814539,-0.0184511328725056,
19.4388083232246));
#58593=CARTESIAN_POINT('Ctrl Pts',(28.8226412643137,0.136461808695805,19.4278238378469));
#58594=CARTESIAN_POINT('Ctrl Pts',(28.8961732267534,0.430084241574931,19.4070038128194));
#58595=CARTESIAN_POINT('Ctrl Pts',(28.9595331463533,0.5664127336681,19.3979778677293));
#58596=CARTESIAN_POINT('Ctrl Pts',(29.137896746023,0.813817787616469,19.3782535402653));
#58597=CARTESIAN_POINT('Ctrl Pts',(29.2533816215898,0.92090330809607,19.3673653008166));
#58598=CARTESIAN_POINT('Ctrl Pts',(29.5158730245192,1.08160589182486,19.3455488072285));
#58599=CARTESIAN_POINT('Ctrl Pts',(29.6595524720356,1.13505921849913,19.3348306663965));
#58600=CARTESIAN_POINT('Ctrl Pts',(29.9586626554596,1.18420822106571,19.3147204900089));
#58601=CARTESIAN_POINT('Ctrl Pts',(30.1111738123977,1.17970362181747,19.305831310076));
#58602=CARTESIAN_POINT('Ctrl Pts',(30.4108580361143,1.11207867833533,19.2850308420592));
#58603=CARTESIAN_POINT('Ctrl Pts',(30.5546592354692,1.0477915906526,19.2739211274165));
#58604=CARTESIAN_POINT('Ctrl Pts',(30.8039627363725,0.870265103601911,19.2523180019705));
#58605=CARTESIAN_POINT('Ctrl Pts',(30.9084512058835,0.760562755820576,19.242012249931));
#58606=CARTESIAN_POINT('Ctrl Pts',(31.0738897348627,0.502419631313023,19.2227009162624));
#58607=CARTESIAN_POINT('Ctrl Pts',(31.1311837638208,0.355135076925594,19.2126817312365));
#58608=CARTESIAN_POINT('Ctrl Pts',(31.1842706831827,0.04913932312708,19.1909843452775));
#58609=CARTESIAN_POINT('Ctrl Pts',(31.1805124566442,-0.106321035688241,
19.1799610439256));
#58610=CARTESIAN_POINT('Ctrl Pts',(31.1143513914742,-0.401996025434437,
19.1589954772754));
#58611=CARTESIAN_POINT('Ctrl Pts',(31.0545027280943,-0.539801328735837,
19.1497832518808));
#58612=CARTESIAN_POINT('Ctrl Pts',(30.8825757787308,-0.791565442014421,
19.1302996391962));
#58613=CARTESIAN_POINT('Ctrl Pts',(30.7698754890686,-0.90154647307845,19.1194797380197));
#58614=CARTESIAN_POINT('Ctrl Pts',(30.5112798180774,-1.06909180183037,19.0976598713853));
#58615=CARTESIAN_POINT('Ctrl Pts',(30.3686300461772,-1.12627173763864,19.0868728383175));
#58616=CARTESIAN_POINT('Ctrl Pts',(30.146651557919,-1.16837939048486,19.071748782068));
#58617=CARTESIAN_POINT('Ctrl Pts',(30.0733297917687,-1.17524047358085,19.0670030119334));
#58618=CARTESIAN_POINT('Ctrl Pts',(30.,-1.17524047358085,19.0625));
#58619=CARTESIAN_POINT('Ctrl Pts',(29.9999999999996,-1.17524047358085,18.9999999999999));
#58620=CARTESIAN_POINT('Ctrl Pts',(30.1208018343283,-1.17524047358085,19.0074181596379));
#58621=CARTESIAN_POINT('Ctrl Pts',(30.2410273417982,-1.15662316578329,19.0154609815185));
#58622=CARTESIAN_POINT('Ctrl Pts',(30.5033214237856,-1.07312795539109,19.0345280681775));
#58623=CARTESIAN_POINT('Ctrl Pts',(30.6395388198866,-0.997960158889978,
19.0455578408927));
#58624=CARTESIAN_POINT('Ctrl Pts',(30.876878941369,-0.797935916319293,19.067223952545));
#58625=CARTESIAN_POINT('Ctrl Pts',(30.9750570407496,-0.674426741281125,
19.0771781033725));
#58626=CARTESIAN_POINT('Ctrl Pts',(31.1146479426385,-0.401644540658674,
19.0965204001729));
#58627=CARTESIAN_POINT('Ctrl Pts',(31.1567939343853,-0.256055794064216,
19.1068437304378));
#58628=CARTESIAN_POINT('Ctrl Pts',(31.1845453028865,0.0488704061743495,
19.1284652770555));
#58629=CARTESIAN_POINT('Ctrl Pts',(31.1676027188842,0.205546638234067,19.1395747929079));
#58630=CARTESIAN_POINT('Ctrl Pts',(31.0749923240704,0.498408501569657,19.1603408878703));
#58631=CARTESIAN_POINT('Ctrl Pts',(31.0021074917097,0.632295920687204,19.1692134966416));
#58632=CARTESIAN_POINT('Ctrl Pts',(30.8090318381138,0.865881565613648,19.1893513074212));
#58633=CARTESIAN_POINT('Ctrl Pts',(30.6904244547157,0.963111668252584,19.2000818814201));
#58634=CARTESIAN_POINT('Ctrl Pts',(30.419302827982,1.10891198567697,19.2218999959461));
#58635=CARTESIAN_POINT('Ctrl Pts',(30.2686205389783,1.15471361101177,19.232776883577));
#58636=CARTESIAN_POINT('Ctrl Pts',(29.9650775926592,1.18413115670169,19.2524597117397));
#58637=CARTESIAN_POINT('Ctrl Pts',(29.8154193388389,1.17018311968912,19.2615139711268));
#58638=CARTESIAN_POINT('Ctrl Pts',(29.5246945745281,1.08577187830739,19.2823593965739));
#58639=CARTESIAN_POINT('Ctrl Pts',(29.3869225275025,1.01437069769904,19.2933510961767));
#58640=CARTESIAN_POINT('Ctrl Pts',(29.1449076103833,0.821179121928182,19.3150620325829));
#58641=CARTESIAN_POINT('Ctrl Pts',(29.0436548787038,0.700625409307818,19.3253204220004));
#58642=CARTESIAN_POINT('Ctrl Pts',(28.8969987915807,0.43246305184088,19.3443351373923));
#58643=CARTESIAN_POINT('Ctrl Pts',(28.8509250755758,0.288512534702925,19.3545423049446));
#58644=CARTESIAN_POINT('Ctrl Pts',(28.8145962917767,-0.0146433580687103,
19.3760383235316));
#58645=CARTESIAN_POINT('Ctrl Pts',(28.8269416915671,-0.171282191603316,
19.3871451875491));
#58646=CARTESIAN_POINT('Ctrl Pts',(28.9109596159865,-0.467218400914038,
19.4081292766188));
#58647=CARTESIAN_POINT('Ctrl Pts',(28.9804361831083,-0.603975745967944,
19.4171374882925));
#58648=CARTESIAN_POINT('Ctrl Pts',(29.167379298401,-0.843150163563664,19.4370968570367));
#58649=CARTESIAN_POINT('Ctrl Pts',(29.2829166096857,-0.943363871775425,
19.447744685016));
#58650=CARTESIAN_POINT('Ctrl Pts',(29.5508199561077,-1.09737775425148,19.4696563740096));
#58651=CARTESIAN_POINT('Ctrl Pts',(29.7018004358378,-1.14764798506443,19.4807100016028));
#58652=CARTESIAN_POINT('Ctrl Pts',(29.9053565213586,-1.17238533019257,19.4940869386326));
#58653=CARTESIAN_POINT('Ctrl Pts',(29.9526999581129,-1.17524047358085,19.4970954144566));
#58654=CARTESIAN_POINT('Ctrl Pts',(29.9999999999997,-1.17524047358085,19.4999999999999));
#58655=CARTESIAN_POINT('Origin',(30.,-1.21864324187371E-14,15.78125));
#58656=CARTESIAN_POINT('',(30.0000000000003,-1.17524047358085,20.0625));
#58657=CARTESIAN_POINT('',(30.,-1.17524047358085,20.));
#58658=CARTESIAN_POINT('',(30.,-1.17524047358085,15.78125));
#58659=CARTESIAN_POINT('Ctrl Pts',(30.0000000000005,-1.17524047358085,20.0625));
#58660=CARTESIAN_POINT('Ctrl Pts',(29.8795085612599,-1.17524047358091,20.0551009010331));
#58661=CARTESIAN_POINT('Ctrl Pts',(29.7595622632698,-1.15671912815303,20.0470786269818));
#58662=CARTESIAN_POINT('Ctrl Pts',(29.4968909328774,-1.07331217196907,20.0279915033172));
#58663=CARTESIAN_POINT('Ctrl Pts',(29.3601452160293,-0.997848639613717,
20.0169188027128));
#58664=CARTESIAN_POINT('Ctrl Pts',(29.1279895360134,-0.801888849412877,
19.9957151555763));
#58665=CARTESIAN_POINT('Ctrl Pts',(29.0334325756294,-0.684937055319331,
19.9860671564471));
#58666=CARTESIAN_POINT('Ctrl Pts',(28.8898211655935,-0.415941538872162,
19.9669933638564));
#58667=CARTESIAN_POINT('Ctrl Pts',(28.8445081931777,-0.265175978908636,
19.956302958832));
#58668=CARTESIAN_POINT('Ctrl Pts',(28.8156113317766,0.0421759568632406,
19.934509409435));
#58669=CARTESIAN_POINT('Ctrl Pts',(28.8311290214712,0.195715280521655,19.9236223238335));
#58670=CARTESIAN_POINT('Ctrl Pts',(28.9191574051752,0.485137216573778,19.9031001454256));
#58671=CARTESIAN_POINT('Ctrl Pts',(28.9896097101006,0.618617028321211,19.8942800985803));
#58672=CARTESIAN_POINT('Ctrl Pts',(29.1815016413357,0.8578593810217,19.8740144260076));
#58673=CARTESIAN_POINT('Ctrl Pts',(29.3033374545183,0.95943115864218,19.8629316730427));
#58674=CARTESIAN_POINT('Ctrl Pts',(29.5744131919249,1.10584185120943,19.8410947363937));
#58675=CARTESIAN_POINT('Ctrl Pts',(29.7199575824398,1.1513488317962,19.8305438014147));
#58676=CARTESIAN_POINT('Ctrl Pts',(30.0223936436952,1.18496921575338,19.8107799381662));
#58677=CARTESIAN_POINT('Ctrl Pts',(30.17645595477,1.17197553997772,19.8015484961906));
#58678=CARTESIAN_POINT('Ctrl Pts',(30.4728526803367,1.08704252391974,19.7803362699347));
#58679=CARTESIAN_POINT('Ctrl Pts',(30.6120360120599,1.01521369720442,19.7692427449689));
#58680=CARTESIAN_POINT('Ctrl Pts',(30.8500255075595,0.825212607475584,19.7478921149936));
#58681=CARTESIAN_POINT('Ctrl Pts',(30.9478859340228,0.710618012755788,19.7378881282691));
#58682=CARTESIAN_POINT('Ctrl Pts',(31.0987101974267,0.445344450081356,19.7190782500187));
#58683=CARTESIAN_POINT('Ctrl Pts',(31.148011535677,0.295869142851177,19.7084793335565));
#58684=CARTESIAN_POINT('Ctrl Pts',(31.1851397417262,-0.0109614779842622,
19.6867227492848));
#58685=CARTESIAN_POINT('Ctrl Pts',(31.1736153786499,-0.165256365490512,
19.6757820885594));
#58686=CARTESIAN_POINT('Ctrl Pts',(31.093043155488,-0.456865689692268,19.6551048079831));
#58687=CARTESIAN_POINT('Ctrl Pts',(31.0262715370984,-0.591802059151614,
19.6462060198927));
#58688=CARTESIAN_POINT('Ctrl Pts',(30.8407896047275,-0.836102523209368,
19.6261546414896));
#58689=CARTESIAN_POINT('Ctrl Pts',(30.7213221432726,-0.941101033293042,
19.6150958330235));
#58690=CARTESIAN_POINT('Ctrl Pts',(30.4533957183897,-1.09478566221008,19.5931944001043));
#58691=CARTESIAN_POINT('Ctrl Pts',(30.3086782810935,-1.14405280540599,19.5825609345826));
#58692=CARTESIAN_POINT('Ctrl Pts',(30.1059062370161,-1.17166523878134,19.5691302110914));
#58693=CARTESIAN_POINT('Ctrl Pts',(30.0529306288365,-1.17524047358084,19.5657503467901));
#58694=CARTESIAN_POINT('Ctrl Pts',(30.0000000000003,-1.17524047358085,19.5625));
#58695=CARTESIAN_POINT('Ctrl Pts',(29.9999999999997,-1.17524047358085,19.4999999999999));
#58696=CARTESIAN_POINT('Ctrl Pts',(30.1013134091967,-1.17524047358085,19.5062214207844));
#58697=CARTESIAN_POINT('Ctrl Pts',(30.2023703512557,-1.16214610944681,19.5128913366607));
#58698=CARTESIAN_POINT('Ctrl Pts',(30.4489451189351,-1.0968832859302,19.530346730545));
#58699=CARTESIAN_POINT('Ctrl Pts',(30.5880725807912,-1.02901377075515,19.5412964522821));
#58700=CARTESIAN_POINT('Ctrl Pts',(30.8343712795547,-0.842194481571482,
19.5630445243813));
#58701=CARTESIAN_POINT('Ctrl Pts',(30.9385897374703,-0.724253666071193,
19.5736257801046));
#58702=CARTESIAN_POINT('Ctrl Pts',(31.0916505061583,-0.460199205120922,
19.5923866032744));
#58703=CARTESIAN_POINT('Ctrl Pts',(31.1412805360793,-0.317836464065441,
19.6024630191855));
#58704=CARTESIAN_POINT('Ctrl Pts',(31.1853286010408,-0.0163533735884271,
19.6238404235873));
#58705=CARTESIAN_POINT('Ctrl Pts',(31.1771308821554,0.140138676220234,19.6349368795415));
#58706=CARTESIAN_POINT('Ctrl Pts',(31.1009443941398,0.438772825443172,19.6561122727154));
#58707=CARTESIAN_POINT('Ctrl Pts',(31.0345585763112,0.578169376036336,19.6653017627446));
#58708=CARTESIAN_POINT('Ctrl Pts',(30.8531427469532,0.82231181712456,19.6850978487155));
#58709=CARTESIAN_POINT('Ctrl Pts',(30.7404083067898,0.925109501957493,19.6956651705268));
#58710=CARTESIAN_POINT('Ctrl Pts',(30.4771535858122,1.08544747135218,19.7175156107599));
#58711=CARTESIAN_POINT('Ctrl Pts',(30.3279214291812,1.13945389596675,19.7285943399309));
#58712=CARTESIAN_POINT('Ctrl Pts',(30.0245530133835,1.1844610145353,19.7488191591971));
#58713=CARTESIAN_POINT('Ctrl Pts',(29.8738446796079,1.17798106878653,19.7576497404222));
#58714=CARTESIAN_POINT('Ctrl Pts',(29.5795308296296,1.10805786067705,19.7782019083499));
#58715=CARTESIAN_POINT('Ctrl Pts',(29.4390520876789,1.04399036655414,19.7890998131999));
#58716=CARTESIAN_POINT('Ctrl Pts',(29.1881857877585,0.86396490371117,19.8108875045287));
#58717=CARTESIAN_POINT('Ctrl Pts',(29.0808654270878,0.748795351686304,19.8215609892382));
#58718=CARTESIAN_POINT('Ctrl Pts',(28.9210185508111,0.489082061917269,19.8405846207479));
#58719=CARTESIAN_POINT('Ctrl Pts',(28.8677194354805,0.348399842158546,19.8502958472478));
#58720=CARTESIAN_POINT('Ctrl Pts',(28.8156254684423,0.0489678765559477,
19.8715278115659));
#58721=CARTESIAN_POINT('Ctrl Pts',(28.8194748723048,-0.107254256712007,
19.88260512842));
#58722=CARTESIAN_POINT('Ctrl Pts',(28.8873579337553,-0.408638429267571,
19.9039755188019));
#58723=CARTESIAN_POINT('Ctrl Pts',(28.9504754704978,-0.550854728104584,
19.9134143320288));
#58724=CARTESIAN_POINT('Ctrl Pts',(29.1260934520651,-0.800139160205639,
19.9330366884507));
#58725=CARTESIAN_POINT('Ctrl Pts',(29.2358570179041,-0.905539531949709,
19.9435138507578));
#58726=CARTESIAN_POINT('Ctrl Pts',(29.4941308064619,-1.07230397107708,19.9652862658853));
#58727=CARTESIAN_POINT('Ctrl Pts',(29.6414537313008,-1.13013161490591,19.9763832300743));
#58728=CARTESIAN_POINT('Ctrl Pts',(29.8633704190017,-1.16928660340085,19.9913988083098));
#58729=CARTESIAN_POINT('Ctrl Pts',(29.9316910379181,-1.17524047358085,19.9958053055382));
#58730=CARTESIAN_POINT('Ctrl Pts',(30.,-1.17524047358085,20.));
#58731=CARTESIAN_POINT('Origin',(30.,-1.21864324187371E-14,15.78125));
#58732=CARTESIAN_POINT('',(30.,-1.17524047358085,20.5625));
#58733=CARTESIAN_POINT('',(30.,-1.17524047358085,20.5));
#58734=CARTESIAN_POINT('',(30.,-1.17524047358085,15.78125));
#58735=CARTESIAN_POINT('Ctrl Pts',(30.0000000000001,-1.17524047358085,20.5625));
#58736=CARTESIAN_POINT('Ctrl Pts',(29.857466677664,-1.17524047358086,20.5537473602351));
#58737=CARTESIAN_POINT('Ctrl Pts',(29.7159780885029,-1.14931710991913,20.5441397949867));
#58738=CARTESIAN_POINT('Ctrl Pts',(29.4386327044728,-1.04389937724848,20.5233712075421));
#58739=CARTESIAN_POINT('Ctrl Pts',(29.3069416102485,-0.961526015490682,
20.5123639202805));
#58740=CARTESIAN_POINT('Ctrl Pts',(29.086333053172,-0.75405497378,20.4914612382194));
#58741=CARTESIAN_POINT('Ctrl Pts',(28.998234525789,-0.632326756560098,20.4823366930552));
#58742=CARTESIAN_POINT('Ctrl Pts',(28.8691902031313,-0.356072447869899,
20.4627481978422));
#58743=CARTESIAN_POINT('Ctrl Pts',(28.8319810448841,-0.203050335093991,
20.4518977863579));
#58744=CARTESIAN_POINT('Ctrl Pts',(28.8195943462911,0.104677105391675,20.4300776108702));
#58745=CARTESIAN_POINT('Ctrl Pts',(28.8430260194231,0.256395499280261,20.419319642799));
#58746=CARTESIAN_POINT('Ctrl Pts',(28.9459812899286,0.541272174450661,20.399119757359));
#58747=CARTESIAN_POINT('Ctrl Pts',(29.0240298052411,0.671873753047622,20.3902782906932));
#58748=CARTESIAN_POINT('Ctrl Pts',(29.2288981247322,0.900554058537053,20.3695902323474));
#58749=CARTESIAN_POINT('Ctrl Pts',(29.3552896087803,0.99495410007641,20.3584819910769));
#58750=CARTESIAN_POINT('Ctrl Pts',(29.6322160097862,1.12628386030684,20.3368204541948));
#58751=CARTESIAN_POINT('Ctrl Pts',(29.7791530812878,1.16405670631925,20.3264582018892));
#58752=CARTESIAN_POINT('Ctrl Pts',(30.0846260087116,1.18247957174534,20.3070466605788));
#58753=CARTESIAN_POINT('Ctrl Pts',(30.2403465146444,1.16089584876694,20.297232309072));
#58754=CARTESIAN_POINT('Ctrl Pts',(30.5330201521523,1.05871377596515,20.2756371654718));
#58755=CARTESIAN_POINT('Ctrl Pts',(30.6672316693715,0.979687699230499,20.2645937786601));
#58756=CARTESIAN_POINT('Ctrl Pts',(30.8935142020877,0.777827856358351,20.2435416089216));
#58757=CARTESIAN_POINT('Ctrl Pts',(30.9847747247484,0.658466900361099,20.2341902246224));
#58758=CARTESIAN_POINT('Ctrl Pts',(31.1210267097183,0.385760488516485,20.2148533018128));
#58759=CARTESIAN_POINT('Ctrl Pts',(31.1622514979646,0.233796400148884,20.2040779121667));
#58760=CARTESIAN_POINT('Ctrl Pts',(31.1827840987885,-0.0738574566284658,
20.1822629543138));
#58761=CARTESIAN_POINT('Ctrl Pts',(31.1632412224874,-0.226525134572718,
20.1714376749082));
#58762=CARTESIAN_POINT('Ctrl Pts',(31.0676501608268,-0.513670659031922,
20.1510769110961));
#58763=CARTESIAN_POINT('Ctrl Pts',(30.9933877261944,-0.645689071009633,
20.1422762056128));
#58764=CARTESIAN_POINT('Ctrl Pts',(30.7949445520148,-0.879653706050947,
20.1217953512642));
#58765=CARTESIAN_POINT('Ctrl Pts',(30.670767244765,-0.977642983856647,20.1106958256016));
#58766=CARTESIAN_POINT('Ctrl Pts',(30.3966473841018,-1.11649688166864,20.0889398730384));
#58767=CARTESIAN_POINT('Ctrl Pts',(30.2503518300705,-1.15811817698529,20.0784805729189));
#58768=CARTESIAN_POINT('Ctrl Pts',(30.0667947188483,-1.17381847353791,20.0666521235228));
#58769=CARTESIAN_POINT('Ctrl Pts',(30.0333795266192,-1.17524047358084,20.0645497590825));
#58770=CARTESIAN_POINT('Ctrl Pts',(30.0000000000005,-1.17524047358085,20.0625));
#58771=CARTESIAN_POINT('Ctrl Pts',(30.,-1.17524047358085,20.));
#58772=CARTESIAN_POINT('Ctrl Pts',(30.0810461612404,-1.17524047358085,20.0049768562329));
#58773=CARTESIAN_POINT('Ctrl Pts',(30.1620390634994,-1.16685998246121,20.0102475616837));
#58774=CARTESIAN_POINT('Ctrl Pts',(30.3910188268312,-1.11873616439623,20.0260148454886));
#58775=CARTESIAN_POINT('Ctrl Pts',(30.5327757448135,-1.05858684074315,20.0368523263699));
#58776=CARTESIAN_POINT('Ctrl Pts',(30.7881241531233,-0.885634167315425,
20.0586644967329));
#58777=CARTESIAN_POINT('Ctrl Pts',(30.8985424642913,-0.773390023616368,
20.0694245027186));
#58778=CARTESIAN_POINT('Ctrl Pts',(31.0652926267422,-0.518183463935382,
20.0887122685505));
#58779=CARTESIAN_POINT('Ctrl Pts',(31.1223297618129,-0.379162720763723,
20.0981145292327));
#58780=CARTESIAN_POINT('Ctrl Pts',(31.182501138976,-0.0818619977066759,
20.1191953725253));
#58781=CARTESIAN_POINT('Ctrl Pts',(31.1830210318339,0.0739680814447177,
20.1302448898124));
#58782=CARTESIAN_POINT('Ctrl Pts',(31.1235906320717,0.378032609170699,20.1518053374088));
#58783=CARTESIAN_POINT('Ctrl Pts',(31.0637982215859,0.523138441463073,20.1615551718639));
#58784=CARTESIAN_POINT('Ctrl Pts',(30.8940186419568,0.777530022608243,20.1810000731231));
#58785=CARTESIAN_POINT('Ctrl Pts',(30.7872728375238,0.885439479392022,20.1913808781633));
#58786=CARTESIAN_POINT('Ctrl Pts',(30.5341117586616,1.05845819784869,20.2130610712561));
#58787=CARTESIAN_POINT('Ctrl Pts',(30.3887837233288,1.12003007025227,20.2241682808161));
#58788=CARTESIAN_POINT('Ctrl Pts',(30.0880464072922,1.18158358213937,20.2448181618436));
#58789=CARTESIAN_POINT('Ctrl Pts',(29.9360438868879,1.18313176496437,20.2536476203627));
#58790=CARTESIAN_POINT('Ctrl Pts',(29.6381705506099,1.1284628410545,20.2738775466838));
#58791=CARTESIAN_POINT('Ctrl Pts',(29.4952627894061,1.07218329111658,20.2846485002308));
#58792=CARTESIAN_POINT('Ctrl Pts',(29.2357076507194,0.906285518142771,20.3064688735353));
#58793=CARTESIAN_POINT('Ctrl Pts',(29.1223265216238,0.796998466553187,20.3173059793119));
#58794=CARTESIAN_POINT('Ctrl Pts',(28.94883850375,0.546283376626024,20.3368482617845));
#58795=CARTESIAN_POINT('Ctrl Pts',(28.8881400415123,0.408839661433748,20.3460102123335));
#58796=CARTESIAN_POINT('Ctrl Pts',(28.8201837019616,0.113659356458156,20.3669407021362));
#58797=CARTESIAN_POINT('Ctrl Pts',(28.8154556440784,-0.0416770716817043,
20.377955215877));
#58798=CARTESIAN_POINT('Ctrl Pts',(28.8666287496698,-0.348241759389233,
20.3996929435023));
#58799=CARTESIAN_POINT('Ctrl Pts',(28.923168044506,-0.496185032937023,20.4097992015263));
#58800=CARTESIAN_POINT('Ctrl Pts',(29.0873034963183,-0.755446668555585,
20.4290701716561));
#58801=CARTESIAN_POINT('Ctrl Pts',(29.1911125253156,-0.865675121623956,
20.4393528532326));
#58802=CARTESIAN_POINT('Ctrl Pts',(29.4392495659902,-1.04453090441881,20.4609314775711));
#58803=CARTESIAN_POINT('Ctrl Pts',(29.5825856119781,-1.10962145963742,20.4720411141544));
#58804=CARTESIAN_POINT('Ctrl Pts',(29.8217321396476,-1.16509155071327,20.4886931681386));
#58805=CARTESIAN_POINT('Ctrl Pts',(29.9108091908387,-1.17524047358086,20.4945229998842));
#58806=CARTESIAN_POINT('Ctrl Pts',(30.0000000000001,-1.17524047358085,20.5));
#58807=CARTESIAN_POINT('Origin',(30.,-1.21864324187371E-14,15.78125));
#58808=CARTESIAN_POINT('',(30.,-1.17524047358085,21.0625));
#58809=CARTESIAN_POINT('',(30.0000000000003,-1.17524047358085,21.));
#58810=CARTESIAN_POINT('',(30.,-1.17524047358085,15.78125));
#58811=CARTESIAN_POINT('Ctrl Pts',(30.,-1.17524047358085,21.0625));
#58812=CARTESIAN_POINT('Ctrl Pts',(29.9930425354756,-1.17524047358085,21.062072758288));
#58813=CARTESIAN_POINT('Ctrl Pts',(29.9860827950433,-1.17517869098314,21.0616431863938));
#58814=CARTESIAN_POINT('Ctrl Pts',(29.8232316065342,-1.17228514735699,21.0515402867957));
#58815=CARTESIAN_POINT('Ctrl Pts',(29.6694853244495,-1.13852257202281,21.0409020757897));
#58816=CARTESIAN_POINT('Ctrl Pts',(29.3867104280309,-1.01415059452875,21.0191280758083));
#58817=CARTESIAN_POINT('Ctrl Pts',(29.2599516823908,-0.925722033008617,
21.0082089931399));
#58818=CARTESIAN_POINT('Ctrl Pts',(29.0500490851207,-0.707886564567504,
20.9875962815068));
#58819=CARTESIAN_POINT('Ctrl Pts',(28.9678750474644,-0.58156955059427,20.9787376277926));
#58820=CARTESIAN_POINT('Ctrl Pts',(28.852209421352,-0.297516308143681,20.9585961298867));
#58821=CARTESIAN_POINT('Ctrl Pts',(28.8227455494544,-0.141401249035421,
20.9475264053908));
#58822=CARTESIAN_POINT('Ctrl Pts',(28.8269065561122,0.16711629798966,20.9256502054441));
#58823=CARTESIAN_POINT('Ctrl Pts',(28.8581354481118,0.316603790040456,20.915050424987));
#58824=CARTESIAN_POINT('Ctrl Pts',(28.9760761175465,0.596699382404322,20.8951895540518));
#58825=CARTESIAN_POINT('Ctrl Pts',(29.0620842641545,0.724424918144287,20.8860783197069));
#58826=CARTESIAN_POINT('Ctrl Pts',(29.2801481558297,0.941880855388224,20.8649778977684));
#58827=CARTESIAN_POINT('Ctrl Pts',(29.4108173740059,1.02868094436595,20.8538764175153));
#58828=CARTESIAN_POINT('Ctrl Pts',(29.6929274853784,1.14422525088517,20.8324562143623));
#58829=CARTESIAN_POINT('Ctrl Pts',(29.8408766090356,1.17398844910975,20.8223157862342));
#58830=CARTESIAN_POINT('Ctrl Pts',(30.146238089068,1.17646530253954,20.8034764343644));
#58831=CARTESIAN_POINT('Ctrl Pts',(30.3008127704194,1.14674523024735,20.7930175246536));
#58832=CARTESIAN_POINT('Ctrl Pts',(30.5871854304481,1.02954198948055,20.7712767528846));
#58833=CARTESIAN_POINT('Ctrl Pts',(30.7164764357369,0.944145175747713,20.7603096568304));
#58834=CARTESIAN_POINT('Ctrl Pts',(30.9318157386174,0.731537563311469,20.7395484367846));
#58835=CARTESIAN_POINT('Ctrl Pts',(31.0169931096024,0.607571893797524,20.7305813882675));
#58836=CARTESIAN_POINT('Ctrl Pts',(31.1392545858023,0.328058458126713,20.7107617965928));
#58837=CARTESIAN_POINT('Ctrl Pts',(31.1726798971535,0.174145191638854,20.6998481956499));
#58838=CARTESIAN_POINT('Ctrl Pts',(31.177452605602,-0.133454152417299,20.6780371031564));
#58839=CARTESIAN_POINT('Ctrl Pts',(31.1504138008343,-0.284195707834949,
20.6673484002337));
#58840=CARTESIAN_POINT('Ctrl Pts',(31.0405663350578,-0.566901684154618,
20.647302433566));
#58841=CARTESIAN_POINT('Ctrl Pts',(30.9589018497076,-0.696179869646961,
20.6383684206626));
#58842=CARTESIAN_POINT('Ctrl Pts',(30.7479829469593,-0.919779045347213,
20.6174889551129));
#58843=CARTESIAN_POINT('Ctrl Pts',(30.6195839675717,-1.0107321163549,20.6063796462101));
#58844=CARTESIAN_POINT('Ctrl Pts',(30.3401820261614,-1.13487834149049,20.5848207753144));
#58845=CARTESIAN_POINT('Ctrl Pts',(30.1927291526794,-1.16899555973842,20.5745564544744));
#58846=CARTESIAN_POINT('Ctrl Pts',(30.02853673898,-1.17498080122699,20.5642615811144));
#58847=CARTESIAN_POINT('Ctrl Pts',(30.0142636931895,-1.17524047358085,20.5633759002187));
#58848=CARTESIAN_POINT('Ctrl Pts',(30.0000000000001,-1.17524047358085,20.5625));
#58849=CARTESIAN_POINT('Ctrl Pts',(30.0000000000001,-1.17524047358085,20.5));
#58850=CARTESIAN_POINT('Ctrl Pts',(30.0615320920417,-1.17524047358085,20.5037785426368));
#58851=CARTESIAN_POINT('Ctrl Pts',(30.1230970944725,-1.17040913175211,20.5077303953467));
#58852=CARTESIAN_POINT('Ctrl Pts',(30.3340845761439,-1.13693724894346,20.5218733491291));
#58853=CARTESIAN_POINT('Ctrl Pts',(30.4779822284686,-1.08432359797014,20.5325751197693));
#58854=CARTESIAN_POINT('Ctrl Pts',(30.7413240882277,-0.925171378815601,
20.5543888717152));
#58855=CARTESIAN_POINT('Ctrl Pts',(30.8574242886598,-0.818746672756081,
20.5652914684918));
#58856=CARTESIAN_POINT('Ctrl Pts',(31.0372296037246,-0.572330389441825,
20.5850692727305));
#58857=CARTESIAN_POINT('Ctrl Pts',(31.1013789298939,-0.436327710632643,
20.5940611041994));
#58858=CARTESIAN_POINT('Ctrl Pts',(31.1765507195451,-0.143169609179877,
20.6148482046583));
#58859=CARTESIAN_POINT('Ctrl Pts',(31.1851707108535,0.0116076749541518,
20.6258230709101));
#58860=CARTESIAN_POINT('Ctrl Pts',(31.1420730921553,0.318093458162843,20.6475552036167));
#58861=CARTESIAN_POINT('Ctrl Pts',(31.0898417933348,0.466589648702242,20.6579510306787));
#58862=CARTESIAN_POINT('Ctrl Pts',(30.9337645237733,0.729159361106415,20.6768444502657));
#58863=CARTESIAN_POINT('Ctrl Pts',(30.8334379992983,0.84198975683026,20.6870055279311));
#58864=CARTESIAN_POINT('Ctrl Pts',(30.591317195237,1.02746666327729,20.7084494527507));
#58865=CARTESIAN_POINT('Ctrl Pts',(30.4504043784541,1.09657907803444,20.7195528744157));
#58866=CARTESIAN_POINT('Ctrl Pts',(30.1527579068286,1.17519666342875,20.7406179390521));
#58867=CARTESIAN_POINT('Ctrl Pts',(29.9992772327099,1.18508027808452,20.7496955256169));
#58868=CARTESIAN_POINT('Ctrl Pts',(29.6980213394833,1.14582802600215,20.7695865882633));
#58869=CARTESIAN_POINT('Ctrl Pts',(29.5531012936116,1.09744171629364,20.7802012666676));
#58870=CARTESIAN_POINT('Ctrl Pts',(29.2844190436536,0.945457598499347,20.8020888235724));
#58871=CARTESIAN_POINT('Ctrl Pts',(29.1643876737344,0.84125826030012,20.8131539267157));
#58872=CARTESIAN_POINT('Ctrl Pts',(28.9773975743441,0.59813879267389,20.8332560474103));
#58873=CARTESIAN_POINT('Ctrl Pts',(28.9097638018428,0.463547729800393,20.8421310013978));
#58874=CARTESIAN_POINT('Ctrl Pts',(28.8274319674294,0.172449502758382,20.8627720413655));
#58875=CARTESIAN_POINT('Ctrl Pts',(28.8149632933605,0.0183235810432114,
20.8737007211534));
#58876=CARTESIAN_POINT('Ctrl Pts',(28.850150967155,-0.288650006351519,20.8954674428227));
#58877=CARTESIAN_POINT('Ctrl Pts',(28.898515176706,-0.438439388541448,20.906088629547));
#58878=CARTESIAN_POINT('Ctrl Pts',(29.047641063206,-0.704596833168998,20.9249611816339));
#58879=CARTESIAN_POINT('Ctrl Pts',(29.1447168471359,-0.819746341645053,
20.9348754556746));
#58880=CARTESIAN_POINT('Ctrl Pts',(29.381325819526,-1.01116668011756,20.9561916286088));
#58881=CARTESIAN_POINT('Ctrl Pts',(29.5199396968772,-1.08386414625954,20.96728098122));
#58882=CARTESIAN_POINT('Ctrl Pts',(29.7764916553148,-1.15925176815251,20.9857080131187));
#58883=CARTESIAN_POINT('Ctrl Pts',(29.8880479255875,-1.1752404735809,20.9931252835322));
#58884=CARTESIAN_POINT('Ctrl Pts',(30.0000000000005,-1.17524047358085,21.));
#58885=CARTESIAN_POINT('Origin',(30.,-1.21864324187371E-14,15.78125));
#58886=CARTESIAN_POINT('',(29.9999999999998,-1.17524047358085,21.5625));
#58887=CARTESIAN_POINT('',(30.0000000000001,-1.17524047358085,21.5));
#58888=CARTESIAN_POINT('',(30.,-1.17524047358085,15.78125));
#58889=CARTESIAN_POINT('Ctrl Pts',(29.9999999999996,-1.17524047358085,21.5625));
#58890=CARTESIAN_POINT('Ctrl Pts',(29.9719988088573,-1.17524047358085,21.5607805119881));
#58891=CARTESIAN_POINT('Ctrl Pts',(29.9439711363572,-1.17423978092491,21.5590239195234));
#58892=CARTESIAN_POINT('Ctrl Pts',(29.7604047377572,-1.16108096387714,21.547285004757));
#58893=CARTESIAN_POINT('Ctrl Pts',(29.6086428973266,-1.11907669828182,21.5364764549777));
#58894=CARTESIAN_POINT('Ctrl Pts',(29.3336394628651,-0.979972388454951,
21.5146573661612));
#58895=CARTESIAN_POINT('Ctrl Pts',(29.2123764352237,-0.885461951955829,
21.503860137555));
#58896=CARTESIAN_POINT('Ctrl Pts',(29.0139169118187,-0.656850944948416,
21.4835680853588));
#58897=CARTESIAN_POINT('Ctrl Pts',(28.9380513713638,-0.525431379870783,
21.4747570119112));
#58898=CARTESIAN_POINT('Ctrl Pts',(28.8379806985326,-0.235334014126339,
21.4541869404899));
#58899=CARTESIAN_POINT('Ctrl Pts',(28.81701218115,-0.0787326333033737,21.4430827321496));
#58900=CARTESIAN_POINT('Ctrl Pts',(28.8372148732154,0.227544173701852,21.4213654174177));
#58901=CARTESIAN_POINT('Ctrl Pts',(28.8758855793473,0.374476178993786,21.4109468400715));
#58902=CARTESIAN_POINT('Ctrl Pts',(29.008483168462,0.64967403277934,21.3914332554072));
#58903=CARTESIAN_POINT('Ctrl Pts',(29.1026400510551,0.774562668949264,21.3818103125428));
#58904=CARTESIAN_POINT('Ctrl Pts',(29.3337333173752,0.980382528955385,21.3603223294383));
#58905=CARTESIAN_POINT('Ctrl Pts',(29.4682481852686,1.05938687455618,21.3492610850172));
#58906=CARTESIAN_POINT('Ctrl Pts',(29.7549668128984,1.15903498567807,21.3281214631321));
#58907=CARTESIAN_POINT('Ctrl Pts',(29.9037091563498,1.1807204220266,21.3186072813687));
#58908=CARTESIAN_POINT('Ctrl Pts',(30.2082836909242,1.16710140483065,21.2994212226452));
#58909=CARTESIAN_POINT('Ctrl Pts',(30.3610942123922,1.12920096767185,21.2886937718569));
#58910=CARTESIAN_POINT('Ctrl Pts',(30.6400777787282,0.99739853025376,21.2668891510646));
#58911=CARTESIAN_POINT('Ctrl Pts',(30.7641225887122,0.905886016702667,21.2560273872475));
#58912=CARTESIAN_POINT('Ctrl Pts',(30.9683193471767,0.682639701404097,21.2355732231612));
#58913=CARTESIAN_POINT('Ctrl Pts',(31.0473475790777,0.553805208866279,21.2267689284532));
#58914=CARTESIAN_POINT('Ctrl Pts',(31.1552799375254,0.266708452111841,21.2064116226359));
#58915=CARTESIAN_POINT('Ctrl Pts',(31.1805191858716,0.110295910456217,21.195320804404));
#58916=CARTESIAN_POINT('Ctrl Pts',(31.1683617956532,-0.197210560675315,
21.173516297295));
#58917=CARTESIAN_POINT('Ctrl Pts',(31.1334138492448,-0.345474524238407,
21.1630032741523));
#58918=CARTESIAN_POINT('Ctrl Pts',(31.0081981695942,-0.623166742222595,
21.1433128204234));
#58919=CARTESIAN_POINT('Ctrl Pts',(30.9181918552343,-0.749490769431124,
21.1339784439808));
#58920=CARTESIAN_POINT('Ctrl Pts',(30.6936733778382,-0.961255467276285,
21.1126834366527));
#58921=CARTESIAN_POINT('Ctrl Pts',(30.5610503971428,-1.04422897430134,21.1015976470182));
#58922=CARTESIAN_POINT('Ctrl Pts',(30.283074075588,-1.14948332004627,21.080796107845));
#58923=CARTESIAN_POINT('Ctrl Pts',(30.1420666819575,-1.17524047358085,21.0712239844648));
#58924=CARTESIAN_POINT('Ctrl Pts',(30.,-1.17524047358085,21.0625));
#58925=CARTESIAN_POINT('Ctrl Pts',(30.0000000000005,-1.17524047358085,21.));
#58926=CARTESIAN_POINT('Ctrl Pts',(30.0409368563611,-1.17524047358083,21.0025138371222));
#58927=CARTESIAN_POINT('Ctrl Pts',(30.0819173014533,-1.17310176285816,21.0051061762144));
#58928=CARTESIAN_POINT('Ctrl Pts',(30.2729829235624,-1.15303120950392,21.0175506477331));
#58929=CARTESIAN_POINT('Ctrl Pts',(30.4187156327833,-1.10844931428969,21.0280803491923));
#58930=CARTESIAN_POINT('Ctrl Pts',(30.6905353954506,-0.963834030798816,
21.0498993207407));
#58931=CARTESIAN_POINT('Ctrl Pts',(30.8129383742835,-0.863111359129209,
21.0609867980498));
#58932=CARTESIAN_POINT('Ctrl Pts',(31.0063964161767,-0.625120486728277,
21.0813042721815));
#58933=CARTESIAN_POINT('Ctrl Pts',(31.0777548462909,-0.49199236060375,21.0901140644785));
#58934=CARTESIAN_POINT('Ctrl Pts',(31.1675962416571,-0.203110857145286,
21.1105979221763));
#58935=CARTESIAN_POINT('Ctrl Pts',(31.1840814343856,-0.0497708726068158,
21.1214708731443));
#58936=CARTESIAN_POINT('Ctrl Pts',(31.1571888276141,0.257674311285982,21.14327103453));
#58937=CARTESIAN_POINT('Ctrl Pts',(31.1128522255693,0.408737402730974,21.1539825367601));
#58938=CARTESIAN_POINT('Ctrl Pts',(30.9710010878299,0.678628541040232,21.1731198356347));
#58939=CARTESIAN_POINT('Ctrl Pts',(30.8772391714915,0.796156039182743,21.1826908232652));
#58940=CARTESIAN_POINT('Ctrl Pts',(30.6464955823919,0.993543206250726,21.2038583630273));
#58941=CARTESIAN_POINT('Ctrl Pts',(30.5103519798164,1.06987223749504,21.214924774365));
#58942=CARTESIAN_POINT('Ctrl Pts',(30.2162079552513,1.16549604568273,21.2363776960251));
#58943=CARTESIAN_POINT('Ctrl Pts',(30.061127965963,1.18379547472913,21.2459429670447));
#58944=CARTESIAN_POINT('Ctrl Pts',(29.7567781749822,1.15962478754955,21.2654893209196));
#58945=CARTESIAN_POINT('Ctrl Pts',(29.6103180879013,1.11893466526318,21.2759257110673));
#58946=CARTESIAN_POINT('Ctrl Pts',(29.3355002124366,0.981897695520532,21.2976601102058));
#58947=CARTESIAN_POINT('Ctrl Pts',(29.2107776319456,0.884773136393355,21.3087624623211));
#58948=CARTESIAN_POINT('Ctrl Pts',(29.0107746609087,0.652081932742376,21.3292939522647));
#58949=CARTESIAN_POINT('Ctrl Pts',(28.9355970901093,0.52040794626517,21.3380991870768));
#58950=CARTESIAN_POINT('Ctrl Pts',(28.8382134265824,0.233810524699486,21.3584210862971));
#58951=CARTESIAN_POINT('Ctrl Pts',(28.8177208295725,0.0813648692728661,
21.3692306226469));
#58952=CARTESIAN_POINT('Ctrl Pts',(28.8362699803681,-0.22632694032349,21.3910482716382));
#58953=CARTESIAN_POINT('Ctrl Pts',(28.8765201026755,-0.378558584509325,
21.4018426329915));
#58954=CARTESIAN_POINT('Ctrl Pts',(29.0110211856253,-0.652134791815677,
21.4212412308003));
#58955=CARTESIAN_POINT('Ctrl Pts',(29.1015077791443,-0.772069972681635,
21.4305317818752));
#58956=CARTESIAN_POINT('Ctrl Pts',(29.3264048767426,-0.975307798634206,
21.4515477299157));
#58957=CARTESIAN_POINT('Ctrl Pts',(29.4600073333855,-1.05515984377402,21.4625829994009));
#58958=CARTESIAN_POINT('Ctrl Pts',(29.7321091399909,-1.15220558787994,21.4827327726726));
#58959=CARTESIAN_POINT('Ctrl Pts',(29.8656344449969,-1.17524047358088,21.4917489238272));
#58960=CARTESIAN_POINT('Ctrl Pts',(30.0000000000003,-1.17524047358085,21.5));
#58961=CARTESIAN_POINT('Origin',(30.,-1.21864324187371E-14,15.78125));
#58962=CARTESIAN_POINT('',(29.9999999999998,-1.17524047358085,22.0625));
#58963=CARTESIAN_POINT('',(30.000000003784,-1.17524047358085,22.0000000004647));
#58964=CARTESIAN_POINT('',(30.,-1.17524047358085,15.78125));
#58965=CARTESIAN_POINT('Ctrl Pts',(29.9999999999997,-1.17524047358085,22.0625));
#58966=CARTESIAN_POINT('Ctrl Pts',(29.9524010211782,-1.17524047358085,22.0595770574349));
#58967=CARTESIAN_POINT('Ctrl Pts',(29.9047586284152,-1.17234913259513,22.0565489400777));
#58968=CARTESIAN_POINT('Ctrl Pts',(29.7009349924679,-1.1474210952591,22.0431488126472));
#58969=CARTESIAN_POINT('Ctrl Pts',(29.5500039838267,-1.09704169086814,22.0320943523472));
#58970=CARTESIAN_POINT('Ctrl Pts',(29.2822334508411,-0.942842462410207,
22.01018424791));
#58971=CARTESIAN_POINT('Ctrl Pts',(29.1667766500969,-0.842552714869588,
21.9995386680174));
#58972=CARTESIAN_POINT('Ctrl Pts',(28.9799931885339,-0.603233884932394,
21.9795839832802));
#58973=CARTESIAN_POINT('Ctrl Pts',(28.910605612196,-0.466400997640195,21.9705713166174));
#58974=CARTESIAN_POINT('Ctrl Pts',(28.8268127379948,-0.170385863417145,
21.9495816311816));
#58975=CARTESIAN_POINT('Ctrl Pts',(28.8145871174915,-0.0137497615287427,
21.9384749608582));
#58976=CARTESIAN_POINT('Ctrl Pts',(28.85113877829,0.289356743861303,21.9169824442057));
#58977=CARTESIAN_POINT('Ctrl Pts',(28.8973142483913,0.433263084581444,21.9067784090915));
#58978=CARTESIAN_POINT('Ctrl Pts',(29.0441562961032,0.701308793511537,21.8877719649526));
#58979=CARTESIAN_POINT('Ctrl Pts',(29.145494108998,0.821789237943167,21.8775043861745));
#58980=CARTESIAN_POINT('Ctrl Pts',(29.3876377187977,1.01480099788269,21.8557919221934));
#58981=CARTESIAN_POINT('Ctrl Pts',(29.5254500415353,1.08610079854932,21.8448013436507));
#58982=CARTESIAN_POINT('Ctrl Pts',(29.8162261597603,1.17031056565349,21.8239599076952));
#58983=CARTESIAN_POINT('Ctrl Pts',(29.965897796871,1.18415559330363,21.814910211276));
#58984=CARTESIAN_POINT('Ctrl Pts',(30.2694248477664,1.15452627142302,21.7952208509568));
#58985=CARTESIAN_POINT('Ctrl Pts',(30.4200757340443,1.10861951539323,21.7843421644183));
#58986=CARTESIAN_POINT('Ctrl Pts',(30.6910871340011,0.962634653497324,21.762524275871));
#58987=CARTESIAN_POINT('Ctrl Pts',(30.8096198631452,0.865330005993902,21.7517956433222));
#58988=CARTESIAN_POINT('Ctrl Pts',(31.0025452942337,0.631606479581076,21.7316621689435));
#58989=CARTESIAN_POINT('Ctrl Pts',(31.075346835895,0.497649504779323,21.7227870693252));
#58990=CARTESIAN_POINT('Ctrl Pts',(31.1677479593254,0.204711362167963,21.7020155655921));
#58991=CARTESIAN_POINT('Ctrl Pts',(31.1845780485819,0.0480344792828584,
21.6909060035913));
#58992=CARTESIAN_POINT('Ctrl Pts',(31.1566162472742,-0.256851307753155,
21.6692873225717));
#58993=CARTESIAN_POINT('Ctrl Pts',(31.1143736239456,-0.402401296420415,
21.6589667405334));
#58994=CARTESIAN_POINT('Ctrl Pts',(30.9745867433069,-0.675115053903835,
21.6396292968631));
#58995=CARTESIAN_POINT('Ctrl Pts',(30.8762946890393,-0.798585224220405,
21.6296650545771));
#58996=CARTESIAN_POINT('Ctrl Pts',(30.6387793080734,-0.998444700485959,
21.6079940222289));
#58997=CARTESIAN_POINT('Ctrl Pts',(30.5025155082578,-1.07350395293815,21.5969652482617));
#58998=CARTESIAN_POINT('Ctrl Pts',(30.2404480736925,-1.15671325182863,21.5779222161248));
#58999=CARTESIAN_POINT('Ctrl Pts',(30.1205093503255,-1.17524047358085,21.5699001988757));
#59000=CARTESIAN_POINT('Ctrl Pts',(29.9999999999996,-1.17524047358085,21.5625));
#59001=CARTESIAN_POINT('Ctrl Pts',(30.0000000000003,-1.17524047358085,21.5));
#59002=CARTESIAN_POINT('Ctrl Pts',(30.0212839202784,-1.17524047358085,21.5013069960338));
#59003=CARTESIAN_POINT('Ctrl Pts',(30.0425864419315,-1.17466229796956,21.5026356328208));
#59004=CARTESIAN_POINT('Ctrl Pts',(30.2139454930837,-1.16533366693515,21.5134891283695));
#59005=CARTESIAN_POINT('Ctrl Pts',(30.3610177391346,-1.12845915530085,21.523827832119));
#59006=CARTESIAN_POINT('Ctrl Pts',(30.6385696146112,-0.998891400827412,
21.5454653082446));
#59007=CARTESIAN_POINT('Ctrl Pts',(30.7654630357173,-0.905335035089088,
21.5565744608423));
#59008=CARTESIAN_POINT('Ctrl Pts',(30.9718229035628,-0.677897335355307,
21.5773100566854));
#59009=CARTESIAN_POINT('Ctrl Pts',(31.0507577571561,-0.547623084998762,
21.5861694304673));
#59010=CARTESIAN_POINT('Ctrl Pts',(31.1570604439752,-0.258809326298121,
21.6066484845527));
#59011=CARTESIAN_POINT('Ctrl Pts',(31.1812214838473,-0.102338491331391,
21.6177434360859));
#59012=CARTESIAN_POINT('Ctrl Pts',(31.1670292938221,0.204877234262332,21.6395273271632));
#59013=CARTESIAN_POINT('Ctrl Pts',(31.1311379778152,0.352813947812694,21.6500171458341));
#59014=CARTESIAN_POINT('Ctrl Pts',(31.0040616369159,0.629882761963365,21.6696633955718));
#59015=CARTESIAN_POINT('Ctrl Pts',(30.9130181373807,0.755846555951633,21.6790645983814));
#59016=CARTESIAN_POINT('Ctrl Pts',(30.6868446220844,0.966129203413541,21.7004086935125));
#59017=CARTESIAN_POINT('Ctrl Pts',(30.553735937256,1.0481102897547,21.711489124086));
#59018=CARTESIAN_POINT('Ctrl Pts',(30.2686762405413,1.15380487275931,21.7327412449065));
#59019=CARTESIAN_POINT('Ctrl Pts',(30.1202468756007,1.17853792824007,21.7424990119962));
#59020=CARTESIAN_POINT('Ctrl Pts',(29.8153503696085,1.17107054155024,21.7614867439455));
#59021=CARTESIAN_POINT('Ctrl Pts',(29.661826921183,1.13627251461424,21.7721479818837));
#59022=CARTESIAN_POINT('Ctrl Pts',(29.3799800833098,1.01003478165367,21.7939311399523));
#59023=CARTESIAN_POINT('Ctrl Pts',(29.253891997555,0.920828765085568,21.8048366026441));
#59024=CARTESIAN_POINT('Ctrl Pts',(29.0454103417907,0.701638656512355,21.8254100846196));
#59025=CARTESIAN_POINT('Ctrl Pts',(28.9640200854668,0.5746995746724,21.8342495048467));
#59026=CARTESIAN_POINT('Ctrl Pts',(28.8502724171258,0.289883112959693,21.8544451207025));
#59027=CARTESIAN_POINT('Ctrl Pts',(28.8218581810328,0.133683866085342,21.8655208147403));
#59028=CARTESIAN_POINT('Ctrl Pts',(28.8280094580603,-0.174601530686287,
21.8873805534988));
#59029=CARTESIAN_POINT('Ctrl Pts',(28.8601657562679,-0.323793761637004,
21.8979593977371));
#59030=CARTESIAN_POINT('Ctrl Pts',(28.9799119697649,-0.603297917389521,
21.9177783313962));
#59031=CARTESIAN_POINT('Ctrl Pts',(29.0669039974813,-0.730676428244075,
21.9269392883002));
#59032=CARTESIAN_POINT('Ctrl Pts',(29.2865672059309,-0.946735069741176,
21.9480883812055));
#59033=CARTESIAN_POINT('Ctrl Pts',(29.4177292577255,-1.03259356038437,21.9591867420451));
#59034=CARTESIAN_POINT('Ctrl Pts',(29.7004129009365,-1.14619538664958,21.98057329627));
#59035=CARTESIAN_POINT('Ctrl Pts',(29.8484560704769,-1.17497884076058,21.9906847639469));
#59036=CARTESIAN_POINT('Ctrl Pts',(29.9986381885534,-1.17523988185415,21.9999163533479));
#59037=CARTESIAN_POINT('Ctrl Pts',(29.9993191103818,-1.17524047358524,21.9999581881525));
#59038=CARTESIAN_POINT('Ctrl Pts',(30.0000000075681,-1.17524047358085,22.0000000004647));
#59039=CARTESIAN_POINT('Origin',(30.,-1.21864324187371E-14,15.78125));
#59040=CARTESIAN_POINT('',(30.,-1.17524047358085,22.5625));
#59041=CARTESIAN_POINT('',(29.9999999999999,-1.17524047358085,22.4999999999999));
#59042=CARTESIAN_POINT('',(30.,-1.17524047358085,15.78125));
#59043=CARTESIAN_POINT('Ctrl Pts',(30.,-1.17524047358085,22.5625));
#59044=CARTESIAN_POINT('Ctrl Pts',(29.9313687068489,-1.17524047358085,22.5582855119371));
#59045=CARTESIAN_POINT('Ctrl Pts',(29.8627268799626,-1.16923029327301,22.55385729367));
#59046=CARTESIAN_POINT('Ctrl Pts',(29.6405360439417,-1.12983827415446,22.5388164770024));
#59047=CARTESIAN_POINT('Ctrl Pts',(29.4932720438495,-1.07189657475161,22.5277190875488));
#59048=CARTESIAN_POINT('Ctrl Pts',(29.2351505504649,-0.904940984815958,
22.505949247503));
#59049=CARTESIAN_POINT('Ctrl Pts',(29.125477326134,-0.799463570556349,22.4954749014128));
#59050=CARTESIAN_POINT('Ctrl Pts',(28.9500348086396,-0.550024618450246,
22.4758578415198));
#59051=CARTESIAN_POINT('Ctrl Pts',(28.8870166724079,-0.407722193677489,
22.4664105508506));
#59052=CARTESIAN_POINT('Ctrl Pts',(28.8193863135494,-0.106256134735224,
22.4450343541119));
#59053=CARTESIAN_POINT('Ctrl Pts',(28.8156683957017,0.0499559751614321,
22.4339577479897));
#59054=CARTESIAN_POINT('Ctrl Pts',(28.8680054797788,0.349324836623415,22.4127302582268));
#59055=CARTESIAN_POINT('Ctrl Pts',(28.9214162690158,0.489956671932254,22.4030291896045));
#59056=CARTESIAN_POINT('Ctrl Pts',(29.0814696037689,0.749536525817022,22.3839976107609));
#59057=CARTESIAN_POINT('Ctrl Pts',(29.1888834831425,0.864620134172483,22.3733214303097));
#59058=CARTESIAN_POINT('Ctrl Pts',(29.4398862783311,1.04443640573476,22.3515327737366));
#59059=CARTESIAN_POINT('Ctrl Pts',(29.5804046735503,1.10838743829029,22.3406365628695));
#59060=CARTESIAN_POINT('Ctrl Pts',(29.874773559948,1.17808176091705,22.320089130129));
#59061=CARTESIAN_POINT('Ctrl Pts',(30.0254999210416,1.18444262102585,22.3112603596819));
#59062=CARTESIAN_POINT('Ctrl Pts',(30.3288317944626,1.13918974891494,22.2910290715165));
#59063=CARTESIAN_POINT('Ctrl Pts',(30.4780087858284,1.08506931516396,22.2799496878662));
#59064=CARTESIAN_POINT('Ctrl Pts',(30.7411182596149,0.924538989516088,22.2581013471772));
#59065=CARTESIAN_POINT('Ctrl Pts',(30.8537656083098,0.82166305580017,22.2475365992352));
#59066=CARTESIAN_POINT('Ctrl Pts',(31.0350106463268,0.577368135111118,22.2277455951917));
#59067=CARTESIAN_POINT('Ctrl Pts',(31.1013006049905,0.437889260334813,22.2185496213456));
#59068=CARTESIAN_POINT('Ctrl Pts',(31.1772437890897,0.139172903087767,22.1973683990083));
#59069=CARTESIAN_POINT('Ctrl Pts',(31.185313349087,-0.0173128950364053,
22.1862723863453));
#59070=CARTESIAN_POINT('Ctrl Pts',(31.1410279217834,-0.318736522964712,
22.1648991982826));
#59071=CARTESIAN_POINT('Ctrl Pts',(31.0912903592309,-0.461049327500964,
22.1548343474741));
#59072=CARTESIAN_POINT('Ctrl Pts',(30.9380306919572,-0.724977765907907,
22.136065778375));
#59073=CARTESIAN_POINT('Ctrl Pts',(30.8337205687989,-0.842838844072579,
22.1254817206889));
#59074=CARTESIAN_POINT('Ctrl Pts',(30.5872857957992,-1.02946130111843,22.1037322710222));
#59075=CARTESIAN_POINT('Ctrl Pts',(30.4481174203718,-1.09722011431045,22.0927839616769));
#59076=CARTESIAN_POINT('Ctrl Pts',(30.2017882631029,-1.16222172164091,22.0753529112466));
#59077=CARTESIAN_POINT('Ctrl Pts',(30.1010204315162,-1.17524047358085,22.0687034297066));
#59078=CARTESIAN_POINT('Ctrl Pts',(29.9999999999997,-1.17524047358085,22.0625));
#59079=CARTESIAN_POINT('Ctrl Pts',(30.0000000075681,-1.17524047358085,22.0000000004647));
#59080=CARTESIAN_POINT('Ctrl Pts',(30.1550617076756,-1.17524047258231,22.0095219788006));
#59081=CARTESIAN_POINT('Ctrl Pts',(30.3087125624576,-1.14455036320512,22.020045399438));
#59082=CARTESIAN_POINT('Ctrl Pts',(30.5936146237504,-1.02583437646268,22.0417494976575));
#59083=CARTESIAN_POINT('Ctrl Pts',(30.7222919834293,-0.9396884903777,22.0527054685765));
#59084=CARTESIAN_POINT('Ctrl Pts',(30.9363028934711,-0.725796874489648,
22.0734306378289));
#59085=CARTESIAN_POINT('Ctrl Pts',(31.0207456221836,-0.60126080890756,22.0823661148205));
#59086=CARTESIAN_POINT('Ctrl Pts',(31.1412832329984,-0.320931550152795,
22.1022435544492));
#59087=CARTESIAN_POINT('Ctrl Pts',(31.1737467539974,-0.166807893544759,
22.1131720736242));
#59088=CARTESIAN_POINT('Ctrl Pts',(31.1765934878998,0.140728845238564,22.1349787269359));
#59089=CARTESIAN_POINT('Ctrl Pts',(31.148646481366,0.291209583454888,22.1456489359696));
#59090=CARTESIAN_POINT('Ctrl Pts',(31.0370532707971,0.573358102978206,22.165655374784));
#59091=CARTESIAN_POINT('Ctrl Pts',(30.9544609034821,0.702301510156061,22.1746213225474));
#59092=CARTESIAN_POINT('Ctrl Pts',(30.7420042686145,0.924591934894812,22.1955488165371));
#59093=CARTESIAN_POINT('Ctrl Pts',(30.6131073712558,1.01465868002552,22.2066572778597));
#59094=CARTESIAN_POINT('Ctrl Pts',(30.3331026676289,1.1369643062698,22.228187906872));
#59095=CARTESIAN_POINT('Ctrl Pts',(30.1855325771707,1.17014774287538,22.2384263196851));
#59096=CARTESIAN_POINT('Ctrl Pts',(29.8783465649041,1.17947691083341,22.2576206519922));
#59097=CARTESIAN_POINT('Ctrl Pts',(29.7215875906434,1.15260328305267,22.2678992314176));
#59098=CARTESIAN_POINT('Ctrl Pts',(29.4314038660401,1.03996407151785,22.2897122199048));
#59099=CARTESIAN_POINT('Ctrl Pts',(29.3003745517226,0.9567417174806,22.3007089687507));
#59100=CARTESIAN_POINT('Ctrl Pts',(29.0812311411824,0.747835374300097,22.3215725663721));
#59101=CARTESIAN_POINT('Ctrl Pts',(28.9939461402353,0.625488946274541,22.3306481587999));
#59102=CARTESIAN_POINT('Ctrl Pts',(28.866779072646,0.34832483100282,22.3503011660994));
#59103=CARTESIAN_POINT('Ctrl Pts',(28.8306169080572,0.195045951299282,22.3611697842779));
#59104=CARTESIAN_POINT('Ctrl Pts',(28.8203429359976,-0.112665031360941,
22.3829887927828));
#59105=CARTESIAN_POINT('Ctrl Pts',(28.844778193878,-0.264121048518041,22.3937281563827));
#59106=CARTESIAN_POINT('Ctrl Pts',(28.9496447173484,-0.548400594969454,
22.4138857009336));
#59107=CARTESIAN_POINT('Ctrl Pts',(29.0286885091485,-0.678634752036216,
22.4227474921567));
#59108=CARTESIAN_POINT('Ctrl Pts',(29.2352313232766,-0.905919594975383,
22.4434889029608));
#59109=CARTESIAN_POINT('Ctrl Pts',(29.3621859947411,-0.999372204838993,
22.454598138267));
#59110=CARTESIAN_POINT('Ctrl Pts',(29.6398139077013,-1.12872343697434,22.4762326071516));
#59111=CARTESIAN_POINT('Ctrl Pts',(29.7869023742936,-1.1654876328242,22.4865683958599));
#59112=CARTESIAN_POINT('Ctrl Pts',(29.9579757834663,-1.17467745886044,22.4973994296432));
#59113=CARTESIAN_POINT('Ctrl Pts',(29.9789969929607,-1.17524047358085,22.4987102541947));
#59114=CARTESIAN_POINT('Ctrl Pts',(29.9999999999997,-1.17524047358085,22.4999999999999));
#59115=CARTESIAN_POINT('Origin',(30.,-1.21864324187371E-14,15.78125));
#59116=CARTESIAN_POINT('',(30.,-1.17524047358085,23.0625));
#59117=CARTESIAN_POINT('',(29.9999999999997,-1.17524047358085,22.9999999999999));
#59118=CARTESIAN_POINT('',(30.,-1.17524047358085,15.78125));
#59119=CARTESIAN_POINT('Ctrl Pts',(30.0000000000001,-1.17524047358085,23.0625));
#59120=CARTESIAN_POINT('Ctrl Pts',(29.9105144759955,-1.17524047358086,23.0570049021313));
#59121=CARTESIAN_POINT('Ctrl Pts',(29.8211453329131,-1.16502438899623,23.0511547525684));
#59122=CARTESIAN_POINT('Ctrl Pts',(29.5817638222111,-1.10931034878277,23.0344796199141));
#59123=CARTESIAN_POINT('Ctrl Pts',(29.4384864599594,-1.04411918186912,23.0233700199021));
#59124=CARTESIAN_POINT('Ctrl Pts',(29.1904963016638,-0.865097093142698,
23.001794519102));
#59125=CARTESIAN_POINT('Ctrl Pts',(29.0867727283959,-0.754802905276228,
22.9915147546188));
#59126=CARTESIAN_POINT('Ctrl Pts',(28.9228010666229,-0.495400927229172,
22.9722488667908));
#59127=CARTESIAN_POINT('Ctrl Pts',(28.8663568012591,-0.347374707529959,
22.9621314630453));
#59128=CARTESIAN_POINT('Ctrl Pts',(28.8154245654916,-0.0407388679671123,
22.9403886902216));
#59129=CARTESIAN_POINT('Ctrl Pts',(28.820274444704,0.114581560721945,22.9293753109615));
#59130=CARTESIAN_POINT('Ctrl Pts',(28.8884563534747,0.409699470717337,22.9084492454292));
#59131=CARTESIAN_POINT('Ctrl Pts',(28.9492618301764,0.547097841052301,22.8992933904858));
#59132=CARTESIAN_POINT('Ctrl Pts',(29.1229462954904,0.797680554149997,22.8797437378863));
#59133=CARTESIAN_POINT('Ctrl Pts',(29.2364128570735,0.906879897838648,22.8689044954722));
#59134=CARTESIAN_POINT('Ctrl Pts',(29.4960880788397,1.07256979024568,22.8470841182882));
#59135=CARTESIAN_POINT('Ctrl Pts',(29.6390279331417,1.12873587584898,22.8363152167134));
#59136=CARTESIAN_POINT('Ctrl Pts',(29.9369514995214,1.18318311725145,22.8160900653519));
#59137=CARTESIAN_POINT('Ctrl Pts',(30.0889739777062,1.18151676550276,22.8072588330028));
#59138=CARTESIAN_POINT('Ctrl Pts',(30.3896701123462,1.11972025811827,22.7866028657307));
#59139=CARTESIAN_POINT('Ctrl Pts',(30.5349379950004,1.05803905954289,22.7754954739854));
#59140=CARTESIAN_POINT('Ctrl Pts',(30.7879462278465,0.88483838172195,22.7538182156715));
#59141=CARTESIAN_POINT('Ctrl Pts',(30.894602280459,0.776856295524231,22.7434403470977));
#59142=CARTESIAN_POINT('Ctrl Pts',(31.0642088755634,0.522314474535101,22.7240007418519));
#59143=CARTESIAN_POINT('Ctrl Pts',(31.1239021773863,0.377122301428262,22.7142407897863));
#59144=CARTESIAN_POINT('Ctrl Pts',(31.1830807507881,0.07297978420699,22.6926748121518));
#59145=CARTESIAN_POINT('Ctrl Pts',(31.1824316194307,-0.0828368341019099,
22.681626249339));
#59146=CARTESIAN_POINT('Ctrl Pts',(31.1220212984731,-0.380073436416841,
22.6605499526862));
#59147=CARTESIAN_POINT('Ctrl Pts',(31.0648726782981,-0.5190454232441,22.6511559208149));
#59148=CARTESIAN_POINT('Ctrl Pts',(30.897916936256,-0.774116322820778,22.6318603404761));
#59149=CARTESIAN_POINT('Ctrl Pts',(30.7874073117601,-0.886271721025917,
22.6210978735108));
#59150=CARTESIAN_POINT('Ctrl Pts',(30.5319280571356,-1.05901132752472,22.5992852221989));
#59151=CARTESIAN_POINT('Ctrl Pts',(30.390134598554,-1.11904322637321,22.5884496605924));
#59152=CARTESIAN_POINT('Ctrl Pts',(30.1614293865023,-1.16692310230727,22.5727078850032));
#59153=CARTESIAN_POINT('Ctrl Pts',(30.0807402688424,-1.17524047358085,22.5674580720923));
#59154=CARTESIAN_POINT('Ctrl Pts',(30.,-1.17524047358085,22.5625));
#59155=CARTESIAN_POINT('Ctrl Pts',(29.9999999999997,-1.17524047358085,22.4999999999999));
#59156=CARTESIAN_POINT('Ctrl Pts',(30.1346907701741,-1.17524047358085,22.5082710468799));
#59157=CARTESIAN_POINT('Ctrl Pts',(30.2685335864829,-1.15209385827977,22.5173106568969));
#59158=CARTESIAN_POINT('Ctrl Pts',(30.5408486178537,-1.05471955701661,22.5374851723845));
#59159=CARTESIAN_POINT('Ctrl Pts',(30.6743758210798,-0.974766233245233,
22.5485194114384));
#59160=CARTESIAN_POINT('Ctrl Pts',(30.8991023951896,-0.771359157149707,
22.5695308885782));
#59161=CARTESIAN_POINT('Ctrl Pts',(30.9894938192057,-0.651353133995038,
22.5788141945814));
#59162=CARTESIAN_POINT('Ctrl Pts',(31.1237789969096,-0.377670022359416,
22.598220372706));
#59163=CARTESIAN_POINT('Ctrl Pts',(31.1639088895479,-0.225405854113982,
22.6090170402582));
#59164=CARTESIAN_POINT('Ctrl Pts',(31.1822136536976,0.0822897394418652,
22.6308349575606));
#59165=CARTESIAN_POINT('Ctrl Pts',(31.1616041653703,0.234707632570292,22.6416425253559));
#59166=CARTESIAN_POINT('Ctrl Pts',(31.0639996311159,0.521237294982461,22.6619596199458));
#59167=CARTESIAN_POINT('Ctrl Pts',(30.9887089758802,0.652868889710107,22.6707656569643));
#59168=CARTESIAN_POINT('Ctrl Pts',(30.7885136410845,0.885402585167096,22.6913033752648));
#59169=CARTESIAN_POINT('Ctrl Pts',(30.6637241461389,0.982420191755087,22.7024060445739));
#59170=CARTESIAN_POINT('Ctrl Pts',(30.38882091141,1.11923262290395,22.724137724694));
#59171=CARTESIAN_POINT('Ctrl Pts',(30.2423409189137,1.15980775171446,22.7345712602384));
#59172=CARTESIAN_POINT('Ctrl Pts',(29.9379463484727,1.1837522744206,22.75411234554));
#59173=CARTESIAN_POINT('Ctrl Pts',(29.7828414350779,1.1653244529442,22.7636867623073));
#59174=CARTESIAN_POINT('Ctrl Pts',(29.4887538037787,1.06944336967731,22.7851453423512));
#59175=CARTESIAN_POINT('Ctrl Pts',(29.3526850446683,0.993007607592932,22.7962109417328));
#59176=CARTESIAN_POINT('Ctrl Pts',(29.1221162292212,0.795444169323972,22.8173739985243));
#59177=CARTESIAN_POINT('Ctrl Pts',(29.0284526004007,0.677845266859518,22.8269357043589));
#59178=CARTESIAN_POINT('Ctrl Pts',(28.8868197290406,0.407843425299078,22.8460808529214));
#59179=CARTESIAN_POINT('Ctrl Pts',(28.8426042638403,0.256743916657897,22.8567949374029));
#59180=CARTESIAN_POINT('Ctrl Pts',(28.8159600292804,-0.0507119050410385,
22.8785958530886));
#59181=CARTESIAN_POINT('Ctrl Pts',(28.8325649861531,-0.204026768591548,
22.8894670227908));
#59182=CARTESIAN_POINT('Ctrl Pts',(28.9226310063267,-0.492841082076786,
22.9099461162173));
#59183=CARTESIAN_POINT('Ctrl Pts',(28.994102015515,-0.625925698199416,22.918754883105));
#59184=CARTESIAN_POINT('Ctrl Pts',(29.1877542901984,-0.863760919482141,
22.9390787662067));
#59185=CARTESIAN_POINT('Ctrl Pts',(29.3102272892874,-0.964377961033194,
22.9501667983144));
#59186=CARTESIAN_POINT('Ctrl Pts',(29.5821386201159,-1.10877008329771,22.9719834809511));
#59187=CARTESIAN_POINT('Ctrl Pts',(29.7278943046296,-1.1532370774207,22.9825105195965));
#59188=CARTESIAN_POINT('Ctrl Pts',(29.9186700556686,-1.17313232338821,22.9949309755051));
#59189=CARTESIAN_POINT('Ctrl Pts',(29.9593567068785,-1.17524047358085,22.9975041899134));
#59190=CARTESIAN_POINT('Ctrl Pts',(29.9999999999995,-1.17524047358085,22.9999999999999));
#59191=CARTESIAN_POINT('Origin',(30.,-1.21864324187371E-14,15.78125));
#59192=CARTESIAN_POINT('',(30.0000000000003,-1.17524047358085,23.5625));
#59193=CARTESIAN_POINT('',(30.,-1.17524047358085,23.5));
#59194=CARTESIAN_POINT('',(30.,-1.17524047358085,15.78125));
#59195=CARTESIAN_POINT('Ctrl Pts',(30.0000000000005,-1.17524047358085,23.5625));
#59196=CARTESIAN_POINT('Ctrl Pts',(29.8877180837681,-1.1752404735809,23.5556050287134));
#59197=CARTESIAN_POINT('Ctrl Pts',(29.7758372881673,-1.15915740880452,23.548164484563));
#59198=CARTESIAN_POINT('Ctrl Pts',(29.5190446425994,-1.08346545175016,23.5297118828087));
#59199=CARTESIAN_POINT('Ctrl Pts',(29.3805019669677,-1.01066023747548,23.5186230824555));
#59200=CARTESIAN_POINT('Ctrl Pts',(29.1440648218203,-0.81906365611398,23.4973112125635));
#59201=CARTESIAN_POINT('Ctrl Pts',(29.0470865676084,-0.703844960553528,
23.4874078682461));
#59202=CARTESIAN_POINT('Ctrl Pts',(28.8981724330839,-0.43757763652763,23.4685275248886));
#59203=CARTESIAN_POINT('Ctrl Pts',(28.8499251562346,-0.287749538271772,
23.4579035929059));
#59204=CARTESIAN_POINT('Ctrl Pts',(28.8149793372208,0.0192409990811535,
23.4361356693579));
#59205=CARTESIAN_POINT('Ctrl Pts',(28.8275655785823,0.173345465604893,23.4252085109033));
#59206=CARTESIAN_POINT('Ctrl Pts',(28.9101166290744,0.46437979734691,23.4045720015899));
#59207=CARTESIAN_POINT('Ctrl Pts',(28.9778580847147,0.598927911512345,23.3956997913279));
#59208=CARTESIAN_POINT('Ctrl Pts',(29.1650362747697,0.841899704480849,23.3755913560416));
#59209=CARTESIAN_POINT('Ctrl Pts',(29.2851376881026,0.945999066866448,23.3645254962114));
#59210=CARTESIAN_POINT('Ctrl Pts',(29.5539135664443,1.09777062977422,23.3426397256705));
#59211=CARTESIAN_POINT('Ctrl Pts',(29.6988585362439,1.14604691671332,23.3320274174642));
#59212=CARTESIAN_POINT('Ctrl Pts',(30.0001600354305,1.18508412542801,23.3121411783529));
#59213=CARTESIAN_POINT('Ctrl Pts',(30.1536625413848,1.17508243739145,23.3030583378086));
#59214=CARTESIAN_POINT('Ctrl Pts',(30.4512625228178,1.09622449574564,23.2819876064994));
#59215=CARTESIAN_POINT('Ctrl Pts',(30.592110439614,1.02700793469459,23.2708844778163));
#59216=CARTESIAN_POINT('Ctrl Pts',(30.8340714315268,0.841360319080231,23.2494443144111));
#59217=CARTESIAN_POINT('Ctrl Pts',(30.9343059293982,0.728463261371192,23.2392865244689));
#59218=CARTESIAN_POINT('Ctrl Pts',(31.0901832738534,0.465790392750319,23.2204017245443));
#59219=CARTESIAN_POINT('Ctrl Pts',(31.1423055420081,0.317257314781848,23.2099959148018));
#59220=CARTESIAN_POINT('Ctrl Pts',(31.1851773743111,0.010751647338072,23.1882623721543));
#59221=CARTESIAN_POINT('Ctrl Pts',(31.1764469607209,-0.144008319910697,
23.1772887337992));
#59222=CARTESIAN_POINT('Ctrl Pts',(31.1010701340243,-0.437108167734962,
23.1565057639579));
#59223=CARTESIAN_POINT('Ctrl Pts',(31.0368218842674,-0.573070176242618,
23.1475180074206));
#59224=CARTESIAN_POINT('Ctrl Pts',(30.8568360573785,-0.819362332337596,
23.1277335191445));
#59225=CARTESIAN_POINT('Ctrl Pts',(30.7406590361852,-0.925703986430565,
23.1168291494862));
#59226=CARTESIAN_POINT('Ctrl Pts',(30.477211273408,-1.08466164141258,23.0950157923094));
#59227=CARTESIAN_POINT('Ctrl Pts',(30.3332866239118,-1.13717003604433,23.0843160955662));
#59228=CARTESIAN_POINT('Ctrl Pts',(30.1225555529996,-1.17045159552602,23.0701956350453));
#59229=CARTESIAN_POINT('Ctrl Pts',(30.0612610274847,-1.17524047358085,23.066261897193));
#59230=CARTESIAN_POINT('Ctrl Pts',(30.0000000000001,-1.17524047358085,23.0625));
#59231=CARTESIAN_POINT('Ctrl Pts',(29.9999999999995,-1.17524047358085,22.9999999999999));
#59232=CARTESIAN_POINT('Ctrl Pts',(30.1122819160637,-1.17524047358085,23.0068949712763));
#59233=CARTESIAN_POINT('Ctrl Pts',(30.2241627114991,-1.15915740885253,23.0143355154149));
#59234=CARTESIAN_POINT('Ctrl Pts',(30.4809553569443,-1.08346545195345,23.0327881171562));
#59235=CARTESIAN_POINT('Ctrl Pts',(30.6194980326123,-1.01066023773368,23.0438769175097));
#59236=CARTESIAN_POINT('Ctrl Pts',(30.8559351778473,-0.819063656461988,
23.0651887874038));
#59237=CARTESIAN_POINT('Ctrl Pts',(30.952913432109,-0.703844960936813,23.0750921317269));
#59238=CARTESIAN_POINT('Ctrl Pts',(31.1018275667414,-0.437577636966923,
23.0939724750804));
#59239=CARTESIAN_POINT('Ctrl Pts',(31.1500748436503,-0.287749538730812,
23.1045964070617));
#59240=CARTESIAN_POINT('Ctrl Pts',(31.1850206627874,0.0192409986134863,
23.126364330609));
#59241=CARTESIAN_POINT('Ctrl Pts',(31.1724344214858,0.173345465148191,23.1372914890643));
#59242=CARTESIAN_POINT('Ctrl Pts',(31.0898833711054,0.464379796922714,23.15792799838));
#59243=CARTESIAN_POINT('Ctrl Pts',(31.0221419155201,0.598927911110121,23.1668002086434));
#59244=CARTESIAN_POINT('Ctrl Pts',(30.8349637255609,0.841899704153978,23.1869086439265));
#59245=CARTESIAN_POINT('Ctrl Pts',(30.7148623122637,0.945999066590532,23.1979745037564));
#59246=CARTESIAN_POINT('Ctrl Pts',(30.4460864339697,1.09777062960664,23.2198602742982));
#59247=CARTESIAN_POINT('Ctrl Pts',(30.3011414641827,1.1460469166018,23.2304725825058));
#59248=CARTESIAN_POINT('Ctrl Pts',(29.9998399650194,1.18508412542607,23.2503588216195));
#59249=CARTESIAN_POINT('Ctrl Pts',(29.8463374590763,1.17508243744973,23.2594416621611));
#59250=CARTESIAN_POINT('Ctrl Pts',(29.5487374776195,1.09622449592641,23.2805123934674));
#59251=CARTESIAN_POINT('Ctrl Pts',(29.4078895607902,1.02700793492841,23.2916155221506));
#59252=CARTESIAN_POINT('Ctrl Pts',(29.1659285687959,0.841360319401014,23.3130556855578));
#59253=CARTESIAN_POINT('Ctrl Pts',(29.0656940708777,0.72846326172594,23.3232134755017));
#59254=CARTESIAN_POINT('Ctrl Pts',(28.9098167263205,0.465790393157422,23.3420982754308));
#59255=CARTESIAN_POINT('Ctrl Pts',(28.8576944581104,0.317257315207477,23.3525040851682));
#59256=CARTESIAN_POINT('Ctrl Pts',(28.8148226256923,0.0107516477743395,
23.3742376278149));
#59257=CARTESIAN_POINT('Ctrl Pts',(28.8235530392262,-0.144008319483296,
23.3852112661707));
#59258=CARTESIAN_POINT('Ctrl Pts',(28.8989298658185,-0.437108167337535,
23.4059942360141));
#59259=CARTESIAN_POINT('Ctrl Pts',(28.9631781155251,-0.573070175865714,
23.4149819925535));
#59260=CARTESIAN_POINT('Ctrl Pts',(29.1431639423218,-0.819362332023802,
23.4347664808262));
#59261=CARTESIAN_POINT('Ctrl Pts',(29.2593409634759,-0.925703986159073,
23.4456708504836));
#59262=CARTESIAN_POINT('Ctrl Pts',(29.5227887261992,-1.08466164124026,23.4674842076606));
#59263=CARTESIAN_POINT('Ctrl Pts',(29.6667133756817,-1.13717003592563,23.4781839044047));
#59264=CARTESIAN_POINT('Ctrl Pts',(29.8774444467245,-1.17045159550418,23.4923043649371));
#59265=CARTESIAN_POINT('Ctrl Pts',(29.9387389723772,-1.17524047358085,23.4962381027985));
#59266=CARTESIAN_POINT('Ctrl Pts',(29.9999999999999,-1.17524047358085,23.5));
#59267=CARTESIAN_POINT('Origin',(30.,-1.21864324187371E-14,15.78125));
#59268=CARTESIAN_POINT('',(30.0000000000001,-1.17524047358085,24.0625));
#59269=CARTESIAN_POINT('',(30.,-1.17524047358085,24.));
#59270=CARTESIAN_POINT('',(30.,-1.17524047358085,15.78125));
#59271=CARTESIAN_POINT('Ctrl Pts',(30.0000000000002,-1.17524047358085,24.0625));
#59272=CARTESIAN_POINT('Ctrl Pts',(29.8653092296601,-1.17524047358088,24.0542289531099));
#59273=CARTESIAN_POINT('Ctrl Pts',(29.7314664131893,-1.15209385822287,24.045189343081));
#59274=CARTESIAN_POINT('Ctrl Pts',(29.4591513817099,-1.05471955679206,24.0250148275808));
#59275=CARTESIAN_POINT('Ctrl Pts',(29.3256241785221,-0.974766232969058,
24.0139805885274));
#59276=CARTESIAN_POINT('Ctrl Pts',(29.1008976044993,-0.771359156787199,
23.99296911139));
#59277=CARTESIAN_POINT('Ctrl Pts',(29.0105061805318,-0.651353133596405,
23.9836858053905));
#59278=CARTESIAN_POINT('Ctrl Pts',(28.876221002938,-0.377670021906335,23.9642796272619));
#59279=CARTESIAN_POINT('Ctrl Pts',(28.8360911103609,-0.225405853644338,
23.9534829597086));
#59280=CARTESIAN_POINT('Ctrl Pts',(28.8177863463358,0.0822897399134218,
23.931665042406));
#59281=CARTESIAN_POINT('Ctrl Pts',(28.8383958347227,0.234707633027682,23.9208574746117));
#59282=CARTESIAN_POINT('Ctrl Pts',(28.9360003690899,0.521237295405437,23.9005403800242));
#59283=CARTESIAN_POINT('Ctrl Pts',(29.0112910243832,0.652868890111379,23.8917343430053));
#59284=CARTESIAN_POINT('Ctrl Pts',(29.211486359277,0.885402585487968,23.8711966247017));
#59285=CARTESIAN_POINT('Ctrl Pts',(29.3362758542566,0.98242019202142,23.8600939553924));
#59286=CARTESIAN_POINT('Ctrl Pts',(29.611179089029,1.11923262305578,23.8383622752737));
#59287=CARTESIAN_POINT('Ctrl Pts',(29.7576590815354,1.15980775180767,23.8279287397307));
#59288=CARTESIAN_POINT('Ctrl Pts',(30.0620536519992,1.1837522743985,23.8083876544318));
#59289=CARTESIAN_POINT('Ctrl Pts',(30.2171585654068,1.16532445285658,23.7988132376599));
#59290=CARTESIAN_POINT('Ctrl Pts',(30.5112461966771,1.06944336945855,23.7773546576131));
#59291=CARTESIAN_POINT('Ctrl Pts',(30.6473149557494,0.993007607319778,23.7662890582319));
#59292=CARTESIAN_POINT('Ctrl Pts',(30.8778837711073,0.795444168961031,23.7451260014428));
#59293=CARTESIAN_POINT('Ctrl Pts',(30.9715473998777,0.67784526646015,23.735564295613));
#59294=CARTESIAN_POINT('Ctrl Pts',(31.1131802711266,0.407843424843195,23.7164191470464));
#59295=CARTESIAN_POINT('Ctrl Pts',(31.1573957362652,0.25674391618342,23.7057050625635));
#59296=CARTESIAN_POINT('Ctrl Pts',(31.1840399706984,-0.0507119055208601,
23.6839041468775));
#59297=CARTESIAN_POINT('Ctrl Pts',(31.1674350137646,-0.204026769058537,
23.6730329771762));
#59298=CARTESIAN_POINT('Ctrl Pts',(31.0773689934766,-0.492841082509219,
23.6525538837521));
#59299=CARTESIAN_POINT('Ctrl Pts',(31.0058979842309,-0.625925698609867,
23.643745116865));
#59300=CARTESIAN_POINT('Ctrl Pts',(30.8122457094484,-0.863760919813326,
23.62342123376));
#59301=CARTESIAN_POINT('Ctrl Pts',(30.6897727103237,-0.964377961310509,
23.612333201652));
#59302=CARTESIAN_POINT('Ctrl Pts',(30.4178613794486,-1.10877008346121,23.5905165190165));
#59303=CARTESIAN_POINT('Ctrl Pts',(30.2721056949232,-1.15323707752562,23.5799894803724));
#59304=CARTESIAN_POINT('Ctrl Pts',(30.081329944032,-1.17313232340388,23.5675690244761));
#59305=CARTESIAN_POINT('Ctrl Pts',(30.0406432929718,-1.17524047358083,23.5649958100773));
#59306=CARTESIAN_POINT('Ctrl Pts',(30.0000000000005,-1.17524047358085,23.5625));
#59307=CARTESIAN_POINT('Ctrl Pts',(29.9999999999999,-1.17524047358085,23.5));
#59308=CARTESIAN_POINT('Ctrl Pts',(30.0894855238544,-1.17524047358085,23.5054950978594));
#59309=CARTESIAN_POINT('Ctrl Pts',(30.178854666788,-1.16502438903023,23.5113452474122));
#59310=CARTESIAN_POINT('Ctrl Pts',(30.4182361773703,-1.10931034894115,23.5280203800546));
#59311=CARTESIAN_POINT('Ctrl Pts',(30.5615135396518,-1.04411918207875,23.5391299800668));
#59312=CARTESIAN_POINT('Ctrl Pts',(30.8095036980223,-0.865097093436967,
23.5607054808684));
#59313=CARTESIAN_POINT('Ctrl Pts',(30.9132272713337,-0.75480290560396,23.5709852453531));
#59314=CARTESIAN_POINT('Ctrl Pts',(31.0771989331901,-0.495400927628404,
23.5902511331837));
#59315=CARTESIAN_POINT('Ctrl Pts',(31.1336431986023,-0.347374707971562,
23.6003685369235));
#59316=CARTESIAN_POINT('Ctrl Pts',(31.1845754344926,-0.0407388684447008,
23.6221113097446));
#59317=CARTESIAN_POINT('Ctrl Pts',(31.1797255553422,0.114581560252514,23.6331246890053));
#59318=CARTESIAN_POINT('Ctrl Pts',(31.1115436466863,0.409699470279596,23.6540507545398));
#59319=CARTESIAN_POINT('Ctrl Pts',(31.0507381700391,0.547097840637693,23.6632066094863));
#59320=CARTESIAN_POINT('Ctrl Pts',(30.877053704825,0.797680553802843,23.6827562620821));
#59321=CARTESIAN_POINT('Ctrl Pts',(30.7635871432854,0.906879897536129,23.6935955044951));
#59322=CARTESIAN_POINT('Ctrl Pts',(30.5039119215803,1.07256979004896,23.7154158816792));
#59323=CARTESIAN_POINT('Ctrl Pts',(30.3609720672946,1.12873587571,23.726184783255));
#59324=CARTESIAN_POINT('Ctrl Pts',(30.0630485009405,1.18318311722529,23.7464099346189));
#59325=CARTESIAN_POINT('Ctrl Pts',(29.9110260227659,1.18151676553675,23.755241166967));
#59326=CARTESIAN_POINT('Ctrl Pts',(29.6103298881048,1.1197202582759,23.7758971342361));
#59327=CARTESIAN_POINT('Ctrl Pts',(29.46506200542,1.05803905975613,23.7870045259814));
#59328=CARTESIAN_POINT('Ctrl Pts',(29.2120537724961,0.884838382027716,23.8086817842968));
#59329=CARTESIAN_POINT('Ctrl Pts',(29.1053977198379,0.776856295866943,23.8190596528721));
#59330=CARTESIAN_POINT('Ctrl Pts',(28.9357911246459,0.52231447495466,23.8384992581206));
#59331=CARTESIAN_POINT('Ctrl Pts',(28.8760978227722,0.377122301892393,23.8482592101808));
#59332=CARTESIAN_POINT('Ctrl Pts',(28.816919249242,0.0729797847098555,23.8698251878126));
#59333=CARTESIAN_POINT('Ctrl Pts',(28.8175683805337,-0.0828368336059415,
23.8808737506258));
#59334=CARTESIAN_POINT('Ctrl Pts',(28.8779787013698,-0.380073435953635,
23.9019500472809));
#59335=CARTESIAN_POINT('Ctrl Pts',(28.9351273214881,-0.519045422805617,
23.9113440791565));
#59336=CARTESIAN_POINT('Ctrl Pts',(29.1020830634255,-0.774116322451291,
23.9306396594913));
#59337=CARTESIAN_POINT('Ctrl Pts',(29.212592687875,-0.88627172070161,23.9414021264554));
#59338=CARTESIAN_POINT('Ctrl Pts',(29.4680719424329,-1.05901132730886,23.963214777767));
#59339=CARTESIAN_POINT('Ctrl Pts',(29.609865400996,-1.11904322621712,23.9740503393744));
#59340=CARTESIAN_POINT('Ctrl Pts',(29.8385706131875,-1.1669231022752,23.9897921149766));
#59341=CARTESIAN_POINT('Ctrl Pts',(29.9192597310019,-1.17524047358085,23.9950419278981));
#59342=CARTESIAN_POINT('Ctrl Pts',(30.,-1.17524047358085,24.));
#59343=CARTESIAN_POINT('Origin',(30.,-1.21864324187371E-14,15.78125));
#59344=CARTESIAN_POINT('',(29.9999999962159,-1.17524047358085,24.5624999995353));
#59345=CARTESIAN_POINT('',(30.0000000000002,-1.17524047358085,24.5));
#59346=CARTESIAN_POINT('',(30.,-1.17524047358085,15.78125));
#59347=CARTESIAN_POINT('Ctrl Pts',(29.9999999924319,-1.17524047358085,24.5624999995353));
#59348=CARTESIAN_POINT('Ctrl Pts',(29.8449382921852,-1.17524047258231,24.5529780211908));
#59349=CARTESIAN_POINT('Ctrl Pts',(29.6912874372683,-1.14455036315003,24.5424546005433));
#59350=CARTESIAN_POINT('Ctrl Pts',(29.4063853758944,-1.0258343762565,24.5207505023134));
#59351=CARTESIAN_POINT('Ctrl Pts',(29.2777080162496,-0.939688490130196,
24.5097945313951));
#59352=CARTESIAN_POINT('Ctrl Pts',(29.0636971062813,-0.72579687417109,24.4890693621447));
#59353=CARTESIAN_POINT('Ctrl Pts',(28.9792543776096,-0.601260808557374,
24.4801338851547));
#59354=CARTESIAN_POINT('Ctrl Pts',(28.8587167668904,-0.3209315497576,24.4602564455228));
#59355=CARTESIAN_POINT('Ctrl Pts',(28.8262532459446,-0.166807893138082,
24.449327926347));
#59356=CARTESIAN_POINT('Ctrl Pts',(28.823406512149,0.140728845641508,24.4275212730356));
#59357=CARTESIAN_POINT('Ctrl Pts',(28.851353518733,0.291209583843224,24.4168510640028));
#59358=CARTESIAN_POINT('Ctrl Pts',(28.9629467293987,0.573358103335639,24.3968446251906));
#59359=CARTESIAN_POINT('Ctrl Pts',(29.0455390967654,0.702301510494977,24.3878786774254));
#59360=CARTESIAN_POINT('Ctrl Pts',(29.2579957317181,0.924591935160839,24.3669511834331));
#59361=CARTESIAN_POINT('Ctrl Pts',(29.3868926291043,1.01465868024229,24.3558427221105));
#59362=CARTESIAN_POINT('Ctrl Pts',(29.6668973327643,1.13696430638437,24.3343120930999));
#59363=CARTESIAN_POINT('Ctrl Pts',(29.8144674232288,1.17014774293813,24.3240736802882));
#59364=CARTESIAN_POINT('Ctrl Pts',(30.1216534355145,1.17947691079308,24.3048793479835));
#59365=CARTESIAN_POINT('Ctrl Pts',(30.2784124097871,1.15260328295164,24.2946007685524));
#59366=CARTESIAN_POINT('Ctrl Pts',(30.5685961343608,1.03996407129779,24.2727877800628));
#59367=CARTESIAN_POINT('Ctrl Pts',(30.6996254486415,0.956741717213513,24.2617910312175));
#59368=CARTESIAN_POINT('Ctrl Pts',(30.9187688591,0.747835373953449,24.2409274335984));
#59369=CARTESIAN_POINT('Ctrl Pts',(31.006053860002,0.625488945893405,24.2318518411732));
#59370=CARTESIAN_POINT('Ctrl Pts',(31.1332209274868,0.348324830571042,24.2121988338701));
#59371=CARTESIAN_POINT('Ctrl Pts',(31.1693830920172,0.195045950853365,24.2013302156905));
#59372=CARTESIAN_POINT('Ctrl Pts',(31.1796570639592,-0.112665031805443,
24.1795112071857));
#59373=CARTESIAN_POINT('Ctrl Pts',(31.1552218060231,-0.264121048947789,
24.1687718435869));
#59374=CARTESIAN_POINT('Ctrl Pts',(31.0503552824464,-0.548400595365726,
24.1486142990383));
#59375=CARTESIAN_POINT('Ctrl Pts',(30.9713114905908,-0.678634752411996,
24.1397525078141));
#59376=CARTESIAN_POINT('Ctrl Pts',(30.7647686763693,-0.905919595273436,
24.119011097007));
#59377=CARTESIAN_POINT('Ctrl Pts',(30.6378140048735,-0.999372205084128,
24.1079018617007));
#59378=CARTESIAN_POINT('Ctrl Pts',(30.3601860918747,-1.12872343710904,24.0862673928177));
#59379=CARTESIAN_POINT('Ctrl Pts',(30.2130976252741,-1.16548763290266,24.0759316041108));
#59380=CARTESIAN_POINT('Ctrl Pts',(30.042024216247,-1.17467745886824,24.065100570339));
#59381=CARTESIAN_POINT('Ctrl Pts',(30.021003006896,-1.17524047358085,24.0637897457965));
#59382=CARTESIAN_POINT('Ctrl Pts',(30.0000000000002,-1.17524047358085,24.0625));
#59383=CARTESIAN_POINT('Ctrl Pts',(30.,-1.17524047358085,24.));
#59384=CARTESIAN_POINT('Ctrl Pts',(30.068631292987,-1.17524047358085,24.0042144880528));
#59385=CARTESIAN_POINT('Ctrl Pts',(30.1372731197099,-1.16923029330172,24.0086427063088));
#59386=CARTESIAN_POINT('Ctrl Pts',(30.3594639555913,-1.12983827430394,24.0236835229636));
#59387=CARTESIAN_POINT('Ctrl Pts',(30.5067279557135,-1.07189657495913,24.034780912417));
#59388=CARTESIAN_POINT('Ctrl Pts',(30.7648494491756,-0.904940985120749,
24.0565507524641));
#59389=CARTESIAN_POINT('Ctrl Pts',(30.8745226735525,-0.799463570900332,
24.0670250985558));
#59390=CARTESIAN_POINT('Ctrl Pts',(31.0499651911362,-0.550024618872908,
24.0866421584515));
#59391=CARTESIAN_POINT('Ctrl Pts',(31.1129833274185,-0.407722194144101,
24.0960894491163));
#59392=CARTESIAN_POINT('Ctrl Pts',(31.1806136864057,-0.106256135243321,
24.117465645852));
#59393=CARTESIAN_POINT('Ctrl Pts',(31.1843316043204,0.0499559746584703,
24.1285422519746));
#59394=CARTESIAN_POINT('Ctrl Pts',(31.131994520367,0.349324836152535,24.1497697417397));
#59395=CARTESIAN_POINT('Ctrl Pts',(31.0785837311869,0.489956671487056,24.1594708103671));
#59396=CARTESIAN_POINT('Ctrl Pts',(30.9185303965388,0.749536525439823,24.1785023892068));
#59397=CARTESIAN_POINT('Ctrl Pts',(30.8111165172128,0.864620133839068,24.1891785696567));
#59398=CARTESIAN_POINT('Ctrl Pts',(30.5601137220937,1.04443640550787,24.2109672262292));
#59399=CARTESIAN_POINT('Ctrl Pts',(30.4195953268947,1.10838743812269,24.2218634370972));
#59400=CARTESIAN_POINT('Ctrl Pts',(30.125226440525,1.17808176086598,24.2424108698401));
#59401=CARTESIAN_POINT('Ctrl Pts',(29.9745000794406,1.18444262103543,24.2512396402881));
#59402=CARTESIAN_POINT('Ctrl Pts',(29.671168206001,1.13918974904968,24.2714709284502));
#59403=CARTESIAN_POINT('Ctrl Pts',(29.5219912146071,1.08506931535676,24.2825503121002));
#59404=CARTESIAN_POINT('Ctrl Pts',(29.2588817407465,0.924538989806815,24.3043986527903));
#59405=CARTESIAN_POINT('Ctrl Pts',(29.1462343920073,0.821663056130735,24.3149634007337));
#59406=CARTESIAN_POINT('Ctrl Pts',(28.9649893539032,0.577368135519195,24.3347544047798));
#59407=CARTESIAN_POINT('Ctrl Pts',(28.8986993951907,0.437889260784583,24.3439503786226));
#59408=CARTESIAN_POINT('Ctrl Pts',(28.8227562109677,0.139172903579825,24.3651316009568));
#59409=CARTESIAN_POINT('Ctrl Pts',(28.814686650905,-0.0173128945475468,
24.3762276136201));
#59410=CARTESIAN_POINT('Ctrl Pts',(28.8589720780878,-0.318736522506238,
24.3976008016849));
#59411=CARTESIAN_POINT('Ctrl Pts',(28.9087096405855,-0.46104932706788,24.4076656524993));
#59412=CARTESIAN_POINT('Ctrl Pts',(29.0619693077579,-0.724977765539007,
24.4264342215945));
#59413=CARTESIAN_POINT('Ctrl Pts',(29.1662794308695,-0.84283884374432,24.4370182792792));
#59414=CARTESIAN_POINT('Ctrl Pts',(29.4127142037999,-1.0294613008905,24.4587677289451));
#59415=CARTESIAN_POINT('Ctrl Pts',(29.5518825792064,-1.09722011413893,24.4697160382912));
#59416=CARTESIAN_POINT('Ctrl Pts',(29.7982117366005,-1.1622217216024,24.4871470887339));
#59417=CARTESIAN_POINT('Ctrl Pts',(29.8989795683345,-1.17524047358088,24.4937965702842));
#59418=CARTESIAN_POINT('Ctrl Pts',(30.0000000000003,-1.17524047358085,24.5));
#59419=CARTESIAN_POINT('Origin',(30.,-1.21864324187371E-14,15.78125));
#59420=CARTESIAN_POINT('',(29.9999999999999,-1.17524047358085,25.0625));
#59421=CARTESIAN_POINT('',(30.0000000000002,-1.17524047358085,25.));
#59422=CARTESIAN_POINT('',(30.,-1.17524047358085,15.78125));
#59423=CARTESIAN_POINT('Ctrl Pts',(29.9999999999998,-1.17524047358085,25.0625));
#59424=CARTESIAN_POINT('Ctrl Pts',(29.9787160795735,-1.17524047358085,25.0611930039571));
#59425=CARTESIAN_POINT('Ctrl Pts',(29.9574135577721,-1.17466229796152,25.0598643671606));
#59426=CARTESIAN_POINT('Ctrl Pts',(29.7860545064693,-1.16533366685381,25.0490108716001));
#59427=CARTESIAN_POINT('Ctrl Pts',(29.638982260427,-1.12845915516134,25.0386721678491));
#59428=CARTESIAN_POINT('Ctrl Pts',(29.3614303849904,-0.998891400573746,
25.0170346917219));
#59429=CARTESIAN_POINT('Ctrl Pts',(29.2345369639167,-0.905335034780717,
25.0059255391243));
#59430=CARTESIAN_POINT('Ctrl Pts',(29.0281770961676,-0.677897334966365,
24.9851899432843));
#59431=CARTESIAN_POINT('Ctrl Pts',(28.9492422426318,-0.547623084588669,
24.9763305695037));
#59432=CARTESIAN_POINT('Ctrl Pts',(28.8429395559285,-0.25880932586385,24.9558515154165));
#59433=CARTESIAN_POINT('Ctrl Pts',(28.8187785161156,-0.102338490894112,
24.9447565638831));
#59434=CARTESIAN_POINT('Ctrl Pts',(28.8329707062525,0.20487723468326,24.9229726728069));
#59435=CARTESIAN_POINT('Ctrl Pts',(28.8688620223111,0.352813948215486,24.9124828541373));
#59436=CARTESIAN_POINT('Ctrl Pts',(28.9959383633127,0.629882762331914,24.8928366044019));
#59437=CARTESIAN_POINT('Ctrl Pts',(29.0869818629053,0.755846556300386,24.8834354015886));
#59438=CARTESIAN_POINT('Ctrl Pts',(29.3131553782924,0.966129203680405,24.8620913064548));
#59439=CARTESIAN_POINT('Ctrl Pts',(29.4462640631474,1.04811028996687,24.8510108758816));
#59440=CARTESIAN_POINT('Ctrl Pts',(29.731323759893,1.1538048728599,24.8297587550632));
#59441=CARTESIAN_POINT('Ctrl Pts',(29.8797531248391,1.17853792828451,24.8200009879783));
#59442=CARTESIAN_POINT('Ctrl Pts',(30.1846496308258,1.17107054148177,24.8010132560253));
#59443=CARTESIAN_POINT('Ctrl Pts',(30.3381730792388,1.13627251448872,24.7903520180859));
#59444=CARTESIAN_POINT('Ctrl Pts',(30.6200199170605,1.01003478142549,24.7685688600169));
#59445=CARTESIAN_POINT('Ctrl Pts',(30.7461080027782,0.920828764814659,24.7576633973259));
#59446=CARTESIAN_POINT('Ctrl Pts',(30.954589658464,0.701638656166971,24.7370899153526));
#59447=CARTESIAN_POINT('Ctrl Pts',(31.0359799147447,0.574699574292555,24.7282504951265));
#59448=CARTESIAN_POINT('Ctrl Pts',(31.1497275829798,0.289883112537678,24.7080548792676));
#59449=CARTESIAN_POINT('Ctrl Pts',(31.1781418190148,0.133683865658838,24.6969791852295));
#59450=CARTESIAN_POINT('Ctrl Pts',(31.1719905418774,-0.174601531099527,
24.6751194464719));
#59451=CARTESIAN_POINT('Ctrl Pts',(31.1398342436188,-0.323793762033814,
24.6645406022347));
#59452=CARTESIAN_POINT('Ctrl Pts',(31.020088030022,-0.603297917753395,24.644721668578));
#59453=CARTESIAN_POINT('Ctrl Pts',(30.9330960022514,-0.730676428588708,
24.6355607116713));
#59454=CARTESIAN_POINT('Ctrl Pts',(30.7134327937131,-0.946735070008641,
24.6144116187632));
#59455=CARTESIAN_POINT('Ctrl Pts',(30.5822707418913,-1.03259356059966,24.6033132579239));
#59456=CARTESIAN_POINT('Ctrl Pts',(30.299587098649,-1.14619538675731,24.5819267037008));
#59457=CARTESIAN_POINT('Ctrl Pts',(30.1515439291036,-1.17497884081411,24.5718152360255));
#59458=CARTESIAN_POINT('Ctrl Pts',(30.0013618111703,-1.17523988185447,24.5625836466351));
#59459=CARTESIAN_POINT('Ctrl Pts',(30.0006808894801,-1.17524047358524,24.5625418118389));
#59460=CARTESIAN_POINT('Ctrl Pts',(29.9999999924319,-1.17524047358085,24.5624999995353));
#59461=CARTESIAN_POINT('Ctrl Pts',(30.0000000000003,-1.17524047358085,24.5));
#59462=CARTESIAN_POINT('Ctrl Pts',(30.0475989786694,-1.17524047358084,24.5029229425557));
#59463=CARTESIAN_POINT('Ctrl Pts',(30.0952413712801,-1.17234913261358,24.5059510599029));
#59464=CARTESIAN_POINT('Ctrl Pts',(30.2990650070911,-1.14742109537484,24.5193511873216));
#59465=CARTESIAN_POINT('Ctrl Pts',(30.4499960157575,-1.0970416910395,24.5304056476212));
#59466=CARTESIAN_POINT('Ctrl Pts',(30.7177665488108,-0.942842462676014,
24.5523157520592));
#59467=CARTESIAN_POINT('Ctrl Pts',(30.833223349596,-0.842552715174129,24.5629613319529));
#59468=CARTESIAN_POINT('Ctrl Pts',(31.0200068112404,-0.603233885310555,
24.5829160166926));
#59469=CARTESIAN_POINT('Ctrl Pts',(31.0893943876237,-0.466400998056969,
24.591928683353));
#59470=CARTESIAN_POINT('Ctrl Pts',(31.1731872619397,-0.170385863873932,
24.612918368786));
#59471=CARTESIAN_POINT('Ctrl Pts',(31.185412882504,-0.0137497619841131,
24.6240250391094));
#59472=CARTESIAN_POINT('Ctrl Pts',(31.1488612218191,0.289356743431089,24.6455175557638));
#59473=CARTESIAN_POINT('Ctrl Pts',(31.1026857517696,0.433263084173784,24.6557215908795));
#59474=CARTESIAN_POINT('Ctrl Pts',(30.9558437041525,0.701308793163264,24.6747280350226));
#59475=CARTESIAN_POINT('Ctrl Pts',(30.8545058913013,0.821789237632239,24.6849956137961));
#59476=CARTESIAN_POINT('Ctrl Pts',(30.6123622815668,1.01480099766359,24.7067080777764));
#59477=CARTESIAN_POINT('Ctrl Pts',(30.4745499588497,1.08610079838188,24.7176986563197));
#59478=CARTESIAN_POINT('Ctrl Pts',(30.1837738406509,1.17031056558872,24.7385400922772));
#59479=CARTESIAN_POINT('Ctrl Pts',(30.0341022035471,1.18415559329136,24.7475897886987));
#59480=CARTESIAN_POINT('Ctrl Pts',(29.7305751526436,1.15452627151871,24.7672791490145));
#59481=CARTESIAN_POINT('Ctrl Pts',(29.5799242663497,1.10861951554252,24.7781578355522));
#59482=CARTESIAN_POINT('Ctrl Pts',(29.3089128663366,0.962634653740643,24.7999757240996));
#59483=CARTESIAN_POINT('Ctrl Pts',(29.1903801371545,0.865330006275208,24.8107043566494));
#59484=CARTESIAN_POINT('Ctrl Pts',(28.9974547059893,0.631606479932577,24.8308378310304));
#59485=CARTESIAN_POINT('Ctrl Pts',(28.9246531642855,0.497649505166107,24.8397129306474));
#59486=CARTESIAN_POINT('Ctrl Pts',(28.8322520407485,0.204711362593916,24.8604844343777));
#59487=CARTESIAN_POINT('Ctrl Pts',(28.8154219514347,0.0480344797090969,
24.8715939963785));
#59488=CARTESIAN_POINT('Ctrl Pts',(28.8433837526351,-0.256851307347509,
24.8932126773996));
#59489=CARTESIAN_POINT('Ctrl Pts',(28.8856263759144,-0.402401296034548,
24.9035332594392));
#59490=CARTESIAN_POINT('Ctrl Pts',(29.0254132564532,-0.675115053553108,
24.9228707031121));
#59491=CARTESIAN_POINT('Ctrl Pts',(29.1237053106631,-0.798585223889617,
24.932834945393));
#59492=CARTESIAN_POINT('Ctrl Pts',(29.3612206915393,-0.998444700238917,
24.9545059777387));
#59493=CARTESIAN_POINT('Ctrl Pts',(29.4974844913312,-1.07350395274647,24.9655347517064));
#59494=CARTESIAN_POINT('Ctrl Pts',(29.7595519260122,-1.15671325178265,24.9845777838555));
#59495=CARTESIAN_POINT('Ctrl Pts',(29.8794906495254,-1.17524047358089,24.9925998011151));
#59496=CARTESIAN_POINT('Ctrl Pts',(30.0000000000004,-1.17524047358085,25.));
#59497=CARTESIAN_POINT('Origin',(30.,-1.21864324187371E-14,15.78125));
#59498=CARTESIAN_POINT('',(29.9999999999997,-1.17524047358085,25.5625));
#59499=CARTESIAN_POINT('',(30.,-1.17524047358085,25.5));
#59500=CARTESIAN_POINT('',(30.,-1.17524047358085,15.78125));
#59501=CARTESIAN_POINT('Ctrl Pts',(29.9999999999995,-1.17524047358085,25.5625));
#59502=CARTESIAN_POINT('Ctrl Pts',(29.9590631434842,-1.17524047358085,25.5599861628683));
#59503=CARTESIAN_POINT('Ctrl Pts',(29.9180826982373,-1.17310176284205,25.557393823766));
#59504=CARTESIAN_POINT('Ctrl Pts',(29.7270170759755,-1.15303120939534,25.5449493522346));
#59505=CARTESIAN_POINT('Ctrl Pts',(29.5812843667667,-1.10844931412058,25.534419650774));
#59506=CARTESIAN_POINT('Ctrl Pts',(29.3094646041477,-0.963834030512161,
25.5126006792245));
#59507=CARTESIAN_POINT('Ctrl Pts',(29.1870616253517,-0.863111358786919,
25.5015132019157));
#59508=CARTESIAN_POINT('Ctrl Pts',(28.9936035835609,-0.625120486304078,
25.4811957277874));
#59509=CARTESIAN_POINT('Ctrl Pts',(28.922245153506,-0.491992360156719,25.4723859354899));
#59510=CARTESIAN_POINT('Ctrl Pts',(28.8324037582581,-0.203110856662721,
25.4519020777895));
#59511=CARTESIAN_POINT('Ctrl Pts',(28.8159185655927,-0.0497708721110285,
25.4410291268206));
#59512=CARTESIAN_POINT('Ctrl Pts',(28.8428111724951,0.257674311776114,25.4192289654353));
#59513=CARTESIAN_POINT('Ctrl Pts',(28.8871477746036,0.408737403201897,25.4085174632064));
#59514=CARTESIAN_POINT('Ctrl Pts',(29.028998912458,0.678628541452795,25.389380164336));
#59515=CARTESIAN_POINT('Ctrl Pts',(29.1227608288482,0.796156039557689,25.3798091767006));
#59516=CARTESIAN_POINT('Ctrl Pts',(29.3535044180399,0.99354320653279,25.3586416369362));
#59517=CARTESIAN_POINT('Ctrl Pts',(29.4896480206548,1.06987223772086,25.3475752255981));
#59518=CARTESIAN_POINT('Ctrl Pts',(29.7837920452496,1.16549604577304,25.326122303941));
#59519=CARTESIAN_POINT('Ctrl Pts',(29.9388720345248,1.18379547475176,25.3165570329261));
#59520=CARTESIAN_POINT('Ctrl Pts',(30.243221825482,1.15962478745302,25.2970106790485));
#59521=CARTESIAN_POINT('Ctrl Pts',(30.3896819125524,1.11893466510606,25.2865742888993));
#59522=CARTESIAN_POINT('Ctrl Pts',(30.664499787972,0.981897695245122,25.2648398897594));
#59523=CARTESIAN_POINT('Ctrl Pts',(30.7892223684277,0.884773136061606,25.2537375376443));
#59524=CARTESIAN_POINT('Ctrl Pts',(30.9892253393634,0.652081932327525,25.233206047704));
#59525=CARTESIAN_POINT('Ctrl Pts',(31.0644029101032,0.520407945827758,25.2244008128923));
#59526=CARTESIAN_POINT('Ctrl Pts',(31.1617865735135,0.233810524226684,25.2040789136694));
#59527=CARTESIAN_POINT('Ctrl Pts',(31.1822791704619,0.0813648687854731,
25.1932693773186));
#59528=CARTESIAN_POINT('Ctrl Pts',(31.1637300195375,-0.226326940808914,
25.1714517283273));
#59529=CARTESIAN_POINT('Ctrl Pts',(31.1234798971667,-0.378558584977568,
25.1606573669753));
#59530=CARTESIAN_POINT('Ctrl Pts',(30.9889788141031,-0.652134792227603,
25.1412587691706));
#59531=CARTESIAN_POINT('Ctrl Pts',(30.8984922205339,-0.772069973056249,
25.1319682180917));
#59532=CARTESIAN_POINT('Ctrl Pts',(30.6735951228457,-0.975307798919531,
25.1109522700489));
#59533=CARTESIAN_POINT('Ctrl Pts',(30.5399926661631,-1.05515984400593,25.0999170005632));
#59534=CARTESIAN_POINT('Ctrl Pts',(30.2678908596704,-1.15220558793873,25.0797672273045));
#59535=CARTESIAN_POINT('Ctrl Pts',(30.1343655548317,-1.17524047358085,25.0707510761622));
#59536=CARTESIAN_POINT('Ctrl Pts',(29.9999999999998,-1.17524047358085,25.0625));
#59537=CARTESIAN_POINT('Ctrl Pts',(30.0000000000004,-1.17524047358085,25.));
#59538=CARTESIAN_POINT('Ctrl Pts',(30.0280011909949,-1.17524047358084,25.0017194880028));
#59539=CARTESIAN_POINT('Ctrl Pts',(30.056028863347,-1.17423978093536,25.0034760804581));
#59540=CARTESIAN_POINT('Ctrl Pts',(30.2395952618035,-1.16108096396762,25.0152149952129));
#59541=CARTESIAN_POINT('Ctrl Pts',(30.3913571022497,-1.11907669842983,25.0260235449911));
#59542=CARTESIAN_POINT('Ctrl Pts',(30.6663605367685,-0.979972388704826,
25.0478426338075));
#59543=CARTESIAN_POINT('Ctrl Pts',(30.7876235644496,-0.885461952247295,
25.0586398624147));
#59544=CARTESIAN_POINT('Ctrl Pts',(30.9860830879355,-0.656850945315206,
25.0789319146131));
#59545=CARTESIAN_POINT('Ctrl Pts',(31.0619486284351,-0.525431380274417,
25.0877429880603));
#59546=CARTESIAN_POINT('Ctrl Pts',(31.162019301378,-0.235334014571736,25.1083130594786));
#59547=CARTESIAN_POINT('Ctrl Pts',(31.182987818821,-0.0787326337506094,
25.1194172678187));
#59548=CARTESIAN_POINT('Ctrl Pts',(31.162785126869,0.227544173273347,25.1411345825519));
#59549=CARTESIAN_POINT('Ctrl Pts',(31.1241144207896,0.374476178584838,25.1515531598995));
#59550=CARTESIAN_POINT('Ctrl Pts',(30.9915168317796,0.649674032406111,25.1710667445663));
#59551=CARTESIAN_POINT('Ctrl Pts',(30.8973599492461,0.774562668596496,25.1806896874262));
#59552=CARTESIAN_POINT('Ctrl Pts',(30.6662666830193,0.980382528688255,25.202177670528));
#59553=CARTESIAN_POINT('Ctrl Pts',(30.531751815152,1.05938687434591,25.2132389149495));
#59554=CARTESIAN_POINT('Ctrl Pts',(30.2450331875533,1.15903498558282,25.2343785368368));
#59555=CARTESIAN_POINT('Ctrl Pts',(30.0962908441082,1.18072042198942,25.2438927186044));
#59556=CARTESIAN_POINT('Ctrl Pts',(29.7917163095273,1.16710140491111,25.2630787773242));
#59557=CARTESIAN_POINT('Ctrl Pts',(29.638905788045,1.12920096781154,25.2738062281113));
#59558=CARTESIAN_POINT('Ctrl Pts',(29.3599222216531,0.997398530499289,25.2956108489033));
#59559=CARTESIAN_POINT('Ctrl Pts',(29.2358774116296,0.905886016991888,25.3064726127214));
#59560=CARTESIAN_POINT('Ctrl Pts',(29.0316806530828,0.682639701770527,25.32692677681));
#59561=CARTESIAN_POINT('Ctrl Pts',(28.9526524211366,0.553805209269406,25.3357310715183));
#59562=CARTESIAN_POINT('Ctrl Pts',(28.844720062577,0.266708452558536,25.3560883773325));
#59563=CARTESIAN_POINT('Ctrl Pts',(28.8194808141697,0.110295910906438,25.3671791955642));
#59564=CARTESIAN_POINT('Ctrl Pts',(28.8316382042729,-0.197210560241239,
25.3889837026743));
#59565=CARTESIAN_POINT('Ctrl Pts',(28.8665861506279,-0.345474523822663,
25.3994967258182));
#59566=CARTESIAN_POINT('Ctrl Pts',(28.9918018301732,-0.623166741842213,
25.4191871795497));
#59567=CARTESIAN_POINT('Ctrl Pts',(29.081808144475,-0.749490769071139,25.4285215559887));
#59568=CARTESIAN_POINT('Ctrl Pts',(29.3063266217772,-0.961255466999539,
25.449816563314));
#59569=CARTESIAN_POINT('Ctrl Pts',(29.438949602445,-1.04422897408056,25.4609023529488));
#59570=CARTESIAN_POINT('Ctrl Pts',(29.7169259241077,-1.14948331999011,25.4817038921344));
#59571=CARTESIAN_POINT('Ctrl Pts',(29.8579333178884,-1.17524047358086,25.4912760155257));
#59572=CARTESIAN_POINT('Ctrl Pts',(30.,-1.17524047358085,25.5));
#59573=CARTESIAN_POINT('Origin',(30.,-1.21864324187371E-14,15.78125));
#59574=CARTESIAN_POINT('',(30.,-1.17524047358085,26.0625));
#59575=CARTESIAN_POINT('',(30.,-1.17524047358085,26.));
#59576=CARTESIAN_POINT('',(30.,-1.17524047358085,15.78125));
#59577=CARTESIAN_POINT('Ctrl Pts',(29.9999999999999,-1.17524047358085,26.0625));
#59578=CARTESIAN_POINT('Ctrl Pts',(29.9384679078155,-1.17524047358085,26.0587214573544));
#59579=CARTESIAN_POINT('Ctrl Pts',(29.8769029052424,-1.17040913172972,26.054769604635));
#59580=CARTESIAN_POINT('Ctrl Pts',(29.6659154234359,-1.13693724882076,26.0406266508408));
#59581=CARTESIAN_POINT('Ctrl Pts',(29.5220177711255,-1.084323597792,26.0299248801994));
#59582=CARTESIAN_POINT('Ctrl Pts',(29.2586759114222,-0.925171378535031,
26.0081111282534));
#59583=CARTESIAN_POINT('Ctrl Pts',(29.1425757110306,-0.818746672431791,
25.9972085314777));
#59584=CARTESIAN_POINT('Ctrl Pts',(28.9627703960609,-0.572330389052239,
25.9774307272425));
#59585=CARTESIAN_POINT('Ctrl Pts',(28.8986210699436,-0.436327710221708,
25.9684388957715));
#59586=CARTESIAN_POINT('Ctrl Pts',(28.8234492804003,-0.143169608738148,
25.9476517953103));
#59587=CARTESIAN_POINT('Ctrl Pts',(28.8148292891501,0.0116076754049962,
25.936676929058));
#59588=CARTESIAN_POINT('Ctrl Pts',(28.8579269079672,0.318093458602922,25.9149447963521));
#59589=CARTESIAN_POINT('Ctrl Pts',(28.910158206845,0.466589649123026,25.9045489692953));
#59590=CARTESIAN_POINT('Ctrl Pts',(29.0662354765119,0.729159361472922,25.8856555497038));
#59591=CARTESIAN_POINT('Ctrl Pts',(29.1665620010353,0.841989757161643,25.8754944720367));
#59592=CARTESIAN_POINT('Ctrl Pts',(29.4086828051808,1.02746666351878,25.8540505472151));
#59593=CARTESIAN_POINT('Ctrl Pts',(29.5495956219979,1.09657907822105,25.84294712555));
#59594=CARTESIAN_POINT('Ctrl Pts',(29.8472420936479,1.17519666348882,25.8218820609165));
#59595=CARTESIAN_POINT('Ctrl Pts',(30.000722767755,1.18508027808238,25.8128044743545));
#59596=CARTESIAN_POINT('Ctrl Pts',(30.3019786609575,1.14582802588677,25.7929134117055));
#59597=CARTESIAN_POINT('Ctrl Pts',(30.4468987068161,1.09744171612032,25.7822987333));
#59598=CARTESIAN_POINT('Ctrl Pts',(30.7155809567247,0.94545759821414,25.7604111763944));
#59599=CARTESIAN_POINT('Ctrl Pts',(30.835612326607,0.841258259962285,25.7493460732515));
#59600=CARTESIAN_POINT('Ctrl Pts',(31.0226024258984,0.598138792258194,25.7292439525602));
#59601=CARTESIAN_POINT('Ctrl Pts',(31.0902361983429,0.463547729361891,25.7203689985712));
#59602=CARTESIAN_POINT('Ctrl Pts',(31.1725680326408,0.172449502286477,25.6997279586011));
#59603=CARTESIAN_POINT('Ctrl Pts',(31.1850367066478,0.0183235805600113,
25.6887992788123));
#59604=CARTESIAN_POINT('Ctrl Pts',(31.149849032726,-0.288650006825612,25.6670325571437));
#59605=CARTESIAN_POINT('Ctrl Pts',(31.1014848231134,-0.438439388995189,
25.6564113704209));
#59606=CARTESIAN_POINT('Ctrl Pts',(30.9523589365019,-0.704596833564904,
25.637538818338));
#59607=CARTESIAN_POINT('Ctrl Pts',(30.8552831525205,-0.819746342004528,
25.6276245442916));
#59608=CARTESIAN_POINT('Ctrl Pts',(30.6186741800399,-1.01116668038418,25.6063083713552));
#59609=CARTESIAN_POINT('Ctrl Pts',(30.4800603026513,-1.08386414646939,25.5952190187437));
#59610=CARTESIAN_POINT('Ctrl Pts',(30.2235083443405,-1.15925176820215,25.5767919868584));
#59611=CARTESIAN_POINT('Ctrl Pts',(30.1119520742388,-1.17524047358085,25.5693747164571));
#59612=CARTESIAN_POINT('Ctrl Pts',(29.9999999999995,-1.17524047358085,25.5625));
#59613=CARTESIAN_POINT('Ctrl Pts',(30.,-1.17524047358085,25.5));
#59614=CARTESIAN_POINT('Ctrl Pts',(30.0069574643761,-1.17524047358085,25.5004272417029));
#59615=CARTESIAN_POINT('Ctrl Pts',(30.01391720466,-1.17517869098561,25.5008568135879));
#59616=CARTESIAN_POINT('Ctrl Pts',(30.1767683930213,-1.17228514742378,25.5109597131747));
#59617=CARTESIAN_POINT('Ctrl Pts',(30.3305146751184,-1.13852257214804,25.5215979241794));
#59618=CARTESIAN_POINT('Ctrl Pts',(30.613289571589,-1.01415059475931,25.5433719241602));
#59619=CARTESIAN_POINT('Ctrl Pts',(30.7400483172667,-0.925722033283128,
25.5542910068295));
#59620=CARTESIAN_POINT('Ctrl Pts',(30.9499509146168,-0.707886564918499,
25.5749037184647));
#59621=CARTESIAN_POINT('Ctrl Pts',(31.0321249523172,-0.581569550980178,
25.5837623721801));
#59622=CARTESIAN_POINT('Ctrl Pts',(31.1477905785375,-0.297516308572578,
25.6039038700829));
#59623=CARTESIAN_POINT('Ctrl Pts',(31.1772544504942,-0.141401249469257,
25.6149735945785));
#59624=CARTESIAN_POINT('Ctrl Pts',(31.1730934439483,0.167116297568546,25.636849794526));
#59625=CARTESIAN_POINT('Ctrl Pts',(31.1418645520009,0.316603789635784,25.6474495749843));
#59626=CARTESIAN_POINT('Ctrl Pts',(31.0239238826678,0.596699382032703,25.6673104459219));
#59627=CARTESIAN_POINT('Ctrl Pts',(30.9379157361151,0.724424917792123,25.6764216802641));
#59628=CARTESIAN_POINT('Ctrl Pts',(30.7198518445296,0.941880855114492,25.6975221021999));
#59629=CARTESIAN_POINT('Ctrl Pts',(30.5891826263813,1.02868094414498,25.7086235824532));
#59630=CARTESIAN_POINT('Ctrl Pts',(30.3070725150413,1.14422525077315,25.730043785608));
#59631=CARTESIAN_POINT('Ctrl Pts',(30.1591233913896,1.1739884490527,25.7401842137377));
#59632=CARTESIAN_POINT('Ctrl Pts',(29.8537619113516,1.17646530259176,25.7590235656117));
#59633=CARTESIAN_POINT('Ctrl Pts',(29.6991872299891,1.1467452303545,25.7694824753175));
#59634=CARTESIAN_POINT('Ctrl Pts',(29.4128145699134,1.02954198968741,25.7912232470859));
#59635=CARTESIAN_POINT('Ctrl Pts',(29.2835235645903,0.944145175996724,25.8021903431407));
#59636=CARTESIAN_POINT('Ctrl Pts',(29.0681842616351,0.731537563632497,25.8229515631887));
#59637=CARTESIAN_POINT('Ctrl Pts',(28.9830068906091,0.607571894150497,25.8319186117076));
#59638=CARTESIAN_POINT('Ctrl Pts',(28.8607454143127,0.328058458525624,25.851738203379));
#59639=CARTESIAN_POINT('Ctrl Pts',(28.8273201029076,0.174145192049772,25.8626518043211));
#59640=CARTESIAN_POINT('Ctrl Pts',(28.8225473943512,-0.133454152009573,
25.8844628968148));
#59641=CARTESIAN_POINT('Ctrl Pts',(28.849586199068,-0.284195707441678,25.8951515997385));
#59642=CARTESIAN_POINT('Ctrl Pts',(28.9594336647467,-0.566901683792667,
25.9151975664084));
#59643=CARTESIAN_POINT('Ctrl Pts',(29.0410981500453,-0.696179869303813,
25.9241315793102));
#59644=CARTESIAN_POINT('Ctrl Pts',(29.2520170527073,-0.919779045076863,
25.9450110448572));
#59645=CARTESIAN_POINT('Ctrl Pts',(29.3804160320669,-1.01073211613404,25.95612035376));
#59646=CARTESIAN_POINT('Ctrl Pts',(29.6598179734432,-1.13487834137248,25.9776792246572));
#59647=CARTESIAN_POINT('Ctrl Pts',(29.8072708469184,-1.1689955596726,25.9879435454987));
#59648=CARTESIAN_POINT('Ctrl Pts',(29.9714632607541,-1.17498080122199,25.9982384188692));
#59649=CARTESIAN_POINT('Ctrl Pts',(29.9857363066776,-1.17524047358085,25.9991240997731));
#59650=CARTESIAN_POINT('Ctrl Pts',(29.9999999999999,-1.17524047358085,26.));
#59651=CARTESIAN_POINT('Origin',(30.,-1.21864324187371E-14,15.78125));
#59652=CARTESIAN_POINT('',(30.,-1.17524047358085,26.5625));
#59653=CARTESIAN_POINT('',(29.9999999999997,-1.17524047358085,26.4999999999999));
#59654=CARTESIAN_POINT('',(30.,-1.17524047358085,15.78125));
#59655=CARTESIAN_POINT('Ctrl Pts',(30.,-1.17524047358085,26.5625));
#59656=CARTESIAN_POINT('Ctrl Pts',(29.9189538385986,-1.17524047358085,26.5575231437572));
#59657=CARTESIAN_POINT('Ctrl Pts',(29.8379609361797,-1.16685998242801,26.5522524382954));
#59658=CARTESIAN_POINT('Ctrl Pts',(29.6089811727034,-1.1187361642345,26.5364851544771));
#59659=CARTESIAN_POINT('Ctrl Pts',(29.4672242547403,-1.05858684051961,26.5256476735947));
#59660=CARTESIAN_POINT('Ctrl Pts',(29.2118758464994,-0.885634166979752,
26.5038355032321));
#59661=CARTESIAN_POINT('Ctrl Pts',(29.1014575353795,-0.773390023233997,
26.4930754972477));
#59662=CARTESIAN_POINT('Ctrl Pts',(28.9347073730369,-0.518183463481665,
26.4737877314199));
#59663=CARTESIAN_POINT('Ctrl Pts',(28.8776702380248,-0.379162720284378,
26.4643854707334));
#59664=CARTESIAN_POINT('Ctrl Pts',(28.8174988609875,-0.0818619971934983,
26.4433046274383));
#59665=CARTESIAN_POINT('Ctrl Pts',(28.8169789681977,0.0739680819649894,
26.4322551101507));
#59666=CARTESIAN_POINT('Ctrl Pts',(28.8764093680924,0.378032609649621,26.4106946625572));
#59667=CARTESIAN_POINT('Ctrl Pts',(28.9362017786302,0.523138441896699,26.4009448281074));
#59668=CARTESIAN_POINT('Ctrl Pts',(29.1059813583505,0.777530022962841,26.3814999268455));
#59669=CARTESIAN_POINT('Ctrl Pts',(29.2127271628307,0.885439479708375,26.3711191218038));
#59670=CARTESIAN_POINT('Ctrl Pts',(29.4658882417733,1.05845819806925,26.3494389287095));
#59671=CARTESIAN_POINT('Ctrl Pts',(29.6112162771377,1.12003007041528,26.3383317191495));
#59672=CARTESIAN_POINT('Ctrl Pts',(29.9119535931961,1.18158358217449,26.3176818381253));
#59673=CARTESIAN_POINT('Ctrl Pts',(30.0639561135899,1.18313176493728,26.308852379607));
#59674=CARTESIAN_POINT('Ctrl Pts',(30.3618294498414,1.12846284091072,26.2886224532834));
#59675=CARTESIAN_POINT('Ctrl Pts',(30.5047372110283,1.07218329091309,26.2778514997354));
#59676=CARTESIAN_POINT('Ctrl Pts',(30.7642923496518,0.906285517829887,26.2560311264309));
#59677=CARTESIAN_POINT('Ctrl Pts',(30.8776734787023,0.796998466194141,26.2451940206555));
#59678=CARTESIAN_POINT('Ctrl Pts',(31.0511614964728,0.546283376197254,26.2256517381869));
#59679=CARTESIAN_POINT('Ctrl Pts',(31.1118599586541,0.408839660981002,26.2164897876345));
#59680=CARTESIAN_POINT('Ctrl Pts',(31.179816298086,0.113659355972694,26.1955592978295));
#59681=CARTESIAN_POINT('Ctrl Pts',(31.1845443559052,-0.0416770721755796,
26.1845447840881));
#59682=CARTESIAN_POINT('Ctrl Pts',(31.1333712501869,-0.348241759846019,
26.1628070564654));
#59683=CARTESIAN_POINT('Ctrl Pts',(31.0768319553006,-0.496185033349922,
26.1527007984472));
#59684=CARTESIAN_POINT('Ctrl Pts',(30.9126965034022,-0.755446668894444,
26.1334298283147));
#59685=CARTESIAN_POINT('Ctrl Pts',(30.8088874743598,-0.865675121928193,
26.1231471467367));
#59686=CARTESIAN_POINT('Ctrl Pts',(30.5607504336079,-1.04453090463544,26.1015685223966));
#59687=CARTESIAN_POINT('Ctrl Pts',(30.4174143875892,-1.10962145980108,26.0904588858133));
#59688=CARTESIAN_POINT('Ctrl Pts',(30.1782678600435,-1.16509155074858,26.0738068318412));
#59689=CARTESIAN_POINT('Ctrl Pts',(30.0891908090061,-1.17524047358085,26.0679770001062));
#59690=CARTESIAN_POINT('Ctrl Pts',(29.9999999999999,-1.17524047358085,26.0625));
#59691=CARTESIAN_POINT('Ctrl Pts',(29.9999999999999,-1.17524047358085,26.));
#59692=CARTESIAN_POINT('Ctrl Pts',(30.1425333221801,-1.17524047358085,26.0087526397553));
#59693=CARTESIAN_POINT('Ctrl Pts',(30.2840219111895,-1.14931710997616,26.0183602049923));
#59694=CARTESIAN_POINT('Ctrl Pts',(30.561367295123,-1.04389937746679,26.0391287924253));
#59695=CARTESIAN_POINT('Ctrl Pts',(30.6930583893841,-0.961526015756511,
26.0501360796874));
#59696=CARTESIAN_POINT('Ctrl Pts',(30.9136669465422,-0.754054974126117,
26.0710387617507));
#59697=CARTESIAN_POINT('Ctrl Pts',(31.0017654739708,-0.632326756940585,
26.0801633069178));
#59698=CARTESIAN_POINT('Ctrl Pts',(31.130809796733,-0.356072448301099,26.0997518021271));
#59699=CARTESIAN_POINT('Ctrl Pts',(31.1680189550385,-0.20305033553964,26.1106022136104));
#59700=CARTESIAN_POINT('Ctrl Pts',(31.1804056537492,0.10467710494643,26.1324223890981));
#59701=CARTESIAN_POINT('Ctrl Pts',(31.1569739806732,0.256395498849484,26.1431803571703));
#59702=CARTESIAN_POINT('Ctrl Pts',(31.0540187102742,0.541272174052999,26.1633802426127));
#59703=CARTESIAN_POINT('Ctrl Pts',(30.9759701950171,0.671873752670431,26.1722217092774));
#59704=CARTESIAN_POINT('Ctrl Pts',(30.7711018756191,0.900554058237447,26.1929097676203));
#59705=CARTESIAN_POINT('Ctrl Pts',(30.6447103916025,0.994954099829424,26.2040180088908));
#59706=CARTESIAN_POINT('Ctrl Pts',(30.3677839906361,1.12628386016982,26.2256795457743));
#59707=CARTESIAN_POINT('Ctrl Pts',(30.2208469191431,1.16405670623833,26.2360417980814));
#59708=CARTESIAN_POINT('Ctrl Pts',(29.9153739917407,1.18247957177519,26.2554533393943));
#59709=CARTESIAN_POINT('Ctrl Pts',(29.7596534858204,1.16089584886057,26.265267690896));
#59710=CARTESIAN_POINT('Ctrl Pts',(29.4669798482834,1.05871377618554,26.2868628344935));
#59711=CARTESIAN_POINT('Ctrl Pts',(29.3327683310263,0.97968769950255,26.2979062213058));
#59712=CARTESIAN_POINT('Ctrl Pts',(29.1064857982236,0.777827856716442,26.3189583910466));
#59713=CARTESIAN_POINT('Ctrl Pts',(29.0152252755147,0.658466900754918,26.3283097753497));
#59714=CARTESIAN_POINT('Ctrl Pts',(28.8789732904358,0.385760488964649,26.3476466981555));
#59715=CARTESIAN_POINT('Ctrl Pts',(28.8377485021289,0.233796400613908,26.3584220878003));
#59716=CARTESIAN_POINT('Ctrl Pts',(28.8172159011814,-0.0738574561607104,
26.3802370456529));
#59717=CARTESIAN_POINT('Ctrl Pts',(28.8367587774233,-0.226525134118623,
26.3910623250595));
#59718=CARTESIAN_POINT('Ctrl Pts',(28.9323498389723,-0.513670658612161,
26.411423088874));
#59719=CARTESIAN_POINT('Ctrl Pts',(29.0066122735479,-0.645689070611162,
26.4202237943573));
#59720=CARTESIAN_POINT('Ctrl Pts',(29.2050554476303,-0.879653705731429,
26.4407046487027));
#59721=CARTESIAN_POINT('Ctrl Pts',(29.329232754846,-0.977642983590833,26.4518041743651));
#59722=CARTESIAN_POINT('Ctrl Pts',(29.6033526154654,-1.11649688151574,26.4735601269295));
#59723=CARTESIAN_POINT('Ctrl Pts',(29.7496481694863,-1.15811817689029,26.4840194270505));
#59724=CARTESIAN_POINT('Ctrl Pts',(29.9332052808561,-1.1738184735254,26.4958478764586));
#59725=CARTESIAN_POINT('Ctrl Pts',(29.9666204732331,-1.17524047358085,26.4979502409084));
#59726=CARTESIAN_POINT('Ctrl Pts',(29.9999999999995,-1.17524047358085,26.4999999999999));
#59727=CARTESIAN_POINT('Origin',(30.,-1.21864324187371E-14,15.78125));
#59728=CARTESIAN_POINT('',(30.0000000000002,-1.17524047358085,27.0625));
#59729=CARTESIAN_POINT('',(29.9999999999999,-1.17524047358085,26.9999999999999));
#59730=CARTESIAN_POINT('',(30.,-1.17524047358085,15.78125));
#59731=CARTESIAN_POINT('Ctrl Pts',(30.0000000000003,-1.17524047358085,27.0625));
#59732=CARTESIAN_POINT('Ctrl Pts',(29.898686590649,-1.17524047358088,27.0562785792061));
#59733=CARTESIAN_POINT('Ctrl Pts',(29.7976296484377,-1.16214610940709,27.0496086633191));
#59734=CARTESIAN_POINT('Ctrl Pts',(29.5510548806291,-1.0968832857528,27.032153269422));
#59735=CARTESIAN_POINT('Ctrl Pts',(29.4119274187945,-1.02901377051944,27.0212035476842));
#59736=CARTESIAN_POINT('Ctrl Pts',(29.1656287201027,-0.842194481232163,
26.9994554755857));
#59737=CARTESIAN_POINT('Ctrl Pts',(29.0614102622354,-0.72425366568988,26.9888742198639));
#59738=CARTESIAN_POINT('Ctrl Pts',(28.9083494936521,-0.460199204673261,
26.9701133966982));
#59739=CARTESIAN_POINT('Ctrl Pts',(28.8587194637877,-0.317836463591476,
26.960036980781));
#59740=CARTESIAN_POINT('Ctrl Pts',(28.8146713989512,-0.0163533730831442,
26.9386595763769));
#59741=CARTESIAN_POINT('Ctrl Pts',(28.8228691179041,0.140138676728786,26.9275631204225));
#59742=CARTESIAN_POINT('Ctrl Pts',(28.8990556060477,0.438772825908234,26.9063877272517));
#59743=CARTESIAN_POINT('Ctrl Pts',(28.9654414239268,0.578169376458166,26.8971982372258));
#59744=CARTESIAN_POINT('Ctrl Pts',(29.1468572533747,0.822311817466142,26.8774021512523));
#59745=CARTESIAN_POINT('Ctrl Pts',(29.259591693584,0.925109502257862,26.8668348294397));
#59746=CARTESIAN_POINT('Ctrl Pts',(29.522846414638,1.08544747155122,26.8449843892055));
#59747=CARTESIAN_POINT('Ctrl Pts',(29.672078571298,1.13945389610578,26.8339056600349));
#59748=CARTESIAN_POINT('Ctrl Pts',(29.9754469871149,1.18446101454497,26.813680840772));
#59749=CARTESIAN_POINT('Ctrl Pts',(30.1261553208811,1.17798106873351,26.804850259546));
#59750=CARTESIAN_POINT('Ctrl Pts',(30.4204691708303,1.10805786050355,26.7842980916158));
#59751=CARTESIAN_POINT('Ctrl Pts',(30.5609479127602,1.04399036631935,26.7734001867649));
#59752=CARTESIAN_POINT('Ctrl Pts',(30.8118142126087,0.8639649033663,26.7516124954367));
#59753=CARTESIAN_POINT('Ctrl Pts',(30.9191345732301,0.748795351296203,26.7409390107287));
#59754=CARTESIAN_POINT('Ctrl Pts',(31.0789814493982,0.489082061456906,26.7219153792232));
#59755=CARTESIAN_POINT('Ctrl Pts',(31.13228056467,0.348399841671576,26.7122041527178));
#59756=CARTESIAN_POINT('Ctrl Pts',(31.1843745315803,0.0489678760358684,
26.6909721883974));
#59757=CARTESIAN_POINT('Ctrl Pts',(31.1805251276485,-0.10725425723734,26.6798948715428));
#59758=CARTESIAN_POINT('Ctrl Pts',(31.112642066065,-0.408638429750164,26.658524481164));
#59759=CARTESIAN_POINT('Ctrl Pts',(31.04952452927,-0.550854728541633,26.6490856679416));
#59760=CARTESIAN_POINT('Ctrl Pts',(30.8739065476105,-0.80013916056119,26.6294633115169));
#59761=CARTESIAN_POINT('Ctrl Pts',(30.7641429817239,-0.90553953226469,26.6189861492083));
#59762=CARTESIAN_POINT('Ctrl Pts',(30.5058691930861,-1.0723039712914,26.5972137340794));
#59763=CARTESIAN_POINT('Ctrl Pts',(30.3585462682162,-1.13013161506019,26.5861167698907));
#59764=CARTESIAN_POINT('Ctrl Pts',(30.1366295806596,-1.1692866034305,26.5711011916684));
#59765=CARTESIAN_POINT('Ctrl Pts',(30.0683089619122,-1.17524047358085,26.5666946944513));
#59766=CARTESIAN_POINT('Ctrl Pts',(30.,-1.17524047358085,26.5625));
#59767=CARTESIAN_POINT('Ctrl Pts',(29.9999999999995,-1.17524047358085,26.4999999999999));
#59768=CARTESIAN_POINT('Ctrl Pts',(30.1204914385722,-1.17524047358085,26.5073990989566));
#59769=CARTESIAN_POINT('Ctrl Pts',(30.2404377363977,-1.1567191282047,26.5154213729959));
#59770=CARTESIAN_POINT('Ctrl Pts',(30.503109066672,-1.07331217218126,26.5345084966475));
#59771=CARTESIAN_POINT('Ctrl Pts',(30.6398547835573,-0.997848639879795,
26.5455811972524));
#59772=CARTESIAN_POINT('Ctrl Pts',(30.8720104636609,-0.801888849767787,
26.566784844391));
#59773=CARTESIAN_POINT('Ctrl Pts',(30.9665674240944,-0.684937055709897,
26.5764328435252));
#59774=CARTESIAN_POINT('Ctrl Pts',(31.1101788342394,-0.415941539318355,
26.595506636112));
#59775=CARTESIAN_POINT('Ctrl Pts',(31.1554918067157,-0.265175979373474,
26.606197041135));
#59776=CARTESIAN_POINT('Ctrl Pts',(31.184388668241,0.0421759563922281,26.6279905905315));
#59777=CARTESIAN_POINT('Ctrl Pts',(31.1688709786064,0.195715280062819,26.6388776761339));
#59778=CARTESIAN_POINT('Ctrl Pts',(31.080842595015,0.4851372161482,26.6593998545441));
#59779=CARTESIAN_POINT('Ctrl Pts',(31.0103902901456,0.618617027917578,26.6682199013902));
#59780=CARTESIAN_POINT('Ctrl Pts',(30.8184983590075,0.857859380695496,26.6884855739597));
#59781=CARTESIAN_POINT('Ctrl Pts',(30.6966625458602,0.959431158368461,26.6995683269243));
#59782=CARTESIAN_POINT('Ctrl Pts',(30.4255868085001,1.10584185104675,26.7214052635744));
#59783=CARTESIAN_POINT('Ctrl Pts',(30.280042417997,1.15134883169079,26.7319561985547));
#59784=CARTESIAN_POINT('Ctrl Pts',(29.9776063567648,1.18496921576007,26.7517200618056));
#59785=CARTESIAN_POINT('Ctrl Pts',(29.8235440457018,1.17197554004672,26.7609515037779));
#59786=CARTESIAN_POINT('Ctrl Pts',(29.5271473201095,1.08704252411486,26.7821637300309));
#59787=CARTESIAN_POINT('Ctrl Pts',(29.3879639883513,1.01521369745337,26.7932572549969));
#59788=CARTESIAN_POINT('Ctrl Pts',(29.1499744927664,0.825212607812385,26.8146078849744));
#59789=CARTESIAN_POINT('Ctrl Pts',(29.0521140662545,0.710618013126823,26.8246118717047));
#59790=CARTESIAN_POINT('Ctrl Pts',(28.9012898027458,0.445344450507133,26.8434217499511));
#59791=CARTESIAN_POINT('Ctrl Pts',(28.8519884644377,0.295869143296566,26.8540206664119));
#59792=CARTESIAN_POINT('Ctrl Pts',(28.8148602582687,-0.0109614775297701,
26.8757772506829));
#59793=CARTESIAN_POINT('Ctrl Pts',(28.8263846212866,-0.165256365046284,
26.886717911409));
#59794=CARTESIAN_POINT('Ctrl Pts',(28.90695684434,-0.456865689279699,26.9073951919876));
#59795=CARTESIAN_POINT('Ctrl Pts',(28.9737284626765,-0.591802058760263,
26.9162939800796));
#59796=CARTESIAN_POINT('Ctrl Pts',(29.1592103949543,-0.836102522890621,
26.9363453584795));
#59797=CARTESIAN_POINT('Ctrl Pts',(29.2786778563743,-0.94110103302348,26.9474041669452));
#59798=CARTESIAN_POINT('Ctrl Pts',(29.5466042812102,-1.09478566204523,26.9693055998652));
#59799=CARTESIAN_POINT('Ctrl Pts',(29.6913217184938,-1.14405280529544,26.9799390653881));
#59800=CARTESIAN_POINT('Ctrl Pts',(29.8940937627055,-1.17166523876262,26.9933697888908));
#59801=CARTESIAN_POINT('Ctrl Pts',(29.9470693710243,-1.17524047358085,26.9967496532013));
#59802=CARTESIAN_POINT('Ctrl Pts',(29.9999999999997,-1.17524047358085,26.9999999999999));
#59803=CARTESIAN_POINT('Origin',(30.,-1.21864324187371E-14,15.78125));
#59804=CARTESIAN_POINT('',(30.0000000000002,-1.17524047358085,27.5625));
#59805=CARTESIAN_POINT('',(30.,-1.17524047358085,27.5));
#59806=CARTESIAN_POINT('',(30.,-1.17524047358085,15.78125));
#59807=CARTESIAN_POINT('Ctrl Pts',(30.0000000000004,-1.17524047358085,27.5625));
#59808=CARTESIAN_POINT('Ctrl Pts',(29.8791981655177,-1.17524047358089,27.5550818403526));
#59809=CARTESIAN_POINT('Ctrl Pts',(29.7589726578968,-1.15662316573575,27.547039018461));
#59810=CARTESIAN_POINT('Ctrl Pts',(29.4966785757901,-1.0731279551929,27.5279719317893));
#59811=CARTESIAN_POINT('Ctrl Pts',(29.3604611797136,-0.99796015863462,27.5169421590736));
#59812=CARTESIAN_POINT('Ctrl Pts',(29.1231210583237,-0.797935915977368,
27.495276047424));
#59813=CARTESIAN_POINT('Ctrl Pts',(29.0249429590029,-0.674426740918645,
27.4853218966019));
#59814=CARTESIAN_POINT('Ctrl Pts',(28.8853520572172,-0.401644540260052,
27.4659795997989));
#59815=CARTESIAN_POINT('Ctrl Pts',(28.8432060655213,-0.256055793645229,
27.4556562695324));
#59816=CARTESIAN_POINT('Ctrl Pts',(28.8154546971309,0.0488704066146756,
27.4340347229132));
#59817=CARTESIAN_POINT('Ctrl Pts',(28.8323972811925,0.205546638674019,27.4229252070608));
#59818=CARTESIAN_POINT('Ctrl Pts',(28.9250076761164,0.498408501969224,27.4021591121013));
#59819=CARTESIAN_POINT('Ctrl Pts',(28.997892508521,0.632295921050251,27.3932865033313));
#59820=CARTESIAN_POINT('Ctrl Pts',(29.1909681621961,0.865881565904131,27.3731486925495));
#59821=CARTESIAN_POINT('Ctrl Pts',(29.3095755456334,0.963111668503783,27.3624181185496));
#59822=CARTESIAN_POINT('Ctrl Pts',(29.5806971724252,1.10891198583092,27.3406000040234));
#59823=CARTESIAN_POINT('Ctrl Pts',(29.7313794614454,1.15471361111034,27.3297231163935));
#59824=CARTESIAN_POINT('Ctrl Pts',(30.0349224077729,1.1841311566887,27.3100402882342));
#59825=CARTESIAN_POINT('Ctrl Pts',(30.1845806615862,1.17018311962186,27.3009860288447));
#59826=CARTESIAN_POINT('Ctrl Pts',(30.4753054258698,1.08577187813399,27.2801406033955));
#59827=CARTESIAN_POINT('Ctrl Pts',(30.6130774728742,1.01437069747224,27.2691489037921));
#59828=CARTESIAN_POINT('Ctrl Pts',(30.8550923899249,0.82117912160722,27.2474379673869));
#59829=CARTESIAN_POINT('Ctrl Pts',(30.9563451215602,0.700625408948211,27.2371795779744));
#59830=CARTESIAN_POINT('Ctrl Pts',(31.1030012085855,0.43246305141941,27.218164862578));
#59831=CARTESIAN_POINT('Ctrl Pts',(31.1490749245368,0.288512534258167,27.207957695024));
#59832=CARTESIAN_POINT('Ctrl Pts',(31.1854037082186,-0.0146433585393976,
27.1864616764351));
#59833=CARTESIAN_POINT('Ctrl Pts',(31.173058308365,-0.171282192075426,27.1753548124176));
#59834=CARTESIAN_POINT('Ctrl Pts',(31.089040383827,-0.467218401344852,27.1543707233508));
#59835=CARTESIAN_POINT('Ctrl Pts',(31.0195638166583,-0.603975746358807,
27.1453625116794));
#59836=CARTESIAN_POINT('Ctrl Pts',(30.8326207012815,-0.843150163878356,
27.1254031429327));
#59837=CARTESIAN_POINT('Ctrl Pts',(30.7170833899544,-0.943363872050058,
27.1147553149523));
#59838=CARTESIAN_POINT('Ctrl Pts',(30.4491800434626,-1.09737775442843,27.0928436259578));
#59839=CARTESIAN_POINT('Ctrl Pts',(30.2981995637065,-1.14764798518389,27.0817899983651));
#59840=CARTESIAN_POINT('Ctrl Pts',(30.0946434783266,-1.17238533021172,27.0684130613475));
#59841=CARTESIAN_POINT('Ctrl Pts',(30.0473000417297,-1.17524047358084,27.0654045855337));
#59842=CARTESIAN_POINT('Ctrl Pts',(30.0000000000003,-1.17524047358085,27.0625));
#59843=CARTESIAN_POINT('Ctrl Pts',(29.9999999999997,-1.17524047358085,26.9999999999999));
#59844=CARTESIAN_POINT('Ctrl Pts',(30.0986058905517,-1.17524047358085,27.0060551583626));
#59845=CARTESIAN_POINT('Ctrl Pts',(30.197001235846,-1.16283641910558,27.0125371577158));
#59846=CARTESIAN_POINT('Ctrl Pts',(30.4435331990926,-1.0993899448342,27.029925526711));
#59847=CARTESIAN_POINT('Ctrl Pts',(30.5849622280491,-1.0311122983099,27.0410310521114));
#59848=CARTESIAN_POINT('Ctrl Pts',(30.8283565317534,-0.84700506573289,27.0625046195245));
#59849=CARTESIAN_POINT('Ctrl Pts',(30.9294172599309,-0.734710314399227,
27.0726917923361));
#59850=CARTESIAN_POINT('Ctrl Pts',(31.0870905034712,-0.472970868314495,
27.0916537809288));
#59851=CARTESIAN_POINT('Ctrl Pts',(31.1401926761717,-0.324772377450416,
27.1019712110874));
#59852=CARTESIAN_POINT('Ctrl Pts',(31.1850952185403,-0.0184511332937437,
27.1236916767454));
#59853=CARTESIAN_POINT('Ctrl Pts',(31.1773587357349,0.136461808282747,27.1346761621237));
#59854=CARTESIAN_POINT('Ctrl Pts',(31.1038267733963,0.430084241190232,27.1554961871532));
#59855=CARTESIAN_POINT('Ctrl Pts',(31.0404668538449,0.566412733303589,27.1645221322455));
#59856=CARTESIAN_POINT('Ctrl Pts',(30.8621032542639,0.813817787312719,27.1842464597062));
#59857=CARTESIAN_POINT('Ctrl Pts',(30.746618378735,0.920903307832853,27.195134699154));
#59858=CARTESIAN_POINT('Ctrl Pts',(30.4841269758582,1.08160589165682,27.2169511927423));
#59859=CARTESIAN_POINT('Ctrl Pts',(30.3404475283553,1.13505921838268,27.2276693335753));
#59860=CARTESIAN_POINT('Ctrl Pts',(30.0413373449537,1.18420822105003,27.2477795099651));
#59861=CARTESIAN_POINT('Ctrl Pts',(29.8888261880251,1.17970362185606,27.2566686898965));
#59862=CARTESIAN_POINT('Ctrl Pts',(29.5891419642887,1.11207867848515,27.2774691579106));
#59863=CARTESIAN_POINT('Ctrl Pts',(29.4453407649054,1.04779159085184,27.2885788725534));
#59864=CARTESIAN_POINT('Ctrl Pts',(29.1960372639306,0.870265103883027,27.3101819980009));
#59865=CARTESIAN_POINT('Ctrl Pts',(29.091548794378,0.760562756134129,27.3204877500418));
#59866=CARTESIAN_POINT('Ctrl Pts',(28.9261102653187,0.502419631695097,27.3397990837129));
#59867=CARTESIAN_POINT('Ctrl Pts',(28.8688162363146,0.355135077347701,27.3498182687336));
#59868=CARTESIAN_POINT('Ctrl Pts',(28.8157293168355,0.0491393235848099,
27.3715156546901));
#59869=CARTESIAN_POINT('Ctrl Pts',(28.8194875433144,-0.106321035237959,
27.3825389560425));
#59870=CARTESIAN_POINT('Ctrl Pts',(28.8856486083743,-0.401996025014571,
27.4035045226948));
#59871=CARTESIAN_POINT('Ctrl Pts',(28.9454972717022,-0.539801328338099,
27.4127167480926));
#59872=CARTESIAN_POINT('Ctrl Pts',(29.11742422097,-0.791565441680741,27.4322003607736));
#59873=CARTESIAN_POINT('Ctrl Pts',(29.2301245105903,-0.901546472787143,
27.4430202619491));
#59874=CARTESIAN_POINT('Ctrl Pts',(29.4887201815225,-1.06909180163981,27.4648401285834));
#59875=CARTESIAN_POINT('Ctrl Pts',(29.6313699534066,-1.1262717375032,27.4756271616522));
#59876=CARTESIAN_POINT('Ctrl Pts',(29.853348441796,-1.16837939045814,27.4907512179135));
#59877=CARTESIAN_POINT('Ctrl Pts',(29.9266702080884,-1.17524047358085,27.4954969880578));
#59878=CARTESIAN_POINT('Ctrl Pts',(30.,-1.17524047358085,27.5));
#59879=CARTESIAN_POINT('Origin',(30.,-1.21864324187371E-14,15.78125));
#59880=CARTESIAN_POINT('',(30.,-1.17524047358085,28.0625));
#59881=CARTESIAN_POINT('',(30.0000000000001,-1.17524047358085,28.));
#59882=CARTESIAN_POINT('',(30.,-1.17524047358085,15.78125));
#59883=CARTESIAN_POINT('Ctrl Pts',(30.,-1.17524047358085,28.0625));
#59884=CARTESIAN_POINT('Ctrl Pts',(29.8576309526277,-1.17524047358085,28.0537574479785));
#59885=CARTESIAN_POINT('Ctrl Pts',(29.7163289872701,-1.14937338079985,28.0441633378768));
#59886=CARTESIAN_POINT('Ctrl Pts',(29.4381412694858,-1.0437960185582,28.0233373652109));
#59887=CARTESIAN_POINT('Ctrl Pts',(29.3055725204167,-0.960712774920266,
28.0122510152415));
#59888=CARTESIAN_POINT('Ctrl Pts',(29.0812375157914,-0.748784364739409,
27.9909614703353));
#59889=CARTESIAN_POINT('Ctrl Pts',(28.991345872443,-0.622420436003701,27.9816342608879));
#59890=CARTESIAN_POINT('Ctrl Pts',(28.8663365712296,-0.344659291734443,
27.9619389197703));
#59891=CARTESIAN_POINT('Ctrl Pts',(28.8314934625426,-0.196359386622749,
27.9514233481032));
#59892=CARTESIAN_POINT('Ctrl Pts',(28.8195620391171,0.111178530712451,27.9296166112233));
#59893=CARTESIAN_POINT('Ctrl Pts',(28.8449209434754,0.267584161126331,27.9185262830501));
#59894=CARTESIAN_POINT('Ctrl Pts',(28.9530728770119,0.554595748995939,27.8981750163432));
#59895=CARTESIAN_POINT('Ctrl Pts',(29.0321899221582,0.683358417415679,27.8893700226253));
#59896=CARTESIAN_POINT('Ctrl Pts',(29.2365478324768,0.90645295573766,27.8689113436395));
#59897=CARTESIAN_POINT('Ctrl Pts',(29.3606700385593,0.997879761432882,27.8580478657718));
#59898=CARTESIAN_POINT('Ctrl Pts',(29.6397630167776,1.12947461119937,27.8362438860083));
#59899=CARTESIAN_POINT('Ctrl Pts',(29.7926014521638,1.16725893043214,27.8255188379057));
#59900=CARTESIAN_POINT('Ctrl Pts',(30.0971888483988,1.18064726325309,27.8063401680006));
#59901=CARTESIAN_POINT('Ctrl Pts',(30.2459190189188,1.15884794264961,27.7968175086224));
#59902=CARTESIAN_POINT('Ctrl Pts',(30.5325764826745,1.05897425995597,27.7756736453134));
#59903=CARTESIAN_POINT('Ctrl Pts',(30.6670400332198,0.979858412729581,27.7646115990219));
#59904=CARTESIAN_POINT('Ctrl Pts',(30.8979501916997,0.773870883397489,27.7431289156398));
#59905=CARTESIAN_POINT('Ctrl Pts',(30.9919903689524,0.648942084588862,27.7335148439956));
#59906=CARTESIAN_POINT('Ctrl Pts',(31.1243827012244,0.373674108325156,27.7139962871235));
#59907=CARTESIAN_POINT('Ctrl Pts',(31.1629506296625,0.226703861102418,27.7035749981386));
#59908=CARTESIAN_POINT('Ctrl Pts',(31.182930645767,-0.0796098768690557,
27.6818550647252));
#59909=CARTESIAN_POINT('Ctrl Pts',(31.1618436472684,-0.236207537040712,
27.6707511202069));
#59910=CARTESIAN_POINT('Ctrl Pts',(31.0615541749908,-0.526222674013738,
27.6501868794201));
#59911=CARTESIAN_POINT('Ctrl Pts',(30.9856010212307,-0.657569956578418,
27.641376820382));
#59912=CARTESIAN_POINT('Ctrl Pts',(30.7869826832863,-0.886033452367878,
27.6210802455783));
#59913=CARTESIAN_POINT('Ctrl Pts',(30.6656419827339,-0.980462303947253,
27.6102811397496));
#59914=CARTESIAN_POINT('Ctrl Pts',(30.3905261901255,-1.11936682731598,27.5884622344572));
#59915=CARTESIAN_POINT('Ctrl Pts',(30.2387339000707,-1.16125829953858,27.5776558137839));
#59916=CARTESIAN_POINT('Ctrl Pts',(30.0554488466051,-1.17426038713893,27.5659397324124));
#59917=CARTESIAN_POINT('Ctrl Pts',(30.0277113777332,-1.17524047358084,27.5642016912446));
#59918=CARTESIAN_POINT('Ctrl Pts',(30.0000000000004,-1.17524047358085,27.5625));
#59919=CARTESIAN_POINT('Ctrl Pts',(30.,-1.17524047358085,27.5));
#59920=CARTESIAN_POINT('Ctrl Pts',(30.0764884643488,-1.17524047358085,27.5046969786688));
#59921=CARTESIAN_POINT('Ctrl Pts',(30.1529528341161,-1.16777574296381,27.5096571303415));
#59922=CARTESIAN_POINT('Ctrl Pts',(30.3817494239676,-1.12246086122216,27.5253135785994));
#59923=CARTESIAN_POINT('Ctrl Pts',(30.5275514222186,-1.06175746883915,27.5364191022575));
#59924=CARTESIAN_POINT('Ctrl Pts',(30.7819194324173,-0.890185564641921,
27.5581221152238));
#59925=CARTESIAN_POINT('Ctrl Pts',(30.8893748791333,-0.782854361740771,
27.5685259964847));
#59926=CARTESIAN_POINT('Ctrl Pts',(31.0605234375151,-0.529653947481304,
27.5880127322271));
#59927=CARTESIAN_POINT('Ctrl Pts',(31.1210989339899,-0.385229961573254,
27.5976843165126));
#59928=CARTESIAN_POINT('Ctrl Pts',(31.1825194576632,-0.0817855747122669,
27.6192007914867));
#59929=CARTESIAN_POINT('Ctrl Pts',(31.1830228429167,0.0741472759213479,
27.63025759604));
#59930=CARTESIAN_POINT('Ctrl Pts',(31.1247432077576,0.371953492117145,27.6513742825742));
#59931=CARTESIAN_POINT('Ctrl Pts',(31.0685868115923,0.511361040320207,27.6608435628079));
#59932=CARTESIAN_POINT('Ctrl Pts',(30.9034614818395,0.767636822344003,27.6800694593713));
#59933=CARTESIAN_POINT('Ctrl Pts',(30.7937668420839,0.880579083554765,27.6908097772536));
#59934=CARTESIAN_POINT('Ctrl Pts',(30.5394580202052,1.05521084982092,27.712617639148));
#59935=CARTESIAN_POINT('Ctrl Pts',(30.3979930311562,1.11628678065312,27.7234700450399));
#59936=CARTESIAN_POINT('Ctrl Pts',(30.102283661711,1.18033932531086,27.7438997716137));
#59937=CARTESIAN_POINT('Ctrl Pts',(29.9510987894339,1.18375239925559,27.752701130013));
#59938=CARTESIAN_POINT('Ctrl Pts',(29.6486955420892,1.13241772430468,27.7730910160496));
#59939=CARTESIAN_POINT('Ctrl Pts',(29.5009111395855,1.07549105438516,27.7841843756164));
#59940=CARTESIAN_POINT('Ctrl Pts',(29.2414417758967,0.910237971539166,27.8059766250036));
#59941=CARTESIAN_POINT('Ctrl Pts',(29.1309679987517,0.805447516109976,27.8164757759223));
#59942=CARTESIAN_POINT('Ctrl Pts',(28.9539689931679,0.557381504423619,27.8361397402596));
#59943=CARTESIAN_POINT('Ctrl Pts',(28.8900701663349,0.415841482478183,27.8455137308899));
#59944=CARTESIAN_POINT('Ctrl Pts',(28.8202010476643,0.115104610378523,27.8668382228314));
#59945=CARTESIAN_POINT('Ctrl Pts',(28.8153164753922,-0.0411926086217122,
27.8779208638252));
#59946=CARTESIAN_POINT('Ctrl Pts',(28.8654961586475,-0.341119160610214,
27.8991878980145));
#59947=CARTESIAN_POINT('Ctrl Pts',(28.9179176762722,-0.482198917057609,
27.9089809285524));
#59948=CARTESIAN_POINT('Ctrl Pts',(29.0761417927703,-0.742958176446737,
27.9279419936907));
#59949=CARTESIAN_POINT('Ctrl Pts',(29.1827253034037,-0.858799901268264,
27.938594061191));
#59950=CARTESIAN_POINT('Ctrl Pts',(29.4325136093474,-1.04046451212148,27.9603736693398));
#59951=CARTESIAN_POINT('Ctrl Pts',(29.5726776549044,-1.10544579696665,27.9712846467122));
#59952=CARTESIAN_POINT('Ctrl Pts',(29.8127786384444,-1.16404144712018,27.9881061243607));
#59953=CARTESIAN_POINT('Ctrl Pts',(29.9063068575872,-1.17524047358087,27.9942465220726));
#59954=CARTESIAN_POINT('Ctrl Pts',(30.0000000000002,-1.17524047358085,28.));
#59955=CARTESIAN_POINT('Origin',(30.,-1.21864324187371E-14,15.78125));
#59956=CARTESIAN_POINT('',(30.,-1.17524047358085,28.5625));
#59957=CARTESIAN_POINT('',(30.0000000000002,-1.17524047358085,28.5));
#59958=CARTESIAN_POINT('',(30.,-1.17524047358085,15.78125));
#59959=CARTESIAN_POINT('Ctrl Pts',(29.9999999999999,-1.17524047358085,28.5625));
#59960=CARTESIAN_POINT('Ctrl Pts',(29.9854755687231,-1.17524047358085,28.5616080884619));
#59961=CARTESIAN_POINT('Ctrl Pts',(29.9709414772303,-1.17497122100143,28.5607060377023));
#59962=CARTESIAN_POINT('Ctrl Pts',(29.8064818821414,-1.16886648226933,28.5503905207309));
#59963=CARTESIAN_POINT('Ctrl Pts',(29.6590422242683,-1.13464684706092,28.5401233803667));
#59964=CARTESIAN_POINT('Ctrl Pts',(29.3797071247853,-1.01029888540339,28.5185614617647));
#59965=CARTESIAN_POINT('Ctrl Pts',(29.251363124374,-0.919248746833339,28.507452087585));
#59966=CARTESIAN_POINT('Ctrl Pts',(29.0406130665321,-0.695506305973089,
28.486577911123));
#59967=CARTESIAN_POINT('Ctrl Pts',(28.9590502383724,-0.56619133070644,28.4776471970656));
#59968=CARTESIAN_POINT('Ctrl Pts',(28.8493945968077,-0.283424288620792,
28.4575969003786));
#59969=CARTESIAN_POINT('Ctrl Pts',(28.8224557263032,-0.132654402250458,
28.4469061885797));
#59970=CARTESIAN_POINT('Ctrl Pts',(28.8274401393345,0.174951078681269,28.4250946609358));
#59971=CARTESIAN_POINT('Ctrl Pts',(28.8609710566448,0.328840848056597,28.4141827261138));
#59972=CARTESIAN_POINT('Ctrl Pts',(28.9834218096268,0.608264397886715,28.394369508017));
#59973=CARTESIAN_POINT('Ctrl Pts',(29.0686800279675,0.732167484395331,28.3853987862865));
#59974=CARTESIAN_POINT('Ctrl Pts',(29.2841654510491,0.944633593842617,28.3646336101487));
#59975=CARTESIAN_POINT('Ctrl Pts',(29.4135237499535,1.0299476859008,28.3536653145426));
#59976=CARTESIAN_POINT('Ctrl Pts',(29.6999884026637,1.14695518646917,28.3319258334386));
#59977=CARTESIAN_POINT('Ctrl Pts',(29.8545850153065,1.1765676391467,28.321476648926));
#59978=CARTESIAN_POINT('Ctrl Pts',(30.1599574738008,1.17387642238167,28.3026290229131));
#59979=CARTESIAN_POINT('Ctrl Pts',(30.3078958483554,1.14400535727984,28.2924854305785));
#59980=CARTESIAN_POINT('Ctrl Pts',(30.5899420117525,1.02824734362325,28.2710615776053));
#59981=CARTESIAN_POINT('Ctrl Pts',(30.7205565666579,0.941343746526345,28.2599597843468));
#59982=CARTESIAN_POINT('Ctrl Pts',(30.9384441962492,0.723734320112842,28.2388647444883));
#59983=CARTESIAN_POINT('Ctrl Pts',(31.0243441752868,0.5959705376245,28.2297587654061));
#59984=CARTESIAN_POINT('Ctrl Pts',(31.1420857275796,0.315809924237744,28.2098932839944));
#59985=CARTESIAN_POINT('Ctrl Pts',(31.1732121728651,0.166290213222924,28.1992912189719));
#59986=CARTESIAN_POINT('Ctrl Pts',(31.1771534741222,-0.14225217236566,28.1774132577855));
#59987=CARTESIAN_POINT('Ctrl Pts',(31.1475738082276,-0.298357527790664,
28.1663442213532));
#59988=CARTESIAN_POINT('Ctrl Pts',(31.0316967203975,-0.582326286717529,
28.1462087139606));
#59989=CARTESIAN_POINT('Ctrl Pts',(30.9494361151523,-0.708574806833004,
28.1373477050794));
#59990=CARTESIAN_POINT('Ctrl Pts',(30.7393766183288,-0.926260402286338,
28.1167306721673));
#59991=CARTESIAN_POINT('Ctrl Pts',(30.6125440370362,-1.01460273603848,28.1058101125197));
#59992=CARTESIAN_POINT('Ctrl Pts',(30.3296673321613,-1.13876808424026,28.0840371864985));
#59993=CARTESIAN_POINT('Ctrl Pts',(30.1758968644013,-1.17241612952657,28.0734015508245));
#59994=CARTESIAN_POINT('Ctrl Pts',(30.0133354780172,-1.17518374723503,28.0633209118452));
#59995=CARTESIAN_POINT('Ctrl Pts',(30.0066666906193,-1.17524047358085,28.0629093859629));
#59996=CARTESIAN_POINT('Ctrl Pts',(30.,-1.17524047358085,28.0625));
#59997=CARTESIAN_POINT('Ctrl Pts',(30.0000000000002,-1.17524047358085,28.));
#59998=CARTESIAN_POINT('Ctrl Pts',(30.055120011526,-1.17524047358084,28.0033847916881));
#59999=CARTESIAN_POINT('Ctrl Pts',(30.1102800819057,-1.17136342893539,28.0069094990185));
#60000=CARTESIAN_POINT('Ctrl Pts',(30.320778299587,-1.14149919825233,28.0208945034877));
#60001=CARTESIAN_POINT('Ctrl Pts',(30.4704399584402,-1.08838822567003,28.0319678602702));
#60002=CARTESIAN_POINT('Ctrl Pts',(30.7348284172129,-0.929562358310031,
28.0538343110362));
#60003=CARTESIAN_POINT('Ctrl Pts',(30.8482436418564,-0.827380507129033,
28.0644216046344));
#60004=CARTESIAN_POINT('Ctrl Pts',(31.0309964109232,-0.58443378950115,28.0842573960977));
#60005=CARTESIAN_POINT('Ctrl Pts',(31.0981318171314,-0.445680080400429,
28.0933979512832));
#60006=CARTESIAN_POINT('Ctrl Pts',(31.1762201438822,-0.147691887981632,
28.1145275412917));
#60007=CARTESIAN_POINT('Ctrl Pts',(31.1854211354334,0.00884554012676132,
28.1256272149066));
#60008=CARTESIAN_POINT('Ctrl Pts',(31.1432517249665,0.310649796547867,28.1470273923742));
#60009=CARTESIAN_POINT('Ctrl Pts',(31.0945166442476,0.453415390384783,28.1571505400084));
#60010=CARTESIAN_POINT('Ctrl Pts',(30.9430034157352,0.718468313966014,28.1759447732979));
#60011=CARTESIAN_POINT('Ctrl Pts',(30.8395316819024,0.837077300041102,28.1864571641064));
#60012=CARTESIAN_POINT('Ctrl Pts',(30.594175126874,1.02551549499305,28.2082047776097));
#60013=CARTESIAN_POINT('Ctrl Pts',(30.4553685567187,1.0942445153416,28.2191652668043));
#60014=CARTESIAN_POINT('Ctrl Pts',(30.1633070228503,1.17335763356101,28.2399049418951));
#60015=CARTESIAN_POINT('Ctrl Pts',(30.0132854694265,1.18458952272981,28.2488527114972));
#60016=CARTESIAN_POINT('Ctrl Pts',(29.7101813599922,1.14957783235101,28.2687069250423));
#60017=CARTESIAN_POINT('Ctrl Pts',(29.5603537745588,1.10100720474222,28.2796294987935));
#60018=CARTESIAN_POINT('Ctrl Pts',(29.2921855827035,0.950361389094781,28.3014380407736));
#60019=CARTESIAN_POINT('Ctrl Pts',(29.1755651130251,0.851181456436058,28.3121157317836));
#60020=CARTESIAN_POINT('Ctrl Pts',(28.9864685212412,0.613960284958293,28.3321380906356));
#60021=CARTESIAN_POINT('Ctrl Pts',(28.9157930252681,0.478217809624506,28.341090783094));
#60022=CARTESIAN_POINT('Ctrl Pts',(28.8287462552022,0.18335177826131,28.3619989885486));
#60023=CARTESIAN_POINT('Ctrl Pts',(28.8147855892159,0.0266848358587583,
28.3731078456949));
#60024=CARTESIAN_POINT('Ctrl Pts',(28.8481057813277,-0.277120858900621,
28.3946499400995));
#60025=CARTESIAN_POINT('Ctrl Pts',(28.8928044130046,-0.421659697790202,
28.4048988240612));
#60026=CARTESIAN_POINT('Ctrl Pts',(29.0376019293491,-0.692609521363159,
28.4241111916336));
#60027=CARTESIAN_POINT('Ctrl Pts',(29.1388311172626,-0.815074867447836,
28.4343484054768));
#60028=CARTESIAN_POINT('Ctrl Pts',(29.3808301647318,-1.01067727789171,28.456143840463));
#60029=CARTESIAN_POINT('Ctrl Pts',(29.5182554521743,-1.08294295653866,28.4671448960526));
#60030=CARTESIAN_POINT('Ctrl Pts',(29.7744135979937,-1.15894806924162,28.4855696371912));
#60031=CARTESIAN_POINT('Ctrl Pts',(29.8869899356779,-1.1752404735809,28.493060314833));
#60032=CARTESIAN_POINT('Ctrl Pts',(30.0000000000005,-1.17524047358085,28.5));
#60033=CARTESIAN_POINT('Origin',(30.,-1.21864324187371E-14,15.78125));
#60034=CARTESIAN_POINT('',(29.9999999999997,-1.17524047358085,29.0625));
#60035=CARTESIAN_POINT('',(30.,-1.17524047358085,29.));
#60036=CARTESIAN_POINT('',(30.,-1.17524047358085,15.78125));
#60037=CARTESIAN_POINT('Ctrl Pts',(29.9999999999995,-1.17524047358085,29.0625));
#60038=CARTESIAN_POINT('Ctrl Pts',(29.9663313283337,-1.17524047358085,29.0604324851927));
#60039=CARTESIAN_POINT('Ctrl Pts',(29.9326266255446,-1.17379373293774,29.0583114654359));
#60040=CARTESIAN_POINT('Ctrl Pts',(29.7487805300534,-1.15793171143038,29.046459536434));
#60041=CARTESIAN_POINT('Ctrl Pts',(29.6025054140808,-1.11619705168394,29.0359974721754));
#60042=CARTESIAN_POINT('Ctrl Pts',(29.3284713606868,-0.977122112422326,
29.0142389520917));
#60043=CARTESIAN_POINT('Ctrl Pts',(29.204360853848,-0.879027723836093,29.003139801917));
#60044=CARTESIAN_POINT('Ctrl Pts',(29.0061078341151,-0.644908297203287,
28.9826651365702));
#60045=CARTESIAN_POINT('Ctrl Pts',(28.9319567448549,-0.512847810431858,
28.9738647427883));
#60046=CARTESIAN_POINT('Ctrl Pts',(28.8365844224207,-0.225635628236165,
28.9534992524445));
#60047=CARTESIAN_POINT('Ctrl Pts',(28.8171575566038,-0.0729412609821712,
28.9426720805673));
#60048=CARTESIAN_POINT('Ctrl Pts',(28.8379321785986,0.234707082052963,28.92085751368));
#60049=CARTESIAN_POINT('Ctrl Pts',(28.8792757590782,0.386638085776581,28.9100844699825));
#60050=CARTESIAN_POINT('Ctrl Pts',(29.0157412244589,0.659238101106546,28.8907550914809));
#60051=CARTESIAN_POINT('Ctrl Pts',(29.107096372761,0.778529076561771,28.8813960362208));
#60052=CARTESIAN_POINT('Ctrl Pts',(29.3335481377689,0.980220242371224,28.8603394545531));
#60053=CARTESIAN_POINT('Ctrl Pts',(29.4678337645529,1.05914504636678,28.8492951073424));
#60054=CARTESIAN_POINT('Ctrl Pts',(29.760564366148,1.1610786562004,28.8277052746509));
#60055=CARTESIAN_POINT('Ctrl Pts',(29.9162604257863,1.18253750642917,28.8179009595418));
#60056=CARTESIAN_POINT('Ctrl Pts',(30.2216914945448,1.16389753053477,28.7984842912973));
#60057=CARTESIAN_POINT('Ctrl Pts',(30.3686116386073,1.12601470107769,28.7881191791422));
#60058=CARTESIAN_POINT('Ctrl Pts',(30.645460693513,0.994469364755083,28.7664547489262));
#60059=CARTESIAN_POINT('Ctrl Pts',(30.7717903384927,0.899966183411579,28.7553466483575));
#60060=CARTESIAN_POINT('Ctrl Pts',(30.9764758301347,0.671134004376585,28.7346644325598));
#60061=CARTESIAN_POINT('Ctrl Pts',(31.0544159221586,0.540492245543279,28.7258249398524));
#60062=CARTESIAN_POINT('Ctrl Pts',(31.1571623293156,0.255550540096121,28.7056204432797));
#60063=CARTESIAN_POINT('Ctrl Pts',(31.1804841833933,0.103803871660056,28.6948604703318));
#60064=CARTESIAN_POINT('Ctrl Pts',(31.1678665590545,-0.203924479708025,
28.6730402302557));
#60065=CARTESIAN_POINT('Ctrl Pts',(31.130543099267,-0.356918086122505,28.6621918400855));
#60066=CARTESIAN_POINT('Ctrl Pts',(31.0012937995436,-0.633072694293491,
28.6426104143845));
#60067=CARTESIAN_POINT('Ctrl Pts',(30.9131062008608,-0.754733454165662,
28.6334802730101));
#60068=CARTESIAN_POINT('Ctrl Pts',(30.6923373486102,-0.962047131628042,
28.6125733267459));
#60069=CARTESIAN_POINT('Ctrl Pts',(30.5605741188135,-1.04432722358406,28.6015649165697));
#60070=CARTESIAN_POINT('Ctrl Pts',(30.2834202387706,-1.14942800624881,28.5808193260016));
#60071=CARTESIAN_POINT('Ctrl Pts',(30.1422284632676,-1.17524047358085,28.5712339190787));
#60072=CARTESIAN_POINT('Ctrl Pts',(29.9999999999999,-1.17524047358085,28.5625));
#60073=CARTESIAN_POINT('Ctrl Pts',(30.0000000000005,-1.17524047358085,28.5));
#60074=CARTESIAN_POINT('Ctrl Pts',(30.0354745744302,-1.17524047358084,28.5021784110951));
#60075=CARTESIAN_POINT('Ctrl Pts',(30.070984899228,-1.17363438892678,28.50441595924));
#60076=CARTESIAN_POINT('Ctrl Pts',(30.2617617366305,-1.15628719000694,28.5167461440698));
#60077=CARTESIAN_POINT('Ctrl Pts',(30.4127085422869,-1.11138228847866,28.527607482843));
#60078=CARTESIAN_POINT('Ctrl Pts',(30.6847642885538,-0.967157900388871,
28.5494270868925));
#60079=CARTESIAN_POINT('Ctrl Pts',(30.804005950619,-0.870565283253422,28.5601740092255));
#60080=CARTESIAN_POINT('Ctrl Pts',(30.9983603111577,-0.638155310621775,
28.5803486604476));
#60081=CARTESIAN_POINT('Ctrl Pts',(31.0719538047089,-0.504858427298666,
28.5892017641887));
#60082=CARTESIAN_POINT('Ctrl Pts',(31.1663430846515,-0.212647773407092,
28.6099216835343));
#60083=CARTESIAN_POINT('Ctrl Pts',(31.1842429187448,-0.0559802512603478,
28.6210305817888));
#60084=CARTESIAN_POINT('Ctrl Pts',(31.1582832767207,0.249283949423046,28.6426760951642));
#60085=CARTESIAN_POINT('Ctrl Pts',(31.1169606007789,0.395199803964739,28.6530226198275));
#60086=CARTESIAN_POINT('Ctrl Pts',(30.9790360194058,0.668562290541804,28.6724060632391));
#60087=CARTESIAN_POINT('Ctrl Pts',(30.8818240300007,0.792402281745908,28.6822761930404));
#60088=CARTESIAN_POINT('Ctrl Pts',(30.6459736712074,0.993822232743541,28.7039003049109));
#60089=CARTESIAN_POINT('Ctrl Pts',(30.5101537410361,1.06991069848525,28.7149383113331));
#60090=CARTESIAN_POINT('Ctrl Pts',(30.2218612846042,1.16368326752433,28.7359662684601));
#60091=CARTESIAN_POINT('Ctrl Pts',(30.0727878905027,1.18239624374933,28.7452765661691));
#60092=CARTESIAN_POINT('Ctrl Pts',(29.7685724316717,1.16273575029291,28.764654767797));
#60093=CARTESIAN_POINT('Ctrl Pts',(29.6165255150965,1.12180125661046,28.7754428960271));
#60094=CARTESIAN_POINT('Ctrl Pts',(29.3404632117996,0.984593855919108,28.797259754998));
#60095=CARTESIAN_POINT('Ctrl Pts',(29.2184662863885,0.890859052794272,28.8080745514575));
#60096=CARTESIAN_POINT('Ctrl Pts',(29.0185031029016,0.663646825495766,28.8284093479536));
#60097=CARTESIAN_POINT('Ctrl Pts',(28.9418083423014,0.532910081337728,28.8372126922591));
#60098=CARTESIAN_POINT('Ctrl Pts',(28.8396688119263,0.243593095049782,28.8577274289443));
#60099=CARTESIAN_POINT('Ctrl Pts',(28.8175791014781,0.0870303940346913,
28.8688288945971));
#60100=CARTESIAN_POINT('Ctrl Pts',(28.8356734059559,-0.219589451967425,
28.8905705333577));
#60101=CARTESIAN_POINT('Ctrl Pts',(28.8733703746263,-0.366880393585839,
28.9010145619721));
#60102=CARTESIAN_POINT('Ctrl Pts',(29.0040267448551,-0.642739671975603,
28.9205750465844));
#60103=CARTESIAN_POINT('Ctrl Pts',(29.0970828699605,-0.768007510288218,
28.9301160290222));
#60104=CARTESIAN_POINT('Ctrl Pts',(29.3264450160403,-0.975407631545752,
28.9515537342264));
#60105=CARTESIAN_POINT('Ctrl Pts',(29.4604715589085,-1.05546393671967,28.9626222876417));
#60106=CARTESIAN_POINT('Ctrl Pts',(29.7327334190531,-1.15230702146743,28.9827747043974));
#60107=CARTESIAN_POINT('Ctrl Pts',(29.8659356312532,-1.17524047358086,28.9917674189746));
#60108=CARTESIAN_POINT('Ctrl Pts',(30.0000000000001,-1.17524047358085,29.));
#60109=CARTESIAN_POINT('Origin',(30.,-1.21864324187371E-14,15.78125));
#60110=CARTESIAN_POINT('',(29.9999999999999,-1.17524047358085,29.5625));
#60111=CARTESIAN_POINT('',(30.,-1.17524047358085,29.5));
#60112=CARTESIAN_POINT('',(30.,-1.17524047358085,15.78125));
#60113=CARTESIAN_POINT('Ctrl Pts',(29.9999999999998,-1.17524047358085,29.5625));
#60114=CARTESIAN_POINT('Ctrl Pts',(29.9467973546619,-1.17524047358085,29.5592329493093));
#60115=CARTESIAN_POINT('Ctrl Pts',(29.8935499193759,-1.17162840400865,29.5558350868076));
#60116=CARTESIAN_POINT('Ctrl Pts',(29.6905156464705,-1.14383638937277,29.5423818936273));
#60117=CARTESIAN_POINT('Ctrl Pts',(29.5458229652857,-1.09446322181842,29.531746189361));
#60118=CARTESIAN_POINT('Ctrl Pts',(29.2779882672223,-0.940574047774209,
29.5098431372833));
#60119=CARTESIAN_POINT('Ctrl Pts',(29.1585890601641,-0.835479489994527,
29.4987851149112));
#60120=CARTESIAN_POINT('Ctrl Pts',(28.9732889450876,-0.591037021395749,
29.4787398668936));
#60121=CARTESIAN_POINT('Ctrl Pts',(28.9066211123554,-0.456058910232785,
29.4698379853235));
#60122=CARTESIAN_POINT('Ctrl Pts',(28.8262612459225,-0.164388119091858,
29.4491563462818));
#60123=CARTESIAN_POINT('Ctrl Pts',(28.8148509180816,-0.0100732314283097,
29.4382142673958));
#60124=CARTESIAN_POINT('Ctrl Pts',(28.852213214805,0.296739305134607,29.4164589654342));
#60125=CARTESIAN_POINT('Ctrl Pts',(28.9016274703356,0.446176311860775,29.405862764764));
#60126=CARTESIAN_POINT('Ctrl Pts',(29.0526565417776,0.711342976877612,29.3870604663565));
#60127=CARTESIAN_POINT('Ctrl Pts',(29.1506118786123,0.825870653466757,29.3770454144149));
#60128=CARTESIAN_POINT('Ctrl Pts',(29.3887681357508,1.01569990993121,29.3556906361267));
#60129=CARTESIAN_POINT('Ctrl Pts',(29.5280199399709,1.08742345397384,29.3445966390884));
#60130=CARTESIAN_POINT('Ctrl Pts',(29.8244665773462,1.17210985589585,29.3233900912571));
#60131=CARTESIAN_POINT('Ctrl Pts',(29.9785058773413,1.18498177307898,29.3141652695437));
#60132=CARTESIAN_POINT('Ctrl Pts',(30.2808965556073,1.15114217787766,29.2943964213012));
#60133=CARTESIAN_POINT('Ctrl Pts',(30.4264177470889,1.1055232193301,29.2838429408837));
#60134=CARTESIAN_POINT('Ctrl Pts',(30.697402601783,0.95889535591386,29.2620038856125));
#60135=CARTESIAN_POINT('Ctrl Pts',(30.819169348162,0.85722095894767,29.2509217356401));
#60136=CARTESIAN_POINT('Ctrl Pts',(31.0108714255578,0.617827319896978,29.2306623578836));
#60137=CARTESIAN_POINT('Ctrl Pts',(31.0812140757987,0.48430476852144,29.221840827786));
#60138=CARTESIAN_POINT('Ctrl Pts',(31.1690224491511,0.194817477900372,29.2013140152506));
#60139=CARTESIAN_POINT('Ctrl Pts',(31.1844226308274,0.0412543787619307,
29.1904252437899));
#60140=CARTESIAN_POINT('Ctrl Pts',(31.1552826086302,-0.266085347349785,
29.1686325601491));
#60141=CARTESIAN_POINT('Ctrl Pts',(31.1098513200658,-0.416814367038074,
29.1579447461033));
#60142=CARTESIAN_POINT('Ctrl Pts',(30.9660264712179,-0.685700945491834,
29.1388786780306));
#60143=CARTESIAN_POINT('Ctrl Pts',(30.8713728192914,-0.802582950873403,
29.1292210796557));
#60144=CARTESIAN_POINT('Ctrl Pts',(30.6390456070483,-0.99836896334456,29.1080130601942));
#60145=CARTESIAN_POINT('Ctrl Pts',(30.5022270643229,-1.07372697770931,29.0969396285291));
#60146=CARTESIAN_POINT('Ctrl Pts',(30.2397868247199,-1.15682002769535,29.0778778247601));
#60147=CARTESIAN_POINT('Ctrl Pts',(30.1201628836901,-1.17524047358085,29.0698789231656));
#60148=CARTESIAN_POINT('Ctrl Pts',(29.9999999999995,-1.17524047358085,29.0625));
#60149=CARTESIAN_POINT('Ctrl Pts',(30.0000000000001,-1.17524047358085,29.));
#60150=CARTESIAN_POINT('Ctrl Pts',(30.0146960045521,-1.17524047358085,29.0009024474538));
#60151=CARTESIAN_POINT('Ctrl Pts',(30.0294011894743,-1.17496482224357,29.0018152315228));
#60152=CARTESIAN_POINT('Ctrl Pts',(30.199932441124,-1.16856010735523,29.0125142300756));
#60153=CARTESIAN_POINT('Ctrl Pts',(30.353002562887,-1.13175546267305,29.0232187723758));
#60154=CARTESIAN_POINT('Ctrl Pts',(30.6330116689674,-1.00191414666784,29.0450168400954));
#60155=CARTESIAN_POINT('Ctrl Pts',(30.7577840016447,-0.911212372347243,
29.0558945356534));
#60156=CARTESIAN_POINT('Ctrl Pts',(30.9634990803743,-0.689398439003151,
29.0763911529622));
#60157=CARTESIAN_POINT('Ctrl Pts',(31.0433641152287,-0.561238966842274,
29.0852039625465));
#60158=CARTESIAN_POINT('Ctrl Pts',(31.1533625468904,-0.274946500315461,
29.1055042381753));
#60159=CARTESIAN_POINT('Ctrl Pts',(31.1797284184379,-0.118602529514694,
29.1165901942211));
#60160=CARTESIAN_POINT('Ctrl Pts',(31.1696998210424,0.189193535485508,29.1384152356998));
#60161=CARTESIAN_POINT('Ctrl Pts',(31.1357401287962,0.337792934955289,29.1489520437553));
#60162=CARTESIAN_POINT('Ctrl Pts',(31.0124667812232,0.616132121424454,29.1686883723852));
#60163=CARTESIAN_POINT('Ctrl Pts',(30.9235367823029,0.742831293967475,29.1779572331897));
#60164=CARTESIAN_POINT('Ctrl Pts',(30.7007442503466,0.956131495282673,29.1992006935594));
#60165=CARTESIAN_POINT('Ctrl Pts',(30.5686344749746,1.04013508390185,29.2102914886907));
#60166=CARTESIAN_POINT('Ctrl Pts',(30.2847340927663,1.14996876391647,29.231619165161));
#60167=CARTESIAN_POINT('Ctrl Pts',(30.1365034722987,1.17678287240203,29.241562955497));
#60168=CARTESIAN_POINT('Ctrl Pts',(29.8314130542368,1.17348866622216,29.2604146402912));
#60169=CARTESIAN_POINT('Ctrl Pts',(29.6774432972388,1.14080144691636,29.271028448982));
#60170=CARTESIAN_POINT('Ctrl Pts',(29.3937190869037,1.01837161158084,29.2927918879254));
#60171=CARTESIAN_POINT('Ctrl Pts',(29.2662697773694,0.930754504522398,29.3037246074232));
#60172=CARTESIAN_POINT('Ctrl Pts',(29.0548960664095,0.714326580132712,29.3243777540292));
#60173=CARTESIAN_POINT('Ctrl Pts',(28.9719101496403,0.588650269969742,29.3332602962825));
#60174=CARTESIAN_POINT('Ctrl Pts',(28.8542643011592,0.305390771595589,29.3533455118009));
#60175=CARTESIAN_POINT('Ctrl Pts',(28.8237155837947,0.14936986715794,29.3644085600269));
#60176=CARTESIAN_POINT('Ctrl Pts',(28.8258171170069,-0.159374372506235,
29.386300834176));
#60177=CARTESIAN_POINT('Ctrl Pts',(28.8560851449643,-0.309160959864127,
29.3969218227258));
#60178=CARTESIAN_POINT('Ctrl Pts',(28.9721608102066,-0.589863983624277,
29.416825765087));
#60179=CARTESIAN_POINT('Ctrl Pts',(29.0571584178456,-0.717947603677171,
29.4258895505263));
#60180=CARTESIAN_POINT('Ctrl Pts',(29.2735722711375,-0.936836489269234,
29.4469394508198));
#60181=CARTESIAN_POINT('Ctrl Pts',(29.4037270862843,-1.02460346918986,29.4580436226767));
#60182=CARTESIAN_POINT('Ctrl Pts',(29.6852328519168,-1.14214540943397,29.4794975379443));
#60183=CARTESIAN_POINT('Ctrl Pts',(29.8330783756557,-1.1729174993834,29.4896673732243));
#60184=CARTESIAN_POINT('Ctrl Pts',(29.9885051427478,-1.17519832475183,29.4992926332218));
#60185=CARTESIAN_POINT('Ctrl Pts',(29.9942534046712,-1.17524047358085,29.4996471149485));
#60186=CARTESIAN_POINT('Ctrl Pts',(30.,-1.17524047358085,29.5));
#60187=CARTESIAN_POINT('Origin',(30.,-1.21864324187371E-14,15.78125));
#60188=CARTESIAN_POINT('',(30.,-1.17524047358085,30.0625));
#60189=CARTESIAN_POINT('',(29.9999999999998,-1.17524047358085,29.9999999999999));
#60190=CARTESIAN_POINT('',(30.,-1.17524047358085,15.78125));
#60191=CARTESIAN_POINT('Ctrl Pts',(30.,-1.17524047358085,30.0625));
#60192=CARTESIAN_POINT('Ctrl Pts',(29.9263916760993,-1.17524047358085,30.0579798840563));
#60193=CARTESIAN_POINT('Ctrl Pts',(29.8527927358329,-1.1683271801588,30.0532152422529));
#60194=CARTESIAN_POINT('Ctrl Pts',(29.6305589174408,-1.12600740432272,30.0380679862212));
#60195=CARTESIAN_POINT('Ctrl Pts',(29.4879403212856,-1.06872004039491,30.0272790588551));
#60196=CARTESIAN_POINT('Ctrl Pts',(29.229459906818,-0.900978381114361,30.0054593092048));
#60197=CARTESIAN_POINT('Ctrl Pts',(29.1168411945232,-0.790914788798306,
29.9946414903997));
#60198=CARTESIAN_POINT('Ctrl Pts',(28.9451007627829,-0.539025681180781,
29.975164899812));
#60199=CARTESIAN_POINT('Ctrl Pts',(28.885353566283,-0.401177024850609,29.9659464494622));
#60200=CARTESIAN_POINT('Ctrl Pts',(28.8194073352897,-0.10544306552401,29.944976701428));
#60201=CARTESIAN_POINT('Ctrl Pts',(28.8157651951869,0.0500317181756064,
29.9339523772439));
#60202=CARTESIAN_POINT('Ctrl Pts',(28.8690807484143,0.355959077177534,29.9122598409872));
#60203=CARTESIAN_POINT('Ctrl Pts',(28.9264649062036,0.503164977506288,29.9022508807468));
#60204=CARTESIAN_POINT('Ctrl Pts',(29.0920593097175,0.761174070029624,29.8829347271204));
#60205=CARTESIAN_POINT('Ctrl Pts',(29.1966290016669,0.870813111888444,29.8726262318314));
#60206=CARTESIAN_POINT('Ctrl Pts',(29.4460717811045,1.04817985046692,29.851020217295));
#60207=CARTESIAN_POINT('Ctrl Pts',(29.5899284156368,1.11237046788542,29.8399105187383));
#60208=CARTESIAN_POINT('Ctrl Pts',(29.8896511606184,1.17977836078127,29.8191153804746));
#60209=CARTESIAN_POINT('Ctrl Pts',(30.042143785172,1.18417711729498,29.810228885603));
#60210=CARTESIAN_POINT('Ctrl Pts',(30.3412103985985,1.13483145488925,29.7901144124214));
#60211=CARTESIAN_POINT('Ctrl Pts',(30.484863334991,1.08127741540018,29.7793943289302));
#60212=CARTESIAN_POINT('Ctrl Pts',(30.7472520600478,0.920389087318013,29.7575775552199));
#60213=CARTESIAN_POINT('Ctrl Pts',(30.8626628342488,0.813224513564577,29.7466910634298));
#60214=CARTESIAN_POINT('Ctrl Pts',(31.0408533066038,0.565701034414209,29.7269731686955));
#60215=CARTESIAN_POINT('Ctrl Pts',(31.1041185100332,0.42933329828376,29.7179429396888));
#60216=CARTESIAN_POINT('Ctrl Pts',(31.1774532864279,0.13565521801398,29.6971189688454));
#60217=CARTESIAN_POINT('Ctrl Pts',(31.185083485025,-0.0192736961984122,
29.6861333508878));
#60218=CARTESIAN_POINT('Ctrl Pts',(31.1399640096901,-0.325574493297471,
29.6644143350789));
#60219=CARTESIAN_POINT('Ctrl Pts',(31.0867572532099,-0.473736864086508,
29.654106159393));
#60220=CARTESIAN_POINT('Ctrl Pts',(30.9288924580137,-0.735375844574816,
29.6351359699395));
#60221=CARTESIAN_POINT('Ctrl Pts',(30.827743660758,-0.847605887956935,29.6249456831495));
#60222=CARTESIAN_POINT('Ctrl Pts',(30.5841967794232,-1.03154789843284,29.6034686040399));
#60223=CARTESIAN_POINT('Ctrl Pts',(30.4427060183441,-1.0997249484081,29.5923628543371));
#60224=CARTESIAN_POINT('Ctrl Pts',(30.1964052482032,-1.16291170221409,29.5749978904338));
#60225=CARTESIAN_POINT('Ctrl Pts',(30.0983061450535,-1.17524047358085,29.5685367516888));
#60226=CARTESIAN_POINT('Ctrl Pts',(29.9999999999998,-1.17524047358085,29.5625));
#60227=CARTESIAN_POINT('Ctrl Pts',(30.,-1.17524047358085,29.5));
#60228=CARTESIAN_POINT('Ctrl Pts',(30.1499565209686,-1.17524047358085,29.5092084811251));
#60229=CARTESIAN_POINT('Ctrl Pts',(30.2986551183888,-1.14654165825818,29.5193571963421));
#60230=CARTESIAN_POINT('Ctrl Pts',(30.5805418737435,-1.03331719508937,29.5406814366056));
#60231=CARTESIAN_POINT('Ctrl Pts',(30.7104602238272,-0.948696043146186,
29.5516595563353));
#60232=CARTESIAN_POINT('Ctrl Pts',(30.9271652336418,-0.73741304903825,29.5724576785973));
#60233=CARTESIAN_POINT('Ctrl Pts',(31.0130985609625,-0.614031092469691,
29.5814606062707));
#60234=CARTESIAN_POINT('Ctrl Pts',(31.1371264539894,-0.335358891062759,
29.6012205481486));
#60235=CARTESIAN_POINT('Ctrl Pts',(31.1715373282526,-0.181667965902616,
29.6121183834297));
#60236=CARTESIAN_POINT('Ctrl Pts',(31.1782875351469,0.125982959094587,29.6339331333974));
#60237=CARTESIAN_POINT('Ctrl Pts',(31.1521830035108,0.27698654047903,29.6446404159195));
#60238=CARTESIAN_POINT('Ctrl Pts',(31.0441268483734,0.560261316579686,29.6647267147429));
#60239=CARTESIAN_POINT('Ctrl Pts',(30.9634093757068,0.689883113720223,29.6736315391227));
#60240=CARTESIAN_POINT('Ctrl Pts',(30.7540662315648,0.914815989860588,29.6944615256665));
#60241=CARTESIAN_POINT('Ctrl Pts',(30.6261826944801,1.0066730037076,29.7055712306082));
#60242=CARTESIAN_POINT('Ctrl Pts',(30.3474095969538,1.1326991331979,29.7271581352984));
#60243=CARTESIAN_POINT('Ctrl Pts',(30.2000827038505,1.16777128079541,29.7374485757904));
#60244=CARTESIAN_POINT('Ctrl Pts',(29.8935937537322,1.18085135992657,29.7567330869508));
#60245=CARTESIAN_POINT('Ctrl Pts',(29.7372662628443,1.15617395643532,29.7668098469142));
#60246=CARTESIAN_POINT('Ctrl Pts',(29.4460305983855,1.04785975410839,29.7885340948419));
#60247=CARTESIAN_POINT('Ctrl Pts',(29.3136703421255,0.966357190577468,29.7995516007362));
#60248=CARTESIAN_POINT('Ctrl Pts',(29.091570241583,0.760352988788506,29.8204938700552));
#60249=CARTESIAN_POINT('Ctrl Pts',(29.0026423680915,0.639251124272773,29.8296723175212));
#60250=CARTESIAN_POINT('Ctrl Pts',(28.8716938065568,0.363925746310141,29.8491949446027));
#60251=CARTESIAN_POINT('Ctrl Pts',(28.8334229675251,0.211172023558316,29.8600263252283));
#60252=CARTESIAN_POINT('Ctrl Pts',(28.8188892259004,-0.0965571382164996,
29.8818466227683));
#60253=CARTESIAN_POINT('Ctrl Pts',(28.8412989000486,-0.248535346834791,
29.8926230136456));
#60254=CARTESIAN_POINT('Ctrl Pts',(28.942312504556,-0.5340148591211,29.9128656447428));
#60255=CARTESIAN_POINT('Ctrl Pts',(29.0193556498266,-0.664990211735325,
29.9216906330323));
#60256=CARTESIAN_POINT('Ctrl Pts',(29.2225255933627,-0.895077676800941,
29.9423242871271));
#60257=CARTESIAN_POINT('Ctrl Pts',(29.3483400060408,-0.990433515042349,
29.9534309783521));
#60258=CARTESIAN_POINT('Ctrl Pts',(29.6245422330139,-1.1237624473258,29.9751189235115));
#60259=CARTESIAN_POINT('Ctrl Pts',(29.7713190573348,-1.16255586776877,29.985507518588));
#60260=CARTESIAN_POINT('Ctrl Pts',(29.9476315409713,-1.1743662864253,29.9967531815485));
#60261=CARTESIAN_POINT('Ctrl Pts',(29.9738286104226,-1.17524047358085,29.9983928758457));
#60262=CARTESIAN_POINT('Ctrl Pts',(29.9999999999996,-1.17524047358085,29.9999999999999));
#60263=CARTESIAN_POINT('Origin',(30.,-1.21864324187371E-14,15.78125));
#60264=CARTESIAN_POINT('',(30.,-1.17524047358085,30.5625));
#60265=CARTESIAN_POINT('',(29.9999999999998,-1.17524047358085,30.4999999999999));
#60266=CARTESIAN_POINT('',(30.,-1.17524047358085,15.78125));
#60267=CARTESIAN_POINT('Ctrl Pts',(29.9999999999999,-1.17524047358085,30.5625));
#60268=CARTESIAN_POINT('Ctrl Pts',(29.87859718881,-1.17524047358085,30.555044935771));
#60269=CARTESIAN_POINT('Ctrl Pts',(29.7578462794256,-1.15643017462348,30.5469630079231));
#60270=CARTESIAN_POINT('Ctrl Pts',(29.5223698659242,-1.08113291221706,30.5298333797947));
#60271=CARTESIAN_POINT('Ctrl Pts',(29.4096002088597,-1.02391620699781,30.5208799114591));
#60272=CARTESIAN_POINT('Ctrl Pts',(29.1820826863431,-0.858187725726655,
30.5010328956616));
#60273=CARTESIAN_POINT('Ctrl Pts',(29.0755864711026,-0.74226695058618,30.4903833861391));
#60274=CARTESIAN_POINT('Ctrl Pts',(28.9175541454242,-0.481384400712606,
30.4714297273205));
#60275=CARTESIAN_POINT('Ctrl Pts',(28.8652363337421,-0.340257481842474,
30.4616267985498));
#60276=CARTESIAN_POINT('Ctrl Pts',(28.815283295232,-0.0402726424447981,
30.4403556313474));
#60277=CARTESIAN_POINT('Ctrl Pts',(28.8202904087434,0.116033016014593,30.4292723919329));
#60278=CARTESIAN_POINT('Ctrl Pts',(28.8903942350679,0.41669295482916,30.4079533551363));
#60279=CARTESIAN_POINT('Ctrl Pts',(28.9543854043788,0.558153128819785,30.3985868124474));
#60280=CARTESIAN_POINT('Ctrl Pts',(29.1315478521803,0.806074678810529,30.3789179332106));
#60281=CARTESIAN_POINT('Ctrl Pts',(29.2421055811419,0.910792536064214,30.3684162008828));
#60282=CARTESIAN_POINT('Ctrl Pts',(29.5017160718709,1.07586594659562,30.3466216552675));
#60283=CARTESIAN_POINT('Ctrl Pts',(29.6495548172672,1.13268560353193,30.3355287526402));
#60284=CARTESIAN_POINT('Ctrl Pts',(29.9519945282947,1.1837871612187,30.3151448923318));
#60285=CARTESIAN_POINT('Ctrl Pts',(30.1031613914609,1.18026105601431,30.3063430973327));
#60286=CARTESIAN_POINT('Ctrl Pts',(30.3988201345177,1.11599305235349,30.2859088407808));
#60287=CARTESIAN_POINT('Ctrl Pts',(30.5402500629299,1.05480717912897,30.2750546900124));
#60288=CARTESIAN_POINT('Ctrl Pts',(30.7944347031296,0.879976451319597,30.2532473998958));
#60289=CARTESIAN_POINT('Ctrl Pts',(30.9040431118398,0.766951615348157,30.2425094496776));
#60290=CARTESIAN_POINT('Ctrl Pts',(31.0689753458081,0.510549117592882,30.223290918131));
#60291=CARTESIAN_POINT('Ctrl Pts',(31.1250271192607,0.371095429137332,30.2138134394961));
#60292=CARTESIAN_POINT('Ctrl Pts',(31.1830815580213,0.0732292938782705,
30.1926925042524));
#60293=CARTESIAN_POINT('Ctrl Pts',(31.1824563525586,-0.0827153416037653,
30.1816348640652));
#60294=CARTESIAN_POINT('Ctrl Pts',(31.1207993480439,-0.386085590380016,
30.1601236460354));
#60295=CARTESIAN_POINT('Ctrl Pts',(31.0601308144882,-0.530428613118422,
30.1504611573687));
#60296=CARTESIAN_POINT('Ctrl Pts',(30.8888193562276,-0.783487027384905,
30.1309694527541));
#60297=CARTESIAN_POINT('Ctrl Pts',(30.7812795445953,-0.890749011015136,
30.1205628449218));
#60298=CARTESIAN_POINT('Ctrl Pts',(30.5267682373962,-1.06214794901788,30.0988571647179));
#60299=CARTESIAN_POINT('Ctrl Pts',(30.3809100882996,-1.12274761000244,30.0877518706328));
#60300=CARTESIAN_POINT('Ctrl Pts',(30.1523604876879,-1.16783357423751,30.0721187053907));
#60301=CARTESIAN_POINT('Ctrl Pts',(30.0761915030069,-1.17524047358085,30.0671787429637));
#60302=CARTESIAN_POINT('Ctrl Pts',(30.,-1.17524047358085,30.0625));
#60303=CARTESIAN_POINT('Ctrl Pts',(29.9999999999996,-1.17524047358085,29.9999999999999));
#60304=CARTESIAN_POINT('Ctrl Pts',(30.1287289986958,-1.17524047358085,30.0079049483617));
#60305=CARTESIAN_POINT('Ctrl Pts',(30.2567455299606,-1.1540988796436,30.0165156942669));
#60306=CARTESIAN_POINT('Ctrl Pts',(30.5250941977629,-1.06268366593765,30.0362353726713));
#60307=CARTESIAN_POINT('Ctrl Pts',(30.659989580509,-0.984598569323181,30.0472873928126));
#60308=CARTESIAN_POINT('Ctrl Pts',(30.8878392789542,-0.78430373476697,30.0683803131598));
#60309=CARTESIAN_POINT('Ctrl Pts',(30.9799768519055,-0.665589512740196,
30.0778047289255));
#60310=CARTESIAN_POINT('Ctrl Pts',(31.1182025022512,-0.393869611947964,
30.0970717007283));
#60311=CARTESIAN_POINT('Ctrl Pts',(31.16052513775,-0.242215229337512,30.1078251299214));
#60312=CARTESIAN_POINT('Ctrl Pts',(31.183296750852,0.0653802899747305,30.1296359512119));
#60313=CARTESIAN_POINT('Ctrl Pts',(31.1648281646971,0.218291541355271,30.1404785017947));
#60314=CARTESIAN_POINT('Ctrl Pts',(31.0712608350547,0.506051914399227,30.1608828629668));
#60315=CARTESIAN_POINT('Ctrl Pts',(30.9980258995704,0.638460005209143,30.1696826775517));
#60316=CARTESIAN_POINT('Ctrl Pts',(30.8013405043472,0.873851821952036,30.1901061897083));
#60317=CARTESIAN_POINT('Ctrl Pts',(30.6777833777517,0.972810187954768,30.2012019893176));
#60318=CARTESIAN_POINT('Ctrl Pts',(30.4044625790663,1.11370354858798,30.222981179922));
#60319=CARTESIAN_POINT('Ctrl Pts',(30.2583590845709,1.15637148267232,30.2334657933678));
#60320=CARTESIAN_POINT('Ctrl Pts',(29.9547860481489,1.18442751029054,30.2531021983901));
#60321=CARTESIAN_POINT('Ctrl Pts',(29.8001302980418,1.16832333064129,30.2625187720286));
#60322=CARTESIAN_POINT('Ctrl Pts',(29.5050358022508,1.07710916045235,30.2838737217699));
#60323=CARTESIAN_POINT('Ctrl Pts',(29.3676216445827,1.00262104003874,30.2949528877718));
#60324=CARTESIAN_POINT('Ctrl Pts',(29.133885390368,0.808265735464436,30.3161967092816));
#60325=CARTESIAN_POINT('Ctrl Pts',(29.0384365029953,0.691955856048158,30.3259351581227));
#60326=CARTESIAN_POINT('Ctrl Pts',(28.8928615291795,0.423965303949737,30.3449376912299));
#60327=CARTESIAN_POINT('Ctrl Pts',(28.8464607134353,0.273539680594875,30.3556039922081));
#60328=CARTESIAN_POINT('Ctrl Pts',(28.8153257979048,-0.0336925494769084,
30.3773890535762));
#60329=CARTESIAN_POINT('Ctrl Pts',(28.8297608924994,-0.187447360914171,
30.3882914188718));
#60330=CARTESIAN_POINT('Ctrl Pts',(28.915763813331,-0.477469105343294,30.4088561281766));
#60331=CARTESIAN_POINT('Ctrl Pts',(28.9852090680907,-0.611342914279369,
30.4176917737044));
#60332=CARTESIAN_POINT('Ctrl Pts',(29.1753547758778,-0.851973319195576,
30.4378994263954));
#60333=CARTESIAN_POINT('Ctrl Pts',(29.296552814894,-0.954486386260336,30.4489763873607));
#60334=CARTESIAN_POINT('Ctrl Pts',(29.5667870728762,-1.10289061661543,30.4708323290802));
#60335=CARTESIAN_POINT('Ctrl Pts',(29.7121150852083,-1.14942616389095,30.4814064433112));
#60336=CARTESIAN_POINT('Ctrl Pts',(29.9080894843003,-1.17254804864973,30.4942605325068));
#60337=CARTESIAN_POINT('Ctrl Pts',(29.9540678655128,-1.17524047358085,30.497179414468));
#60338=CARTESIAN_POINT('Ctrl Pts',(29.9999999999996,-1.17524047358085,30.4999999999999));
#60339=CARTESIAN_POINT('Origin',(30.,-1.21864324187371E-14,15.78125));
#60340=CARTESIAN_POINT('',(30.8234078741651,-0.838564036615812,30.5625));
#60341=CARTESIAN_POINT('Ctrl Pts',(29.9999999999996,-1.17524047358085,30.4999999999999));
#60342=CARTESIAN_POINT('Ctrl Pts',(30.1063627165445,-1.17524047358085,30.506531487003));
#60343=CARTESIAN_POINT('Ctrl Pts',(30.2124142608556,-1.16080842479057,30.5135555357051));
#60344=CARTESIAN_POINT('Ctrl Pts',(30.4106617155444,-1.10559796456395,30.5276868678729));
#60345=CARTESIAN_POINT('Ctrl Pts',(30.5022820820407,-1.06709869288998,30.5346780045058));
#60346=CARTESIAN_POINT('Ctrl Pts',(30.673678737238,-0.968061456707972,30.5487143145253));
#60347=CARTESIAN_POINT('Ctrl Pts',(30.7527765496958,-0.90791877422844,30.555703810039));
#60348=CARTESIAN_POINT('Ctrl Pts',(30.823407874166,-0.83856403661491,30.5625000000001));
#60349=CARTESIAN_POINT('Origin',(30.,-1.56558793706907E-14,30.5625000000001));
#60350=CARTESIAN_POINT('Origin',(30.,-1.32966554433622E-14,16.));
#60351=CARTESIAN_POINT('Origin',(30.,-1.32966554433622E-14,16.));
#60352=CARTESIAN_POINT('',(31.2041934952953,-0.894381364904537,16.3247595264192));
#60353=CARTESIAN_POINT('Ctrl Pts',(29.1765921258349,-0.838564036615844,
16.));
#60354=CARTESIAN_POINT('Ctrl Pts',(29.2487520159976,-0.936812680701164,
16.0195455809545));
#60355=CARTESIAN_POINT('Ctrl Pts',(29.3353435467743,-1.0235639347367,16.039234228078));
#60356=CARTESIAN_POINT('Ctrl Pts',(29.5376779891223,-1.17276771461038,16.0788670880384));
#60357=CARTESIAN_POINT('Ctrl Pts',(29.6536089107031,-1.23245734148137,16.0985110228563));
#60358=CARTESIAN_POINT('Ctrl Pts',(29.9561347058367,-1.33132329595442,16.1436679915754));
#60359=CARTESIAN_POINT('Ctrl Pts',(30.1342881765676,-1.34356937043143,16.1651272257976));
#60360=CARTESIAN_POINT('Ctrl Pts',(30.4639364648848,-1.31596498262617,16.2103767681647));
#60361=CARTESIAN_POINT('Ctrl Pts',(30.6256204275016,-1.27296147517128,16.233574208582));
#60362=CARTESIAN_POINT('Ctrl Pts',(30.9367837613818,-1.12785658919505,16.2803666131763));
#60363=CARTESIAN_POINT('Ctrl Pts',(31.0819753809162,-1.0232586553723,16.3034869854933));
#60364=CARTESIAN_POINT('Ctrl Pts',(31.2041934952953,-0.894381364904556,
16.3247595264192));
#60365=CARTESIAN_POINT('',(30.2433378840047,-1.48013062741372,16.3247595264192));
#60366=CARTESIAN_POINT('Origin',(30.,-1.32966554433622E-14,16.3247595264192));
#60367=CARTESIAN_POINT('Ctrl Pts',(30.0000000000046,1.33373412263454,16.1584936490537));
#60368=CARTESIAN_POINT('Ctrl Pts',(29.9229566197526,1.33637706265986,16.161136589079));
#60369=CARTESIAN_POINT('Ctrl Pts',(29.8544450638259,1.33215454753135,16.163603109717));
#60370=CARTESIAN_POINT('Ctrl Pts',(29.6282514683273,1.30599264999734,16.1719556820851));
#60371=CARTESIAN_POINT('Ctrl Pts',(29.4645017898244,1.25493599443995,16.1785525854589));
#60372=CARTESIAN_POINT('Ctrl Pts',(29.1556314965168,1.0904442613039,16.1921322573206));
#60373=CARTESIAN_POINT('Ctrl Pts',(29.0151927695643,0.975180135374777,16.1989814826418));
#60374=CARTESIAN_POINT('Ctrl Pts',(28.7777605589636,0.68493937081347,16.2122079855113));
#60375=CARTESIAN_POINT('Ctrl Pts',(28.6970848553023,0.520026749838233,16.218047438772));
#60376=CARTESIAN_POINT('Ctrl Pts',(28.5955913245901,0.191124499754384,16.2305887595464));
#60377=CARTESIAN_POINT('Ctrl Pts',(28.5759298114947,0.010043627653028,16.2373963058958));
#60378=CARTESIAN_POINT('Ctrl Pts',(28.6063542045486,-0.355647637044131,
16.2509482038391));
#60379=CARTESIAN_POINT('Ctrl Pts',(28.6584675525716,-0.536586390481523,
16.2575508938686));
#60380=CARTESIAN_POINT('Ctrl Pts',(28.804769485922,-0.819110586341092,16.2677424893791));
#60381=CARTESIAN_POINT('Ctrl Pts',(28.9031317119719,-0.969713974958467,
16.273653025791));
#60382=CARTESIAN_POINT('Ctrl Pts',(29.199410976174,-1.23941646392093,16.2879449223019));
#60383=CARTESIAN_POINT('Ctrl Pts',(29.3637987944395,-1.33889148571261,16.2948596529243));
#60384=CARTESIAN_POINT('Ctrl Pts',(29.6508112528307,-1.44362228182862,16.3055460935814));
#60385=CARTESIAN_POINT('Ctrl Pts',(29.7632922636866,-1.47020844863719,16.3094443635539));
#60386=CARTESIAN_POINT('Ctrl Pts',(29.9994132050485,-1.49732183809384,16.3170683877131));
#60387=CARTESIAN_POINT('Ctrl Pts',(30.1229027402064,-1.49587628373705,16.3207589898335));
#60388=CARTESIAN_POINT('Ctrl Pts',(30.2433378840021,-1.48013062741405,16.3247595264191));
#60389=CARTESIAN_POINT('Origin',(30.,-1.32966554433622E-14,16.));
#60390=CARTESIAN_POINT('Ctrl Pts',(30.0000000000002,-1.50000000000001,16.8125));
#60391=CARTESIAN_POINT('Ctrl Pts',(29.8374309170617,-1.50000000000001,16.8046783913503));
#60392=CARTESIAN_POINT('Ctrl Pts',(29.6757197620765,-1.47357729444258,16.7961640957352));
#60393=CARTESIAN_POINT('Ctrl Pts',(29.3345753610171,-1.35867108066285,16.7765589388149));
#60394=CARTESIAN_POINT('Ctrl Pts',(29.1621497524653,-1.25967607222118,16.7655132465099));
#60395=CARTESIAN_POINT('Ctrl Pts',(28.8706191056789,-1.00528518925076,16.7444205583108));
#60396=CARTESIAN_POINT('Ctrl Pts',(28.7525289442937,-0.85433413605806,16.7349630075588));
#60397=CARTESIAN_POINT('Ctrl Pts',(28.5748830688675,-0.508513347476126,
16.7157507415264));
#60398=CARTESIAN_POINT('Ctrl Pts',(28.5201083225798,-0.315342861227666,
16.705019047846));
#60399=CARTESIAN_POINT('Ctrl Pts',(28.4893812381258,0.0768796360488758,
16.6832289091084));
#60400=CARTESIAN_POINT('Ctrl Pts',(28.5120877046559,0.272040866827356,16.6723866185096));
#60401=CARTESIAN_POINT('Ctrl Pts',(28.6297398561329,0.63947572665909,16.6519735707412));
#60402=CARTESIAN_POINT('Ctrl Pts',(28.7222788636186,0.808683440996407,16.6431776245867));
#60403=CARTESIAN_POINT('Ctrl Pts',(28.9715826684579,1.11011928821307,16.6228097717056));
#60404=CARTESIAN_POINT('Ctrl Pts',(29.1285972489479,1.2371944826493,16.6117255376675));
#60405=CARTESIAN_POINT('Ctrl Pts',(29.4764211128784,1.41875808710319,16.5899474207545));
#60406=CARTESIAN_POINT('Ctrl Pts',(29.6625283053455,1.47415762233606,16.5794544583034));
#60407=CARTESIAN_POINT('Ctrl Pts',(30.0492497355351,1.51196727264003,16.5597980467542));
#60408=CARTESIAN_POINT('Ctrl Pts',(30.2463054645629,1.49258742024928,16.5504437178179));
#60409=CARTESIAN_POINT('Ctrl Pts',(30.6231564270347,1.37865583779414,16.529147701253));
#60410=CARTESIAN_POINT('Ctrl Pts',(30.7990856424485,1.28470816478719,16.5180736453463));
#60411=CARTESIAN_POINT('Ctrl Pts',(31.0988336211311,1.03864170876325,16.4968168346638));
#60412=CARTESIAN_POINT('Ctrl Pts',(31.2215556301223,0.891049402060874,16.4870027445589));
#60413=CARTESIAN_POINT('Ctrl Pts',(31.4094506590971,0.550436181771672,16.4680797878762));
#60414=CARTESIAN_POINT('Ctrl Pts',(31.4699049158396,0.359005410515039,16.4574447450286));
#60415=CARTESIAN_POINT('Ctrl Pts',(31.5122933091642,-0.0326520383467692,
16.4356859978696));
#60416=CARTESIAN_POINT('Ctrl Pts',(31.4952196858866,-0.228959953862231,
16.4247800025632));
#60417=CARTESIAN_POINT('Ctrl Pts',(31.3881172406464,-0.599526626811694,
16.4041929651771));
#60418=CARTESIAN_POINT('Ctrl Pts',(31.300844426577,-0.770779121647004,16.3953430421646));
#60419=CARTESIAN_POINT('Ctrl Pts',(31.0690211851343,-1.06871793972269,16.3759133629805));
#60420=CARTESIAN_POINT('Ctrl Pts',(30.9276174608134,-1.1935139431374,16.3656435174717));
#60421=CARTESIAN_POINT('Ctrl Pts',(30.6058972740411,-1.3849221656676,16.3448478526983));
#60422=CARTESIAN_POINT('Ctrl Pts',(30.4282952255496,-1.44972308953241,16.3345029444933));
#60423=CARTESIAN_POINT('Ctrl Pts',(30.2433378840032,-1.48013062741398,16.3247595264191));
#60424=CARTESIAN_POINT('Ctrl Pts',(31.2041934952953,-0.894381364904531,
16.3247595264192));
#60425=CARTESIAN_POINT('Ctrl Pts',(31.2978308567217,-0.768308186313297,
16.33276668881));
#60426=CARTESIAN_POINT('Ctrl Pts',(31.3710758402094,-0.628345765505124,
16.3400919019164));
#60427=CARTESIAN_POINT('Ctrl Pts',(31.4735871865681,-0.324510524004584,
16.3569716375553));
#60428=CARTESIAN_POINT('Ctrl Pts',(31.5001727925959,-0.161986730686535,
16.3660007371841));
#60429=CARTESIAN_POINT('Ctrl Pts',(31.4997859079869,0.202485940247452,16.3862492189027));
#60430=CARTESIAN_POINT('Ctrl Pts',(31.4592164909323,0.401327421311596,16.3972959678507));
#60431=CARTESIAN_POINT('Ctrl Pts',(31.3063109849155,0.761415726638002,16.4173008737022));
#60432=CARTESIAN_POINT('Ctrl Pts',(31.1993149527403,0.920789441682028,16.4262087502572));
#60433=CARTESIAN_POINT('Ctrl Pts',(30.927737201713,1.19478997630558,16.4468861668575));
#60434=CARTESIAN_POINT('Ctrl Pts',(30.7642938567671,1.30539963746525,16.4578223290454));
#60435=CARTESIAN_POINT('Ctrl Pts',(30.4012071029328,1.45894804482998,16.4795565821721));
#60436=CARTESIAN_POINT('Ctrl Pts',(30.2045613271838,1.49922584611532,16.4901365342825));
#60437=CARTESIAN_POINT('Ctrl Pts',(29.8153532439137,1.50071981302521,16.5089038160006));
#60438=CARTESIAN_POINT('Ctrl Pts',(29.6264615866043,1.46518905889,16.5189388458803));
#60439=CARTESIAN_POINT('Ctrl Pts',(29.2652001883276,1.32257698188105,16.5402814895924));
#60440=CARTESIAN_POINT('Ctrl Pts',(29.0973517156097,1.21423683760981,16.5513665514533));
#60441=CARTESIAN_POINT('Ctrl Pts',(28.8152158635768,0.940440031832944,16.5725462857904));
#60442=CARTESIAN_POINT('Ctrl Pts',(28.7029935775965,0.778399491568193,16.5817555838018));
#60443=CARTESIAN_POINT('Ctrl Pts',(28.5479560175053,0.422736814401416,16.6015146214222));
#60444=CARTESIAN_POINT('Ctrl Pts',(28.5057189580682,0.232905312381588,16.6120608159788));
#60445=CARTESIAN_POINT('Ctrl Pts',(28.4951590610144,-0.159927799856357,
16.6338848777698));
#60446=CARTESIAN_POINT('Ctrl Pts',(28.5299387266544,-0.359247208886169,
16.6449581782715));
#60447=CARTESIAN_POINT('Ctrl Pts',(28.6722713443677,-0.723556115441905,
16.665197561969));
#60448=CARTESIAN_POINT('Ctrl Pts',(28.7749427214916,-0.886360478602884,
16.6740138619457));
#60449=CARTESIAN_POINT('Ctrl Pts',(29.0386829229376,-1.16785093047933,16.6945222475229));
#60450=CARTESIAN_POINT('Ctrl Pts',(29.1984334219549,-1.28276611305493,16.7054003353954));
#60451=CARTESIAN_POINT('Ctrl Pts',(29.5564186818177,-1.44663336596446,16.7271757773774));
#60452=CARTESIAN_POINT('Ctrl Pts',(29.7518446854206,-1.49263399091841,16.7378560104973));
#60453=CARTESIAN_POINT('Ctrl Pts',(29.9670564156215,-1.49972884223086,16.7484074688974));
#60454=CARTESIAN_POINT('Ctrl Pts',(29.9835330897433,-1.50000000000001,16.7492077354109));
#60455=CARTESIAN_POINT('Ctrl Pts',(30.,-1.50000000000001,16.75));
#60456=CARTESIAN_POINT('Origin',(27.4975425688509,1.03655180724329,15.7235432561772));
#60457=CARTESIAN_POINT('',(27.507537153458,1.0459948352816,31.5905494329235));
#60458=CARTESIAN_POINT('',(27.4979325782409,1.02280733953167,31.5905494329235));
#60459=CARTESIAN_POINT('Origin',(27.4975191258909,1.03656151763528,31.5962151370756));
#60460=CARTESIAN_POINT('',(27.4979325782409,1.02280733953167,33.8969505670765));
#60461=CARTESIAN_POINT('',(27.4979325782409,1.02280733953167,15.7235432561772));
#60462=CARTESIAN_POINT('',(27.507537153458,1.0459948352816,33.8969505670765));
#60463=CARTESIAN_POINT('Origin',(27.4975191258914,1.03656151763504,33.891284862925));
#60464=CARTESIAN_POINT('',(27.507537153458,1.0459948352816,15.7235432561772));
#60465=CARTESIAN_POINT('Origin',(27.4239298924869,0.837015916807854,15.7235432561772));
#60466=CARTESIAN_POINT('',(27.4331527756843,0.847214001212616,31.5905494329235));
#60467=CARTESIAN_POINT('',(27.4253970781159,0.823344418487269,31.5905494329235));
#60468=CARTESIAN_POINT('Origin',(27.4239057599253,0.837023757952457,31.5962151370753));
#60469=CARTESIAN_POINT('',(27.4253970781159,0.823344418487269,33.8969505670765));
#60470=CARTESIAN_POINT('',(27.4253970781159,0.823344418487269,15.7235432561772));
#60471=CARTESIAN_POINT('',(27.4331527756843,0.847214001212616,33.8969505670765));
#60472=CARTESIAN_POINT('Origin',(27.4239057599256,0.837023757952334,33.8912848629251));
#60473=CARTESIAN_POINT('',(27.4331527756843,0.847214001212616,15.7235432561772));
#60474=CARTESIAN_POINT('Origin',(27.3661995449658,0.632319544909263,15.7235432561772));
#60475=CARTESIAN_POINT('',(27.3745938646118,0.643209811098917,31.5905494329235));
#60476=CARTESIAN_POINT('',(27.3687348611468,0.618805305313091,31.5905494329235));
#60477=CARTESIAN_POINT('Origin',(27.3661748715877,0.632325468463276,31.5962151370755));
#60478=CARTESIAN_POINT('',(27.3687348611468,0.618805305313091,33.8969505670765));
#60479=CARTESIAN_POINT('',(27.3687348611468,0.618805305313091,15.7235432561772));
#60480=CARTESIAN_POINT('',(27.3745938646118,0.643209811098917,33.8969505670765));
#60481=CARTESIAN_POINT('Origin',(27.3661748715881,0.632325468463155,33.891284862925));
#60482=CARTESIAN_POINT('',(27.3745938646118,0.643209811098917,15.7235432561772));
#60483=CARTESIAN_POINT('Origin',(27.3247074530776,0.423724712748722,15.7235432561772));
#60484=CARTESIAN_POINT('',(27.3322214554001,0.435240018610828,31.5905494329235));
#60485=CARTESIAN_POINT('',(27.328295268743,0.410451051658016,31.5905494329235));
#60486=CARTESIAN_POINT('Origin',(27.3246823910025,0.423728682191457,31.5962151370754));
#60487=CARTESIAN_POINT('',(27.328295268743,0.410451051658016,33.8969505670765));
#60488=CARTESIAN_POINT('',(27.328295268743,0.410451051658016,15.7235432561772));
#60489=CARTESIAN_POINT('',(27.3322214554001,0.435240018610828,33.8969505670765));
#60490=CARTESIAN_POINT('Origin',(27.3246823910029,0.423728682191396,33.891284862925));
#60491=CARTESIAN_POINT('',(27.3322214554001,0.435240018610828,15.7235432561772));
#60492=CARTESIAN_POINT('Origin',(27.2997094293662,0.212517476831317,15.7235432561772));
#60493=CARTESIAN_POINT('',(27.3062967880422,0.224586826676008,31.5905494329235));
#60494=CARTESIAN_POINT('',(27.3043276244395,0.199566230780642,31.5905494329235));
#60495=CARTESIAN_POINT('Origin',(27.2996841331102,0.212519467689854,31.5962151370755));
#60496=CARTESIAN_POINT('',(27.3043276244395,0.199566230780642,33.8969505670765));
#60497=CARTESIAN_POINT('',(27.3043276244395,0.199566230780642,15.7235432561772));
#60498=CARTESIAN_POINT('',(27.3062967880422,0.224586826676008,33.8969505670765));
#60499=CARTESIAN_POINT('Origin',(27.2996841331108,0.212519467689809,33.8912848629251));
#60500=CARTESIAN_POINT('',(27.3062967880422,0.224586826676008,15.7235432561772));
#60501=CARTESIAN_POINT('Origin',(27.2913595949605,1.54398896472578E-14,
15.7235432561772));
#60502=CARTESIAN_POINT('',(27.2969796967333,0.0125489822720319,31.5905494329235));
#60503=CARTESIAN_POINT('',(27.2969796967333,-0.0125489822720016,31.5905494329235));
#60504=CARTESIAN_POINT('Origin',(27.2913342204835,1.66533453693773E-14,
31.5962151370755));
#60505=CARTESIAN_POINT('',(27.2969796967333,-0.0125489822720016,33.8969505670765));
#60506=CARTESIAN_POINT('',(27.2969796967333,-0.0125489822720016,15.7235432561772));
#60507=CARTESIAN_POINT('',(27.2969796967333,0.0125489822720319,33.8969505670765));
#60508=CARTESIAN_POINT('Origin',(27.2913342204839,1.44047100636424E-14,
33.891284862925));
#60509=CARTESIAN_POINT('',(27.2969796967333,0.0125489822720319,15.7235432561772));
#60510=CARTESIAN_POINT('Origin',(27.5865837274296,1.22969701109861,15.7235432561772));
#60511=CARTESIAN_POINT('',(27.5972883935087,1.23832676336248,31.5905494329235));
#60512=CARTESIAN_POINT('',(27.5858941560429,1.2159643132099,31.5905494329235));
#60513=CARTESIAN_POINT('Origin',(27.586561118605,1.22970853087013,31.5962151370754));
#60514=CARTESIAN_POINT('',(27.5858941560429,1.2159643132099,33.8969505670765));
#60515=CARTESIAN_POINT('',(27.5858941560429,1.2159643132099,15.7235432561772));
#60516=CARTESIAN_POINT('',(27.5972883935087,1.23832676336248,33.8969505670765));
#60517=CARTESIAN_POINT('Origin',(27.5865611186055,1.22970853086989,33.891284862925));
#60518=CARTESIAN_POINT('',(27.5972883935087,1.23832676336248,15.7235432561772));
#60519=CARTESIAN_POINT('Origin',(27.690504399871,1.41526072396476,15.7235432561772));
#60520=CARTESIAN_POINT('',(27.701853149596,1.42302399516181,31.5905494329235));
#60521=CARTESIAN_POINT('',(27.6887394991445,1.40162446254803,31.5905494329235));
#60522=CARTESIAN_POINT('Origin',(27.6904827645727,1.41527398209261,31.5962151370755));
#60523=CARTESIAN_POINT('',(27.6887394991445,1.40162446254803,33.8969505670765));
#60524=CARTESIAN_POINT('',(27.6887394991445,1.40162446254803,15.7235432561772));
#60525=CARTESIAN_POINT('',(27.701853149596,1.42302399516181,33.8969505670765));
#60526=CARTESIAN_POINT('Origin',(27.6904827645732,1.41527398209234,33.891284862925));
#60527=CARTESIAN_POINT('',(27.701853149596,1.42302399516181,15.7235432561772));
#60528=CARTESIAN_POINT('Origin',(27.8086638806724,1.59209888384573,15.7235432561772));
#60529=CARTESIAN_POINT('',(27.8205867452275,1.59894781082746,31.5905494329235));
#60530=CARTESIAN_POINT('',(27.805834531806,1.57864313098712,31.5905494329235));
#60531=CARTESIAN_POINT('Origin',(27.8086433522893,1.59211379858911,31.5962151370755));
#60532=CARTESIAN_POINT('',(27.805834531806,1.57864313098712,33.8969505670765));
#60533=CARTESIAN_POINT('',(27.805834531806,1.57864313098712,15.7235432561772));
#60534=CARTESIAN_POINT('',(27.8205867452275,1.59894781082746,33.8969505670765));
#60535=CARTESIAN_POINT('Origin',(27.8086433522896,1.59211379858882,33.8912848629251));
#60536=CARTESIAN_POINT('',(27.8205867452275,1.59894781082746,15.7235432561772));
#60537=CARTESIAN_POINT('Origin',(27.9403336773427,1.75912122468118,15.7235432561772));
#60538=CARTESIAN_POINT('',(27.9527571483031,1.76501358153527,31.5905494329235));
#60539=CARTESIAN_POINT('',(27.9364573242129,1.74592893957157,31.5905494329235));
#60540=CARTESIAN_POINT('Origin',(27.9403143824389,1.75913770408581,31.5962151370755));
#60541=CARTESIAN_POINT('',(27.9364573242129,1.74592893957157,33.8969505670765));
#60542=CARTESIAN_POINT('',(27.9364573242129,1.74592893957157,15.7235432561772));
#60543=CARTESIAN_POINT('',(27.9527571483031,1.76501358153527,33.8969505670765));
#60544=CARTESIAN_POINT('Origin',(27.9403143824393,1.75913770408551,33.891284862925));
#60545=CARTESIAN_POINT('',(27.9527571483031,1.76501358153527,15.7235432561772));
#60546=CARTESIAN_POINT('Origin',(28.0847020018007,1.9152979981993,15.7235432561772));
#60547=CARTESIAN_POINT('',(28.0975494843367,1.92019745658633,31.5905494329235));
#60548=CARTESIAN_POINT('',(28.0798025434137,1.90245051566326,31.5905494329235));
#60549=CARTESIAN_POINT('Origin',(28.0846840593359,1.9153159406641,31.5962151370755));
#60550=CARTESIAN_POINT('',(28.0798025434137,1.90245051566326,33.8969505670765));
#60551=CARTESIAN_POINT('',(28.0798025434137,1.90245051566326,15.7235432561772));
#60552=CARTESIAN_POINT('',(28.0975494843367,1.92019745658633,33.8969505670765));
#60553=CARTESIAN_POINT('Origin',(28.0846840593363,1.91531594066375,33.891284862925));
#60554=CARTESIAN_POINT('',(28.0975494843367,1.92019745658633,15.7235432561772));
#60555=CARTESIAN_POINT('Origin',(28.2408787753188,2.05966632265731,15.7235432561772));
#60556=CARTESIAN_POINT('',(28.2540710604285,2.06354267578708,31.5905494329235));
#60557=CARTESIAN_POINT('',(28.2349864184648,2.0472428516969,31.5905494329235));
#60558=CARTESIAN_POINT('Origin',(28.2408622959143,2.05968561756092,31.5962151370754));
#60559=CARTESIAN_POINT('',(28.2349864184648,2.0472428516969,33.8969505670765));
#60560=CARTESIAN_POINT('',(28.2349864184648,2.0472428516969,15.7235432561772));
#60561=CARTESIAN_POINT('',(28.2540710604285,2.06354267578708,33.8969505670765));
#60562=CARTESIAN_POINT('Origin',(28.2408622959145,2.05968561756065,33.891284862925));
#60563=CARTESIAN_POINT('',(28.2540710604285,2.06354267578708,15.7235432561772));
#60564=CARTESIAN_POINT('Origin',(28.4079011161543,2.19133611932758,15.7235432561772));
#60565=CARTESIAN_POINT('',(28.4213568690129,2.19416546819404,31.5905494329235));
#60566=CARTESIAN_POINT('',(28.4010521891726,2.1794132547725,31.5905494329235));
#60567=CARTESIAN_POINT('Origin',(28.407886201411,2.19135664771063,31.5962151370753));
#60568=CARTESIAN_POINT('',(28.4010521891726,2.1794132547725,33.8969505670765));
#60569=CARTESIAN_POINT('',(28.4010521891726,2.1794132547725,15.7235432561772));
#60570=CARTESIAN_POINT('',(28.4213568690129,2.19416546819404,33.8969505670765));
#60571=CARTESIAN_POINT('Origin',(28.4078862014112,2.19135664771024,33.8912848629252));
#60572=CARTESIAN_POINT('',(28.4213568690129,2.19416546819404,15.7235432561772));
#60573=CARTESIAN_POINT('Origin',(28.5847392760353,2.309495600129,15.7235432561772));
#60574=CARTESIAN_POINT('',(28.598375537452,2.31126050085552,31.5905494329235));
#60575=CARTESIAN_POINT('',(28.5769760048382,2.29814685040398,31.5905494329235));
#60576=CARTESIAN_POINT('Origin',(28.5847260179075,2.30951723542729,31.5962151370754));
#60577=CARTESIAN_POINT('',(28.5769760048382,2.29814685040398,33.8969505670765));
#60578=CARTESIAN_POINT('',(28.5769760048382,2.29814685040398,15.7235432561772));
#60579=CARTESIAN_POINT('',(28.598375537452,2.31126050085552,33.8969505670765));
#60580=CARTESIAN_POINT('Origin',(28.5847260179077,2.30951723542689,33.891284862925));
#60581=CARTESIAN_POINT('',(28.598375537452,2.31126050085552,15.7235432561772));
#60582=CARTESIAN_POINT('Origin',(28.7703029889014,2.4134162725704,15.7235432561772));
#60583=CARTESIAN_POINT('',(28.7840356867901,2.41410584395713,31.5905494329235));
#60584=CARTESIAN_POINT('',(28.7616732366375,2.40271160649133,31.5905494329235));
#60585=CARTESIAN_POINT('Origin',(28.7702914691299,2.41343888139489,31.5962151370753));
#60586=CARTESIAN_POINT('',(28.7616732366375,2.40271160649133,33.8969505670765));
#60587=CARTESIAN_POINT('',(28.7616732366375,2.40271160649133,15.7235432561772));
#60588=CARTESIAN_POINT('',(28.7840356867901,2.41410584395713,33.8969505670765));
#60589=CARTESIAN_POINT('Origin',(28.7702914691301,2.41343888139455,33.8912848629251));
#60590=CARTESIAN_POINT('',(28.7840356867901,2.41410584395713,15.7235432561772));
#60591=CARTESIAN_POINT('Origin',(30.,-1.32966554433622E-14,34.));
#60592=CARTESIAN_POINT('',(28.75,0.721687836487017,33.8917468245269));
#60593=CARTESIAN_POINT('',(28.75,-1.44824191072421E-14,33.6983711515529));
#60594=CARTESIAN_POINT('Ctrl Pts',(28.75,0.72168783648698,33.8917468245269));
#60595=CARTESIAN_POINT('Ctrl Pts',(28.75,0.334936490538873,33.6983711515529));
#60596=CARTESIAN_POINT('Ctrl Pts',(28.75,-1.55145598201422E-14,33.6983711515529));
#60597=CARTESIAN_POINT('',(30.,1.44337567297405,33.8917468245269));
#60598=CARTESIAN_POINT('Ctrl Pts',(30.,1.44337567297404,33.8917468245269));
#60599=CARTESIAN_POINT('Ctrl Pts',(29.375,1.08253175473053,33.5309029062834));
#60600=CARTESIAN_POINT('Ctrl Pts',(28.75,0.721687836487025,33.8917468245269));
#60601=CARTESIAN_POINT('',(31.25,0.721687836487017,33.891746824527));
#60602=CARTESIAN_POINT('Ctrl Pts',(31.25,0.721687836487027,33.8917468245269));
#60603=CARTESIAN_POINT('Ctrl Pts',(30.625,1.08253175473053,33.5309029062834));
#60604=CARTESIAN_POINT('Ctrl Pts',(30.,1.44337567297404,33.8917468245269));
#60605=CARTESIAN_POINT('',(31.25,-0.72168783648704,33.8917468245269));
#60606=CARTESIAN_POINT('Ctrl Pts',(31.25,-0.721687836487026,33.8917468245269));
#60607=CARTESIAN_POINT('Ctrl Pts',(31.25,-1.26287869051112E-14,33.5309029062834));
#60608=CARTESIAN_POINT('Ctrl Pts',(31.25,0.721687836487001,33.8917468245269));
#60609=CARTESIAN_POINT('',(30.,-1.44337567297407,33.8917468245269));
#60610=CARTESIAN_POINT('Ctrl Pts',(30.,-1.44337567297406,33.8917468245269));
#60611=CARTESIAN_POINT('Ctrl Pts',(30.625,-1.08253175473056,33.5309029062834));
#60612=CARTESIAN_POINT('Ctrl Pts',(31.25,-0.721687836487049,33.8917468245269));
#60613=CARTESIAN_POINT('',(28.75,-0.721687836487044,33.8917468245269));
#60614=CARTESIAN_POINT('Ctrl Pts',(28.75,-0.721687836487053,33.8917468245269));
#60615=CARTESIAN_POINT('Ctrl Pts',(29.375,-1.08253175473056,33.5309029062834));
#60616=CARTESIAN_POINT('Ctrl Pts',(30.,-1.44337567297406,33.8917468245269));
#60617=CARTESIAN_POINT('Ctrl Pts',(28.75,-1.55145598201422E-14,33.6983711515529));
#60618=CARTESIAN_POINT('Ctrl Pts',(28.75,-0.334936490538901,33.6983711515529));
#60619=CARTESIAN_POINT('Ctrl Pts',(28.75,-0.721687836487005,33.8917468245269));
#60620=CARTESIAN_POINT('',(28.4483711515529,-1.34873480853811E-14,34.));
#60621=CARTESIAN_POINT('',(28.4483711515529,-1.34873480853811E-14,34.));
#60622=CARTESIAN_POINT('Origin',(30.,-1.32966554433622E-14,34.));
#60623=CARTESIAN_POINT('Origin',(30.,-1.32966554433622E-14,33.953125));
#60624=CARTESIAN_POINT('',(30.,-2.6137293696319,33.9862706303681));
#60625=CARTESIAN_POINT('Origin',(30.,-1.32966554433622E-14,33.9862706303681));
#60626=CARTESIAN_POINT('',(30.,-2.58058373926378,34.));
#60627=CARTESIAN_POINT('Origin',(30.,-2.58058373926378,33.953125));
#60628=CARTESIAN_POINT('Origin',(30.,-1.32966554433622E-14,34.));
#60629=CARTESIAN_POINT('Origin',(30.,-1.32966554433622E-14,33.8637293696319));
#60630=CARTESIAN_POINT('',(30.012548982272,-2.70302030326669,33.8969505670765));
#60631=CARTESIAN_POINT('',(30.,-2.69489040503949,33.9051095949605));
#60632=CARTESIAN_POINT('Ctrl Pts',(30.012548982272,-2.70302030326672,33.8969505670765));
#60633=CARTESIAN_POINT('Ctrl Pts',(30.0117595027242,-2.70125749446881,33.8987170220581));
#60634=CARTESIAN_POINT('Ctrl Pts',(30.0105608813139,-2.69960157002983,33.9003782103613));
#60635=CARTESIAN_POINT('Ctrl Pts',(30.0079476416933,-2.69733049287042,33.9026580100842));
#60636=CARTESIAN_POINT('Ctrl Pts',(30.0065751610721,-2.69644647069985,33.9035459832655));
#60637=CARTESIAN_POINT('Ctrl Pts',(30.0034509360646,-2.69522714758869,33.9047710768107));
#60638=CARTESIAN_POINT('Ctrl Pts',(30.0017003028408,-2.69489040503949,33.9051095949605));
#60639=CARTESIAN_POINT('Ctrl Pts',(30.,-2.69489040503949,33.9051095949605));
#60640=CARTESIAN_POINT('',(30.027378900953,-2.73613365141358,33.8637293696319));
#60641=CARTESIAN_POINT('Ctrl Pts',(30.0273789009518,-2.73613365141079,33.8637293696347));
#60642=CARTESIAN_POINT('Ctrl Pts',(30.019918653996,-2.71947585577342,33.8804609779984));
#60643=CARTESIAN_POINT('Ctrl Pts',(30.0125489822686,-2.70302030325915,33.8969505670841));
#60644=CARTESIAN_POINT('',(30.1873800711417,-2.72984718831552,33.8637293696319));
#60645=CARTESIAN_POINT('Origin',(30.,-1.32966554433622E-14,33.8637293696319));
#60646=CARTESIAN_POINT('',(30.1995662307806,-2.69567237556051,33.8969505670765));
#60647=CARTESIAN_POINT('Ctrl Pts',(30.1995662307834,-2.69567237555272,33.8969505670841));
#60648=CARTESIAN_POINT('Ctrl Pts',(30.1935103650644,-2.71265541886991,33.8804609779983));
#60649=CARTESIAN_POINT('Ctrl Pts',(30.1873800711428,-2.72984718831265,33.8637293696347));
#60650=CARTESIAN_POINT('',(30.224586826676,-2.69370321195777,33.8969505670765));
#60651=CARTESIAN_POINT('Origin',(30.2125187883694,-2.70030745889015,33.8912937927563));
#60652=CARTESIAN_POINT('',(30.241969073019,-2.72555094069392,33.8637293696319));
#60653=CARTESIAN_POINT('Ctrl Pts',(30.2419690730176,-2.72555094069121,33.8637293696347));
#60654=CARTESIAN_POINT('Ctrl Pts',(30.233224867931,-2.70952981970859,33.8804609779984));
#60655=CARTESIAN_POINT('Ctrl Pts',(30.2245868266721,-2.69370321195052,33.8969505670841));
#60656=CARTESIAN_POINT('',(30.4009837827878,-2.70673030953518,33.8637293696319));
#60657=CARTESIAN_POINT('Origin',(30.,-1.32966554433622E-14,33.8637293696319));
#60658=CARTESIAN_POINT('',(30.410451051658,-2.67170473125697,33.8969505670765));
#60659=CARTESIAN_POINT('Ctrl Pts',(30.4104510516601,-2.67170473124899,33.8969505670841));
#60660=CARTESIAN_POINT('Ctrl Pts',(30.4057463283755,-2.68911055925959,33.8804609779983));
#60661=CARTESIAN_POINT('Ctrl Pts',(30.4009837827886,-2.70673030953223,33.8637293696347));
#60662=CARTESIAN_POINT('',(30.4352400186108,-2.66777854459992,33.8969505670765));
#60663=CARTESIAN_POINT('Origin',(30.4237273077484,-2.67530902338216,33.8912940899387));
#60664=CARTESIAN_POINT('',(30.455067425287,-2.69816430208722,33.8637293696319));
#60665=CARTESIAN_POINT('Ctrl Pts',(30.4550674252854,-2.69816430208464,33.8637293696347));
#60666=CARTESIAN_POINT('Ctrl Pts',(30.445093173,-2.68287863129519,33.8804609779983));
#60667=CARTESIAN_POINT('Ctrl Pts',(30.4352400186063,-2.667778544593,33.8969505670841));
#60668=CARTESIAN_POINT('',(30.6121152960723,-2.66692553831739,33.8637293696319));
#60669=CARTESIAN_POINT('Origin',(30.,-1.32966554433622E-14,33.8637293696319));
#60670=CARTESIAN_POINT('',(30.618805305313,-2.63126513885325,33.8969505670765));
#60671=CARTESIAN_POINT('Ctrl Pts',(30.6188053053145,-2.63126513884514,33.8969505670841));
#60672=CARTESIAN_POINT('Ctrl Pts',(30.6154807306477,-2.64898643883144,33.8804609779984));
#60673=CARTESIAN_POINT('Ctrl Pts',(30.6121152960728,-2.66692553831439,33.8637293696347));
#60674=CARTESIAN_POINT('',(30.6432098110989,-2.62540613538822,33.8969505670765));
#60675=CARTESIAN_POINT('Origin',(30.6323233823986,-2.63381649164655,33.8912943077151));
#60676=CARTESIAN_POINT('',(30.6653601355529,-2.65414258332748,33.8637293696319));
#60677=CARTESIAN_POINT('Ctrl Pts',(30.665360135551,-2.65414258332505,33.8637293696347));
#60678=CARTESIAN_POINT('Ctrl Pts',(30.6542173306489,-2.63968660397218,33.8804609779983));
#60679=CARTESIAN_POINT('Ctrl Pts',(30.6432098110939,-2.62540613538168,33.8969505670841));
#60680=CARTESIAN_POINT('',(30.8194729150075,-2.61067828431314,33.8637293696319));
#60681=CARTESIAN_POINT('Origin',(30.,-1.32966554433622E-14,33.8637293696319));
#60682=CARTESIAN_POINT('',(30.8233444184872,-2.57460292188405,33.8969505670765));
#60683=CARTESIAN_POINT('Ctrl Pts',(30.8233444184881,-2.57460292187584,33.8969505670841));
#60684=CARTESIAN_POINT('Ctrl Pts',(30.8214204895475,-2.59253043613051,33.8804609779984));
#60685=CARTESIAN_POINT('Ctrl Pts',(30.8194729150079,-2.61067828431011,33.8637293696347));
#60686=CARTESIAN_POINT('',(30.8472140012126,-2.56684722431573,33.8969505670765));
#60687=CARTESIAN_POINT('Origin',(30.837020957759,-2.57608565616367,33.891294472568));
#60688=CARTESIAN_POINT('',(30.8715506793283,-2.59375719294955,33.8637293696319));
#60689=CARTESIAN_POINT('Ctrl Pts',(30.8715506793263,-2.59375719294726,33.8637293696347));
#60690=CARTESIAN_POINT('Ctrl Pts',(30.8593080209051,-2.58022003095079,33.8804609779983));
#60691=CARTESIAN_POINT('Ctrl Pts',(30.8472140012071,-2.5668472243096,33.8969505670841));
#60692=CARTESIAN_POINT('',(31.0217782109194,-2.53833533054748,33.8637293696319));
#60693=CARTESIAN_POINT('Origin',(30.,-1.32966554433622E-14,33.8637293696319));
#60694=CARTESIAN_POINT('',(31.0228073395316,-2.5020674217591,33.8969505670765));
#60695=CARTESIAN_POINT('Ctrl Pts',(31.0228073395319,-2.50206742175084,33.8969505670841));
#60696=CARTESIAN_POINT('Ctrl Pts',(31.0222959179792,-2.52009062118698,33.8804609779983));
#60697=CARTESIAN_POINT('Ctrl Pts',(31.0217782109195,-2.53833533054442,33.8637293696347));
#60698=CARTESIAN_POINT('',(31.0459948352815,-2.49246284654201,33.8969505670765));
#60699=CARTESIAN_POINT('Origin',(31.0365580110689,-2.50247243285094,33.8912946002427));
#60700=CARTESIAN_POINT('',(31.0723678233457,-2.51738042696529,33.8637293696319));
#60701=CARTESIAN_POINT('Ctrl Pts',(31.0723678233435,-2.51738042696321,33.8637293696347));
#60702=CARTESIAN_POINT('Ctrl Pts',(31.0591007914634,-2.5048455434284,33.8804609779984));
#60703=CARTESIAN_POINT('Ctrl Pts',(31.0459948352755,-2.49246284653634,33.8969505670841));
#60704=CARTESIAN_POINT('',(31.2177839043851,-2.45034269538684,33.8637293696319));
#60705=CARTESIAN_POINT('Origin',(30.,-1.32966554433622E-14,33.8637293696319));
#60706=CARTESIAN_POINT('',(31.2159643132098,-2.41410584395714,33.8969505670765));
#60707=CARTESIAN_POINT('Ctrl Pts',(31.2159643132094,-2.4141058439489,33.8969505670841));
#60708=CARTESIAN_POINT('Ctrl Pts',(31.2168685521286,-2.43211360954869,33.8804609779984));
#60709=CARTESIAN_POINT('Ctrl Pts',(31.2177839043849,-2.4503426953838,33.8637293696347));
#60710=CARTESIAN_POINT('',(31.2383267633624,-2.40271160649135,33.8969505670765));
#60711=CARTESIAN_POINT('Origin',(31.2297043338602,-2.41343066267494,33.891294700665));
#60712=CARTESIAN_POINT('',(31.2665734631337,-2.42548317353486,33.8637293696319));
#60713=CARTESIAN_POINT('Ctrl Pts',(31.2665734631313,-2.42548317353296,33.8637293696347));
#60714=CARTESIAN_POINT('Ctrl Pts',(31.2523638534557,-2.41402785018508,33.8804609779983));
#60715=CARTESIAN_POINT('Ctrl Pts',(31.238326763356,-2.40271160648617,33.8969505670841));
#60716=CARTESIAN_POINT('',(31.4062815551261,-2.34724288268751,33.8637293696319));
#60717=CARTESIAN_POINT('Origin',(30.,-1.32966554433622E-14,33.8637293696319));
#60718=CARTESIAN_POINT('',(31.401624462548,-2.31126050085554,33.8969505670765));
#60719=CARTESIAN_POINT('Ctrl Pts',(31.4016244625469,-2.31126050084735,33.8969505670841));
#60720=CARTESIAN_POINT('Ctrl Pts',(31.4039387870044,-2.32914180874765,33.8804609779983));
#60721=CARTESIAN_POINT('Ctrl Pts',(31.4062815551258,-2.34724288268448,33.8637293696347));
#60722=CARTESIAN_POINT('',(31.4230239951618,-2.29814685040399,33.8969505670765));
#60723=CARTESIAN_POINT('Origin',(31.4152691174526,-2.30950931155476,33.8912947803757));
#60724=CARTESIAN_POINT('',(31.452970256343,-2.31863200978458,33.8637293696319));
#60725=CARTESIAN_POINT('Ctrl Pts',(31.4529702563405,-2.31863200978284,33.8637293696347));
#60726=CARTESIAN_POINT('Ctrl Pts',(31.4379056758382,-2.30832687249962,33.8804609779984));
#60727=CARTESIAN_POINT('Ctrl Pts',(31.423023995155,-2.29814685039932,33.8969505670841));
#60728=CARTESIAN_POINT('',(31.5861090124437,-2.22967153707895,33.8637293696319));
#60729=CARTESIAN_POINT('Origin',(30.,-1.32966554433622E-14,33.8637293696319));
#60730=CARTESIAN_POINT('',(31.5786431309871,-2.19416546819406,33.8969505670765));
#60731=CARTESIAN_POINT('Ctrl Pts',(31.5786431309854,-2.19416546818597,33.8969505670841));
#60732=CARTESIAN_POINT('Ctrl Pts',(31.5823532724012,-2.21181007417745,33.8804609779984));
#60733=CARTESIAN_POINT('Ctrl Pts',(31.5861090124431,-2.22967153707596,33.8637293696347));
#60734=CARTESIAN_POINT('',(31.5989478108274,-2.17941325477251,33.8969505670765));
#60735=CARTESIAN_POINT('Origin',(31.5921082951429,-2.19134908471607,33.891294843835));
#60736=CARTESIAN_POINT('',(31.6304090047603,-2.1974857086706,33.8637293696319));
#60737=CARTESIAN_POINT('Ctrl Pts',(31.6304090047577,-2.19748570866908,33.8637293696347));
#60738=CARTESIAN_POINT('Ctrl Pts',(31.6145823315769,-2.18839429204867,33.8804609779984));
#60739=CARTESIAN_POINT('Ctrl Pts',(31.5989478108202,-2.1794132547684,33.8969505670841));
#60740=CARTESIAN_POINT('',(31.7561575802648,-2.09835352500328,33.8637293696319));
#60741=CARTESIAN_POINT('Origin',(30.,-1.32966554433622E-14,33.8637293696319));
#60742=CARTESIAN_POINT('',(31.7459289395715,-2.0635426757871,33.8969505670765));
#60743=CARTESIAN_POINT('Ctrl Pts',(31.7459289395692,-2.06354267577917,33.8969505670841));
#60744=CARTESIAN_POINT('Ctrl Pts',(31.7510120236878,-2.08084179499847,33.8804609779983));
#60745=CARTESIAN_POINT('Ctrl Pts',(31.7561575802639,-2.09835352500035,33.8637293696347));
#60746=CARTESIAN_POINT('',(31.7650135815352,-2.04724285169692,33.8969505670765));
#60747=CARTESIAN_POINT('Origin',(31.7591315960217,-2.05967847590834,33.8912948941586));
#60748=CARTESIAN_POINT('',(31.7977957394973,-2.06279117742452,33.8637293696319));
#60749=CARTESIAN_POINT('Ctrl Pts',(31.7977957394945,-2.06279117742322,33.8637293696347));
#60750=CARTESIAN_POINT('Ctrl Pts',(31.7813045503384,-2.05496953307228,33.8804609779984));
#60751=CARTESIAN_POINT('Ctrl Pts',(31.7650135815277,-2.04724285169338,33.8969505670841));
#60752=CARTESIAN_POINT('',(31.9153788526219,-1.9540984656726,33.8637293696319));
#60753=CARTESIAN_POINT('Origin',(30.,-1.32966554433622E-14,33.8637293696319));
#60754=CARTESIAN_POINT('',(31.9024505156632,-1.92019745658634,33.8969505670765));
#60755=CARTESIAN_POINT('Ctrl Pts',(31.9024505156603,-1.92019745657863,33.8969505670841));
#60756=CARTESIAN_POINT('Ctrl Pts',(31.9088752035777,-1.93704443420321,33.8804609779984));
#60757=CARTESIAN_POINT('Ctrl Pts',(31.9153788526208,-1.95409846566976,33.8637293696347));
#60758=CARTESIAN_POINT('',(31.9201974565863,-1.90245051566327,33.8969505670765));
#60759=CARTESIAN_POINT('Origin',(31.9153092670123,-1.91530927561705,33.891294933562));
#60760=CARTESIAN_POINT('',(31.9540984656725,-1.91537885262194,33.8637293696319));
#60761=CARTESIAN_POINT('Ctrl Pts',(31.9540984656697,-1.91537885262084,33.8637293696347));
#60762=CARTESIAN_POINT('Ctrl Pts',(31.9370444342032,-1.90887520357777,33.8804609779984));
#60763=CARTESIAN_POINT('Ctrl Pts',(31.9201974565786,-1.90245051566033,33.8969505670841));
#60764=CARTESIAN_POINT('',(32.0627911774245,-1.79779573949737,33.8637293696319));
#60765=CARTESIAN_POINT('Origin',(30.,-1.32966554433622E-14,33.8637293696319));
#60766=CARTESIAN_POINT('',(32.0472428516969,-1.76501358153528,33.8969505670765));
#60767=CARTESIAN_POINT('Ctrl Pts',(32.0472428516934,-1.76501358152781,33.8969505670841));
#60768=CARTESIAN_POINT('Ctrl Pts',(32.0549695330723,-1.78130455033843,33.8804609779983));
#60769=CARTESIAN_POINT('Ctrl Pts',(32.0627911774232,-1.7977957394946,33.8637293696347));
#60770=CARTESIAN_POINT('',(32.063542675787,-1.74592893957158,33.8969505670765));
#60771=CARTESIAN_POINT('Origin',(32.0596784217459,-1.75913156587025,33.8912949636253));
#60772=CARTESIAN_POINT('',(32.0983535250032,-1.75615758026484,33.8637293696319));
#60773=CARTESIAN_POINT('Ctrl Pts',(32.0983535250003,-1.75615758026399,33.8637293696347));
#60774=CARTESIAN_POINT('Ctrl Pts',(32.0808417949984,-1.75101202368781,33.8804609779984));
#60775=CARTESIAN_POINT('Ctrl Pts',(32.0635426757791,-1.74592893956926,33.8969505670841));
#60776=CARTESIAN_POINT('',(32.1974857086705,-1.63040900476039,33.8637293696319));
#60777=CARTESIAN_POINT('Origin',(30.,-1.32966554433622E-14,33.8637293696319));
#60778=CARTESIAN_POINT('',(32.1794132547725,-1.59894781082747,33.8969505670765));
#60779=CARTESIAN_POINT('Ctrl Pts',(32.1794132547683,-1.59894781082035,33.8969505670841));
#60780=CARTESIAN_POINT('Ctrl Pts',(32.1883942920486,-1.61458233157699,33.8804609779984));
#60781=CARTESIAN_POINT('Ctrl Pts',(32.197485708669,-1.63040900475776,33.8637293696347));
#60782=CARTESIAN_POINT('',(32.194165468194,-1.57864313098713,33.8969505670765));
#60783=CARTESIAN_POINT('Origin',(32.1913489771416,-1.59210823242541,33.8912949854673));
#60784=CARTESIAN_POINT('',(32.2296715370789,-1.58610901244375,33.8637293696319));
#60785=CARTESIAN_POINT('Ctrl Pts',(32.2296715370759,-1.58610901244313,33.8637293696347));
#60786=CARTESIAN_POINT('Ctrl Pts',(32.2118100741774,-1.58235327240121,33.8804609779984));
#60787=CARTESIAN_POINT('Ctrl Pts',(32.1941654681859,-1.57864313098543,33.8969505670841));
#60788=CARTESIAN_POINT('',(32.3186320097845,-1.45297025634306,33.8637293696319));
#60789=CARTESIAN_POINT('Origin',(30.,-1.32966554433622E-14,33.8637293696319));
#60790=CARTESIAN_POINT('',(32.2981468504039,-1.42302399516182,33.8969505670765));
#60791=CARTESIAN_POINT('Ctrl Pts',(32.2981468503993,-1.42302399515499,33.8969505670841));
#60792=CARTESIAN_POINT('Ctrl Pts',(32.3083268724996,-1.4379056758382,33.8804609779984));
#60793=CARTESIAN_POINT('Ctrl Pts',(32.3186320097828,-1.45297025634053,33.8637293696347));
#60794=CARTESIAN_POINT('',(32.3112605008555,-1.40162446254804,33.8969505670765));
#60795=CARTESIAN_POINT('Origin',(32.3095091411127,-1.41526902814879,33.891294999854));
#60796=CARTESIAN_POINT('',(32.3472428826875,-1.40628155512619,33.8637293696319));
#60797=CARTESIAN_POINT('Ctrl Pts',(32.3472428826845,-1.4062815551258,33.8637293696347));
#60798=CARTESIAN_POINT('Ctrl Pts',(32.3291418087476,-1.4039387870044,33.8804609779983));
#60799=CARTESIAN_POINT('Ctrl Pts',(32.3112605008473,-1.40162446254698,33.8969505670841));
#60800=CARTESIAN_POINT('',(32.4254831735348,-1.26657346313373,33.8637293696319));
#60801=CARTESIAN_POINT('Origin',(30.,-1.32966554433622E-14,33.8637293696319));
#60802=CARTESIAN_POINT('',(32.4027116064913,-1.2383267633625,33.8969505670765));
#60803=CARTESIAN_POINT('Ctrl Pts',(32.4027116064861,-1.23832676335608,33.8969505670841));
#60804=CARTESIAN_POINT('Ctrl Pts',(32.414027850185,-1.25236385345577,33.8804609779983));
#60805=CARTESIAN_POINT('Ctrl Pts',(32.4254831735329,-1.26657346313137,33.8637293696347));
#60806=CARTESIAN_POINT('',(32.4141058439571,-1.21596431320991,33.8969505670765));
#60807=CARTESIAN_POINT('Origin',(32.4134304175703,-1.22970422416536,33.8912950072666));
#60808=CARTESIAN_POINT('',(32.4503426953868,-1.21778390438519,33.8637293696319));
#60809=CARTESIAN_POINT('Ctrl Pts',(32.4503426953838,-1.21778390438504,33.8637293696347));
#60810=CARTESIAN_POINT('Ctrl Pts',(32.4321136095486,-1.21686855212869,33.8804609779984));
#60811=CARTESIAN_POINT('Ctrl Pts',(32.4141058439489,-1.2159643132095,33.8969505670841));
#60812=CARTESIAN_POINT('',(32.5173804269652,-1.07236782334576,33.8637293696319));
#60813=CARTESIAN_POINT('Origin',(30.,-1.32966554433622E-14,33.8637293696319));
#60814=CARTESIAN_POINT('',(32.492462846542,-1.0459948352816,33.8969505670765));
#60815=CARTESIAN_POINT('Ctrl Pts',(32.4924628465363,-1.04599483527564,33.8969505670841));
#60816=CARTESIAN_POINT('Ctrl Pts',(32.5048455434283,-1.05910079146353,33.8804609779984));
#60817=CARTESIAN_POINT('Ctrl Pts',(32.5173804269631,-1.07236782334356,33.8637293696347));
#60818=CARTESIAN_POINT('',(32.5020674217591,-1.02280733953168,33.8969505670765));
#60819=CARTESIAN_POINT('Origin',(32.5024720978725,-1.03655788791108,33.8912950079413));
#60820=CARTESIAN_POINT('',(32.5383353305474,-1.02177821091943,33.8637293696319));
#60821=CARTESIAN_POINT('Ctrl Pts',(32.5383353305444,-1.02177821091952,33.8637293696347));
#60822=CARTESIAN_POINT('Ctrl Pts',(32.5200906211869,-1.02229591797926,33.8804609779983));
#60823=CARTESIAN_POINT('Ctrl Pts',(32.5020674217508,-1.02280733953191,33.8969505670841));
#60824=CARTESIAN_POINT('',(32.5937571929495,-0.871550679328387,33.8637293696319));
#60825=CARTESIAN_POINT('Origin',(30.,-1.32966554433622E-14,33.8637293696319));
#60826=CARTESIAN_POINT('',(32.5668472243157,-0.847214001212625,33.8969505670765));
#60827=CARTESIAN_POINT('Ctrl Pts',(32.5668472243096,-0.847214001207098,
33.8969505670841));
#60828=CARTESIAN_POINT('Ctrl Pts',(32.5802200309508,-0.859308020905142,
33.8804609779983));
#60829=CARTESIAN_POINT('Ctrl Pts',(32.5937571929472,-0.871550679326345,
33.8637293696347));
#60830=CARTESIAN_POINT('',(32.574602921884,-0.823344418487278,33.8969505670765));
#60831=CARTESIAN_POINT('Origin',(32.5760852110325,-0.837020829522246,33.8912950018862));
#60832=CARTESIAN_POINT('',(32.6106782843131,-0.819472915007605,33.8637293696319));
#60833=CARTESIAN_POINT('Ctrl Pts',(32.6106782843101,-0.819472915007929,
33.8637293696347));
#60834=CARTESIAN_POINT('Ctrl Pts',(32.5925304361305,-0.821420489547588,
33.8804609779984));
#60835=CARTESIAN_POINT('Ctrl Pts',(32.5746029218758,-0.823344418488157,
33.8969505670841));
#60836=CARTESIAN_POINT('',(32.6541425833274,-0.665360135552938,33.8637293696319));
#60837=CARTESIAN_POINT('Origin',(30.,-1.32966554433622E-14,33.8637293696319));
#60838=CARTESIAN_POINT('',(32.6254061353882,-0.643209811098926,33.8969505670765));
#60839=CARTESIAN_POINT('Ctrl Pts',(32.6254061353816,-0.643209811093906,
33.8969505670841));
#60840=CARTESIAN_POINT('Ctrl Pts',(32.6396866039721,-0.65421733064898,33.8804609779984));
#60841=CARTESIAN_POINT('Ctrl Pts',(32.654142583325,-0.665360135551083,33.8637293696347));
#60842=CARTESIAN_POINT('',(32.6312651388532,-0.6188053053131,33.8969505670765));
#60843=CARTESIAN_POINT('Origin',(32.633815908334,-0.632323260043048,33.8912949888765));
#60844=CARTESIAN_POINT('',(32.6669255383174,-0.612115296072366,33.8637293696319));
#60845=CARTESIAN_POINT('Ctrl Pts',(32.6669255383144,-0.612115296072921,
33.8637293696347));
#60846=CARTESIAN_POINT('Ctrl Pts',(32.6489864388314,-0.615480730647825,
33.8804609779983));
#60847=CARTESIAN_POINT('Ctrl Pts',(32.6312651388451,-0.618805305314621,
33.8969505670841));
#60848=CARTESIAN_POINT('',(32.6981643020872,-0.455067425287109,33.8637293696319));
#60849=CARTESIAN_POINT('Origin',(30.,-1.32966554433622E-14,33.8637293696319));
#60850=CARTESIAN_POINT('',(32.6677785445999,-0.435240018610835,33.8969505670765));
#60851=CARTESIAN_POINT('Ctrl Pts',(32.667778544593,-0.43524001860635,33.8969505670841));
#60852=CARTESIAN_POINT('Ctrl Pts',(32.6828786312952,-0.445093173000037,
33.8804609779984));
#60853=CARTESIAN_POINT('Ctrl Pts',(32.6981643020846,-0.45506742528547,33.8637293696347));
#60854=CARTESIAN_POINT('',(32.6717047312569,-0.410451051658023,33.8969505670765));
#60855=CARTESIAN_POINT('Origin',(32.6753082614924,-0.423727206709312,33.8912949684251));
#60856=CARTESIAN_POINT('',(32.7067303095351,-0.400983782787849,33.8637293696319));
#60857=CARTESIAN_POINT('Ctrl Pts',(32.7067303095322,-0.400983782788643,
33.8637293696347));
#60858=CARTESIAN_POINT('Ctrl Pts',(32.6891105592595,-0.405746328375509,
33.8804609779984));
#60859=CARTESIAN_POINT('Ctrl Pts',(32.6717047312489,-0.410451051660171,
33.8969505670841));
#60860=CARTESIAN_POINT('',(32.7255509406939,-0.241969073019109,33.8637293696319));
#60861=CARTESIAN_POINT('Origin',(30.,-1.32966554433622E-14,33.8637293696319));
#60862=CARTESIAN_POINT('',(32.6937032119577,-0.224586826676015,33.8969505670765));
#60863=CARTESIAN_POINT('Ctrl Pts',(32.6937032119505,-0.224586826672072,
33.8969505670841));
#60864=CARTESIAN_POINT('Ctrl Pts',(32.7095298197086,-0.233224867931026,
33.8804609779984));
#60865=CARTESIAN_POINT('Ctrl Pts',(32.7255509406912,-0.241969073017673,
33.8637293696347));
#60866=CARTESIAN_POINT('',(32.6956723755605,-0.199566230780649,33.8969505670765));
#60867=CARTESIAN_POINT('Origin',(32.7003064571198,-0.212518732061269,33.8912949397143));
#60868=CARTESIAN_POINT('',(32.7298471883155,-0.187380071141808,33.8637293696319));
#60869=CARTESIAN_POINT('Ctrl Pts',(32.7298471883126,-0.187380071142835,
33.8637293696347));
#60870=CARTESIAN_POINT('Ctrl Pts',(32.7126554188699,-0.19351036506442,33.8804609779983));
#60871=CARTESIAN_POINT('Ctrl Pts',(32.6956723755527,-0.199566230783424,
33.8969505670841));
#60872=CARTESIAN_POINT('',(32.7361336514135,-0.0273789009530657,33.8637293696319));
#60873=CARTESIAN_POINT('Origin',(30.,-1.32966554433622E-14,33.8637293696319));
#60874=CARTESIAN_POINT('',(32.7030203032667,-0.0125489822720396,33.8969505670765));
#60875=CARTESIAN_POINT('Ctrl Pts',(32.7030203032592,-0.0125489822686859,
33.8969505670841));
#60876=CARTESIAN_POINT('Ctrl Pts',(32.7194758557734,-0.0199186539960853,
33.8804609779984));
#60877=CARTESIAN_POINT('Ctrl Pts',(32.7361336514107,-0.0273789009518218,
33.8637293696347));
#60878=CARTESIAN_POINT('',(32.7030203032667,0.0125489822719939,33.8969505670765));
#60879=CARTESIAN_POINT('Origin',(32.7086563646857,-6.24428584025816E-9,
33.8912949140187));
#60880=CARTESIAN_POINT('',(32.7361336514135,0.0273789009530202,33.8637293696319));
#60881=CARTESIAN_POINT('Ctrl Pts',(32.7361336514108,0.027378900951751,33.8637293696347));
#60882=CARTESIAN_POINT('Ctrl Pts',(32.7194758557734,0.0199186539960142,
33.8804609779984));
#60883=CARTESIAN_POINT('Ctrl Pts',(32.7030203032592,0.0125489822686146,
33.8969505670841));
#60884=CARTESIAN_POINT('',(32.7298471883155,0.187380071141762,33.8637293696319));
#60885=CARTESIAN_POINT('Origin',(30.,-1.32966554433622E-14,33.8637293696319));
#60886=CARTESIAN_POINT('',(32.6956723755605,0.199566230780603,33.8969505670765));
#60887=CARTESIAN_POINT('Ctrl Pts',(32.6956723755527,0.199566230783364,33.8969505670841));
#60888=CARTESIAN_POINT('Ctrl Pts',(32.7126554188699,0.193510365064359,33.8804609779983));
#60889=CARTESIAN_POINT('Ctrl Pts',(32.7298471883126,0.187380071142775,33.8637293696347));
#60890=CARTESIAN_POINT('',(32.6937032119577,0.224586826675969,33.8969505670765));
#60891=CARTESIAN_POINT('Origin',(32.7003074588901,0.212518788369426,33.8912937927563));
#60892=CARTESIAN_POINT('',(32.7255509406939,0.241969073019064,33.8637293696319));
#60893=CARTESIAN_POINT('Ctrl Pts',(32.7255509406912,0.241969073017624,33.8637293696347));
#60894=CARTESIAN_POINT('Ctrl Pts',(32.7095298197086,0.233224867930978,33.8804609779984));
#60895=CARTESIAN_POINT('Ctrl Pts',(32.6937032119505,0.224586826672025,33.8969505670841));
#60896=CARTESIAN_POINT('',(32.7067303095351,0.400983782787804,33.8637293696319));
#60897=CARTESIAN_POINT('Origin',(30.,-1.32966554433622E-14,33.8637293696319));
#60898=CARTESIAN_POINT('',(32.6717047312569,0.410451051657977,33.8969505670765));
#60899=CARTESIAN_POINT('Ctrl Pts',(32.6717047312489,0.410451051660138,33.8969505670841));
#60900=CARTESIAN_POINT('Ctrl Pts',(32.6891105592595,0.405746328375475,33.8804609779984));
#60901=CARTESIAN_POINT('Ctrl Pts',(32.7067303095322,0.400983782788608,33.8637293696347));
#60902=CARTESIAN_POINT('',(32.6677785445999,0.435240018610789,33.8969505670765));
#60903=CARTESIAN_POINT('Origin',(32.6753090233822,0.423727307748461,33.8912940899386));
#60904=CARTESIAN_POINT('',(32.6981643020872,0.455067425287063,33.8637293696319));
#60905=CARTESIAN_POINT('Ctrl Pts',(32.6981643020846,0.455067425285395,33.8637293696347));
#60906=CARTESIAN_POINT('Ctrl Pts',(32.6828786312952,0.445093172999962,33.8804609779983));
#60907=CARTESIAN_POINT('Ctrl Pts',(32.667778544593,0.435240018606276,33.8969505670841));
#60908=CARTESIAN_POINT('',(32.6669255383174,0.61211529607232,33.8637293696319));
#60909=CARTESIAN_POINT('Origin',(30.,-1.32966554433622E-14,33.8637293696319));
#60910=CARTESIAN_POINT('',(32.6312651388532,0.618805305313054,33.8969505670765));
#60911=CARTESIAN_POINT('Ctrl Pts',(32.6312651388451,0.618805305314574,33.8969505670841));
#60912=CARTESIAN_POINT('Ctrl Pts',(32.6489864388314,0.615480730647778,33.8804609779983));
#60913=CARTESIAN_POINT('Ctrl Pts',(32.6669255383144,0.612115296072874,33.8637293696347));
#60914=CARTESIAN_POINT('',(32.6254061353882,0.64320981109888,33.8969505670765));
#60915=CARTESIAN_POINT('Origin',(32.6338164916465,0.632323382398585,33.8912943077151));
#60916=CARTESIAN_POINT('',(32.6541425833274,0.665360135552893,33.8637293696319));
#60917=CARTESIAN_POINT('Ctrl Pts',(32.654142583325,0.665360135551018,33.8637293696347));
#60918=CARTESIAN_POINT('Ctrl Pts',(32.6396866039721,0.654217330648915,33.8804609779984));
#60919=CARTESIAN_POINT('Ctrl Pts',(32.6254061353817,0.643209811093841,33.8969505670841));
#60920=CARTESIAN_POINT('',(32.6106782843131,0.81947291500756,33.8637293696319));
#60921=CARTESIAN_POINT('Origin',(30.,-1.32966554433622E-14,33.8637293696319));
#60922=CARTESIAN_POINT('',(32.574602921884,0.823344418487232,33.8969505670765));
#60923=CARTESIAN_POINT('Ctrl Pts',(32.5746029218758,0.823344418488117,33.8969505670841));
#60924=CARTESIAN_POINT('Ctrl Pts',(32.5925304361305,0.821420489547548,33.8804609779984));
#60925=CARTESIAN_POINT('Ctrl Pts',(32.6106782843101,0.819472915007888,33.8637293696347));
#60926=CARTESIAN_POINT('',(32.5668472243157,0.84721400121258,33.8969505670765));
#60927=CARTESIAN_POINT('Origin',(32.5760856561636,0.83702095775897,33.891294472568));
#60928=CARTESIAN_POINT('',(32.5937571929495,0.871550679328342,33.8637293696319));
#60929=CARTESIAN_POINT('Ctrl Pts',(32.5937571929473,0.871550679326287,33.8637293696347));
#60930=CARTESIAN_POINT('Ctrl Pts',(32.5802200309508,0.859308020905083,33.8804609779984));
#60931=CARTESIAN_POINT('Ctrl Pts',(32.5668472243096,0.847214001207037,33.8969505670841));
#60932=CARTESIAN_POINT('',(32.5383353305474,1.02177821091938,33.8637293696319));
#60933=CARTESIAN_POINT('Origin',(30.,-1.32966554433622E-14,33.8637293696319));
#60934=CARTESIAN_POINT('',(32.5020674217591,1.02280733953163,33.8969505670765));
#60935=CARTESIAN_POINT('Ctrl Pts',(32.5020674217508,1.02280733953187,33.8969505670841));
#60936=CARTESIAN_POINT('Ctrl Pts',(32.520090621187,1.02229591797922,33.8804609779984));
#60937=CARTESIAN_POINT('Ctrl Pts',(32.5383353305444,1.02177821091947,33.8637293696347));
#60938=CARTESIAN_POINT('',(32.492462846542,1.04599483528156,33.8969505670765));
#60939=CARTESIAN_POINT('Origin',(32.5024724328509,1.03655801106889,33.8912946002427));
#60940=CARTESIAN_POINT('',(32.5173804269653,1.07236782334572,33.8637293696319));
#60941=CARTESIAN_POINT('Ctrl Pts',(32.5173804269632,1.0723678233435,33.8637293696347));
#60942=CARTESIAN_POINT('Ctrl Pts',(32.5048455434284,1.05910079146346,33.8804609779983));
#60943=CARTESIAN_POINT('Ctrl Pts',(32.4924628465363,1.04599483527555,33.8969505670841));
#60944=CARTESIAN_POINT('',(32.4503426953868,1.21778390438515,33.8637293696319));
#60945=CARTESIAN_POINT('Origin',(30.,-1.32966554433622E-14,33.8637293696319));
#60946=CARTESIAN_POINT('',(32.4141058439571,1.21596431320987,33.8969505670765));
#60947=CARTESIAN_POINT('Ctrl Pts',(32.4141058439489,1.21596431320946,33.8969505670841));
#60948=CARTESIAN_POINT('Ctrl Pts',(32.4321136095487,1.21686855212866,33.8804609779984));
#60949=CARTESIAN_POINT('Ctrl Pts',(32.4503426953838,1.217783904385,33.8637293696347));
#60950=CARTESIAN_POINT('',(32.4027116064913,1.23832676336245,33.8969505670765));
#60951=CARTESIAN_POINT('Origin',(32.4134306626749,1.22970433386022,33.891294700665));
#60952=CARTESIAN_POINT('',(32.4254831735348,1.26657346313369,33.8637293696319));
#60953=CARTESIAN_POINT('Ctrl Pts',(32.4254831735329,1.26657346313132,33.8637293696347));
#60954=CARTESIAN_POINT('Ctrl Pts',(32.414027850185,1.25236385345572,33.8804609779984));
#60955=CARTESIAN_POINT('Ctrl Pts',(32.4027116064861,1.23832676335603,33.8969505670841));
#60956=CARTESIAN_POINT('',(32.3472428826875,1.40628155512614,33.8637293696319));
#60957=CARTESIAN_POINT('Origin',(30.,-1.32966554433622E-14,33.8637293696319));
#60958=CARTESIAN_POINT('',(32.3112605008555,1.401624462548,33.8969505670765));
#60959=CARTESIAN_POINT('Ctrl Pts',(32.3112605008473,1.40162446254694,33.8969505670841));
#60960=CARTESIAN_POINT('Ctrl Pts',(32.3291418087476,1.40393878700437,33.8804609779984));
#60961=CARTESIAN_POINT('Ctrl Pts',(32.3472428826845,1.40628155512576,33.8637293696347));
#60962=CARTESIAN_POINT('',(32.298146850404,1.42302399516178,33.8969505670765));
#60963=CARTESIAN_POINT('Origin',(32.3095093115547,1.41526911745259,33.8912947803757));
#60964=CARTESIAN_POINT('',(32.3186320097845,1.45297025634302,33.8637293696319));
#60965=CARTESIAN_POINT('Ctrl Pts',(32.3186320097828,1.45297025634046,33.8637293696347));
#60966=CARTESIAN_POINT('Ctrl Pts',(32.3083268724996,1.43790567583815,33.8804609779983));
#60967=CARTESIAN_POINT('Ctrl Pts',(32.2981468503993,1.42302399515495,33.8969505670841));
#60968=CARTESIAN_POINT('',(32.2296715370789,1.58610901244371,33.8637293696319));
#60969=CARTESIAN_POINT('Origin',(30.,-1.32966554433622E-14,33.8637293696319));
#60970=CARTESIAN_POINT('',(32.194165468194,1.57864313098709,33.8969505670765));
#60971=CARTESIAN_POINT('Ctrl Pts',(32.1941654681859,1.57864313098539,33.8969505670841));
#60972=CARTESIAN_POINT('Ctrl Pts',(32.2118100741774,1.58235327240116,33.8804609779984));
#60973=CARTESIAN_POINT('Ctrl Pts',(32.2296715370759,1.58610901244308,33.8637293696347));
#60974=CARTESIAN_POINT('',(32.1794132547725,1.59894781082743,33.8969505670765));
#60975=CARTESIAN_POINT('Origin',(32.191349084716,1.59210829514292,33.891294843835));
#60976=CARTESIAN_POINT('',(32.1974857086706,1.63040900476035,33.8637293696319));
#60977=CARTESIAN_POINT('Ctrl Pts',(32.1974857086691,1.6304090047577,33.8637293696347));
#60978=CARTESIAN_POINT('Ctrl Pts',(32.1883942920486,1.61458233157692,33.8804609779983));
#60979=CARTESIAN_POINT('Ctrl Pts',(32.1794132547684,1.59894781082026,33.8969505670841));
#60980=CARTESIAN_POINT('',(32.0983535250032,1.7561575802648,33.8637293696319));
#60981=CARTESIAN_POINT('Origin',(30.,-1.32966554433622E-14,33.8637293696319));
#60982=CARTESIAN_POINT('',(32.0635426757871,1.74592893957153,33.8969505670765));
#60983=CARTESIAN_POINT('Ctrl Pts',(32.0635426757792,1.74592893956921,33.8969505670841));
#60984=CARTESIAN_POINT('Ctrl Pts',(32.0808417949984,1.75101202368776,33.8804609779983));
#60985=CARTESIAN_POINT('Ctrl Pts',(32.0983535250003,1.75615758026393,33.8637293696347));
#60986=CARTESIAN_POINT('',(32.0472428516969,1.76501358153524,33.8969505670765));
#60987=CARTESIAN_POINT('Origin',(32.0596784759083,1.75913159602166,33.8912948941586));
#60988=CARTESIAN_POINT('',(32.0627911774245,1.79779573949733,33.8637293696319));
#60989=CARTESIAN_POINT('Ctrl Pts',(32.0627911774232,1.79779573949457,33.8637293696347));
#60990=CARTESIAN_POINT('Ctrl Pts',(32.0549695330723,1.78130455033839,33.8804609779984));
#60991=CARTESIAN_POINT('Ctrl Pts',(32.0472428516934,1.76501358152777,33.8969505670841));
#60992=CARTESIAN_POINT('',(31.9540984656726,1.9153788526219,33.8637293696319));
#60993=CARTESIAN_POINT('Origin',(30.,-1.32966554433622E-14,33.8637293696319));
#60994=CARTESIAN_POINT('',(31.9201974565863,1.90245051566323,33.8969505670765));
#60995=CARTESIAN_POINT('Ctrl Pts',(31.9201974565786,1.90245051566028,33.8969505670841));
#60996=CARTESIAN_POINT('Ctrl Pts',(31.9370444342032,1.90887520357773,33.8804609779983));
#60997=CARTESIAN_POINT('Ctrl Pts',(31.9540984656697,1.91537885262081,33.8637293696347));
#60998=CARTESIAN_POINT('',(31.9024505156632,1.9201974565863,33.8969505670765));
#60999=CARTESIAN_POINT('Origin',(31.915309275617,1.91530926701235,33.891294933562));
#61000=CARTESIAN_POINT('',(31.9153788526219,1.95409846567256,33.8637293696319));
#61001=CARTESIAN_POINT('Ctrl Pts',(31.9153788526208,1.95409846566973,33.8637293696347));
#61002=CARTESIAN_POINT('Ctrl Pts',(31.9088752035777,1.93704443420319,33.8804609779984));
#61003=CARTESIAN_POINT('Ctrl Pts',(31.9024505156603,1.9201974565786,33.8969505670841));
#61004=CARTESIAN_POINT('',(31.7977957394973,2.06279117742448,33.8637293696319));
#61005=CARTESIAN_POINT('Origin',(30.,-1.32966554433622E-14,33.8637293696319));
#61006=CARTESIAN_POINT('',(31.7650135815352,2.04724285169688,33.8969505670765));
#61007=CARTESIAN_POINT('Ctrl Pts',(31.7650135815278,2.04724285169333,33.8969505670841));
#61008=CARTESIAN_POINT('Ctrl Pts',(31.7813045503384,2.05496953307223,33.8804609779984));
#61009=CARTESIAN_POINT('Ctrl Pts',(31.7977957394946,2.06279117742316,33.8637293696347));
#61010=CARTESIAN_POINT('',(31.7459289395715,2.06354267578706,33.8969505670765));
#61011=CARTESIAN_POINT('Origin',(31.7591315658702,2.05967842174595,33.8912949636253));
#61012=CARTESIAN_POINT('',(31.7561575802648,2.09835352500324,33.8637293696319));
#61013=CARTESIAN_POINT('Ctrl Pts',(31.7561575802639,2.09835352500033,33.8637293696347));
#61014=CARTESIAN_POINT('Ctrl Pts',(31.7510120236877,2.08084179499845,33.8804609779984));
#61015=CARTESIAN_POINT('Ctrl Pts',(31.7459289395692,2.06354267577915,33.8969505670841));
#61016=CARTESIAN_POINT('',(31.6304090047604,2.19748570867057,33.8637293696319));
#61017=CARTESIAN_POINT('Origin',(30.,-1.32966554433622E-14,33.8637293696319));
#61018=CARTESIAN_POINT('',(31.5989478108274,2.17941325477248,33.8969505670765));
#61019=CARTESIAN_POINT('Ctrl Pts',(31.5989478108202,2.17941325476838,33.8969505670841));
#61020=CARTESIAN_POINT('Ctrl Pts',(31.6145823315769,2.18839429204865,33.8804609779983));
#61021=CARTESIAN_POINT('Ctrl Pts',(31.6304090047577,2.19748570866908,33.8637293696347));
#61022=CARTESIAN_POINT('',(31.5786431309871,2.19416546819402,33.8969505670765));
#61023=CARTESIAN_POINT('Origin',(31.5921082324254,2.19134897714166,33.8912949854673));
#61024=CARTESIAN_POINT('',(31.5861090124437,2.22967153707891,33.8637293696319));
#61025=CARTESIAN_POINT('Ctrl Pts',(31.5861090124431,2.22967153707593,33.8637293696347));
#61026=CARTESIAN_POINT('Ctrl Pts',(31.5823532724012,2.21181007417742,33.8804609779984));
#61027=CARTESIAN_POINT('Ctrl Pts',(31.5786431309854,2.19416546818594,33.8969505670841));
#61028=CARTESIAN_POINT('',(31.452970256343,2.31863200978455,33.8637293696319));
#61029=CARTESIAN_POINT('Origin',(30.,-1.32966554433622E-14,33.8637293696319));
#61030=CARTESIAN_POINT('',(31.4230239951618,2.29814685040396,33.8969505670765));
#61031=CARTESIAN_POINT('Ctrl Pts',(31.423023995155,2.29814685039929,33.8969505670841));
#61032=CARTESIAN_POINT('Ctrl Pts',(31.4379056758382,2.30832687249959,33.8804609779983));
#61033=CARTESIAN_POINT('Ctrl Pts',(31.4529702563405,2.31863200978281,33.8637293696347));
#61034=CARTESIAN_POINT('',(31.401624462548,2.3112605008555,33.8969505670765));
#61035=CARTESIAN_POINT('Origin',(31.4152690281487,2.30950914111275,33.891294999854));
#61036=CARTESIAN_POINT('',(31.4062815551261,2.34724288268748,33.8637293696319));
#61037=CARTESIAN_POINT('Ctrl Pts',(31.4062815551258,2.34724288268445,33.8637293696347));
#61038=CARTESIAN_POINT('Ctrl Pts',(31.4039387870044,2.32914180874762,33.8804609779983));
#61039=CARTESIAN_POINT('Ctrl Pts',(31.4016244625469,2.31126050084732,33.8969505670841));
#61040=CARTESIAN_POINT('',(31.2665734631337,2.42548317353483,33.8637293696319));
#61041=CARTESIAN_POINT('Origin',(30.,-1.32966554433622E-14,33.8637293696319));
#61042=CARTESIAN_POINT('',(31.2383267633625,2.40271160649132,33.8969505670765));
#61043=CARTESIAN_POINT('Ctrl Pts',(31.2383267633561,2.40271160648613,33.8969505670841));
#61044=CARTESIAN_POINT('Ctrl Pts',(31.2523638534557,2.41402785018503,33.8804609779983));
#61045=CARTESIAN_POINT('Ctrl Pts',(31.2665734631313,2.4254831735329,33.8637293696347));
#61046=CARTESIAN_POINT('',(31.2159643132099,2.41410584395711,33.8969505670765));
#61047=CARTESIAN_POINT('Origin',(31.2297042241653,2.41343041757031,33.8912950072666));
#61048=CARTESIAN_POINT('',(31.2177839043851,2.45034269538681,33.8637293696319));
#61049=CARTESIAN_POINT('Ctrl Pts',(31.217783904385,2.45034269538375,33.8637293696347));
#61050=CARTESIAN_POINT('Ctrl Pts',(31.2168685521287,2.43211360954864,33.8804609779984));
#61051=CARTESIAN_POINT('Ctrl Pts',(31.2159643132095,2.41410584394886,33.8969505670841));
#61052=CARTESIAN_POINT('',(31.0723678233457,2.51738042696526,33.8637293696319));
#61053=CARTESIAN_POINT('Origin',(30.,-1.32966554433622E-14,33.8637293696319));
#61054=CARTESIAN_POINT('',(31.0459948352816,2.49246284654197,33.8969505670765));
#61055=CARTESIAN_POINT('Ctrl Pts',(31.0459948352756,2.4924628465363,33.8969505670841));
#61056=CARTESIAN_POINT('Ctrl Pts',(31.0591007914635,2.50484554342835,33.8804609779983));
#61057=CARTESIAN_POINT('Ctrl Pts',(31.0723678233435,2.51738042696315,33.8637293696347));
#61058=CARTESIAN_POINT('',(31.0228073395316,2.50206742175906,33.8969505670765));
#61059=CARTESIAN_POINT('Origin',(31.036557887911,2.50247209787251,33.8912950079413));
#61060=CARTESIAN_POINT('',(31.0217782109194,2.53833533054745,33.8637293696319));
#61061=CARTESIAN_POINT('Ctrl Pts',(31.0217782109194,2.5383353305444,33.8637293696347));
#61062=CARTESIAN_POINT('Ctrl Pts',(31.0222959179792,2.52009062118696,33.8804609779984));
#61063=CARTESIAN_POINT('Ctrl Pts',(31.0228073395318,2.50206742175081,33.8969505670841));
#61064=CARTESIAN_POINT('',(30.8715506793283,2.59375719294951,33.8637293696319));
#61065=CARTESIAN_POINT('Origin',(30.,-1.32966554433622E-14,33.8637293696319));
#61066=CARTESIAN_POINT('',(30.8472140012126,2.5668472243157,33.8969505670765));
#61067=CARTESIAN_POINT('Ctrl Pts',(30.847214001207,2.56684722430959,33.8969505670841));
#61068=CARTESIAN_POINT('Ctrl Pts',(30.8593080209051,2.58022003095078,33.8804609779984));
#61069=CARTESIAN_POINT('Ctrl Pts',(30.8715506793263,2.59375719294725,33.8637293696347));
#61070=CARTESIAN_POINT('',(30.8233444184872,2.57460292188402,33.8969505670765));
#61071=CARTESIAN_POINT('Origin',(30.8370208295222,2.57608521103255,33.8912950018862));
#61072=CARTESIAN_POINT('',(30.8194729150076,2.61067828431311,33.8637293696319));
#61073=CARTESIAN_POINT('Ctrl Pts',(30.8194729150079,2.61067828431008,33.8637293696347));
#61074=CARTESIAN_POINT('Ctrl Pts',(30.8214204895475,2.59253043613048,33.8804609779984));
#61075=CARTESIAN_POINT('Ctrl Pts',(30.8233444184881,2.57460292187581,33.8969505670841));
#61076=CARTESIAN_POINT('',(30.6653601355529,2.65414258332745,33.8637293696319));
#61077=CARTESIAN_POINT('Origin',(30.,-1.32966554433622E-14,33.8637293696319));
#61078=CARTESIAN_POINT('',(30.6432098110989,2.62540613538819,33.8969505670765));
#61079=CARTESIAN_POINT('Ctrl Pts',(30.6432098110938,2.62540613538167,33.8969505670841));
#61080=CARTESIAN_POINT('Ctrl Pts',(30.6542173306489,2.63968660397217,33.8804609779983));
#61081=CARTESIAN_POINT('Ctrl Pts',(30.665360135551,2.65414258332504,33.8637293696347));
#61082=CARTESIAN_POINT('',(30.6188053053131,2.63126513885322,33.8969505670765));
#61083=CARTESIAN_POINT('Origin',(30.632323260043,2.633815908334,33.8912949888765));
#61084=CARTESIAN_POINT('',(30.6121152960723,2.66692553831736,33.8637293696319));
#61085=CARTESIAN_POINT('Ctrl Pts',(30.6121152960729,2.66692553831437,33.8637293696347));
#61086=CARTESIAN_POINT('Ctrl Pts',(30.6154807306478,2.6489864388314,33.8804609779983));
#61087=CARTESIAN_POINT('Ctrl Pts',(30.6188053053146,2.63126513884509,33.8969505670841));
#61088=CARTESIAN_POINT('',(30.4550674252871,2.69816430208719,33.8637293696319));
#61089=CARTESIAN_POINT('Origin',(30.,-1.32966554433622E-14,33.8637293696319));
#61090=CARTESIAN_POINT('',(30.4352400186108,2.66777854459989,33.8969505670765));
#61091=CARTESIAN_POINT('Ctrl Pts',(30.4352400186063,2.66777854459299,33.8969505670841));
#61092=CARTESIAN_POINT('Ctrl Pts',(30.4450931729999,2.68287863129519,33.8804609779983));
#61093=CARTESIAN_POINT('Ctrl Pts',(30.4550674252854,2.69816430208465,33.8637293696347));
#61094=CARTESIAN_POINT('',(30.410451051658,2.67170473125694,33.8969505670765));
#61095=CARTESIAN_POINT('Origin',(30.4237272067093,2.67530826149246,33.891294968425));
#61096=CARTESIAN_POINT('',(30.4009837827878,2.70673030953515,33.8637293696319));
#61097=CARTESIAN_POINT('Ctrl Pts',(30.4009837827886,2.7067303095322,33.8637293696347));
#61098=CARTESIAN_POINT('Ctrl Pts',(30.4057463283755,2.68911055925956,33.8804609779984));
#61099=CARTESIAN_POINT('Ctrl Pts',(30.4104510516602,2.67170473124897,33.8969505670841));
#61100=CARTESIAN_POINT('',(30.2419690730191,2.72555094069389,33.8637293696319));
#61101=CARTESIAN_POINT('Origin',(30.,-1.32966554433622E-14,33.8637293696319));
#61102=CARTESIAN_POINT('',(30.224586826676,2.69370321195774,33.8969505670765));
#61103=CARTESIAN_POINT('Ctrl Pts',(30.224586826672,2.6937032119505,33.8969505670841));
#61104=CARTESIAN_POINT('Ctrl Pts',(30.233224867931,2.70952981970859,33.8804609779983));
#61105=CARTESIAN_POINT('Ctrl Pts',(30.2419690730176,2.72555094069122,33.8637293696347));
#61106=CARTESIAN_POINT('',(30.1995662307806,2.69567237556048,33.8969505670765));
#61107=CARTESIAN_POINT('Origin',(30.2125187320612,2.70030645711979,33.8912949397143));
#61108=CARTESIAN_POINT('',(30.1873800711418,2.72984718831549,33.8637293696319));
#61109=CARTESIAN_POINT('Ctrl Pts',(30.1873800711428,2.7298471883126,33.8637293696347));
#61110=CARTESIAN_POINT('Ctrl Pts',(30.1935103650644,2.71265541886987,33.8804609779983));
#61111=CARTESIAN_POINT('Ctrl Pts',(30.1995662307834,2.6956723755527,33.8969505670841));
#61112=CARTESIAN_POINT('',(30.027378900953,2.73613365141356,33.8637293696319));
#61113=CARTESIAN_POINT('Origin',(30.,-1.32966554433622E-14,33.8637293696319));
#61114=CARTESIAN_POINT('',(30.012548982272,2.70302030326666,33.8969505670765));
#61115=CARTESIAN_POINT('Ctrl Pts',(30.0125489822686,2.70302030325912,33.8969505670841));
#61116=CARTESIAN_POINT('Ctrl Pts',(30.019918653996,2.71947585577339,33.8804609779983));
#61117=CARTESIAN_POINT('Ctrl Pts',(30.0273789009518,2.73613365141076,33.8637293696347));
#61118=CARTESIAN_POINT('',(29.987451017728,2.70302030326666,33.8969505670765));
#61119=CARTESIAN_POINT('Origin',(30.,2.70866577951602,33.891284862925));
#61120=CARTESIAN_POINT('',(29.9726210990469,2.73613365141356,33.8637293696319));
#61121=CARTESIAN_POINT('Ctrl Pts',(29.9726210990482,2.73613365141079,33.8637293696347));
#61122=CARTESIAN_POINT('Ctrl Pts',(29.980081346004,2.7194758557734,33.8804609779983));
#61123=CARTESIAN_POINT('Ctrl Pts',(29.9874510177314,2.70302030325912,33.8969505670841));
#61124=CARTESIAN_POINT('',(29.8126199288582,2.72984718831549,33.8637293696319));
#61125=CARTESIAN_POINT('Origin',(30.,-1.32966554433622E-14,33.8637293696319));
#61126=CARTESIAN_POINT('',(29.8004337692194,2.69567237556048,33.8969505670765));
#61127=CARTESIAN_POINT('Ctrl Pts',(29.8004337692166,2.6956723755527,33.8969505670841));
#61128=CARTESIAN_POINT('Ctrl Pts',(29.8064896349356,2.71265541886987,33.8804609779983));
#61129=CARTESIAN_POINT('Ctrl Pts',(29.8126199288572,2.7298471883126,33.8637293696347));
#61130=CARTESIAN_POINT('',(29.775413173324,2.69370321195775,33.8969505670765));
#61131=CARTESIAN_POINT('Origin',(29.7874812116306,2.70030745889017,33.8912937927563));
#61132=CARTESIAN_POINT('',(29.7580309269809,2.72555094069389,33.8637293696319));
#61133=CARTESIAN_POINT('Ctrl Pts',(29.7580309269824,2.72555094069121,33.8637293696347));
#61134=CARTESIAN_POINT('Ctrl Pts',(29.766775132069,2.70952981970858,33.8804609779983));
#61135=CARTESIAN_POINT('Ctrl Pts',(29.775413173328,2.69370321195049,33.8969505670841));
#61136=CARTESIAN_POINT('',(29.5990162172122,2.70673030953515,33.8637293696319));
#61137=CARTESIAN_POINT('Origin',(30.,-1.32966554433622E-14,33.8637293696319));
#61138=CARTESIAN_POINT('',(29.589548948342,2.67170473125694,33.8969505670765));
#61139=CARTESIAN_POINT('Ctrl Pts',(29.5895489483398,2.67170473124897,33.8969505670841));
#61140=CARTESIAN_POINT('Ctrl Pts',(29.5942536716245,2.68911055925956,33.8804609779983));
#61141=CARTESIAN_POINT('Ctrl Pts',(29.5990162172114,2.7067303095322,33.8637293696347));
#61142=CARTESIAN_POINT('',(29.5647599813892,2.6677785445999,33.8969505670765));
#61143=CARTESIAN_POINT('Origin',(29.5762726922515,2.67530902338217,33.8912940899386));
#61144=CARTESIAN_POINT('',(29.5449325747129,2.6981643020872,33.8637293696319));
#61145=CARTESIAN_POINT('Ctrl Pts',(29.5449325747146,2.69816430208465,33.8637293696347));
#61146=CARTESIAN_POINT('Ctrl Pts',(29.554906827,2.68287863129518,33.8804609779983));
#61147=CARTESIAN_POINT('Ctrl Pts',(29.5647599813937,2.66777854459298,33.8969505670841));
#61148=CARTESIAN_POINT('',(29.3878847039277,2.66692553831737,33.8637293696319));
#61149=CARTESIAN_POINT('Origin',(30.,-1.32966554433622E-14,33.8637293696319));
#61150=CARTESIAN_POINT('',(29.3811946946869,2.63126513885323,33.8969505670765));
#61151=CARTESIAN_POINT('Ctrl Pts',(29.3811946946854,2.6312651388451,33.8969505670841));
#61152=CARTESIAN_POINT('Ctrl Pts',(29.3845192693522,2.64898643883141,33.8804609779983));
#61153=CARTESIAN_POINT('Ctrl Pts',(29.3878847039271,2.66692553831437,33.8637293696347));
#61154=CARTESIAN_POINT('',(29.3567901889011,2.6254061353882,33.8969505670765));
#61155=CARTESIAN_POINT('Origin',(29.3676766176014,2.6338164916465,33.8912943077151));
#61156=CARTESIAN_POINT('',(29.3346398644471,2.65414258332745,33.8637293696319));
#61157=CARTESIAN_POINT('Ctrl Pts',(29.334639864449,2.65414258332502,33.8637293696347));
#61158=CARTESIAN_POINT('Ctrl Pts',(29.3457826693511,2.63968660397215,33.8804609779983));
#61159=CARTESIAN_POINT('Ctrl Pts',(29.3567901889061,2.62540613538165,33.8969505670841));
#61160=CARTESIAN_POINT('',(29.1805270849924,2.61067828431312,33.8637293696319));
#61161=CARTESIAN_POINT('Origin',(30.,-1.32966554433622E-14,33.8637293696319));
#61162=CARTESIAN_POINT('',(29.1766555815128,2.57460292188403,33.8969505670765));
#61163=CARTESIAN_POINT('Ctrl Pts',(29.1766555815118,2.57460292187581,33.8969505670841));
#61164=CARTESIAN_POINT('Ctrl Pts',(29.1785795104524,2.59253043613048,33.8804609779983));
#61165=CARTESIAN_POINT('Ctrl Pts',(29.1805270849921,2.61067828431008,33.8637293696347));
#61166=CARTESIAN_POINT('',(29.1527859987874,2.56684722431571,33.8969505670765));
#61167=CARTESIAN_POINT('Origin',(29.162979042241,2.57608565616365,33.891294472568));
#61168=CARTESIAN_POINT('',(29.1284493206716,2.59375719294953,33.8637293696319));
#61169=CARTESIAN_POINT('Ctrl Pts',(29.1284493206737,2.59375719294727,33.8637293696347));
#61170=CARTESIAN_POINT('Ctrl Pts',(29.1406919790949,2.58022003095078,33.8804609779983));
#61171=CARTESIAN_POINT('Ctrl Pts',(29.1527859987929,2.56684722430958,33.8969505670841));
#61172=CARTESIAN_POINT('',(28.9782217890806,2.53833533054746,33.8637293696319));
#61173=CARTESIAN_POINT('Origin',(30.,-1.32966554433622E-14,33.8637293696319));
#61174=CARTESIAN_POINT('',(28.9771926604684,2.50206742175908,33.8969505670765));
#61175=CARTESIAN_POINT('Ctrl Pts',(28.9771926604681,2.50206742175082,33.8969505670841));
#61176=CARTESIAN_POINT('Ctrl Pts',(28.9777040820208,2.52009062118696,33.8804609779983));
#61177=CARTESIAN_POINT('Ctrl Pts',(28.9782217890805,2.5383353305444,33.8637293696347));
#61178=CARTESIAN_POINT('',(28.9540051647184,2.49246284654199,33.8969505670765));
#61179=CARTESIAN_POINT('Origin',(28.9634419889311,2.50247243285091,33.8912946002427));
#61180=CARTESIAN_POINT('',(28.9276321766543,2.51738042696527,33.8637293696319));
#61181=CARTESIAN_POINT('Ctrl Pts',(28.9276321766565,2.51738042696315,33.8637293696347));
#61182=CARTESIAN_POINT('Ctrl Pts',(28.9408992085365,2.50484554342835,33.8804609779983));
#61183=CARTESIAN_POINT('Ctrl Pts',(28.9540051647244,2.49246284653631,33.8969505670841));
#61184=CARTESIAN_POINT('',(28.7822160956148,2.45034269538683,33.8637293696319));
#61185=CARTESIAN_POINT('Origin',(30.,-1.32966554433622E-14,33.8637293696319));
#61186=CARTESIAN_POINT('Ctrl Pts',(28.7840356867905,2.41410584394887,33.8969505670841));
#61187=CARTESIAN_POINT('Ctrl Pts',(28.7831314478713,2.43211360954865,33.8804609779983));
#61188=CARTESIAN_POINT('Ctrl Pts',(28.782216095615,2.45034269538377,33.8637293696347));
#61189=CARTESIAN_POINT('',(28.7334265368663,2.42548317353484,33.8637293696319));
#61190=CARTESIAN_POINT('Ctrl Pts',(28.7334265368687,2.42548317353291,33.8637293696347));
#61191=CARTESIAN_POINT('Ctrl Pts',(28.7476361465443,2.41402785018503,33.8804609779983));
#61192=CARTESIAN_POINT('Ctrl Pts',(28.7616732366439,2.40271160648614,33.8969505670841));
#61193=CARTESIAN_POINT('',(28.5937184448738,2.3472428826875,33.8637293696319));
#61194=CARTESIAN_POINT('Origin',(30.,-1.32966554433622E-14,33.8637293696319));
#61195=CARTESIAN_POINT('Ctrl Pts',(28.5983755374531,2.31126050084732,33.8969505670841));
#61196=CARTESIAN_POINT('Ctrl Pts',(28.5960612129956,2.32914180874763,33.8804609779983));
#61197=CARTESIAN_POINT('Ctrl Pts',(28.5937184448742,2.34724288268447,33.8637293696347));
#61198=CARTESIAN_POINT('',(28.547029743657,2.31863200978457,33.8637293696319));
#61199=CARTESIAN_POINT('Ctrl Pts',(28.5470297436595,2.31863200978283,33.8637293696347));
#61200=CARTESIAN_POINT('Ctrl Pts',(28.5620943241618,2.30832687249961,33.8804609779983));
#61201=CARTESIAN_POINT('Ctrl Pts',(28.576976004845,2.29814685039931,33.8969505670841));
#61202=CARTESIAN_POINT('',(28.4138909875563,2.22967153707894,33.8637293696319));
#61203=CARTESIAN_POINT('Origin',(30.,-1.32966554433622E-14,33.8637293696319));
#61204=CARTESIAN_POINT('Ctrl Pts',(28.4213568690146,2.19416546818595,33.8969505670841));
#61205=CARTESIAN_POINT('Ctrl Pts',(28.4176467275988,2.21181007417744,33.8804609779983));
#61206=CARTESIAN_POINT('Ctrl Pts',(28.4138909875569,2.22967153707594,33.8637293696347));
#61207=CARTESIAN_POINT('',(28.3695909952396,2.19748570867059,33.8637293696319));
#61208=CARTESIAN_POINT('Ctrl Pts',(28.3695909952423,2.19748570866909,33.8637293696347));
#61209=CARTESIAN_POINT('Ctrl Pts',(28.3854176684231,2.18839429204867,33.8804609779983));
#61210=CARTESIAN_POINT('Ctrl Pts',(28.4010521891798,2.17941325476839,33.8969505670841));
#61211=CARTESIAN_POINT('',(28.2438424197352,2.09835352500326,33.8637293696319));
#61212=CARTESIAN_POINT('Origin',(30.,-1.32966554433622E-14,33.8637293696319));
#61213=CARTESIAN_POINT('Ctrl Pts',(28.2540710604308,2.06354267577915,33.8969505670841));
#61214=CARTESIAN_POINT('Ctrl Pts',(28.2489879763122,2.08084179499845,33.8804609779983));
#61215=CARTESIAN_POINT('Ctrl Pts',(28.2438424197361,2.09835352500033,33.8637293696347));
#61216=CARTESIAN_POINT('',(28.2022042605027,2.0627911774245,33.8637293696319));
#61217=CARTESIAN_POINT('Ctrl Pts',(28.2022042605055,2.0627911774232,33.8637293696347));
#61218=CARTESIAN_POINT('Ctrl Pts',(28.2186954496616,2.05496953307227,33.8804609779984));
#61219=CARTESIAN_POINT('Ctrl Pts',(28.2349864184722,2.04724285169337,33.8969505670841));
#61220=CARTESIAN_POINT('',(28.0846211473781,1.95409846567259,33.8637293696319));
#61221=CARTESIAN_POINT('Origin',(30.,-1.32966554433622E-14,33.8637293696319));
#61222=CARTESIAN_POINT('Ctrl Pts',(28.0975494843397,1.92019745657863,33.8969505670841));
#61223=CARTESIAN_POINT('Ctrl Pts',(28.0911247964223,1.9370444342032,33.8804609779983));
#61224=CARTESIAN_POINT('Ctrl Pts',(28.0846211473792,1.95409846566974,33.8637293696347));
#61225=CARTESIAN_POINT('',(28.0459015343274,1.91537885262192,33.8637293696319));
#61226=CARTESIAN_POINT('Ctrl Pts',(28.0459015343303,1.91537885262084,33.8637293696347));
#61227=CARTESIAN_POINT('Ctrl Pts',(28.0629555657968,1.90887520357776,33.8804609779983));
#61228=CARTESIAN_POINT('Ctrl Pts',(28.0798025434214,1.90245051566032,33.8969505670841));
#61229=CARTESIAN_POINT('',(27.9372088225755,1.79779573949736,33.8637293696319));
#61230=CARTESIAN_POINT('Origin',(30.,-1.32966554433622E-14,33.8637293696319));
#61231=CARTESIAN_POINT('Ctrl Pts',(27.9527571483066,1.76501358152779,33.8969505670841));
#61232=CARTESIAN_POINT('Ctrl Pts',(27.9450304669277,1.78130455033841,33.8804609779983));
#61233=CARTESIAN_POINT('Ctrl Pts',(27.9372088225768,1.79779573949458,33.8637293696347));
#61234=CARTESIAN_POINT('',(27.9016464749967,1.75615758026483,33.8637293696319));
#61235=CARTESIAN_POINT('Ctrl Pts',(27.9016464749997,1.75615758026397,33.8637293696347));
#61236=CARTESIAN_POINT('Ctrl Pts',(27.9191582050016,1.75101202368779,33.8804609779983));
#61237=CARTESIAN_POINT('Ctrl Pts',(27.9364573242208,1.74592893956924,33.8969505670841));
#61238=CARTESIAN_POINT('',(27.8025142913294,1.63040900476038,33.8637293696319));
#61239=CARTESIAN_POINT('Origin',(30.,-1.32966554433622E-14,33.8637293696319));
#61240=CARTESIAN_POINT('Ctrl Pts',(27.8205867452316,1.59894781082027,33.8969505670841));
#61241=CARTESIAN_POINT('Ctrl Pts',(27.8116057079513,1.61458233157693,33.8804609779983));
#61242=CARTESIAN_POINT('Ctrl Pts',(27.8025142913309,1.63040900475771,33.8637293696347));
#61243=CARTESIAN_POINT('',(27.7703284629211,1.58610901244374,33.8637293696319));
#61244=CARTESIAN_POINT('Ctrl Pts',(27.7703284629241,1.58610901244311,33.8637293696347));
#61245=CARTESIAN_POINT('Ctrl Pts',(27.7881899258226,1.5823532724012,33.8804609779984));
#61246=CARTESIAN_POINT('Ctrl Pts',(27.8058345318141,1.57864313098542,33.8969505670841));
#61247=CARTESIAN_POINT('',(27.6813679902154,1.45297025634305,33.8637293696319));
#61248=CARTESIAN_POINT('Origin',(30.,-1.32966554433622E-14,33.8637293696319));
#61249=CARTESIAN_POINT('Ctrl Pts',(27.7018531496007,1.423023995155,33.8969505670841));
#61250=CARTESIAN_POINT('Ctrl Pts',(27.6916731275004,1.43790567583821,33.8804609779983));
#61251=CARTESIAN_POINT('Ctrl Pts',(27.6813679902172,1.45297025634054,33.8637293696347));
#61252=CARTESIAN_POINT('',(27.6527571173125,1.40628155512618,33.8637293696319));
#61253=CARTESIAN_POINT('Ctrl Pts',(27.6527571173155,1.40628155512578,33.8637293696347));
#61254=CARTESIAN_POINT('Ctrl Pts',(27.6708581912524,1.40393878700439,33.8804609779983));
#61255=CARTESIAN_POINT('Ctrl Pts',(27.6887394991527,1.40162446254697,33.8969505670841));
#61256=CARTESIAN_POINT('',(27.5745168264652,1.26657346313372,33.8637293696319));
#61257=CARTESIAN_POINT('Origin',(30.,-1.32966554433622E-14,33.8637293696319));
#61258=CARTESIAN_POINT('Ctrl Pts',(27.5972883935138,1.23832676335601,33.8969505670841));
#61259=CARTESIAN_POINT('Ctrl Pts',(27.5859721498149,1.2523638534557,33.8804609779984));
#61260=CARTESIAN_POINT('Ctrl Pts',(27.5745168264671,1.26657346313129,33.8637293696347));
#61261=CARTESIAN_POINT('',(27.5496573046132,1.21778390438518,33.8637293696319));
#61262=CARTESIAN_POINT('Ctrl Pts',(27.5496573046163,1.21778390438503,33.8637293696347));
#61263=CARTESIAN_POINT('Ctrl Pts',(27.5678863904514,1.21686855212868,33.8804609779984));
#61264=CARTESIAN_POINT('Ctrl Pts',(27.5858941560511,1.21596431320949,33.8969505670841));
#61265=CARTESIAN_POINT('',(27.4826195730347,1.07236782334576,33.8637293696319));
#61266=CARTESIAN_POINT('Origin',(30.,-1.32966554433622E-14,33.8637293696319));
#61267=CARTESIAN_POINT('Ctrl Pts',(27.5075371534637,1.04599483527557,33.8969505670841));
#61268=CARTESIAN_POINT('Ctrl Pts',(27.4951544565716,1.05910079146348,33.8804609779983));
#61269=CARTESIAN_POINT('Ctrl Pts',(27.4826195730368,1.07236782334352,33.8637293696347));
#61270=CARTESIAN_POINT('',(27.4616646694525,1.02177821091942,33.8637293696319));
#61271=CARTESIAN_POINT('Ctrl Pts',(27.4616646694556,1.0217782109195,33.8637293696347));
#61272=CARTESIAN_POINT('Ctrl Pts',(27.479909378813,1.02229591797925,33.8804609779983));
#61273=CARTESIAN_POINT('Ctrl Pts',(27.4979325782492,1.0228073395319,33.8969505670841));
#61274=CARTESIAN_POINT('',(27.4062428070505,0.871550679328378,33.8637293696319));
#61275=CARTESIAN_POINT('Origin',(30.,-1.32966554433622E-14,33.8637293696319));
#61276=CARTESIAN_POINT('Ctrl Pts',(27.4331527756904,0.847214001207086,33.8969505670841));
#61277=CARTESIAN_POINT('Ctrl Pts',(27.4197799690492,0.859308020905129,33.8804609779984));
#61278=CARTESIAN_POINT('Ctrl Pts',(27.4062428070528,0.871550679326332,33.8637293696347));
#61279=CARTESIAN_POINT('',(27.3893217156869,0.819472915007596,33.8637293696319));
#61280=CARTESIAN_POINT('Ctrl Pts',(27.3893217156899,0.819472915007932,33.8637293696347));
#61281=CARTESIAN_POINT('Ctrl Pts',(27.4074695638695,0.821420489547589,33.8804609779983));
#61282=CARTESIAN_POINT('Ctrl Pts',(27.4253970781241,0.823344418488154,33.8969505670841));
#61283=CARTESIAN_POINT('',(27.3458574166725,0.665360135552929,33.8637293696319));
#61284=CARTESIAN_POINT('Origin',(30.,-1.32966554433622E-14,33.8637293696319));
#61285=CARTESIAN_POINT('Ctrl Pts',(27.3745938646183,0.643209811093841,33.8969505670841));
#61286=CARTESIAN_POINT('Ctrl Pts',(27.3603133960278,0.654217330648928,33.8804609779983));
#61287=CARTESIAN_POINT('Ctrl Pts',(27.3458574166749,0.665360135551045,33.8637293696347));
#61288=CARTESIAN_POINT('',(27.3330744616826,0.612115296072357,33.8637293696319));
#61289=CARTESIAN_POINT('Ctrl Pts',(27.3330744616856,0.612115296072913,33.8637293696347));
#61290=CARTESIAN_POINT('Ctrl Pts',(27.3510135611686,0.615480730647817,33.8804609779983));
#61291=CARTESIAN_POINT('Ctrl Pts',(27.3687348611549,0.618805305314613,33.8969505670841));
#61292=CARTESIAN_POINT('',(27.3018356979128,0.455067425287102,33.8637293696319));
#61293=CARTESIAN_POINT('Origin',(30.,-1.32966554433622E-14,33.8637293696319));
#61294=CARTESIAN_POINT('Ctrl Pts',(27.332221455407,0.435240018606297,33.8969505670841));
#61295=CARTESIAN_POINT('Ctrl Pts',(27.3171213687048,0.445093172999983,33.8804609779983));
#61296=CARTESIAN_POINT('Ctrl Pts',(27.3018356979154,0.455067425285416,33.8637293696347));
#61297=CARTESIAN_POINT('',(27.2932696904648,0.400983782787843,33.8637293696319));
#61298=CARTESIAN_POINT('Ctrl Pts',(27.2932696904678,0.40098378278865,33.8637293696347));
#61299=CARTESIAN_POINT('Ctrl Pts',(27.3108894407404,0.405746328375518,33.8804609779983));
#61300=CARTESIAN_POINT('Ctrl Pts',(27.328295268751,0.410451051660182,33.8969505670841));
#61301=CARTESIAN_POINT('',(27.2744490593061,0.241969073019103,33.8637293696319));
#61302=CARTESIAN_POINT('Origin',(30.,-1.32966554433622E-14,33.8637293696319));
#61303=CARTESIAN_POINT('Ctrl Pts',(27.3062967880495,0.224586826672042,33.8969505670841));
#61304=CARTESIAN_POINT('Ctrl Pts',(27.2904701802914,0.233224867930985,33.8804609779983));
#61305=CARTESIAN_POINT('Ctrl Pts',(27.2744490593088,0.24196907301762,33.8637293696347));
#61306=CARTESIAN_POINT('',(27.2701528116845,0.1873800711418,33.8637293696319));
#61307=CARTESIAN_POINT('Ctrl Pts',(27.2701528116874,0.187380071142834,33.8637293696347));
#61308=CARTESIAN_POINT('Ctrl Pts',(27.2873445811301,0.193510365064418,33.8804609779983));
#61309=CARTESIAN_POINT('Ctrl Pts',(27.3043276244473,0.199566230783421,33.8969505670841));
#61310=CARTESIAN_POINT('',(27.2638663485864,0.0273789009530583,33.8637293696319));
#61311=CARTESIAN_POINT('Origin',(30.,-1.32966554433622E-14,33.8637293696319));
#61312=CARTESIAN_POINT('Ctrl Pts',(27.2969796967408,0.0125489822686371,
33.8969505670841));
#61313=CARTESIAN_POINT('Ctrl Pts',(27.2805241442266,0.0199186539960461,
33.8804609779983));
#61314=CARTESIAN_POINT('Ctrl Pts',(27.2638663485892,0.0273789009517924,
33.8637293696347));
#61315=CARTESIAN_POINT('',(27.2638663485864,-0.0273789009530277,33.8637293696319));
#61316=CARTESIAN_POINT('Ctrl Pts',(27.2638663485892,-0.0273789009517733,
33.8637293696347));
#61317=CARTESIAN_POINT('Ctrl Pts',(27.2805241442266,-0.0199186539960275,
33.8804609779983));
#61318=CARTESIAN_POINT('Ctrl Pts',(27.2969796967409,-0.012548982268619,
33.8969505670841));
#61319=CARTESIAN_POINT('',(27.2701528116845,-0.18738007114177,33.8637293696319));
#61320=CARTESIAN_POINT('Origin',(30.,-1.32966554433622E-14,33.8637293696319));
#61321=CARTESIAN_POINT('',(27.3043276244395,-0.199566230780611,33.8969505670765));
#61322=CARTESIAN_POINT('Ctrl Pts',(27.3043276244473,-0.199566230783401,
33.8969505670841));
#61323=CARTESIAN_POINT('Ctrl Pts',(27.2873445811301,-0.193510365064398,
33.8804609779983));
#61324=CARTESIAN_POINT('Ctrl Pts',(27.2701528116874,-0.187380071142813,
33.8637293696347));
#61325=CARTESIAN_POINT('',(27.3062967880422,-0.224586826675978,33.8969505670765));
#61326=CARTESIAN_POINT('Origin',(27.2996925411099,-0.212518788369432,33.8912937927564));
#61327=CARTESIAN_POINT('',(27.2744490593061,-0.241969073019072,33.8637293696319));
#61328=CARTESIAN_POINT('Ctrl Pts',(27.2744490593088,-0.241969073017592,
33.8637293696347));
#61329=CARTESIAN_POINT('Ctrl Pts',(27.2904701802914,-0.233224867930958,
33.8804609779983));
#61330=CARTESIAN_POINT('Ctrl Pts',(27.3062967880495,-0.224586826672017,
33.8969505670841));
#61331=CARTESIAN_POINT('',(27.2932696904648,-0.400983782787811,33.8637293696319));
#61332=CARTESIAN_POINT('Origin',(30.,-1.32966554433622E-14,33.8637293696319));
#61333=CARTESIAN_POINT('',(27.328295268743,-0.410451051657984,33.8969505670765));
#61334=CARTESIAN_POINT('Ctrl Pts',(27.328295268751,-0.410451051660133,33.8969505670841));
#61335=CARTESIAN_POINT('Ctrl Pts',(27.3108894407404,-0.40574632837547,33.8804609779983));
#61336=CARTESIAN_POINT('Ctrl Pts',(27.2932696904678,-0.400983782788603,
33.8637293696347));
#61337=CARTESIAN_POINT('',(27.3322214554001,-0.435240018610796,33.8969505670765));
#61338=CARTESIAN_POINT('Origin',(27.3246909766178,-0.423727307748468,33.8912940899386));
#61339=CARTESIAN_POINT('',(27.3018356979128,-0.45506742528707,33.8637293696319));
#61340=CARTESIAN_POINT('Ctrl Pts',(27.3018356979154,-0.455067425285398,
33.8637293696347));
#61341=CARTESIAN_POINT('Ctrl Pts',(27.3171213687048,-0.445093172999969,
33.8804609779984));
#61342=CARTESIAN_POINT('Ctrl Pts',(27.332221455407,-0.435240018606285,33.8969505670841));
#61343=CARTESIAN_POINT('',(27.3330744616826,-0.612115296072328,33.8637293696319));
#61344=CARTESIAN_POINT('Origin',(30.,-1.32966554433622E-14,33.8637293696319));
#61345=CARTESIAN_POINT('',(27.3687348611467,-0.618805305313063,33.8969505670765));
#61346=CARTESIAN_POINT('Ctrl Pts',(27.3687348611549,-0.618805305314591,
33.8969505670841));
#61347=CARTESIAN_POINT('Ctrl Pts',(27.3510135611686,-0.615480730647799,
33.8804609779983));
#61348=CARTESIAN_POINT('Ctrl Pts',(27.3330744616856,-0.6121152960729,33.8637293696347));
#61349=CARTESIAN_POINT('',(27.3745938646118,-0.643209811098888,33.8969505670765));
#61350=CARTESIAN_POINT('Origin',(27.3661835083535,-0.632323382398592,33.8912943077151));
#61351=CARTESIAN_POINT('',(27.3458574166725,-0.665360135552901,33.8637293696319));
#61352=CARTESIAN_POINT('Ctrl Pts',(27.345857416675,-0.665360135551053,33.8637293696347));
#61353=CARTESIAN_POINT('Ctrl Pts',(27.3603133960278,-0.654217330648938,
33.8804609779984));
#61354=CARTESIAN_POINT('Ctrl Pts',(27.3745938646183,-0.643209811093851,
33.8969505670841));
#61355=CARTESIAN_POINT('',(27.3893217156868,-0.819472915007569,33.8637293696319));
#61356=CARTESIAN_POINT('Origin',(30.,-1.32966554433622E-14,33.8637293696319));
#61357=CARTESIAN_POINT('',(27.4253970781159,-0.823344418487241,33.8969505670765));
#61358=CARTESIAN_POINT('Ctrl Pts',(27.4253970781241,-0.823344418488121,
33.8969505670841));
#61359=CARTESIAN_POINT('Ctrl Pts',(27.4074695638695,-0.821420489547552,
33.8804609779983));
#61360=CARTESIAN_POINT('Ctrl Pts',(27.3893217156899,-0.819472915007892,
33.8637293696347));
#61361=CARTESIAN_POINT('',(27.4331527756843,-0.847214001212589,33.8969505670765));
#61362=CARTESIAN_POINT('Origin',(27.4239143438363,-0.837020957758988,33.8912944725679));
#61363=CARTESIAN_POINT('',(27.4062428070504,-0.871550679328351,33.8637293696319));
#61364=CARTESIAN_POINT('Ctrl Pts',(27.4062428070527,-0.871550679326329,
33.8637293696347));
#61365=CARTESIAN_POINT('Ctrl Pts',(27.4197799690492,-0.859308020905111,
33.8804609779983));
#61366=CARTESIAN_POINT('Ctrl Pts',(27.4331527756904,-0.847214001207053,
33.8969505670841));
#61367=CARTESIAN_POINT('',(27.4616646694525,-1.02177821091939,33.8637293696319));
#61368=CARTESIAN_POINT('Origin',(30.,-1.32966554433622E-14,33.8637293696319));
#61369=CARTESIAN_POINT('',(27.4979325782409,-1.02280733953164,33.8969505670765));
#61370=CARTESIAN_POINT('Ctrl Pts',(27.4979325782492,-1.02280733953187,33.8969505670841));
#61371=CARTESIAN_POINT('Ctrl Pts',(27.479909378813,-1.02229591797922,33.8804609779983));
#61372=CARTESIAN_POINT('Ctrl Pts',(27.4616646694556,-1.02177821091947,33.8637293696347));
#61373=CARTESIAN_POINT('',(27.507537153458,-1.04599483528157,33.8969505670765));
#61374=CARTESIAN_POINT('Origin',(27.4975275671491,-1.03655801106889,33.8912946002427));
#61375=CARTESIAN_POINT('',(27.4826195730347,-1.07236782334573,33.8637293696319));
#61376=CARTESIAN_POINT('Ctrl Pts',(27.4826195730368,-1.07236782334351,33.8637293696347));
#61377=CARTESIAN_POINT('Ctrl Pts',(27.4951544565716,-1.05910079146347,33.8804609779983));
#61378=CARTESIAN_POINT('Ctrl Pts',(27.5075371534637,-1.04599483527557,33.8969505670841));
#61379=CARTESIAN_POINT('',(27.5496573046131,-1.21778390438516,33.8637293696319));
#61380=CARTESIAN_POINT('Origin',(30.,-1.32966554433622E-14,33.8637293696319));
#61381=CARTESIAN_POINT('',(27.5858941560428,-1.21596431320988,33.8969505670765));
#61382=CARTESIAN_POINT('Ctrl Pts',(27.5858941560511,-1.21596431320946,33.8969505670841));
#61383=CARTESIAN_POINT('Ctrl Pts',(27.5678863904513,-1.21686855212866,33.8804609779983));
#61384=CARTESIAN_POINT('Ctrl Pts',(27.5496573046162,-1.217783904385,33.8637293696347));
#61385=CARTESIAN_POINT('',(27.5972883935086,-1.23832676336246,33.8969505670765));
#61386=CARTESIAN_POINT('Origin',(27.5865693373251,-1.22970433386023,33.891294700665));
#61387=CARTESIAN_POINT('',(27.5745168264651,-1.2665734631337,33.8637293696319));
#61388=CARTESIAN_POINT('Ctrl Pts',(27.574516826467,-1.26657346313129,33.8637293696347));
#61389=CARTESIAN_POINT('Ctrl Pts',(27.5859721498149,-1.2523638534557,33.8804609779983));
#61390=CARTESIAN_POINT('Ctrl Pts',(27.5972883935138,-1.23832676335601,33.8969505670841));
#61391=CARTESIAN_POINT('',(27.6527571173125,-1.40628155512615,33.8637293696319));
#61392=CARTESIAN_POINT('Origin',(30.,-1.32966554433622E-14,33.8637293696319));
#61393=CARTESIAN_POINT('',(27.6887394991444,-1.40162446254801,33.8969505670765));
#61394=CARTESIAN_POINT('Ctrl Pts',(27.6887394991526,-1.40162446254695,33.8969505670841));
#61395=CARTESIAN_POINT('Ctrl Pts',(27.6708581912523,-1.40393878700437,33.8804609779983));
#61396=CARTESIAN_POINT('Ctrl Pts',(27.6527571173155,-1.40628155512576,33.8637293696347));
#61397=CARTESIAN_POINT('',(27.701853149596,-1.42302399516179,33.8969505670765));
#61398=CARTESIAN_POINT('Origin',(27.6904906884452,-1.4152691174526,33.8912947803756));
#61399=CARTESIAN_POINT('',(27.6813679902154,-1.45297025634303,33.8637293696319));
#61400=CARTESIAN_POINT('Ctrl Pts',(27.6813679902171,-1.4529702563405,33.8637293696347));
#61401=CARTESIAN_POINT('Ctrl Pts',(27.6916731275004,-1.43790567583818,33.8804609779983));
#61402=CARTESIAN_POINT('Ctrl Pts',(27.7018531496007,-1.42302399515497,33.8969505670841));
#61403=CARTESIAN_POINT('',(27.770328462921,-1.58610901244372,33.8637293696319));
#61404=CARTESIAN_POINT('Origin',(30.,-1.32966554433622E-14,33.8637293696319));
#61405=CARTESIAN_POINT('',(27.8058345318059,-1.5786431309871,33.8969505670765));
#61406=CARTESIAN_POINT('Ctrl Pts',(27.805834531814,-1.5786431309854,33.8969505670841));
#61407=CARTESIAN_POINT('Ctrl Pts',(27.7881899258225,-1.58235327240118,33.8804609779983));
#61408=CARTESIAN_POINT('Ctrl Pts',(27.770328462924,-1.5861090124431,33.8637293696347));
#61409=CARTESIAN_POINT('',(27.8205867452275,-1.59894781082744,33.8969505670765));
#61410=CARTESIAN_POINT('Origin',(27.8086509152839,-1.59210829514295,33.8912948438349));
#61411=CARTESIAN_POINT('',(27.8025142913294,-1.63040900476036,33.8637293696319));
#61412=CARTESIAN_POINT('Ctrl Pts',(27.8025142913309,-1.63040900475772,33.8637293696347));
#61413=CARTESIAN_POINT('Ctrl Pts',(27.8116057079513,-1.61458233157693,33.8804609779984));
#61414=CARTESIAN_POINT('Ctrl Pts',(27.8205867452316,-1.59894781082027,33.8969505670841));
#61415=CARTESIAN_POINT('',(27.9016464749967,-1.75615758026481,33.8637293696319));
#61416=CARTESIAN_POINT('Origin',(30.,-1.32966554433622E-14,33.8637293696319));
#61417=CARTESIAN_POINT('',(27.9364573242129,-1.74592893957155,33.8969505670765));
#61418=CARTESIAN_POINT('Ctrl Pts',(27.9364573242208,-1.74592893956922,33.8969505670841));
#61419=CARTESIAN_POINT('Ctrl Pts',(27.9191582050015,-1.75101202368778,33.8804609779983));
#61420=CARTESIAN_POINT('Ctrl Pts',(27.9016464749996,-1.75615758026396,33.8637293696347));
#61421=CARTESIAN_POINT('',(27.9527571483031,-1.76501358153525,33.8969505670765));
#61422=CARTESIAN_POINT('Origin',(27.9403215240917,-1.75913159602167,33.8912948941586));
#61423=CARTESIAN_POINT('',(27.9372088225755,-1.79779573949734,33.8637293696319));
#61424=CARTESIAN_POINT('Ctrl Pts',(27.9372088225768,-1.79779573949458,33.8637293696347));
#61425=CARTESIAN_POINT('Ctrl Pts',(27.9450304669278,-1.78130455033841,33.8804609779984));
#61426=CARTESIAN_POINT('Ctrl Pts',(27.9527571483066,-1.76501358152779,33.8969505670841));
#61427=CARTESIAN_POINT('',(28.0459015343274,-1.91537885262191,33.8637293696319));
#61428=CARTESIAN_POINT('Origin',(30.,-1.32966554433622E-14,33.8637293696319));
#61429=CARTESIAN_POINT('',(28.0798025434136,-1.90245051566325,33.8969505670765));
#61430=CARTESIAN_POINT('Ctrl Pts',(28.0798025434214,-1.90245051566032,33.8969505670841));
#61431=CARTESIAN_POINT('Ctrl Pts',(28.0629555657968,-1.90887520357775,33.8804609779983));
#61432=CARTESIAN_POINT('Ctrl Pts',(28.0459015343303,-1.91537885262082,33.8637293696347));
#61433=CARTESIAN_POINT('',(28.0975494843367,-1.92019745658631,33.8969505670765));
#61434=CARTESIAN_POINT('Origin',(28.0846907243829,-1.91530926701236,33.891294933562));
#61435=CARTESIAN_POINT('',(28.084621147378,-1.95409846567257,33.8637293696319));
#61436=CARTESIAN_POINT('Ctrl Pts',(28.0846211473791,-1.9540984656697,33.8637293696347));
#61437=CARTESIAN_POINT('Ctrl Pts',(28.0911247964222,-1.93704443420316,33.8804609779983));
#61438=CARTESIAN_POINT('Ctrl Pts',(28.0975494843396,-1.92019745657857,33.8969505670841));
#61439=CARTESIAN_POINT('',(28.2022042605026,-2.06279117742449,33.8637293696319));
#61440=CARTESIAN_POINT('Origin',(30.,-1.32966554433622E-14,33.8637293696319));
#61441=CARTESIAN_POINT('',(28.2349864184647,-2.04724285169689,33.8969505670765));
#61442=CARTESIAN_POINT('Ctrl Pts',(28.2349864184722,-2.04724285169334,33.8969505670841));
#61443=CARTESIAN_POINT('Ctrl Pts',(28.2186954496616,-2.05496953307223,33.8804609779983));
#61444=CARTESIAN_POINT('Ctrl Pts',(28.2022042605054,-2.06279117742317,33.8637293696347));
#61445=CARTESIAN_POINT('',(28.2540710604284,-2.06354267578707,33.8969505670765));
#61446=CARTESIAN_POINT('Origin',(28.2408684341297,-2.05967842174595,33.8912949636253));
#61447=CARTESIAN_POINT('',(28.2438424197351,-2.09835352500325,33.8637293696319));
#61448=CARTESIAN_POINT('Ctrl Pts',(28.243842419736,-2.09835352500031,33.8637293696347));
#61449=CARTESIAN_POINT('Ctrl Pts',(28.2489879763122,-2.08084179499844,33.8804609779983));
#61450=CARTESIAN_POINT('Ctrl Pts',(28.2540710604307,-2.06354267577914,33.8969505670841));
#61451=CARTESIAN_POINT('',(28.3695909952396,-2.19748570867058,33.8637293696319));
#61452=CARTESIAN_POINT('Origin',(30.,-1.32966554433622E-14,33.8637293696319));
#61453=CARTESIAN_POINT('',(28.4010521891725,-2.17941325477249,33.8969505670765));
#61454=CARTESIAN_POINT('Ctrl Pts',(28.4010521891797,-2.17941325476838,33.8969505670841));
#61455=CARTESIAN_POINT('Ctrl Pts',(28.385417668423,-2.18839429204864,33.8804609779983));
#61456=CARTESIAN_POINT('Ctrl Pts',(28.3695909952423,-2.19748570866905,33.8637293696347));
#61457=CARTESIAN_POINT('',(28.4213568690129,-2.19416546819403,33.8969505670765));
#61458=CARTESIAN_POINT('Origin',(28.4078917675746,-2.19134897714168,33.8912949854673));
#61459=CARTESIAN_POINT('',(28.4138909875562,-2.22967153707893,33.8637293696319));
#61460=CARTESIAN_POINT('Ctrl Pts',(28.4138909875569,-2.22967153707595,33.8637293696347));
#61461=CARTESIAN_POINT('Ctrl Pts',(28.4176467275988,-2.21181007417744,33.8804609779984));
#61462=CARTESIAN_POINT('Ctrl Pts',(28.4213568690146,-2.19416546818595,33.8969505670841));
#61463=CARTESIAN_POINT('',(28.5470297436569,-2.31863200978456,33.8637293696319));
#61464=CARTESIAN_POINT('Origin',(30.,-1.32966554433622E-14,33.8637293696319));
#61465=CARTESIAN_POINT('',(28.5769760048382,-2.29814685040397,33.8969505670765));
#61466=CARTESIAN_POINT('Ctrl Pts',(28.576976004845,-2.29814685039931,33.8969505670841));
#61467=CARTESIAN_POINT('Ctrl Pts',(28.5620943241618,-2.30832687249962,33.8804609779983));
#61468=CARTESIAN_POINT('Ctrl Pts',(28.5470297436595,-2.31863200978285,33.8637293696347));
#61469=CARTESIAN_POINT('',(28.5983755374519,-2.31126050085552,33.8969505670765));
#61470=CARTESIAN_POINT('Origin',(28.5847309718512,-2.30950914111276,33.891294999854));
#61471=CARTESIAN_POINT('',(28.5937184448738,-2.3472428826875,33.8637293696319));
#61472=CARTESIAN_POINT('Ctrl Pts',(28.5937184448742,-2.34724288268445,33.8637293696347));
#61473=CARTESIAN_POINT('Ctrl Pts',(28.5960612129955,-2.32914180874762,33.8804609779983));
#61474=CARTESIAN_POINT('Ctrl Pts',(28.598375537453,-2.31126050084731,33.8969505670841));
#61475=CARTESIAN_POINT('',(28.7334265368663,-2.42548317353484,33.8637293696319));
#61476=CARTESIAN_POINT('Origin',(30.,-1.32966554433622E-14,33.8637293696319));
#61477=CARTESIAN_POINT('',(28.7616732366375,-2.40271160649133,33.8969505670765));
#61478=CARTESIAN_POINT('Ctrl Pts',(28.761673236644,-2.40271160648615,33.8969505670841));
#61479=CARTESIAN_POINT('Ctrl Pts',(28.7476361465443,-2.41402785018505,33.8804609779983));
#61480=CARTESIAN_POINT('Ctrl Pts',(28.7334265368687,-2.42548317353292,33.8637293696347));
#61481=CARTESIAN_POINT('',(28.7840356867901,-2.41410584395713,33.8969505670765));
#61482=CARTESIAN_POINT('Origin',(28.7702957758346,-2.41343041757033,33.8912950072666));
#61483=CARTESIAN_POINT('',(28.7822160956148,-2.45034269538683,33.8637293696319));
#61484=CARTESIAN_POINT('Ctrl Pts',(28.782216095615,-2.45034269538378,33.8637293696347));
#61485=CARTESIAN_POINT('Ctrl Pts',(28.7831314478713,-2.43211360954867,33.8804609779983));
#61486=CARTESIAN_POINT('Ctrl Pts',(28.7840356867905,-2.41410584394888,33.8969505670841));
#61487=CARTESIAN_POINT('',(28.9276321766542,-2.51738042696528,33.8637293696319));
#61488=CARTESIAN_POINT('Origin',(30.,-1.32966554433622E-14,33.8637293696319));
#61489=CARTESIAN_POINT('',(28.9540051647184,-2.49246284654199,33.8969505670765));
#61490=CARTESIAN_POINT('Ctrl Pts',(28.9540051647244,-2.49246284653629,33.8969505670841));
#61491=CARTESIAN_POINT('Ctrl Pts',(28.9408992085365,-2.50484554342835,33.8804609779984));
#61492=CARTESIAN_POINT('Ctrl Pts',(28.9276321766564,-2.51738042696316,33.8637293696347));
#61493=CARTESIAN_POINT('',(28.9771926604683,-2.50206742175908,33.8969505670765));
#61494=CARTESIAN_POINT('Origin',(28.9634421120889,-2.50247209787259,33.8912950079413));
#61495=CARTESIAN_POINT('',(28.9782217890806,-2.53833533054747,33.8637293696319));
#61496=CARTESIAN_POINT('Ctrl Pts',(28.9782217890805,-2.53833533054441,33.8637293696347));
#61497=CARTESIAN_POINT('Ctrl Pts',(28.9777040820207,-2.52009062118697,33.8804609779983));
#61498=CARTESIAN_POINT('Ctrl Pts',(28.9771926604681,-2.50206742175082,33.8969505670841));
#61499=CARTESIAN_POINT('',(29.1284493206716,-2.59375719294953,33.8637293696319));
#61500=CARTESIAN_POINT('Origin',(30.,-1.32966554433622E-14,33.8637293696319));
#61501=CARTESIAN_POINT('',(29.1527859987874,-2.56684722431572,33.8969505670765));
#61502=CARTESIAN_POINT('Ctrl Pts',(29.1527859987929,-2.56684722430957,33.8969505670841));
#61503=CARTESIAN_POINT('Ctrl Pts',(29.1406919790949,-2.58022003095078,33.8804609779984));
#61504=CARTESIAN_POINT('Ctrl Pts',(29.1284493206736,-2.59375719294726,33.8637293696347));
#61505=CARTESIAN_POINT('',(29.1766555815127,-2.57460292188404,33.8969505670765));
#61506=CARTESIAN_POINT('Origin',(29.1629791704777,-2.57608521103258,33.8912950018861));
#61507=CARTESIAN_POINT('',(29.1805270849924,-2.61067828431313,33.8637293696319));
#61508=CARTESIAN_POINT('Ctrl Pts',(29.1805270849921,-2.61067828431009,33.8637293696347));
#61509=CARTESIAN_POINT('Ctrl Pts',(29.1785795104524,-2.59253043613049,33.8804609779983));
#61510=CARTESIAN_POINT('Ctrl Pts',(29.1766555815118,-2.57460292187582,33.8969505670841));
#61511=CARTESIAN_POINT('',(29.334639864447,-2.65414258332747,33.8637293696319));
#61512=CARTESIAN_POINT('Origin',(30.,-1.32966554433622E-14,33.8637293696319));
#61513=CARTESIAN_POINT('',(29.3567901889011,-2.62540613538822,33.8969505670765));
#61514=CARTESIAN_POINT('Ctrl Pts',(29.3567901889061,-2.62540613538166,33.8969505670841));
#61515=CARTESIAN_POINT('Ctrl Pts',(29.345782669351,-2.63968660397217,33.8804609779983));
#61516=CARTESIAN_POINT('Ctrl Pts',(29.3346398644489,-2.65414258332506,33.8637293696347));
#61517=CARTESIAN_POINT('',(29.3811946946869,-2.63126513885324,33.8969505670765));
#61518=CARTESIAN_POINT('Origin',(29.3676767399569,-2.63381590833404,33.8912949888765));
#61519=CARTESIAN_POINT('',(29.3878847039276,-2.66692553831738,33.8637293696319));
#61520=CARTESIAN_POINT('Ctrl Pts',(29.3878847039271,-2.66692553831437,33.8637293696347));
#61521=CARTESIAN_POINT('Ctrl Pts',(29.3845192693522,-2.64898643883142,33.8804609779983));
#61522=CARTESIAN_POINT('Ctrl Pts',(29.3811946946854,-2.63126513884512,33.8969505670841));
#61523=CARTESIAN_POINT('',(29.5449325747129,-2.69816430208721,33.8637293696319));
#61524=CARTESIAN_POINT('Origin',(30.,-1.32966554433622E-14,33.8637293696319));
#61525=CARTESIAN_POINT('',(29.5647599813891,-2.66777854459992,33.8969505670765));
#61526=CARTESIAN_POINT('Ctrl Pts',(29.5647599813936,-2.667778544593,33.8969505670841));
#61527=CARTESIAN_POINT('Ctrl Pts',(29.554906827,-2.68287863129519,33.8804609779983));
#61528=CARTESIAN_POINT('Ctrl Pts',(29.5449325747145,-2.69816430208464,33.8637293696347));
#61529=CARTESIAN_POINT('',(29.589548948342,-2.67170473125696,33.8969505670765));
#61530=CARTESIAN_POINT('Origin',(29.5762727932907,-2.67530826149246,33.8912949684251));
#61531=CARTESIAN_POINT('',(29.5990162172121,-2.70673030953517,33.8637293696319));
#61532=CARTESIAN_POINT('Ctrl Pts',(29.5990162172114,-2.70673030953221,33.8637293696347));
#61533=CARTESIAN_POINT('Ctrl Pts',(29.5942536716245,-2.68911055925957,33.8804609779984));
#61534=CARTESIAN_POINT('Ctrl Pts',(29.5895489483398,-2.67170473124899,33.8969505670841));
#61535=CARTESIAN_POINT('',(29.7580309269809,-2.72555094069392,33.8637293696319));
#61536=CARTESIAN_POINT('Origin',(30.,-1.32966554433622E-14,33.8637293696319));
#61537=CARTESIAN_POINT('',(29.775413173324,-2.69370321195777,33.8969505670765));
#61538=CARTESIAN_POINT('Ctrl Pts',(29.7754131733279,-2.6937032119505,33.8969505670841));
#61539=CARTESIAN_POINT('Ctrl Pts',(29.766775132069,-2.70952981970859,33.8804609779984));
#61540=CARTESIAN_POINT('Ctrl Pts',(29.7580309269823,-2.72555094069122,33.8637293696347));
#61541=CARTESIAN_POINT('',(29.8004337692193,-2.6956723755605,33.8969505670765));
#61542=CARTESIAN_POINT('Origin',(29.7874812679387,-2.70030645711978,33.8912949397144));
#61543=CARTESIAN_POINT('',(29.8126199288582,-2.72984718831551,33.8637293696319));
#61544=CARTESIAN_POINT('Ctrl Pts',(29.8126199288571,-2.72984718831264,33.8637293696347));
#61545=CARTESIAN_POINT('Ctrl Pts',(29.8064896349355,-2.7126554188699,33.8804609779983));
#61546=CARTESIAN_POINT('Ctrl Pts',(29.8004337692165,-2.69567237555272,33.8969505670841));
#61547=CARTESIAN_POINT('',(29.9726210990469,-2.73613365141358,33.8637293696319));
#61548=CARTESIAN_POINT('Origin',(30.,-1.32966554433622E-14,33.8637293696319));
#61549=CARTESIAN_POINT('',(29.987451017728,-2.70302030326669,33.8969505670765));
#61550=CARTESIAN_POINT('Ctrl Pts',(29.9874510177314,-2.70302030325915,33.8969505670841));
#61551=CARTESIAN_POINT('Ctrl Pts',(29.980081346004,-2.71947585577343,33.8804609779983));
#61552=CARTESIAN_POINT('Ctrl Pts',(29.9726210990482,-2.73613365141081,33.8637293696347));
#61553=CARTESIAN_POINT('Ctrl Pts',(30.,-2.69489040503949,33.9051095949605));
#61554=CARTESIAN_POINT('Ctrl Pts',(29.9982996971592,-2.69489040503949,33.9051095949605));
#61555=CARTESIAN_POINT('Ctrl Pts',(29.9965490639354,-2.69522714758869,33.9047710768107));
#61556=CARTESIAN_POINT('Ctrl Pts',(29.9934248389279,-2.69644647069985,33.9035459832655));
#61557=CARTESIAN_POINT('Ctrl Pts',(29.9920523583067,-2.69733049287042,33.9026580100842));
#61558=CARTESIAN_POINT('Ctrl Pts',(29.9894391186861,-2.69960157002983,33.9003782103613));
#61559=CARTESIAN_POINT('Ctrl Pts',(29.9882404972758,-2.7012574944688,33.8987170220582));
#61560=CARTESIAN_POINT('Ctrl Pts',(29.987451017728,-2.7030203032667,33.8969505670765));
#61561=CARTESIAN_POINT('',(30.,-2.73627063036813,33.8637293696319));
#61562=CARTESIAN_POINT('Origin',(30.,-1.32966554433622E-14,31.5762293696319));
#61563=CARTESIAN_POINT('',(30.012548982272,2.70302030326666,31.5905494329235));
#61564=CARTESIAN_POINT('',(30.,2.69489040503946,31.5823904050395));
#61565=CARTESIAN_POINT('Ctrl Pts',(30.012548982272,2.70302030326668,31.5905494329235));
#61566=CARTESIAN_POINT('Ctrl Pts',(30.0117595027242,2.70125749446877,31.5887829779419));
#61567=CARTESIAN_POINT('Ctrl Pts',(30.0105608813139,2.6996015700298,31.5871217896387));
#61568=CARTESIAN_POINT('Ctrl Pts',(30.0079476416933,2.69733049287039,31.5848419899159));
#61569=CARTESIAN_POINT('Ctrl Pts',(30.0065751610721,2.69644647069982,31.5839540167345));
#61570=CARTESIAN_POINT('Ctrl Pts',(30.0034509360646,2.69522714758867,31.5827289231894));
#61571=CARTESIAN_POINT('Ctrl Pts',(30.0017003028408,2.69489040503946,31.5823904050395));
#61572=CARTESIAN_POINT('Ctrl Pts',(30.,2.69489040503946,31.5823904050395));
#61573=CARTESIAN_POINT('',(30.0273789009535,2.73613365141461,31.6237706303691));
#61574=CARTESIAN_POINT('Ctrl Pts',(30.0273789009505,2.73613365140797,31.6237706303625));
#61575=CARTESIAN_POINT('Ctrl Pts',(30.0199186539932,2.71947585576695,31.6070390219952));
#61576=CARTESIAN_POINT('Ctrl Pts',(30.0125489822642,2.70302030324912,31.5905494329059));
#61577=CARTESIAN_POINT('',(30.1873800711414,2.72984718831658,31.6237706303691));
#61578=CARTESIAN_POINT('Origin',(30.,-1.32966554433622E-14,31.6237706303681));
#61579=CARTESIAN_POINT('',(30.1995662307806,2.69567237556048,31.5905494329235));
#61580=CARTESIAN_POINT('Ctrl Pts',(30.1995662307774,2.69567237556935,31.5905494329321));
#61581=CARTESIAN_POINT('Ctrl Pts',(30.1935103650619,2.71265541887687,31.6070390220085));
#61582=CARTESIAN_POINT('Ctrl Pts',(30.1873800711438,2.72984718830972,31.6237706303625));
#61583=CARTESIAN_POINT('',(30.224586826676,2.69370321195774,31.5905494329235));
#61584=CARTESIAN_POINT('Origin',(30.2125187883694,2.70030745889013,31.5962062072437));
#61585=CARTESIAN_POINT('',(30.2419690730196,2.72555094069491,31.6237706303691));
#61586=CARTESIAN_POINT('Ctrl Pts',(30.2419690730161,2.72555094068852,31.6237706303625));
#61587=CARTESIAN_POINT('Ctrl Pts',(30.2332248679276,2.70952981970239,31.6070390219952));
#61588=CARTESIAN_POINT('Ctrl Pts',(30.2245868266668,2.69370321194088,31.5905494329059));
#61589=CARTESIAN_POINT('',(30.4009837827875,2.70673030953627,31.6237706303691));
#61590=CARTESIAN_POINT('Origin',(30.,-1.32966554433622E-14,31.6237706303681));
#61591=CARTESIAN_POINT('',(30.410451051658,2.67170473125694,31.5905494329235));
#61592=CARTESIAN_POINT('Ctrl Pts',(30.4104510516555,2.67170473126603,31.5905494329321));
#61593=CARTESIAN_POINT('Ctrl Pts',(30.4057463283736,2.68911055926674,31.6070390220085));
#61594=CARTESIAN_POINT('Ctrl Pts',(30.4009837827894,2.70673030952925,31.6237706303625));
#61595=CARTESIAN_POINT('',(30.4352400186108,2.66777854459989,31.5905494329235));
#61596=CARTESIAN_POINT('Origin',(30.4237273077485,2.6753090233822,31.5962059100614));
#61597=CARTESIAN_POINT('',(30.4550674252877,2.69816430208816,31.6237706303691));
#61598=CARTESIAN_POINT('Ctrl Pts',(30.4550674252837,2.69816430208208,31.6237706303625));
#61599=CARTESIAN_POINT('Ctrl Pts',(30.4450931729961,2.68287863128927,31.6070390219952));
#61600=CARTESIAN_POINT('Ctrl Pts',(30.4352400186003,2.66777854458381,31.5905494329059));
#61601=CARTESIAN_POINT('',(30.6121152960721,2.6669255383185,31.6237706303691));
#61602=CARTESIAN_POINT('Origin',(30.,-1.32966554433622E-14,31.6237706303681));
#61603=CARTESIAN_POINT('',(30.6188053053131,2.63126513885322,31.5905494329235));
#61604=CARTESIAN_POINT('Ctrl Pts',(30.6188053053114,2.63126513886247,31.5905494329321));
#61605=CARTESIAN_POINT('Ctrl Pts',(30.6154807306465,2.64898643883871,31.6070390220085));
#61606=CARTESIAN_POINT('Ctrl Pts',(30.6121152960735,2.66692553831135,31.6237706303626));
#61607=CARTESIAN_POINT('',(30.6432098110989,2.62540613538819,31.5905494329235));
#61608=CARTESIAN_POINT('Origin',(30.6323233823986,2.63381649164648,31.5962056922849));
#61609=CARTESIAN_POINT('',(30.6653601355536,2.65414258332836,31.6237706303691));
#61610=CARTESIAN_POINT('Ctrl Pts',(30.6653601355491,2.65414258332261,31.6237706303625));
#61611=CARTESIAN_POINT('Ctrl Pts',(30.6542173306446,2.63968660396658,31.6070390219952));
#61612=CARTESIAN_POINT('Ctrl Pts',(30.6432098110871,2.62540613537299,31.5905494329059));
#61613=CARTESIAN_POINT('',(30.8194729150074,2.61067828431427,31.6237706303691));
#61614=CARTESIAN_POINT('Origin',(30.,-1.32966554433622E-14,31.6237706303681));
#61615=CARTESIAN_POINT('',(30.8233444184872,2.57460292188402,31.5905494329235));
#61616=CARTESIAN_POINT('Ctrl Pts',(30.8233444184862,2.57460292189339,31.5905494329321));
#61617=CARTESIAN_POINT('Ctrl Pts',(30.8214204895467,2.59253043613788,31.6070390220085));
#61618=CARTESIAN_POINT('Ctrl Pts',(30.8194729150082,2.61067828430704,31.6237706303625));
#61619=CARTESIAN_POINT('',(30.8472140012126,2.5668472243157,31.5905494329235));
#61620=CARTESIAN_POINT('Origin',(30.837020957759,2.57608565616362,31.596205527432));
#61621=CARTESIAN_POINT('',(30.8715506793291,2.59375719295037,31.6237706303691));
#61622=CARTESIAN_POINT('Ctrl Pts',(30.8715506793242,2.59375719294498,31.6237706303625));
#61623=CARTESIAN_POINT('Ctrl Pts',(30.8593080209003,2.58022003094555,31.6070390219952));
#61624=CARTESIAN_POINT('Ctrl Pts',(30.8472140011997,2.56684722430147,31.5905494329059));
#61625=CARTESIAN_POINT('',(31.0217782109193,2.53833533054861,31.6237706303691));
#61626=CARTESIAN_POINT('Origin',(30.,-1.32966554433622E-14,31.6237706303681));
#61627=CARTESIAN_POINT('',(31.0228073395316,2.50206742175906,31.5905494329235));
#61628=CARTESIAN_POINT('Ctrl Pts',(31.0228073395313,2.50206742176848,31.5905494329321));
#61629=CARTESIAN_POINT('Ctrl Pts',(31.022295917979,2.52009062119439,31.6070390220085));
#61630=CARTESIAN_POINT('Ctrl Pts',(31.0217782109195,2.53833533054134,31.6237706303625));
#61631=CARTESIAN_POINT('',(31.0459948352816,2.49246284654197,31.5905494329235));
#61632=CARTESIAN_POINT('Origin',(31.0365580110689,2.5024724328509,31.5962053997573));
#61633=CARTESIAN_POINT('',(31.0723678233466,2.51738042696606,31.6237706303691));
#61634=CARTESIAN_POINT('Ctrl Pts',(31.0723678233413,2.51738042696106,31.6237706303625));
#61635=CARTESIAN_POINT('Ctrl Pts',(31.0591007914584,2.50484554342351,31.6070390219952));
#61636=CARTESIAN_POINT('Ctrl Pts',(31.0459948352676,2.49246284652878,31.5905494329059));
#61637=CARTESIAN_POINT('',(31.2177839043852,2.45034269538797,31.6237706303691));
#61638=CARTESIAN_POINT('Origin',(30.,-1.32966554433622E-14,31.6237706303681));
#61639=CARTESIAN_POINT('',(31.2159643132099,2.41410584395711,31.5905494329235));
#61640=CARTESIAN_POINT('Ctrl Pts',(31.2159643132104,2.41410584396651,31.5905494329321));
#61641=CARTESIAN_POINT('Ctrl Pts',(31.216868552129,2.43211360955606,31.6070390220085));
#61642=CARTESIAN_POINT('Ctrl Pts',(31.2177839043849,2.4503426953807,31.6237706303625));
#61643=CARTESIAN_POINT('',(31.2383267633625,2.40271160649132,31.5905494329235));
#61644=CARTESIAN_POINT('Origin',(31.2297043338602,2.41343066267493,31.5962052993351));
#61645=CARTESIAN_POINT('',(31.2665734631346,2.42548317353555,31.6237706303691));
#61646=CARTESIAN_POINT('Ctrl Pts',(31.266573463129,2.42548317353098,31.6237706303625));
#61647=CARTESIAN_POINT('Ctrl Pts',(31.2523638534503,2.4140278501806,31.6070390219952));
#61648=CARTESIAN_POINT('Ctrl Pts',(31.2383267633475,2.40271160647926,31.5905494329059));
#61649=CARTESIAN_POINT('',(31.4062815551263,2.34724288268863,31.6237706303691));
#61650=CARTESIAN_POINT('Origin',(30.,-1.32966554433622E-14,31.6237706303681));
#61651=CARTESIAN_POINT('',(31.401624462548,2.3112605008555,31.5905494329235));
#61652=CARTESIAN_POINT('Ctrl Pts',(31.4016244625492,2.31126050086484,31.5905494329321));
#61653=CARTESIAN_POINT('Ctrl Pts',(31.4039387870053,2.32914180875499,31.6070390220085));
#61654=CARTESIAN_POINT('Ctrl Pts',(31.4062815551254,2.34724288268141,31.6237706303625));
#61655=CARTESIAN_POINT('',(31.4230239951618,2.29814685040396,31.5905494329235));
#61656=CARTESIAN_POINT('Origin',(31.4152691174526,2.30950931155475,31.5962052196244));
#61657=CARTESIAN_POINT('',(31.452970256344,2.3186320097852,31.6237706303691));
#61658=CARTESIAN_POINT('Ctrl Pts',(31.452970256338,2.31863200978109,31.6237706303625));
#61659=CARTESIAN_POINT('Ctrl Pts',(31.4379056758324,2.30832687249561,31.6070390219952));
#61660=CARTESIAN_POINT('Ctrl Pts',(31.4230239951459,2.2981468503931,31.5905494329059));
#61661=CARTESIAN_POINT('',(31.5861090124439,2.22967153708005,31.6237706303691));
#61662=CARTESIAN_POINT('Origin',(30.,-1.32966554433622E-14,31.6237706303681));
#61663=CARTESIAN_POINT('',(31.5786431309871,2.19416546819402,31.5905494329235));
#61664=CARTESIAN_POINT('Ctrl Pts',(31.578643130989,2.19416546820324,31.5905494329321));
#61665=CARTESIAN_POINT('Ctrl Pts',(31.5823532724027,2.21181007418469,31.6070390220085));
#61666=CARTESIAN_POINT('Ctrl Pts',(31.5861090124425,2.22967153707293,31.6237706303625));
#61667=CARTESIAN_POINT('',(31.5989478108274,2.17941325477248,31.5905494329235));
#61668=CARTESIAN_POINT('Origin',(31.5921082951429,2.19134908471604,31.596205156165));
#61669=CARTESIAN_POINT('',(31.6304090047614,2.19748570867114,31.6237706303691));
#61670=CARTESIAN_POINT('Ctrl Pts',(31.6304090047551,2.19748570866755,31.6237706303626));
#61671=CARTESIAN_POINT('Ctrl Pts',(31.6145823315708,2.18839429204514,31.6070390219952));
#61672=CARTESIAN_POINT('Ctrl Pts',(31.5989478108108,2.17941325476293,31.5905494329059));
#61673=CARTESIAN_POINT('',(31.7561575802651,2.09835352500435,31.6237706303691));
#61674=CARTESIAN_POINT('Origin',(30.,-1.32966554433622E-14,31.6237706303681));
#61675=CARTESIAN_POINT('',(31.7459289395715,2.06354267578706,31.5905494329235));
#61676=CARTESIAN_POINT('Ctrl Pts',(31.7459289395742,2.06354267579611,31.5905494329321));
#61677=CARTESIAN_POINT('Ctrl Pts',(31.7510120236898,2.08084179500558,31.6070390220085));
#61678=CARTESIAN_POINT('Ctrl Pts',(31.7561575802631,2.09835352499738,31.6237706303625));
#61679=CARTESIAN_POINT('',(31.7650135815352,2.04724285169688,31.5905494329235));
#61680=CARTESIAN_POINT('Origin',(31.7591315960216,2.05967847590828,31.5962051058414));
#61681=CARTESIAN_POINT('',(31.7977957394984,2.06279117742498,31.6237706303691));
#61682=CARTESIAN_POINT('Ctrl Pts',(31.7977957394918,2.06279117742187,31.6237706303625));
#61683=CARTESIAN_POINT('Ctrl Pts',(31.781304550332,2.05496953306921,31.6070390219952));
#61684=CARTESIAN_POINT('Ctrl Pts',(31.7650135815179,2.04724285168864,31.5905494329059));
#61685=CARTESIAN_POINT('',(31.9153788526223,1.95409846567364,31.6237706303691));
#61686=CARTESIAN_POINT('Origin',(30.,-1.32966554433622E-14,31.6237706303681));
#61687=CARTESIAN_POINT('',(31.9024505156632,1.9201974565863,31.5905494329235));
#61688=CARTESIAN_POINT('Ctrl Pts',(31.9024505156666,1.92019745659511,31.5905494329321));
#61689=CARTESIAN_POINT('Ctrl Pts',(31.9088752035804,1.93704443421013,31.6070390220085));
#61690=CARTESIAN_POINT('Ctrl Pts',(31.9153788526197,1.95409846566686,31.6237706303625));
#61691=CARTESIAN_POINT('',(31.9201974565863,1.90245051566323,31.5905494329235));
#61692=CARTESIAN_POINT('Origin',(31.9153092670123,1.91530927561703,31.596205066438));
#61693=CARTESIAN_POINT('',(31.9540984656736,1.91537885262231,31.6237706303691));
#61694=CARTESIAN_POINT('Ctrl Pts',(31.9540984656668,1.9153788526197,31.6237706303625));
#61695=CARTESIAN_POINT('Ctrl Pts',(31.9370444341966,1.90887520357521,31.6070390219952));
#61696=CARTESIAN_POINT('Ctrl Pts',(31.9201974565683,1.90245051565638,31.5905494329059));
#61697=CARTESIAN_POINT('',(32.062791177425,1.79779573949838,31.6237706303691));
#61698=CARTESIAN_POINT('Origin',(30.,-1.32966554433622E-14,31.6237706303681));
#61699=CARTESIAN_POINT('',(32.0472428516969,1.76501358153524,31.5905494329235));
#61700=CARTESIAN_POINT('Ctrl Pts',(32.0472428517009,1.76501358154374,31.5905494329321));
#61701=CARTESIAN_POINT('Ctrl Pts',(32.0549695330754,1.78130455034511,31.6070390220085));
#61702=CARTESIAN_POINT('Ctrl Pts',(32.0627911774219,1.7977957394918,31.6237706303625));
#61703=CARTESIAN_POINT('',(32.0635426757871,1.74592893957153,31.5905494329235));
#61704=CARTESIAN_POINT('Origin',(32.059678421746,1.75913156587022,31.5962050363748));
#61705=CARTESIAN_POINT('',(32.0983535250043,1.75615758026513,31.6237706303691));
#61706=CARTESIAN_POINT('Ctrl Pts',(32.0983535249974,1.75615758026307,31.6237706303625));
#61707=CARTESIAN_POINT('Ctrl Pts',(32.0808417949917,1.75101202368577,31.6070390219952));
#61708=CARTESIAN_POINT('Ctrl Pts',(32.0635426757687,1.74592893956612,31.5905494329059));
#61709=CARTESIAN_POINT('',(32.1974857086711,1.63040900476136,31.6237706303691));
#61710=CARTESIAN_POINT('Origin',(30.,-1.32966554433622E-14,31.6237706303681));
#61711=CARTESIAN_POINT('',(32.1794132547725,1.59894781082743,31.5905494329235));
#61712=CARTESIAN_POINT('Ctrl Pts',(32.1794132547772,1.59894781083559,31.5905494329321));
#61713=CARTESIAN_POINT('Ctrl Pts',(32.1883942920524,1.61458233158336,31.6070390220085));
#61714=CARTESIAN_POINT('Ctrl Pts',(32.1974857086675,1.63040900475503,31.6237706303625));
#61715=CARTESIAN_POINT('',(32.194165468194,1.57864313098709,31.5905494329235));
#61716=CARTESIAN_POINT('Origin',(32.1913489771416,1.59210823242537,31.5962050145327));
#61717=CARTESIAN_POINT('',(32.22967153708,1.58610901244395,31.6237706303691));
#61718=CARTESIAN_POINT('Ctrl Pts',(32.2296715370729,1.58610901244245,31.6237706303625));
#61719=CARTESIAN_POINT('Ctrl Pts',(32.2118100741705,1.58235327239971,31.6070390219952));
#61720=CARTESIAN_POINT('Ctrl Pts',(32.1941654681752,1.57864313098313,31.5905494329059));
#61721=CARTESIAN_POINT('',(32.3186320097852,1.45297025634397,31.6237706303691));
#61722=CARTESIAN_POINT('Origin',(30.,-1.32966554433622E-14,31.6237706303681));
#61723=CARTESIAN_POINT('',(32.298146850404,1.42302399516178,31.5905494329235));
#61724=CARTESIAN_POINT('Ctrl Pts',(32.2981468504093,1.42302399516954,31.5905494329321));
#61725=CARTESIAN_POINT('Ctrl Pts',(32.3083268725038,1.43790567584429,31.6070390220085));
#61726=CARTESIAN_POINT('Ctrl Pts',(32.3186320097811,1.45297025633794,31.6237706303625));
#61727=CARTESIAN_POINT('',(32.3112605008555,1.401624462548,31.5905494329235));
#61728=CARTESIAN_POINT('Origin',(32.3095091411128,1.41526902814876,31.596205000146));
#61729=CARTESIAN_POINT('',(32.3472428826886,1.40628155512629,31.6237706303691));
#61730=CARTESIAN_POINT('Ctrl Pts',(32.3472428826814,1.40628155512536,31.6237706303625));
#61731=CARTESIAN_POINT('Ctrl Pts',(32.3291418087406,1.40393878700346,31.6070390219952));
#61732=CARTESIAN_POINT('Ctrl Pts',(32.3112605008365,1.40162446254554,31.5905494329059));
#61733=CARTESIAN_POINT('',(32.4254831735355,1.26657346313459,31.6237706303691));
#61734=CARTESIAN_POINT('Origin',(30.,-1.32966554433622E-14,31.6237706303681));
#61735=CARTESIAN_POINT('',(32.4027116064913,1.23832676336245,31.5905494329235));
#61736=CARTESIAN_POINT('Ctrl Pts',(32.4027116064972,1.23832676336979,31.5905494329321));
#61737=CARTESIAN_POINT('Ctrl Pts',(32.4140278501897,1.2523638534615,31.6070390220085));
#61738=CARTESIAN_POINT('Ctrl Pts',(32.425483173531,1.26657346312893,31.6237706303625));
#61739=CARTESIAN_POINT('',(32.4141058439571,1.21596431320987,31.5905494329235));
#61740=CARTESIAN_POINT('Origin',(32.4134304175703,1.22970422416531,31.5962049927334));
#61741=CARTESIAN_POINT('',(32.450342695388,1.21778390438521,31.6237706303691));
#61742=CARTESIAN_POINT('Ctrl Pts',(32.4503426953807,1.21778390438485,31.6237706303625));
#61743=CARTESIAN_POINT('Ctrl Pts',(32.4321136095416,1.2168685521283,31.6070390219952));
#61744=CARTESIAN_POINT('Ctrl Pts',(32.4141058439379,1.21596431320891,31.5905494329059));
#61745=CARTESIAN_POINT('',(32.517380426966,1.07236782334656,31.6237706303691));
#61746=CARTESIAN_POINT('Origin',(30.,-1.32966554433622E-14,31.6237706303681));
#61747=CARTESIAN_POINT('',(32.492462846542,1.04599483528156,31.5905494329235));
#61748=CARTESIAN_POINT('Ctrl Pts',(32.4924628465485,1.04599483528841,31.5905494329321));
#61749=CARTESIAN_POINT('Ctrl Pts',(32.5048455434335,1.05910079146886,31.6070390220085));
#61750=CARTESIAN_POINT('Ctrl Pts',(32.5173804269611,1.07236782334125,31.6237706303625));
#61751=CARTESIAN_POINT('',(32.5020674217591,1.02280733953163,31.5905494329235));
#61752=CARTESIAN_POINT('Origin',(32.5024720978725,1.03655788791103,31.5962049920587));
#61753=CARTESIAN_POINT('',(32.5383353305486,1.02177821091935,31.6237706303691));
#61754=CARTESIAN_POINT('Ctrl Pts',(32.5383353305413,1.02177821091956,31.6237706303625));
#61755=CARTESIAN_POINT('Ctrl Pts',(32.5200906211799,1.02229591797942,31.6070390219952));
#61756=CARTESIAN_POINT('Ctrl Pts',(32.5020674217399,1.02280733953218,31.5905494329059));
#61757=CARTESIAN_POINT('',(32.5937571929504,0.87155067932912,31.6237706303691));
#61758=CARTESIAN_POINT('Origin',(30.,-1.32966554433622E-14,31.6237706303681));
#61759=CARTESIAN_POINT('',(32.5668472243157,0.84721400121258,31.5905494329235));
#61760=CARTESIAN_POINT('Ctrl Pts',(32.5668472243227,0.847214001218895,31.5905494329321));
#61761=CARTESIAN_POINT('Ctrl Pts',(32.5802200309563,0.859308020910075,31.6070390220085));
#61762=CARTESIAN_POINT('Ctrl Pts',(32.593757192945,0.871550679324244,31.6237706303625));
#61763=CARTESIAN_POINT('',(32.574602921884,0.823344418487232,31.5905494329235));
#61764=CARTESIAN_POINT('Origin',(32.5760852110325,0.837020829522203,31.5962049981138));
#61765=CARTESIAN_POINT('',(32.6106782843143,0.819472915007436,31.6237706303691));
#61766=CARTESIAN_POINT('Ctrl Pts',(32.6106782843071,0.819472915008212,31.6237706303625));
#61767=CARTESIAN_POINT('Ctrl Pts',(32.5925304361235,0.8214204895483,31.6070390219952));
#61768=CARTESIAN_POINT('Ctrl Pts',(32.5746029218649,0.823344418489286,31.5905494329059));
#61769=CARTESIAN_POINT('',(32.6541425833284,0.665360135553601,31.6237706303691));
#61770=CARTESIAN_POINT('Origin',(30.,-1.32966554433622E-14,31.6237706303681));
#61771=CARTESIAN_POINT('',(32.6254061353882,0.64320981109888,31.5905494329235));
#61772=CARTESIAN_POINT('Ctrl Pts',(32.6254061353957,0.643209811104633,31.5905494329321));
#61773=CARTESIAN_POINT('Ctrl Pts',(32.639686603978,0.654217330653466,31.6070390220085));
#61774=CARTESIAN_POINT('Ctrl Pts',(32.6541425833226,0.665360135549173,31.6237706303625));
#61775=CARTESIAN_POINT('',(32.6312651388532,0.618805305313054,31.5905494329235));
#61776=CARTESIAN_POINT('Origin',(32.633815908334,0.632323260043002,31.5962050111235));
#61777=CARTESIAN_POINT('',(32.6669255383185,0.612115296072106,31.6237706303691));
#61778=CARTESIAN_POINT('Ctrl Pts',(32.6669255383114,0.61211529607344,31.6237706303625));
#61779=CARTESIAN_POINT('Ctrl Pts',(32.6489864388245,0.61548073064908,31.6070390219952));
#61780=CARTESIAN_POINT('Ctrl Pts',(32.6312651388343,0.618805305316593,31.5905494329059));
#61781=CARTESIAN_POINT('',(32.6981643020882,0.455067425287697,31.6237706303691));
#61782=CARTESIAN_POINT('Origin',(30.,-1.32966554433622E-14,31.6237706303681));
#61783=CARTESIAN_POINT('',(32.6677785445999,0.435240018610789,31.5905494329235));
#61784=CARTESIAN_POINT('Ctrl Pts',(32.6677785446078,0.435240018615936,31.5905494329321));
#61785=CARTESIAN_POINT('Ctrl Pts',(32.6828786313014,0.44509317300403,31.6070390220085));
#61786=CARTESIAN_POINT('Ctrl Pts',(32.6981643020821,0.455067425283731,31.6237706303625));
#61787=CARTESIAN_POINT('',(32.6717047312569,0.410451051657977,31.5905494329235));
#61788=CARTESIAN_POINT('Origin',(32.6753082614925,0.423727206709275,31.596205031575));
#61789=CARTESIAN_POINT('',(32.7067303095363,0.400983782787501,31.6237706303691));
#61790=CARTESIAN_POINT('Ctrl Pts',(32.7067303095293,0.400983782789396,31.6237706303625));
#61791=CARTESIAN_POINT('Ctrl Pts',(32.6891105592528,0.405746328377311,31.6070390219952));
#61792=CARTESIAN_POINT('Ctrl Pts',(32.6717047312384,0.410451051662997,31.5905494329059));
#61793=CARTESIAN_POINT('',(32.7255509406949,0.24196907301962,31.6237706303691));
#61794=CARTESIAN_POINT('Origin',(30.,-1.32966554433622E-14,31.6237706303681));
#61795=CARTESIAN_POINT('',(32.6937032119577,0.224586826675969,31.5905494329235));
#61796=CARTESIAN_POINT('Ctrl Pts',(32.693703211966,0.224586826680493,31.5905494329321));
#61797=CARTESIAN_POINT('Ctrl Pts',(32.7095298197151,0.233224867934539,31.6070390220085));
#61798=CARTESIAN_POINT('Ctrl Pts',(32.7255509406885,0.241969073016156,31.6237706303625));
#61799=CARTESIAN_POINT('',(32.6956723755605,0.199566230780603,31.5905494329235));
#61800=CARTESIAN_POINT('Origin',(32.7003064571198,0.212518732061222,31.5962050602857));
#61801=CARTESIAN_POINT('',(32.7298471883166,0.187380071141372,31.6237706303691));
#61802=CARTESIAN_POINT('Ctrl Pts',(32.7298471883097,0.187380071143799,31.6237706303625));
#61803=CARTESIAN_POINT('Ctrl Pts',(32.7126554188632,0.193510365066728,31.6070390219952));
#61804=CARTESIAN_POINT('Ctrl Pts',(32.6956723755424,0.199566230787043,31.5905494329059));
#61805=CARTESIAN_POINT('',(32.7361336514146,0.0273789009534945,31.6237706303691));
#61806=CARTESIAN_POINT('Origin',(30.,-1.32966554433622E-14,31.6237706303681));
#61807=CARTESIAN_POINT('',(32.7030203032667,0.0125489822719939,31.5905494329235));
#61808=CARTESIAN_POINT('Ctrl Pts',(32.7030203032753,0.0125489822758371,
31.5905494329321));
#61809=CARTESIAN_POINT('Ctrl Pts',(32.7194758557802,0.0199186539990537,
31.6070390220085));
#61810=CARTESIAN_POINT('Ctrl Pts',(32.736133651408,0.0273789009505039,31.6237706303625));
#61811=CARTESIAN_POINT('',(32.7030203032667,-0.0125489822720396,31.5905494329235));
#61812=CARTESIAN_POINT('Origin',(32.7086563646858,6.24424376688964E-9,31.5962050859813));
#61813=CARTESIAN_POINT('',(32.7361336514146,-0.02737890095354,31.6237706303691));
#61814=CARTESIAN_POINT('Ctrl Pts',(32.736133651408,-0.0273789009505768,
31.6237706303625));
#61815=CARTESIAN_POINT('Ctrl Pts',(32.719475855767,-0.0199186539932038,
31.6070390219952));
#61816=CARTESIAN_POINT('Ctrl Pts',(32.7030203032491,-0.0125489822642076,
31.5905494329059));
#61817=CARTESIAN_POINT('',(32.7298471883166,-0.187380071141418,31.6237706303691));
#61818=CARTESIAN_POINT('Origin',(30.,-1.32966554433622E-14,31.6237706303681));
#61819=CARTESIAN_POINT('',(32.6956723755605,-0.199566230780649,31.5905494329235));
#61820=CARTESIAN_POINT('Ctrl Pts',(32.6956723755694,-0.199566230777489,
31.5905494329321));
#61821=CARTESIAN_POINT('Ctrl Pts',(32.7126554188769,-0.193510365061924,
31.6070390220085));
#61822=CARTESIAN_POINT('Ctrl Pts',(32.7298471883097,-0.187380071143864,
31.6237706303625));
#61823=CARTESIAN_POINT('',(32.6937032119577,-0.224586826676015,31.5905494329235));
#61824=CARTESIAN_POINT('Origin',(32.7003074588902,-0.212518788369472,31.5962062072437));
#61825=CARTESIAN_POINT('',(32.7255509406949,-0.241969073019665,31.6237706303691));
#61826=CARTESIAN_POINT('Ctrl Pts',(32.7255509406885,-0.241969073016199,
31.6237706303625));
#61827=CARTESIAN_POINT('Ctrl Pts',(32.7095298197024,-0.23322486792764,31.6070390219952));
#61828=CARTESIAN_POINT('Ctrl Pts',(32.6937032119408,-0.22458682666682,31.5905494329059));
#61829=CARTESIAN_POINT('',(32.7067303095363,-0.400983782787547,31.6237706303691));
#61830=CARTESIAN_POINT('Origin',(30.,-1.32966554433622E-14,31.6237706303681));
#61831=CARTESIAN_POINT('',(32.6717047312569,-0.410451051658023,31.5905494329235));
#61832=CARTESIAN_POINT('Ctrl Pts',(32.671704731266,-0.41045105165556,31.5905494329321));
#61833=CARTESIAN_POINT('Ctrl Pts',(32.6891105592667,-0.405746328373564,
31.6070390220085));
#61834=CARTESIAN_POINT('Ctrl Pts',(32.7067303095293,-0.40098378278943,31.6237706303625));
#61835=CARTESIAN_POINT('',(32.6677785445999,-0.435240018610835,31.5905494329235));
#61836=CARTESIAN_POINT('Origin',(32.6753090233822,-0.42372730774851,31.5962059100614));
#61837=CARTESIAN_POINT('',(32.6981643020882,-0.455067425287743,31.6237706303691));
#61838=CARTESIAN_POINT('Ctrl Pts',(32.6981643020821,-0.455067425283808,
31.6237706303625));
#61839=CARTESIAN_POINT('Ctrl Pts',(32.6828786312893,-0.445093172996188,
31.6070390219952));
#61840=CARTESIAN_POINT('Ctrl Pts',(32.6677785445838,-0.435240018600367,
31.5905494329059));
#61841=CARTESIAN_POINT('',(32.6669255383185,-0.612115296072152,31.6237706303691));
#61842=CARTESIAN_POINT('Origin',(30.,-1.32966554433622E-14,31.6237706303681));
#61843=CARTESIAN_POINT('',(32.6312651388532,-0.6188053053131,31.5905494329235));
#61844=CARTESIAN_POINT('Ctrl Pts',(32.6312651388625,-0.618805305311361,
31.5905494329321));
#61845=CARTESIAN_POINT('Ctrl Pts',(32.6489864388387,-0.615480730646455,
31.6070390220085));
#61846=CARTESIAN_POINT('Ctrl Pts',(32.6669255383114,-0.612115296073488,
31.6237706303625));
#61847=CARTESIAN_POINT('',(32.6254061353882,-0.643209811098926,31.5905494329235));
#61848=CARTESIAN_POINT('Origin',(32.6338164916465,-0.632323382398633,31.5962056922849));
#61849=CARTESIAN_POINT('',(32.6541425833284,-0.665360135553646,31.6237706303691));
#61850=CARTESIAN_POINT('Ctrl Pts',(32.6541425833226,-0.665360135549238,
31.6237706303625));
#61851=CARTESIAN_POINT('Ctrl Pts',(32.6396866039666,-0.654217330644686,
31.6070390219952));
#61852=CARTESIAN_POINT('Ctrl Pts',(32.625406135373,-0.643209811087222,31.5905494329059));
#61853=CARTESIAN_POINT('',(32.6106782843143,-0.819472915007481,31.6237706303691));
#61854=CARTESIAN_POINT('Origin',(30.,-1.32966554433622E-14,31.6237706303681));
#61855=CARTESIAN_POINT('',(32.574602921884,-0.823344418487278,31.5905494329235));
#61856=CARTESIAN_POINT('Ctrl Pts',(32.5746029218934,-0.823344418486272,
31.5905494329321));
#61857=CARTESIAN_POINT('Ctrl Pts',(32.5925304361379,-0.821420489546795,
31.6070390220085));
#61858=CARTESIAN_POINT('Ctrl Pts',(32.610678284307,-0.819472915008254,31.6237706303626));
#61859=CARTESIAN_POINT('',(32.5668472243157,-0.847214001212625,31.5905494329235));
#61860=CARTESIAN_POINT('Origin',(32.5760856561636,-0.837020957759021,31.596205527432));
#61861=CARTESIAN_POINT('',(32.5937571929504,-0.871550679329165,31.6237706303691));
#61862=CARTESIAN_POINT('Ctrl Pts',(32.593757192945,-0.871550679324299,31.6237706303625));
#61863=CARTESIAN_POINT('Ctrl Pts',(32.5802200309455,-0.859308020900409,
31.6070390219952));
#61864=CARTESIAN_POINT('Ctrl Pts',(32.5668472243014,-0.847214001199744,
31.5905494329059));
#61865=CARTESIAN_POINT('',(32.5383353305486,-1.02177821091939,31.6237706303691));
#61866=CARTESIAN_POINT('Origin',(30.,-1.32966554433622E-14,31.6237706303681));
#61867=CARTESIAN_POINT('',(32.5020674217591,-1.02280733953168,31.5905494329235));
#61868=CARTESIAN_POINT('Ctrl Pts',(32.5020674217685,-1.02280733953141,31.5905494329321));
#61869=CARTESIAN_POINT('Ctrl Pts',(32.5200906211944,-1.02229591797905,31.6070390220085));
#61870=CARTESIAN_POINT('Ctrl Pts',(32.5383353305413,-1.0217782109196,31.6237706303625));
#61871=CARTESIAN_POINT('',(32.492462846542,-1.0459948352816,31.5905494329235));
#61872=CARTESIAN_POINT('Origin',(32.5024724328509,-1.03655801106895,31.5962053997573));
#61873=CARTESIAN_POINT('',(32.517380426966,-1.07236782334661,31.6237706303691));
#61874=CARTESIAN_POINT('Ctrl Pts',(32.517380426961,-1.07236782334134,31.6237706303625));
#61875=CARTESIAN_POINT('Ctrl Pts',(32.5048455434235,-1.0591007914584,31.6070390219952));
#61876=CARTESIAN_POINT('Ctrl Pts',(32.4924628465288,-1.04599483526767,31.5905494329059));
#61877=CARTESIAN_POINT('',(32.450342695388,-1.21778390438525,31.6237706303691));
#61878=CARTESIAN_POINT('Origin',(30.,-1.32966554433622E-14,31.6237706303681));
#61879=CARTESIAN_POINT('',(32.4141058439571,-1.21596431320991,31.5905494329235));
#61880=CARTESIAN_POINT('Ctrl Pts',(32.4141058439665,-1.21596431321038,31.5905494329321));
#61881=CARTESIAN_POINT('Ctrl Pts',(32.4321136095561,-1.21686855212907,31.6070390220085));
#61882=CARTESIAN_POINT('Ctrl Pts',(32.4503426953807,-1.21778390438489,31.6237706303625));
#61883=CARTESIAN_POINT('',(32.4027116064913,-1.2383267633625,31.5905494329235));
#61884=CARTESIAN_POINT('Origin',(32.4134306626749,-1.2297043338603,31.5962052993351));
#61885=CARTESIAN_POINT('',(32.4254831735355,-1.26657346313463,31.6237706303691));
#61886=CARTESIAN_POINT('Ctrl Pts',(32.425483173531,-1.26657346312898,31.6237706303625));
#61887=CARTESIAN_POINT('Ctrl Pts',(32.4140278501806,-1.25236385345028,31.6070390219952));
#61888=CARTESIAN_POINT('Ctrl Pts',(32.4027116064792,-1.23832676334755,31.5905494329059));
#61889=CARTESIAN_POINT('',(32.3472428826886,-1.40628155512633,31.6237706303691));
#61890=CARTESIAN_POINT('Origin',(30.,-1.32966554433622E-14,31.6237706303681));
#61891=CARTESIAN_POINT('',(32.3112605008555,-1.40162446254804,31.5905494329235));
#61892=CARTESIAN_POINT('Ctrl Pts',(32.3112605008648,-1.40162446254925,31.5905494329321));
#61893=CARTESIAN_POINT('Ctrl Pts',(32.329141808755,-1.40393878700536,31.6070390220085));
#61894=CARTESIAN_POINT('Ctrl Pts',(32.3472428826814,-1.4062815551254,31.6237706303625));
#61895=CARTESIAN_POINT('',(32.2981468504039,-1.42302399516182,31.5905494329235));
#61896=CARTESIAN_POINT('Origin',(32.3095093115547,-1.41526911745265,31.5962052196244));
#61897=CARTESIAN_POINT('',(32.3186320097852,-1.45297025634402,31.6237706303691));
#61898=CARTESIAN_POINT('Ctrl Pts',(32.3186320097811,-1.45297025633802,31.6237706303625));
#61899=CARTESIAN_POINT('Ctrl Pts',(32.3083268724956,-1.43790567583238,31.6070390219952));
#61900=CARTESIAN_POINT('Ctrl Pts',(32.2981468503931,-1.42302399514595,31.5905494329059));
#61901=CARTESIAN_POINT('',(32.22967153708,-1.58610901244399,31.6237706303691));
#61902=CARTESIAN_POINT('Origin',(30.,-1.32966554433622E-14,31.6237706303681));
#61903=CARTESIAN_POINT('',(32.194165468194,-1.57864313098713,31.5905494329235));
#61904=CARTESIAN_POINT('Ctrl Pts',(32.1941654682032,-1.57864313098907,31.5905494329321));
#61905=CARTESIAN_POINT('Ctrl Pts',(32.2118100741847,-1.58235327240274,31.6070390220085));
#61906=CARTESIAN_POINT('Ctrl Pts',(32.2296715370729,-1.58610901244249,31.6237706303625));
#61907=CARTESIAN_POINT('',(32.1794132547725,-1.59894781082747,31.5905494329235));
#61908=CARTESIAN_POINT('Origin',(32.191349084716,-1.59210829514296,31.596205156165));
#61909=CARTESIAN_POINT('',(32.1974857086711,-1.6304090047614,31.6237706303691));
#61910=CARTESIAN_POINT('Ctrl Pts',(32.1974857086675,-1.63040900475512,31.6237706303625));
#61911=CARTESIAN_POINT('Ctrl Pts',(32.1883942920451,-1.61458233157088,31.6070390219952));
#61912=CARTESIAN_POINT('Ctrl Pts',(32.1794132547629,-1.59894781081085,31.5905494329059));
#61913=CARTESIAN_POINT('',(32.0983535250043,-1.75615758026517,31.6237706303691));
#61914=CARTESIAN_POINT('Origin',(30.,-1.32966554433622E-14,31.6237706303681));
#61915=CARTESIAN_POINT('',(32.063542675787,-1.74592893957158,31.5905494329235));
#61916=CARTESIAN_POINT('Ctrl Pts',(32.0635426757961,-1.74592893957424,31.5905494329321));
#61917=CARTESIAN_POINT('Ctrl Pts',(32.0808417950055,-1.75101202368991,31.6070390220085));
#61918=CARTESIAN_POINT('Ctrl Pts',(32.0983535249973,-1.75615758026313,31.6237706303625));
#61919=CARTESIAN_POINT('',(32.0472428516969,-1.76501358153528,31.5905494329235));
#61920=CARTESIAN_POINT('Origin',(32.0596784759083,-1.75913159602171,31.5962051058414));
#61921=CARTESIAN_POINT('',(32.062791177425,-1.79779573949842,31.6237706303691));
#61922=CARTESIAN_POINT('Ctrl Pts',(32.0627911774219,-1.79779573949184,31.6237706303625));
#61923=CARTESIAN_POINT('Ctrl Pts',(32.0549695330692,-1.78130455033205,31.6070390219952));
#61924=CARTESIAN_POINT('Ctrl Pts',(32.0472428516887,-1.76501358151791,31.5905494329059));
#61925=CARTESIAN_POINT('',(31.9540984656736,-1.91537885262235,31.6237706303691));
#61926=CARTESIAN_POINT('Origin',(30.,-1.32966554433622E-14,31.6237706303681));
#61927=CARTESIAN_POINT('',(31.9201974565863,-1.90245051566327,31.5905494329235));
#61928=CARTESIAN_POINT('Ctrl Pts',(31.9201974565951,-1.90245051566663,31.5905494329321));
#61929=CARTESIAN_POINT('Ctrl Pts',(31.9370444342101,-1.90887520358042,31.6070390220085));
#61930=CARTESIAN_POINT('Ctrl Pts',(31.9540984656668,-1.91537885261975,31.6237706303625));
#61931=CARTESIAN_POINT('',(31.9024505156632,-1.92019745658634,31.5905494329235));
#61932=CARTESIAN_POINT('Origin',(31.915309275617,-1.91530926701241,31.5962050664381));
#61933=CARTESIAN_POINT('',(31.9153788526223,-1.95409846567368,31.6237706303691));
#61934=CARTESIAN_POINT('Ctrl Pts',(31.9153788526197,-1.9540984656669,31.6237706303625));
#61935=CARTESIAN_POINT('Ctrl Pts',(31.9088752035752,-1.93704443419662,31.6070390219952));
#61936=CARTESIAN_POINT('Ctrl Pts',(31.9024505156564,-1.92019745656839,31.5905494329059));
#61937=CARTESIAN_POINT('',(31.7977957394984,-2.06279117742501,31.6237706303691));
#61938=CARTESIAN_POINT('Origin',(30.,-1.32966554433622E-14,31.6237706303681));
#61939=CARTESIAN_POINT('',(31.7650135815352,-2.04724285169692,31.5905494329235));
#61940=CARTESIAN_POINT('Ctrl Pts',(31.7650135815437,-2.04724285170096,31.5905494329321));
#61941=CARTESIAN_POINT('Ctrl Pts',(31.7813045503451,-2.05496953307547,31.6070390220085));
#61942=CARTESIAN_POINT('Ctrl Pts',(31.7977957394918,-2.06279117742192,31.6237706303625));
#61943=CARTESIAN_POINT('',(31.7459289395715,-2.0635426757871,31.5905494329235));
#61944=CARTESIAN_POINT('Origin',(31.7591315658702,-2.05967842174604,31.5962050363748));
#61945=CARTESIAN_POINT('',(31.7561575802651,-2.09835352500439,31.6237706303691));
#61946=CARTESIAN_POINT('Ctrl Pts',(31.7561575802631,-2.09835352499741,31.6237706303625));
#61947=CARTESIAN_POINT('Ctrl Pts',(31.7510120236858,-2.08084179499169,31.6070390219952));
#61948=CARTESIAN_POINT('Ctrl Pts',(31.7459289395661,-2.06354267576866,31.5905494329059));
#61949=CARTESIAN_POINT('',(31.6304090047613,-2.19748570867118,31.6237706303691));
#61950=CARTESIAN_POINT('Origin',(30.,-1.32966554433622E-14,31.6237706303681));
#61951=CARTESIAN_POINT('',(31.5989478108274,-2.17941325477251,31.5905494329235));
#61952=CARTESIAN_POINT('Ctrl Pts',(31.5989478108356,-2.17941325477721,31.5905494329321));
#61953=CARTESIAN_POINT('Ctrl Pts',(31.6145823315833,-2.18839429205237,31.6070390220085));
#61954=CARTESIAN_POINT('Ctrl Pts',(31.630409004755,-2.19748570866756,31.6237706303625));
#61955=CARTESIAN_POINT('',(31.5786431309871,-2.19416546819406,31.5905494329235));
#61956=CARTESIAN_POINT('Origin',(31.5921082324253,-2.19134897714169,31.5962050145327));
#61957=CARTESIAN_POINT('',(31.5861090124439,-2.22967153708009,31.6237706303691));
#61958=CARTESIAN_POINT('Ctrl Pts',(31.5861090124425,-2.22967153707296,31.6237706303625));
#61959=CARTESIAN_POINT('Ctrl Pts',(31.5823532723997,-2.21181007417054,31.6070390219952));
#61960=CARTESIAN_POINT('Ctrl Pts',(31.5786431309832,-2.19416546817524,31.5905494329059));
#61961=CARTESIAN_POINT('',(31.452970256344,-2.31863200978524,31.6237706303691));
#61962=CARTESIAN_POINT('Origin',(30.,-1.32966554433622E-14,31.6237706303681));
#61963=CARTESIAN_POINT('',(31.4230239951618,-2.29814685040399,31.5905494329235));
#61964=CARTESIAN_POINT('Ctrl Pts',(31.4230239951696,-2.2981468504093,31.5905494329321));
#61965=CARTESIAN_POINT('Ctrl Pts',(31.4379056758443,-2.30832687250383,31.6070390220085));
#61966=CARTESIAN_POINT('Ctrl Pts',(31.452970256338,-2.31863200978113,31.6237706303625));
#61967=CARTESIAN_POINT('',(31.401624462548,-2.31126050085554,31.5905494329235));
#61968=CARTESIAN_POINT('Origin',(31.4152690281487,-2.30950914111279,31.596205000146));
#61969=CARTESIAN_POINT('',(31.4062815551263,-2.34724288268866,31.6237706303691));
#61970=CARTESIAN_POINT('Ctrl Pts',(31.4062815551254,-2.34724288268144,31.6237706303625));
#61971=CARTESIAN_POINT('Ctrl Pts',(31.4039387870035,-2.32914180874065,31.6070390219952));
#61972=CARTESIAN_POINT('Ctrl Pts',(31.4016244625455,-2.31126050083648,31.5905494329059));
#61973=CARTESIAN_POINT('',(31.2665734631346,-2.42548317353559,31.6237706303691));
#61974=CARTESIAN_POINT('Origin',(30.,-1.32966554433622E-14,31.6237706303681));
#61975=CARTESIAN_POINT('',(31.2383267633624,-2.40271160649135,31.5905494329235));
#61976=CARTESIAN_POINT('Ctrl Pts',(31.2383267633697,-2.40271160649727,31.5905494329321));
#61977=CARTESIAN_POINT('Ctrl Pts',(31.2523638534615,-2.41402785018975,31.6070390220085));
#61978=CARTESIAN_POINT('Ctrl Pts',(31.2665734631289,-2.42548317353104,31.6237706303625));
#61979=CARTESIAN_POINT('',(31.2159643132098,-2.41410584395714,31.5905494329235));
#61980=CARTESIAN_POINT('Origin',(31.2297042241653,-2.41343041757036,31.5962049927334));
#61981=CARTESIAN_POINT('',(31.2177839043852,-2.450342695388,31.6237706303691));
#61982=CARTESIAN_POINT('Ctrl Pts',(31.2177839043848,-2.45034269538075,31.6237706303625));
#61983=CARTESIAN_POINT('Ctrl Pts',(31.2168685521282,-2.43211360954164,31.6070390219952));
#61984=CARTESIAN_POINT('Ctrl Pts',(31.2159643132088,-2.41410584393796,31.5905494329059));
#61985=CARTESIAN_POINT('',(31.0723678233465,-2.51738042696609,31.6237706303691));
#61986=CARTESIAN_POINT('Origin',(30.,-1.32966554433622E-14,31.6237706303681));
#61987=CARTESIAN_POINT('',(31.0459948352815,-2.49246284654201,31.5905494329235));
#61988=CARTESIAN_POINT('Ctrl Pts',(31.0459948352884,-2.49246284654849,31.5905494329321));
#61989=CARTESIAN_POINT('Ctrl Pts',(31.0591007914688,-2.5048455434335,31.6070390220085));
#61990=CARTESIAN_POINT('Ctrl Pts',(31.0723678233412,-2.51738042696111,31.6237706303625));
#61991=CARTESIAN_POINT('',(31.0228073395316,-2.5020674217591,31.5905494329235));
#61992=CARTESIAN_POINT('Origin',(31.036557887911,-2.50247209787259,31.5962049920587));
#61993=CARTESIAN_POINT('',(31.0217782109193,-2.53833533054864,31.6237706303691));
#61994=CARTESIAN_POINT('Ctrl Pts',(31.0217782109196,-2.53833533054137,31.6237706303625));
#61995=CARTESIAN_POINT('Ctrl Pts',(31.0222959179794,-2.52009062117993,31.6070390219952));
#61996=CARTESIAN_POINT('Ctrl Pts',(31.0228073395322,-2.50206742173989,31.5905494329059));
#61997=CARTESIAN_POINT('',(30.8715506793291,-2.59375719295041,31.6237706303691));
#61998=CARTESIAN_POINT('Origin',(30.,-1.32966554433622E-14,31.6237706303681));
#61999=CARTESIAN_POINT('',(30.8472140012126,-2.56684722431573,31.5905494329235));
#62000=CARTESIAN_POINT('Ctrl Pts',(30.8472140012189,-2.56684722432271,31.5905494329321));
#62001=CARTESIAN_POINT('Ctrl Pts',(30.8593080209101,-2.58022003095631,31.6070390220085));
#62002=CARTESIAN_POINT('Ctrl Pts',(30.8715506793242,-2.593757192945,31.6237706303625));
#62003=CARTESIAN_POINT('',(30.8233444184872,-2.57460292188405,31.5905494329235));
#62004=CARTESIAN_POINT('Origin',(30.8370208295222,-2.5760852110326,31.5962049981139));
#62005=CARTESIAN_POINT('',(30.8194729150074,-2.6106782843143,31.6237706303691));
#62006=CARTESIAN_POINT('Ctrl Pts',(30.8194729150082,-2.61067828430707,31.6237706303625));
#62007=CARTESIAN_POINT('Ctrl Pts',(30.8214204895483,-2.5925304361235,31.6070390219952));
#62008=CARTESIAN_POINT('Ctrl Pts',(30.8233444184892,-2.57460292186495,31.5905494329059));
#62009=CARTESIAN_POINT('',(30.6653601355536,-2.65414258332839,31.6237706303691));
#62010=CARTESIAN_POINT('Origin',(30.,-1.32966554433622E-14,31.6237706303681));
#62011=CARTESIAN_POINT('',(30.6432098110989,-2.62540613538822,31.5905494329235));
#62012=CARTESIAN_POINT('Ctrl Pts',(30.6432098111046,-2.62540613539568,31.5905494329321));
#62013=CARTESIAN_POINT('Ctrl Pts',(30.6542173306535,-2.63968660397806,31.6070390220085));
#62014=CARTESIAN_POINT('Ctrl Pts',(30.6653601355492,-2.65414258332262,31.6237706303625));
#62015=CARTESIAN_POINT('',(30.618805305313,-2.63126513885325,31.5905494329235));
#62016=CARTESIAN_POINT('Origin',(30.632323260043,-2.63381590833404,31.5962050111235));
#62017=CARTESIAN_POINT('',(30.6121152960721,-2.66692553831853,31.6237706303691));
#62018=CARTESIAN_POINT('Ctrl Pts',(30.6121152960734,-2.66692553831138,31.6237706303625));
#62019=CARTESIAN_POINT('Ctrl Pts',(30.615480730649,-2.6489864388245,31.6070390219952));
#62020=CARTESIAN_POINT('Ctrl Pts',(30.6188053053166,-2.63126513883437,31.5905494329059));
#62021=CARTESIAN_POINT('',(30.4550674252877,-2.69816430208819,31.6237706303691));
#62022=CARTESIAN_POINT('Origin',(30.,-1.32966554433622E-14,31.6237706303681));
#62023=CARTESIAN_POINT('',(30.4352400186108,-2.66777854459992,31.5905494329235));
#62024=CARTESIAN_POINT('Ctrl Pts',(30.435240018616,-2.6677785446078,31.5905494329321));
#62025=CARTESIAN_POINT('Ctrl Pts',(30.445093173004,-2.68287863130142,31.6070390220085));
#62026=CARTESIAN_POINT('Ctrl Pts',(30.4550674252837,-2.69816430208209,31.6237706303625));
#62027=CARTESIAN_POINT('',(30.410451051658,-2.67170473125697,31.5905494329235));
#62028=CARTESIAN_POINT('Origin',(30.4237272067093,-2.67530826149246,31.5962050315749));
#62029=CARTESIAN_POINT('',(30.4009837827875,-2.7067303095363,31.6237706303691));
#62030=CARTESIAN_POINT('Ctrl Pts',(30.4009837827894,-2.70673030952928,31.6237706303625));
#62031=CARTESIAN_POINT('Ctrl Pts',(30.4057463283773,-2.68911055925278,31.6070390219952));
#62032=CARTESIAN_POINT('Ctrl Pts',(30.410451051663,-2.67170473123841,31.5905494329059));
#62033=CARTESIAN_POINT('',(30.2419690730196,-2.72555094069494,31.6237706303691));
#62034=CARTESIAN_POINT('Origin',(30.,-1.32966554433622E-14,31.6237706303681));
#62035=CARTESIAN_POINT('',(30.224586826676,-2.69370321195777,31.5905494329235));
#62036=CARTESIAN_POINT('Ctrl Pts',(30.2245868266805,-2.69370321196604,31.5905494329321));
#62037=CARTESIAN_POINT('Ctrl Pts',(30.2332248679346,-2.70952981971513,31.6070390220085));
#62038=CARTESIAN_POINT('Ctrl Pts',(30.2419690730162,-2.72555094068854,31.6237706303625));
#62039=CARTESIAN_POINT('',(30.1995662307806,-2.69567237556051,31.5905494329235));
#62040=CARTESIAN_POINT('Origin',(30.2125187320612,-2.70030645711985,31.5962050602857));
#62041=CARTESIAN_POINT('',(30.1873800711414,-2.72984718831661,31.6237706303691));
#62042=CARTESIAN_POINT('Ctrl Pts',(30.1873800711438,-2.72984718830975,31.6237706303625));
#62043=CARTESIAN_POINT('Ctrl Pts',(30.1935103650667,-2.71265541886325,31.6070390219952));
#62044=CARTESIAN_POINT('Ctrl Pts',(30.199566230787,-2.6956723755424,31.5905494329059));
#62045=CARTESIAN_POINT('',(30.0273789009535,-2.73613365141464,31.6237706303691));
#62046=CARTESIAN_POINT('Origin',(30.,-1.32966554433622E-14,31.6237706303681));
#62047=CARTESIAN_POINT('',(30.012548982272,-2.70302030326669,31.5905494329235));
#62048=CARTESIAN_POINT('Ctrl Pts',(30.0125489822759,-2.70302030327528,31.5905494329321));
#62049=CARTESIAN_POINT('Ctrl Pts',(30.0199186539991,-2.7194758557802,31.6070390220085));
#62050=CARTESIAN_POINT('Ctrl Pts',(30.0273789009505,-2.736133651408,31.6237706303625));
#62051=CARTESIAN_POINT('',(29.987451017728,-2.70302030326669,31.5905494329235));
#62052=CARTESIAN_POINT('Origin',(30.,-2.7086657795165,31.5962151370754));
#62053=CARTESIAN_POINT('',(29.9726210990465,-2.73613365141464,31.6237706303691));
#62054=CARTESIAN_POINT('Ctrl Pts',(29.9726210990495,-2.73613365140799,31.6237706303625));
#62055=CARTESIAN_POINT('Ctrl Pts',(29.9800813460068,-2.71947585576697,31.6070390219952));
#62056=CARTESIAN_POINT('Ctrl Pts',(29.9874510177359,-2.70302030324915,31.5905494329059));
#62057=CARTESIAN_POINT('',(29.8126199288586,-2.72984718831661,31.6237706303691));
#62058=CARTESIAN_POINT('Origin',(30.,-1.32966554433622E-14,31.6237706303681));
#62059=CARTESIAN_POINT('',(29.8004337692193,-2.6956723755605,31.5905494329235));
#62060=CARTESIAN_POINT('Ctrl Pts',(29.8004337692225,-2.69567237556937,31.5905494329321));
#62061=CARTESIAN_POINT('Ctrl Pts',(29.806489634938,-2.71265541887691,31.6070390220085));
#62062=CARTESIAN_POINT('Ctrl Pts',(29.8126199288561,-2.72984718830976,31.6237706303625));
#62063=CARTESIAN_POINT('',(29.775413173324,-2.69370321195777,31.5905494329235));
#62064=CARTESIAN_POINT('Origin',(29.7874812116305,-2.70030745889015,31.5962062072437));
#62065=CARTESIAN_POINT('',(29.7580309269803,-2.72555094069494,31.6237706303691));
#62066=CARTESIAN_POINT('Ctrl Pts',(29.7580309269838,-2.72555094068855,31.6237706303625));
#62067=CARTESIAN_POINT('Ctrl Pts',(29.7667751320723,-2.7095298197024,31.6070390219952));
#62068=CARTESIAN_POINT('Ctrl Pts',(29.7754131733332,-2.69370321194088,31.5905494329059));
#62069=CARTESIAN_POINT('',(29.5990162172124,-2.70673030953629,31.6237706303691));
#62070=CARTESIAN_POINT('Origin',(30.,-1.32966554433622E-14,31.6237706303681));
#62071=CARTESIAN_POINT('',(29.589548948342,-2.67170473125696,31.5905494329235));
#62072=CARTESIAN_POINT('Ctrl Pts',(29.5895489483445,-2.67170473126605,31.5905494329321));
#62073=CARTESIAN_POINT('Ctrl Pts',(29.5942536716264,-2.68911055926676,31.6070390220085));
#62074=CARTESIAN_POINT('Ctrl Pts',(29.5990162172106,-2.70673030952926,31.6237706303625));
#62075=CARTESIAN_POINT('',(29.5647599813891,-2.66777854459992,31.5905494329235));
#62076=CARTESIAN_POINT('Origin',(29.5762726922515,-2.67530902338218,31.5962059100614));
#62077=CARTESIAN_POINT('',(29.5449325747122,-2.69816430208819,31.6237706303691));
#62078=CARTESIAN_POINT('Ctrl Pts',(29.5449325747162,-2.6981643020821,31.6237706303625));
#62079=CARTESIAN_POINT('Ctrl Pts',(29.5549068270038,-2.68287863128929,31.6070390219952));
#62080=CARTESIAN_POINT('Ctrl Pts',(29.5647599813996,-2.66777854458383,31.5905494329059));
#62081=CARTESIAN_POINT('',(29.3878847039278,-2.66692553831852,31.6237706303691));
#62082=CARTESIAN_POINT('Origin',(30.,-1.32966554433622E-14,31.6237706303681));
#62083=CARTESIAN_POINT('',(29.3811946946869,-2.63126513885324,31.5905494329235));
#62084=CARTESIAN_POINT('Ctrl Pts',(29.3811946946886,-2.63126513886249,31.5905494329321));
#62085=CARTESIAN_POINT('Ctrl Pts',(29.3845192693535,-2.64898643883873,31.6070390220085));
#62086=CARTESIAN_POINT('Ctrl Pts',(29.3878847039265,-2.66692553831137,31.6237706303625));
#62087=CARTESIAN_POINT('',(29.3567901889011,-2.62540613538822,31.5905494329235));
#62088=CARTESIAN_POINT('Origin',(29.3676766176013,-2.63381649164654,31.5962056922849));
#62089=CARTESIAN_POINT('',(29.3346398644463,-2.65414258332839,31.6237706303691));
#62090=CARTESIAN_POINT('Ctrl Pts',(29.3346398644508,-2.65414258332263,31.6237706303626));
#62091=CARTESIAN_POINT('Ctrl Pts',(29.3457826693553,-2.63968660396658,31.6070390219952));
#62092=CARTESIAN_POINT('Ctrl Pts',(29.3567901889128,-2.62540613537299,31.5905494329059));
#62093=CARTESIAN_POINT('',(29.1805270849925,-2.61067828431429,31.6237706303691));
#62094=CARTESIAN_POINT('Origin',(30.,-1.32966554433622E-14,31.6237706303681));
#62095=CARTESIAN_POINT('',(29.1766555815127,-2.57460292188404,31.5905494329235));
#62096=CARTESIAN_POINT('Ctrl Pts',(29.1766555815137,-2.5746029218934,31.5905494329321));
#62097=CARTESIAN_POINT('Ctrl Pts',(29.1785795104532,-2.59253043613788,31.6070390220085));
#62098=CARTESIAN_POINT('Ctrl Pts',(29.1805270849917,-2.61067828430705,31.6237706303625));
#62099=CARTESIAN_POINT('',(29.1527859987874,-2.56684722431572,31.5905494329235));
#62100=CARTESIAN_POINT('Origin',(29.162979042241,-2.57608565616368,31.5962055274321));
#62101=CARTESIAN_POINT('',(29.1284493206708,-2.59375719295039,31.6237706303691));
#62102=CARTESIAN_POINT('Ctrl Pts',(29.1284493206757,-2.593757192945,31.6237706303625));
#62103=CARTESIAN_POINT('Ctrl Pts',(29.1406919790996,-2.58022003094555,31.6070390219952));
#62104=CARTESIAN_POINT('Ctrl Pts',(29.1527859988003,-2.56684722430145,31.5905494329059));
#62105=CARTESIAN_POINT('',(28.9782217890806,-2.53833533054863,31.6237706303691));
#62106=CARTESIAN_POINT('Origin',(30.,-1.32966554433622E-14,31.6237706303681));
#62107=CARTESIAN_POINT('',(28.9771926604683,-2.50206742175908,31.5905494329235));
#62108=CARTESIAN_POINT('Ctrl Pts',(28.9771926604686,-2.50206742176849,31.5905494329321));
#62109=CARTESIAN_POINT('Ctrl Pts',(28.9777040820209,-2.5200906211944,31.6070390220085));
#62110=CARTESIAN_POINT('Ctrl Pts',(28.9782217890804,-2.53833533054136,31.6237706303625));
#62111=CARTESIAN_POINT('',(28.9540051647184,-2.49246284654199,31.5905494329235));
#62112=CARTESIAN_POINT('Origin',(28.963441988931,-2.50247243285095,31.5962053997573));
#62113=CARTESIAN_POINT('',(28.9276321766534,-2.51738042696608,31.6237706303691));
#62114=CARTESIAN_POINT('Ctrl Pts',(28.9276321766587,-2.51738042696105,31.6237706303625));
#62115=CARTESIAN_POINT('Ctrl Pts',(28.9408992085416,-2.5048455434235,31.6070390219952));
#62116=CARTESIAN_POINT('Ctrl Pts',(28.9540051647323,-2.49246284652876,31.5905494329059));
#62117=CARTESIAN_POINT('',(28.7822160956147,-2.45034269538798,31.6237706303691));
#62118=CARTESIAN_POINT('Origin',(30.,-1.32966554433622E-14,31.6237706303681));
#62119=CARTESIAN_POINT('',(28.7840356867901,-2.41410584395713,31.5905494329235));
#62120=CARTESIAN_POINT('Ctrl Pts',(28.7840356867896,-2.41410584396654,31.5905494329321));
#62121=CARTESIAN_POINT('Ctrl Pts',(28.783131447871,-2.43211360955609,31.6070390220085));
#62122=CARTESIAN_POINT('Ctrl Pts',(28.7822160956151,-2.45034269538072,31.6237706303625));
#62123=CARTESIAN_POINT('',(28.7616732366375,-2.40271160649133,31.5905494329235));
#62124=CARTESIAN_POINT('Origin',(28.7702956661397,-2.41343066267495,31.5962052993351));
#62125=CARTESIAN_POINT('',(28.7334265368654,-2.42548317353557,31.6237706303691));
#62126=CARTESIAN_POINT('Ctrl Pts',(28.7334265368711,-2.425483173531,31.6237706303625));
#62127=CARTESIAN_POINT('Ctrl Pts',(28.7476361465498,-2.41402785018062,31.6070390219952));
#62128=CARTESIAN_POINT('Ctrl Pts',(28.7616732366525,-2.40271160647928,31.5905494329059));
#62129=CARTESIAN_POINT('',(28.5937184448736,-2.34724288268865,31.6237706303691));
#62130=CARTESIAN_POINT('Origin',(30.,-1.32966554433622E-14,31.6237706303681));
#62131=CARTESIAN_POINT('',(28.5983755374519,-2.31126050085552,31.5905494329235));
#62132=CARTESIAN_POINT('Ctrl Pts',(28.5983755374507,-2.31126050086484,31.5905494329321));
#62133=CARTESIAN_POINT('Ctrl Pts',(28.5960612129946,-2.32914180875499,31.6070390220085));
#62134=CARTESIAN_POINT('Ctrl Pts',(28.5937184448745,-2.34724288268142,31.6237706303625));
#62135=CARTESIAN_POINT('',(28.5769760048382,-2.29814685040397,31.5905494329235));
#62136=CARTESIAN_POINT('Origin',(28.5847308825473,-2.30950931155478,31.5962052196244));
#62137=CARTESIAN_POINT('',(28.547029743656,-2.31863200978522,31.6237706303691));
#62138=CARTESIAN_POINT('Ctrl Pts',(28.547029743662,-2.31863200978111,31.6237706303625));
#62139=CARTESIAN_POINT('Ctrl Pts',(28.5620943241676,-2.30832687249563,31.6070390219952));
#62140=CARTESIAN_POINT('Ctrl Pts',(28.5769760048541,-2.29814685039312,31.5905494329059));
#62141=CARTESIAN_POINT('',(28.413890987556,-2.22967153708007,31.6237706303691));
#62142=CARTESIAN_POINT('Origin',(30.,-1.32966554433622E-14,31.6237706303681));
#62143=CARTESIAN_POINT('',(28.4213568690129,-2.19416546819403,31.5905494329235));
#62144=CARTESIAN_POINT('Ctrl Pts',(28.421356869011,-2.19416546820326,31.5905494329321));
#62145=CARTESIAN_POINT('Ctrl Pts',(28.4176467275973,-2.21181007418472,31.6070390220085));
#62146=CARTESIAN_POINT('Ctrl Pts',(28.4138909875575,-2.22967153707296,31.6237706303625));
#62147=CARTESIAN_POINT('',(28.4010521891725,-2.17941325477249,31.5905494329235));
#62148=CARTESIAN_POINT('Origin',(28.407891704857,-2.19134908471608,31.596205156165));
#62149=CARTESIAN_POINT('',(28.3695909952386,-2.19748570867116,31.6237706303691));
#62150=CARTESIAN_POINT('Ctrl Pts',(28.3695909952449,-2.19748570866753,31.6237706303625));
#62151=CARTESIAN_POINT('Ctrl Pts',(28.3854176684292,-2.18839429204513,31.6070390219952));
#62152=CARTESIAN_POINT('Ctrl Pts',(28.4010521891892,-2.17941325476292,31.5905494329059));
#62153=CARTESIAN_POINT('',(28.2438424197348,-2.09835352500436,31.6237706303691));
#62154=CARTESIAN_POINT('Origin',(30.,-1.32966554433622E-14,31.6237706303681));
#62155=CARTESIAN_POINT('',(28.2540710604284,-2.06354267578707,31.5905494329235));
#62156=CARTESIAN_POINT('Ctrl Pts',(28.2540710604258,-2.0635426757961,31.5905494329321));
#62157=CARTESIAN_POINT('Ctrl Pts',(28.2489879763101,-2.08084179500557,31.6070390220085));
#62158=CARTESIAN_POINT('Ctrl Pts',(28.2438424197369,-2.09835352499738,31.6237706303625));
#62159=CARTESIAN_POINT('',(28.2349864184647,-2.04724285169689,31.5905494329235));
#62160=CARTESIAN_POINT('Origin',(28.2408684039783,-2.05967847590829,31.5962051058414));
#62161=CARTESIAN_POINT('',(28.2022042605016,-2.06279117742499,31.6237706303691));
#62162=CARTESIAN_POINT('Ctrl Pts',(28.2022042605082,-2.06279117742185,31.6237706303625));
#62163=CARTESIAN_POINT('Ctrl Pts',(28.2186954496679,-2.0549695330692,31.6070390219952));
#62164=CARTESIAN_POINT('Ctrl Pts',(28.2349864184821,-2.04724285168864,31.5905494329059));
#62165=CARTESIAN_POINT('',(28.0846211473776,-1.95409846567366,31.6237706303691));
#62166=CARTESIAN_POINT('Origin',(30.,-1.32966554433622E-14,31.6237706303681));
#62167=CARTESIAN_POINT('',(28.0975494843367,-1.92019745658631,31.5905494329235));
#62168=CARTESIAN_POINT('Ctrl Pts',(28.0975494843333,-1.92019745659509,31.5905494329321));
#62169=CARTESIAN_POINT('Ctrl Pts',(28.0911247964195,-1.93704443421011,31.6070390220085));
#62170=CARTESIAN_POINT('Ctrl Pts',(28.0846211473802,-1.95409846566685,31.6237706303626));
#62171=CARTESIAN_POINT('',(28.0798025434136,-1.90245051566325,31.5905494329235));
#62172=CARTESIAN_POINT('Origin',(28.0846907329876,-1.91530927561707,31.5962050664381));
#62173=CARTESIAN_POINT('',(28.0459015343263,-1.91537885262232,31.6237706303691));
#62174=CARTESIAN_POINT('Ctrl Pts',(28.0459015343331,-1.91537885261973,31.6237706303625));
#62175=CARTESIAN_POINT('Ctrl Pts',(28.0629555658034,-1.90887520357524,31.6070390219952));
#62176=CARTESIAN_POINT('Ctrl Pts',(28.0798025434316,-1.90245051565641,31.5905494329059));
#62177=CARTESIAN_POINT('',(27.937208822575,-1.79779573949839,31.6237706303691));
#62178=CARTESIAN_POINT('Origin',(30.,-1.32966554433622E-14,31.6237706303681));
#62179=CARTESIAN_POINT('',(27.9527571483031,-1.76501358153525,31.5905494329235));
#62180=CARTESIAN_POINT('Ctrl Pts',(27.9527571482991,-1.76501358154376,31.5905494329321));
#62181=CARTESIAN_POINT('Ctrl Pts',(27.9450304669246,-1.78130455034514,31.6070390220085));
#62182=CARTESIAN_POINT('Ctrl Pts',(27.9372088225781,-1.79779573949183,31.6237706303625));
#62183=CARTESIAN_POINT('',(27.9364573242129,-1.74592893957155,31.5905494329235));
#62184=CARTESIAN_POINT('Origin',(27.940321578254,-1.75913156587022,31.5962050363747));
#62185=CARTESIAN_POINT('',(27.9016464749956,-1.75615758026514,31.6237706303691));
#62186=CARTESIAN_POINT('Ctrl Pts',(27.9016464750026,-1.75615758026309,31.6237706303625));
#62187=CARTESIAN_POINT('Ctrl Pts',(27.9191582050083,-1.75101202368579,31.6070390219952));
#62188=CARTESIAN_POINT('Ctrl Pts',(27.9364573242313,-1.74592893956614,31.5905494329059));
#62189=CARTESIAN_POINT('',(27.8025142913288,-1.63040900476137,31.6237706303691));
#62190=CARTESIAN_POINT('Origin',(30.,-1.32966554433622E-14,31.6237706303681));
#62191=CARTESIAN_POINT('',(27.8205867452275,-1.59894781082744,31.5905494329235));
#62192=CARTESIAN_POINT('Ctrl Pts',(27.8205867452228,-1.59894781083561,31.5905494329321));
#62193=CARTESIAN_POINT('Ctrl Pts',(27.8116057079476,-1.61458233158338,31.6070390220085));
#62194=CARTESIAN_POINT('Ctrl Pts',(27.8025142913325,-1.63040900475507,31.6237706303625));
#62195=CARTESIAN_POINT('',(27.8058345318059,-1.5786431309871,31.5905494329235));
#62196=CARTESIAN_POINT('Origin',(27.8086510228583,-1.5921082324254,31.5962050145327));
#62197=CARTESIAN_POINT('',(27.7703284629199,-1.58610901244396,31.6237706303691));
#62198=CARTESIAN_POINT('Ctrl Pts',(27.770328462927,-1.58610901244246,31.6237706303625));
#62199=CARTESIAN_POINT('Ctrl Pts',(27.7881899258294,-1.58235327239973,31.6070390219952));
#62200=CARTESIAN_POINT('Ctrl Pts',(27.8058345318247,-1.57864313098315,31.5905494329059));
#62201=CARTESIAN_POINT('',(27.6813679902147,-1.45297025634398,31.6237706303691));
#62202=CARTESIAN_POINT('Origin',(30.,-1.32966554433622E-14,31.6237706303681));
#62203=CARTESIAN_POINT('',(27.701853149596,-1.42302399516179,31.5905494329235));
#62204=CARTESIAN_POINT('Ctrl Pts',(27.7018531495907,-1.42302399516956,31.5905494329321));
#62205=CARTESIAN_POINT('Ctrl Pts',(27.6916731274962,-1.43790567584432,31.6070390220085));
#62206=CARTESIAN_POINT('Ctrl Pts',(27.6813679902189,-1.45297025633799,31.6237706303626));
#62207=CARTESIAN_POINT('',(27.6887394991444,-1.40162446254801,31.5905494329235));
#62208=CARTESIAN_POINT('Origin',(27.6904908588872,-1.41526902814876,31.596205000146));
#62209=CARTESIAN_POINT('',(27.6527571173113,-1.4062815551263,31.6237706303691));
#62210=CARTESIAN_POINT('Ctrl Pts',(27.6527571173185,-1.40628155512537,31.6237706303626));
#62211=CARTESIAN_POINT('Ctrl Pts',(27.6708581912593,-1.40393878700346,31.6070390219953));
#62212=CARTESIAN_POINT('Ctrl Pts',(27.6887394991635,-1.40162446254554,31.5905494329059));
#62213=CARTESIAN_POINT('',(27.5745168264644,-1.2665734631346,31.6237706303691));
#62214=CARTESIAN_POINT('Origin',(30.,-1.32966554433622E-14,31.6237706303681));
#62215=CARTESIAN_POINT('',(27.5972883935086,-1.23832676336246,31.5905494329235));
#62216=CARTESIAN_POINT('Ctrl Pts',(27.5972883935027,-1.23832676336977,31.5905494329321));
#62217=CARTESIAN_POINT('Ctrl Pts',(27.5859721498102,-1.25236385346148,31.6070390220085));
#62218=CARTESIAN_POINT('Ctrl Pts',(27.574516826469,-1.2665734631289,31.6237706303626));
#62219=CARTESIAN_POINT('',(27.5858941560428,-1.21596431320988,31.5905494329235));
#62220=CARTESIAN_POINT('Origin',(27.5865695824296,-1.22970422416533,31.5962049927334));
#62221=CARTESIAN_POINT('',(27.549657304612,-1.21778390438522,31.6237706303691));
#62222=CARTESIAN_POINT('Ctrl Pts',(27.5496573046193,-1.21778390438485,31.6237706303625));
#62223=CARTESIAN_POINT('Ctrl Pts',(27.5678863904584,-1.2168685521283,31.6070390219952));
#62224=CARTESIAN_POINT('Ctrl Pts',(27.585894156062,-1.21596431320891,31.5905494329059));
#62225=CARTESIAN_POINT('',(27.4826195730339,-1.07236782334657,31.6237706303691));
#62226=CARTESIAN_POINT('Origin',(30.,-1.32966554433622E-14,31.6237706303681));
#62227=CARTESIAN_POINT('',(27.507537153458,-1.04599483528157,31.5905494329235));
#62228=CARTESIAN_POINT('Ctrl Pts',(27.5075371534515,-1.04599483528841,31.5905494329321));
#62229=CARTESIAN_POINT('Ctrl Pts',(27.4951544565665,-1.05910079146888,31.6070390220085));
#62230=CARTESIAN_POINT('Ctrl Pts',(27.4826195730389,-1.07236782334129,31.6237706303626));
#62231=CARTESIAN_POINT('',(27.4979325782409,-1.02280733953164,31.5905494329235));
#62232=CARTESIAN_POINT('Origin',(27.4975279021274,-1.03655788791105,31.5962049920587));
#62233=CARTESIAN_POINT('',(27.4616646694513,-1.02177821091936,31.6237706303691));
#62234=CARTESIAN_POINT('Ctrl Pts',(27.4616646694586,-1.02177821091956,31.6237706303626));
#62235=CARTESIAN_POINT('Ctrl Pts',(27.4799093788201,-1.02229591797942,31.6070390219952));
#62236=CARTESIAN_POINT('Ctrl Pts',(27.4979325782601,-1.02280733953218,31.5905494329059));
#62237=CARTESIAN_POINT('',(27.4062428070496,-0.871550679329129,31.6237706303691));
#62238=CARTESIAN_POINT('Origin',(30.,-1.32966554433622E-14,31.6237706303681));
#62239=CARTESIAN_POINT('',(27.4331527756843,-0.847214001212589,31.5905494329235));
#62240=CARTESIAN_POINT('Ctrl Pts',(27.4331527756773,-0.847214001218912,
31.5905494329321));
#62241=CARTESIAN_POINT('Ctrl Pts',(27.4197799690437,-0.859308020910092,
31.6070390220085));
#62242=CARTESIAN_POINT('Ctrl Pts',(27.406242807055,-0.871550679324261,31.6237706303625));
#62243=CARTESIAN_POINT('',(27.4253970781159,-0.823344418487241,31.5905494329235));
#62244=CARTESIAN_POINT('Origin',(27.4239147889674,-0.837020829522197,31.5962049981138));
#62245=CARTESIAN_POINT('',(27.3893217156857,-0.819472915007445,31.6237706303691));
#62246=CARTESIAN_POINT('Ctrl Pts',(27.3893217156929,-0.819472915008222,
31.6237706303625));
#62247=CARTESIAN_POINT('Ctrl Pts',(27.4074695638765,-0.821420489548307,
31.6070390219952));
#62248=CARTESIAN_POINT('Ctrl Pts',(27.425397078135,-0.823344418489291,31.590549432906));
#62249=CARTESIAN_POINT('',(27.3458574166716,-0.665360135553609,31.6237706303691));
#62250=CARTESIAN_POINT('Origin',(30.,-1.32966554433622E-14,31.6237706303681));
#62251=CARTESIAN_POINT('',(27.3745938646118,-0.643209811098888,31.5905494329235));
#62252=CARTESIAN_POINT('Ctrl Pts',(27.3745938646043,-0.643209811104637,
31.5905494329321));
#62253=CARTESIAN_POINT('Ctrl Pts',(27.3603133960219,-0.65421733065347,31.6070390220085));
#62254=CARTESIAN_POINT('Ctrl Pts',(27.3458574166774,-0.665360135549176,
31.6237706303625));
#62255=CARTESIAN_POINT('',(27.3687348611467,-0.618805305313063,31.5905494329235));
#62256=CARTESIAN_POINT('Origin',(27.3661840916659,-0.632323260043008,31.5962050111235));
#62257=CARTESIAN_POINT('',(27.3330744616815,-0.612115296072114,31.6237706303691));
#62258=CARTESIAN_POINT('Ctrl Pts',(27.3330744616886,-0.612115296073467,
31.6237706303625));
#62259=CARTESIAN_POINT('Ctrl Pts',(27.3510135611755,-0.615480730649101,
31.6070390219952));
#62260=CARTESIAN_POINT('Ctrl Pts',(27.3687348611656,-0.61880530531661,31.590549432906));
#62261=CARTESIAN_POINT('',(27.3018356979118,-0.455067425287704,31.6237706303691));
#62262=CARTESIAN_POINT('Origin',(30.,-1.32966554433622E-14,31.6237706303681));
#62263=CARTESIAN_POINT('',(27.3322214554001,-0.435240018610796,31.5905494329235));
#62264=CARTESIAN_POINT('Ctrl Pts',(27.3322214553922,-0.435240018615941,
31.5905494329321));
#62265=CARTESIAN_POINT('Ctrl Pts',(27.3171213686986,-0.445093173004034,
31.6070390220085));
#62266=CARTESIAN_POINT('Ctrl Pts',(27.3018356979179,-0.455067425283735,
31.6237706303625));
#62267=CARTESIAN_POINT('',(27.328295268743,-0.410451051657984,31.5905494329235));
#62268=CARTESIAN_POINT('Origin',(27.3246917385075,-0.423727206709274,31.5962050315749));
#62269=CARTESIAN_POINT('',(27.2932696904637,-0.400983782787508,31.6237706303691));
#62270=CARTESIAN_POINT('Ctrl Pts',(27.2932696904707,-0.400983782789399,
31.6237706303625));
#62271=CARTESIAN_POINT('Ctrl Pts',(27.3108894407472,-0.405746328377308,
31.6070390219952));
#62272=CARTESIAN_POINT('Ctrl Pts',(27.3282952687616,-0.410451051662988,
31.5905494329059));
#62273=CARTESIAN_POINT('',(27.274449059305,-0.241969073019628,31.6237706303691));
#62274=CARTESIAN_POINT('Origin',(30.,-1.32966554433622E-14,31.6237706303681));
#62275=CARTESIAN_POINT('',(27.3062967880422,-0.224586826675978,31.5905494329235));
#62276=CARTESIAN_POINT('Ctrl Pts',(27.306296788034,-0.224586826680481,31.5905494329321));
#62277=CARTESIAN_POINT('Ctrl Pts',(27.2904701802848,-0.233224867934527,
31.6070390220085));
#62278=CARTESIAN_POINT('Ctrl Pts',(27.2744490593114,-0.241969073016143,
31.6237706303626));
#62279=CARTESIAN_POINT('',(27.3043276244395,-0.199566230780611,31.5905494329235));
#62280=CARTESIAN_POINT('Origin',(27.2996935428802,-0.212518732061225,31.5962050602856));
#62281=CARTESIAN_POINT('',(27.2701528116834,-0.18738007114138,31.6237706303691));
#62282=CARTESIAN_POINT('Ctrl Pts',(27.2701528116903,-0.187380071143839,
31.6237706303625));
#62283=CARTESIAN_POINT('Ctrl Pts',(27.2873445811368,-0.193510365066767,
31.6070390219952));
#62284=CARTESIAN_POINT('Ctrl Pts',(27.3043276244576,-0.199566230787083,
31.5905494329059));
#62285=CARTESIAN_POINT('',(27.2638663485853,-0.027378900953502,31.6237706303691));
#62286=CARTESIAN_POINT('Origin',(30.,-1.32966554433622E-14,31.6237706303681));
#62287=CARTESIAN_POINT('Ctrl Pts',(27.2969796967247,-0.0125489822758455,
31.5905494329321));
#62288=CARTESIAN_POINT('Ctrl Pts',(27.2805241442198,-0.0199186539990725,
31.6070390220085));
#62289=CARTESIAN_POINT('Ctrl Pts',(27.263866348592,-0.0273789009505331,
31.6237706303626));
#62290=CARTESIAN_POINT('',(27.2638663485853,0.0273789009535324,31.6237706303691));
#62291=CARTESIAN_POINT('Ctrl Pts',(27.263866348592,0.0273789009505529,31.6237706303626));
#62292=CARTESIAN_POINT('Ctrl Pts',(27.280524144233,0.0199186539931685,31.6070390219952));
#62293=CARTESIAN_POINT('Ctrl Pts',(27.2969796967508,0.012548982264161,31.5905494329059));
#62294=CARTESIAN_POINT('',(27.2701528116834,0.187380071141411,31.6237706303691));
#62295=CARTESIAN_POINT('Origin',(30.,-1.32966554433622E-14,31.6237706303681));
#62296=CARTESIAN_POINT('Ctrl Pts',(27.3043276244306,0.199566230777481,31.5905494329321));
#62297=CARTESIAN_POINT('Ctrl Pts',(27.2873445811231,0.193510365061917,31.6070390220085));
#62298=CARTESIAN_POINT('Ctrl Pts',(27.2701528116902,0.187380071143857,31.6237706303625));
#62299=CARTESIAN_POINT('',(27.2744490593051,0.241969073019658,31.6237706303691));
#62300=CARTESIAN_POINT('Ctrl Pts',(27.2744490593115,0.241969073016152,31.6237706303625));
#62301=CARTESIAN_POINT('Ctrl Pts',(27.2904701802976,0.233224867927605,31.6070390219952));
#62302=CARTESIAN_POINT('Ctrl Pts',(27.3062967880591,0.224586826666795,31.5905494329059));
#62303=CARTESIAN_POINT('',(27.2932696904637,0.40098378278754,31.6237706303691));
#62304=CARTESIAN_POINT('Origin',(30.,-1.32966554433622E-14,31.6237706303681));
#62305=CARTESIAN_POINT('Ctrl Pts',(27.3282952687339,0.410451051655568,31.5905494329321));
#62306=CARTESIAN_POINT('Ctrl Pts',(27.3108894407332,0.405746328373579,31.6070390220085));
#62307=CARTESIAN_POINT('Ctrl Pts',(27.2932696904707,0.400983782789452,31.6237706303626));
#62308=CARTESIAN_POINT('',(27.3018356979118,0.455067425287736,31.6237706303691));
#62309=CARTESIAN_POINT('Ctrl Pts',(27.3018356979179,0.455067425283746,31.6237706303626));
#62310=CARTESIAN_POINT('Ctrl Pts',(27.3171213687107,0.445093172996126,31.6070390219952));
#62311=CARTESIAN_POINT('Ctrl Pts',(27.3322214554162,0.435240018600305,31.5905494329059));
#62312=CARTESIAN_POINT('',(27.3330744616815,0.612115296072143,31.6237706303691));
#62313=CARTESIAN_POINT('Origin',(30.,-1.32966554433622E-14,31.6237706303681));
#62314=CARTESIAN_POINT('Ctrl Pts',(27.3687348611375,0.618805305311351,31.5905494329321));
#62315=CARTESIAN_POINT('Ctrl Pts',(27.3510135611613,0.615480730646445,31.6070390220085));
#62316=CARTESIAN_POINT('Ctrl Pts',(27.3330744616886,0.612115296073478,31.6237706303625));
#62317=CARTESIAN_POINT('',(27.3458574166716,0.665360135553637,31.6237706303691));
#62318=CARTESIAN_POINT('Ctrl Pts',(27.3458574166774,0.665360135549173,31.6237706303626));
#62319=CARTESIAN_POINT('Ctrl Pts',(27.3603133960334,0.65421733064462,31.6070390219952));
#62320=CARTESIAN_POINT('Ctrl Pts',(27.374593864627,0.643209811087154,31.5905494329059));
#62321=CARTESIAN_POINT('',(27.3893217156857,0.819472915007473,31.6237706303691));
#62322=CARTESIAN_POINT('Origin',(30.,-1.32966554433622E-14,31.6237706303681));
#62323=CARTESIAN_POINT('Ctrl Pts',(27.4253970781066,0.823344418486268,31.5905494329322));
#62324=CARTESIAN_POINT('Ctrl Pts',(27.4074695638621,0.821420489546793,31.6070390220085));
#62325=CARTESIAN_POINT('Ctrl Pts',(27.3893217156929,0.819472915008255,31.6237706303625));
#62326=CARTESIAN_POINT('',(27.4062428070496,0.871550679329156,31.6237706303691));
#62327=CARTESIAN_POINT('Ctrl Pts',(27.406242807055,0.87155067932429,31.6237706303625));
#62328=CARTESIAN_POINT('Ctrl Pts',(27.4197799690545,0.8593080209004,31.6070390219952));
#62329=CARTESIAN_POINT('Ctrl Pts',(27.4331527756986,0.847214001199735,31.5905494329059));
#62330=CARTESIAN_POINT('',(27.4616646694514,1.02177821091938,31.6237706303691));
#62331=CARTESIAN_POINT('Origin',(30.,-1.32966554433622E-14,31.6237706303681));
#62332=CARTESIAN_POINT('Ctrl Pts',(27.4979325782315,1.0228073395314,31.5905494329321));
#62333=CARTESIAN_POINT('Ctrl Pts',(27.4799093788056,1.02229591797904,31.6070390220085));
#62334=CARTESIAN_POINT('Ctrl Pts',(27.4616646694587,1.02177821091959,31.6237706303625));
#62335=CARTESIAN_POINT('',(27.4826195730339,1.0723678233466,31.6237706303691));
#62336=CARTESIAN_POINT('Ctrl Pts',(27.4826195730389,1.0723678233413,31.6237706303626));
#62337=CARTESIAN_POINT('Ctrl Pts',(27.4951544565765,1.05910079145835,31.6070390219952));
#62338=CARTESIAN_POINT('Ctrl Pts',(27.5075371534712,1.04599483526761,31.5905494329059));
#62339=CARTESIAN_POINT('',(27.549657304612,1.21778390438524,31.6237706303691));
#62340=CARTESIAN_POINT('Origin',(30.,-1.32966554433622E-14,31.6237706303681));
#62341=CARTESIAN_POINT('Ctrl Pts',(27.5858941560335,1.21596431321037,31.5905494329321));
#62342=CARTESIAN_POINT('Ctrl Pts',(27.5678863904439,1.21686855212906,31.6070390220085));
#62343=CARTESIAN_POINT('Ctrl Pts',(27.5496573046193,1.21778390438488,31.6237706303626));
#62344=CARTESIAN_POINT('',(27.5745168264644,1.26657346313462,31.6237706303691));
#62345=CARTESIAN_POINT('Ctrl Pts',(27.574516826469,1.26657346312892,31.6237706303626));
#62346=CARTESIAN_POINT('Ctrl Pts',(27.5859721498194,1.25236385345021,31.6070390219952));
#62347=CARTESIAN_POINT('Ctrl Pts',(27.5972883935207,1.23832676334747,31.5905494329059));
#62348=CARTESIAN_POINT('',(27.6527571173114,1.40628155512632,31.6237706303691));
#62349=CARTESIAN_POINT('Origin',(30.,-1.32966554433622E-14,31.6237706303681));
#62350=CARTESIAN_POINT('Ctrl Pts',(27.6887394991352,1.40162446254924,31.5905494329321));
#62351=CARTESIAN_POINT('Ctrl Pts',(27.670858191245,1.40393878700535,31.6070390220085));
#62352=CARTESIAN_POINT('Ctrl Pts',(27.6527571173186,1.40628155512539,31.6237706303625));
#62353=CARTESIAN_POINT('',(27.6813679902148,1.45297025634401,31.6237706303691));
#62354=CARTESIAN_POINT('Ctrl Pts',(27.6813679902189,1.452970256338,31.6237706303625));
#62355=CARTESIAN_POINT('Ctrl Pts',(27.6916731275044,1.43790567583238,31.6070390219952));
#62356=CARTESIAN_POINT('Ctrl Pts',(27.7018531496069,1.42302399514596,31.5905494329059));
#62357=CARTESIAN_POINT('',(27.7703284629199,1.58610901244398,31.6237706303691));
#62358=CARTESIAN_POINT('Origin',(30.,-1.32966554433622E-14,31.6237706303681));
#62359=CARTESIAN_POINT('Ctrl Pts',(27.8058345317968,1.57864313098906,31.5905494329321));
#62360=CARTESIAN_POINT('Ctrl Pts',(27.7881899258153,1.58235327240273,31.6070390220085));
#62361=CARTESIAN_POINT('Ctrl Pts',(27.770328462927,1.58610901244249,31.6237706303626));
#62362=CARTESIAN_POINT('',(27.8025142913288,1.63040900476139,31.6237706303691));
#62363=CARTESIAN_POINT('Ctrl Pts',(27.8025142913324,1.63040900475507,31.6237706303626));
#62364=CARTESIAN_POINT('Ctrl Pts',(27.8116057079549,1.61458233157081,31.6070390219952));
#62365=CARTESIAN_POINT('Ctrl Pts',(27.8205867452371,1.59894781081078,31.5905494329059));
#62366=CARTESIAN_POINT('',(27.9016464749956,1.75615758026516,31.6237706303691));
#62367=CARTESIAN_POINT('Origin',(30.,-1.32966554433622E-14,31.6237706303681));
#62368=CARTESIAN_POINT('Ctrl Pts',(27.9364573242039,1.74592893957422,31.5905494329321));
#62369=CARTESIAN_POINT('Ctrl Pts',(27.9191582049944,1.75101202368989,31.6070390220085));
#62370=CARTESIAN_POINT('Ctrl Pts',(27.9016464750026,1.7561575802631,31.6237706303626));
#62371=CARTESIAN_POINT('',(27.937208822575,1.79779573949841,31.6237706303691));
#62372=CARTESIAN_POINT('Ctrl Pts',(27.9372088225781,1.79779573949182,31.6237706303625));
#62373=CARTESIAN_POINT('Ctrl Pts',(27.9450304669308,1.78130455033204,31.6070390219952));
#62374=CARTESIAN_POINT('Ctrl Pts',(27.9527571483113,1.76501358151789,31.5905494329059));
#62375=CARTESIAN_POINT('',(28.0459015343263,1.91537885262234,31.6237706303691));
#62376=CARTESIAN_POINT('Origin',(30.,-1.32966554433622E-14,31.6237706303681));
#62377=CARTESIAN_POINT('Ctrl Pts',(28.0798025434049,1.90245051566662,31.5905494329321));
#62378=CARTESIAN_POINT('Ctrl Pts',(28.0629555657899,1.90887520358041,31.6070390220085));
#62379=CARTESIAN_POINT('Ctrl Pts',(28.0459015343331,1.91537885261975,31.6237706303626));
#62380=CARTESIAN_POINT('',(28.0846211473777,1.95409846567367,31.6237706303691));
#62381=CARTESIAN_POINT('Ctrl Pts',(28.0846211473803,1.95409846566688,31.6237706303625));
#62382=CARTESIAN_POINT('Ctrl Pts',(28.0911247964248,1.93704443419661,31.6070390219952));
#62383=CARTESIAN_POINT('Ctrl Pts',(28.0975494843436,1.9201974565684,31.5905494329059));
#62384=CARTESIAN_POINT('',(28.2022042605016,2.062791177425,31.6237706303691));
#62385=CARTESIAN_POINT('Origin',(30.,-1.32966554433622E-14,31.6237706303681));
#62386=CARTESIAN_POINT('Ctrl Pts',(28.2349864184563,2.04724285170094,31.5905494329321));
#62387=CARTESIAN_POINT('Ctrl Pts',(28.2186954496549,2.05496953307545,31.6070390220085));
#62388=CARTESIAN_POINT('Ctrl Pts',(28.2022042605082,2.0627911774219,31.6237706303626));
#62389=CARTESIAN_POINT('',(28.2438424197349,2.09835352500437,31.6237706303691));
#62390=CARTESIAN_POINT('Ctrl Pts',(28.2438424197369,2.09835352499738,31.6237706303625));
#62391=CARTESIAN_POINT('Ctrl Pts',(28.2489879763142,2.08084179499167,31.6070390219952));
#62392=CARTESIAN_POINT('Ctrl Pts',(28.2540710604339,2.06354267576863,31.5905494329059));
#62393=CARTESIAN_POINT('',(28.3695909952386,2.19748570867117,31.6237706303691));
#62394=CARTESIAN_POINT('Origin',(30.,-1.32966554433622E-14,31.6237706303681));
#62395=CARTESIAN_POINT('Ctrl Pts',(28.4010521891644,2.17941325477719,31.5905494329321));
#62396=CARTESIAN_POINT('Ctrl Pts',(28.3854176684167,2.18839429205237,31.6070390220085));
#62397=CARTESIAN_POINT('Ctrl Pts',(28.369590995245,2.19748570866756,31.6237706303626));
#62398=CARTESIAN_POINT('',(28.413890987556,2.22967153708007,31.6237706303691));
#62399=CARTESIAN_POINT('Ctrl Pts',(28.4138909875575,2.22967153707294,31.6237706303625));
#62400=CARTESIAN_POINT('Ctrl Pts',(28.4176467276003,2.21181007417053,31.6070390219952));
#62401=CARTESIAN_POINT('Ctrl Pts',(28.4213568690169,2.19416546817523,31.5905494329059));
#62402=CARTESIAN_POINT('',(28.547029743656,2.31863200978522,31.6237706303691));
#62403=CARTESIAN_POINT('Origin',(30.,-1.32966554433622E-14,31.6237706303681));
#62404=CARTESIAN_POINT('Ctrl Pts',(28.5769760048304,2.29814685040929,31.5905494329321));
#62405=CARTESIAN_POINT('Ctrl Pts',(28.5620943241557,2.30832687250382,31.6070390220085));
#62406=CARTESIAN_POINT('Ctrl Pts',(28.547029743662,2.31863200978111,31.6237706303625));
#62407=CARTESIAN_POINT('',(28.5937184448737,2.34724288268865,31.6237706303691));
#62408=CARTESIAN_POINT('Ctrl Pts',(28.5937184448746,2.34724288268143,31.6237706303626));
#62409=CARTESIAN_POINT('Ctrl Pts',(28.5960612129965,2.32914180874063,31.6070390219952));
#62410=CARTESIAN_POINT('Ctrl Pts',(28.5983755374545,2.31126050083645,31.5905494329059));
#62411=CARTESIAN_POINT('',(28.7334265368654,2.42548317353557,31.6237706303691));
#62412=CARTESIAN_POINT('Origin',(30.,-1.32966554433622E-14,31.6237706303681));
#62413=CARTESIAN_POINT('Ctrl Pts',(28.7616732366302,2.40271160649724,31.5905494329321));
#62414=CARTESIAN_POINT('Ctrl Pts',(28.7476361465385,2.4140278501897,31.6070390220085));
#62415=CARTESIAN_POINT('Ctrl Pts',(28.7334265368711,2.42548317353099,31.6237706303625));
#62416=CARTESIAN_POINT('',(28.7822160956148,2.45034269538798,31.6237706303691));
#62417=CARTESIAN_POINT('Ctrl Pts',(28.7822160956151,2.45034269538071,31.6237706303626));
#62418=CARTESIAN_POINT('Ctrl Pts',(28.7831314478717,2.4321136095416,31.6070390219952));
#62419=CARTESIAN_POINT('Ctrl Pts',(28.7840356867911,2.41410584393792,31.5905494329059));
#62420=CARTESIAN_POINT('',(28.9276321766534,2.51738042696607,31.6237706303691));
#62421=CARTESIAN_POINT('Origin',(30.,-1.32966554433622E-14,31.6237706303681));
#62422=CARTESIAN_POINT('',(28.9540051647184,2.49246284654199,31.5905494329235));
#62423=CARTESIAN_POINT('Ctrl Pts',(28.9540051647116,2.49246284654845,31.5905494329321));
#62424=CARTESIAN_POINT('Ctrl Pts',(28.9408992085311,2.50484554343346,31.6070390220085));
#62425=CARTESIAN_POINT('Ctrl Pts',(28.9276321766587,2.51738042696107,31.6237706303625));
#62426=CARTESIAN_POINT('',(28.9771926604684,2.50206742175908,31.5905494329235));
#62427=CARTESIAN_POINT('Origin',(28.9634421120889,2.50247209787257,31.5962049920587));
#62428=CARTESIAN_POINT('',(28.9782217890806,2.53833533054862,31.6237706303691));
#62429=CARTESIAN_POINT('Ctrl Pts',(28.9782217890804,2.53833533054134,31.6237706303625));
#62430=CARTESIAN_POINT('Ctrl Pts',(28.9777040820206,2.52009062117991,31.6070390219952));
#62431=CARTESIAN_POINT('Ctrl Pts',(28.9771926604678,2.50206742173986,31.5905494329059));
#62432=CARTESIAN_POINT('',(29.1284493206709,2.59375719295039,31.6237706303691));
#62433=CARTESIAN_POINT('Origin',(30.,-1.32966554433622E-14,31.6237706303681));
#62434=CARTESIAN_POINT('',(29.1527859987874,2.56684722431571,31.5905494329235));
#62435=CARTESIAN_POINT('Ctrl Pts',(29.1527859987811,2.56684722432269,31.5905494329321));
#62436=CARTESIAN_POINT('Ctrl Pts',(29.1406919790899,2.58022003095629,31.6070390220085));
#62437=CARTESIAN_POINT('Ctrl Pts',(29.1284493206758,2.59375719294498,31.6237706303625));
#62438=CARTESIAN_POINT('',(29.1766555815128,2.57460292188403,31.5905494329235));
#62439=CARTESIAN_POINT('Origin',(29.1629791704778,2.57608521103256,31.5962049981139));
#62440=CARTESIAN_POINT('',(29.1805270849926,2.61067828431428,31.6237706303691));
#62441=CARTESIAN_POINT('Ctrl Pts',(29.1805270849917,2.61067828430704,31.6237706303626));
#62442=CARTESIAN_POINT('Ctrl Pts',(29.1785795104516,2.59253043612347,31.6070390219952));
#62443=CARTESIAN_POINT('Ctrl Pts',(29.1766555815107,2.57460292186492,31.5905494329059));
#62444=CARTESIAN_POINT('',(29.3346398644464,2.65414258332837,31.6237706303691));
#62445=CARTESIAN_POINT('Origin',(30.,-1.32966554433622E-14,31.6237706303681));
#62446=CARTESIAN_POINT('',(29.3567901889011,2.6254061353882,31.5905494329235));
#62447=CARTESIAN_POINT('Ctrl Pts',(29.3567901888954,2.62540613539565,31.5905494329321));
#62448=CARTESIAN_POINT('Ctrl Pts',(29.3457826693465,2.63968660397804,31.6070390220085));
#62449=CARTESIAN_POINT('Ctrl Pts',(29.3346398644508,2.6541425833226,31.6237706303625));
#62450=CARTESIAN_POINT('',(29.3811946946869,2.63126513885323,31.5905494329235));
#62451=CARTESIAN_POINT('Origin',(29.367676739957,2.63381590833401,31.5962050111235));
#62452=CARTESIAN_POINT('',(29.3878847039279,2.66692553831851,31.6237706303691));
#62453=CARTESIAN_POINT('Ctrl Pts',(29.3878847039265,2.66692553831136,31.6237706303626));
#62454=CARTESIAN_POINT('Ctrl Pts',(29.3845192693509,2.64898643882447,31.6070390219952));
#62455=CARTESIAN_POINT('Ctrl Pts',(29.3811946946833,2.63126513883434,31.5905494329059));
#62456=CARTESIAN_POINT('',(29.5449325747123,2.69816430208817,31.6237706303691));
#62457=CARTESIAN_POINT('Origin',(30.,-1.32966554433622E-14,31.6237706303681));
#62458=CARTESIAN_POINT('',(29.5647599813892,2.6677785445999,31.5905494329235));
#62459=CARTESIAN_POINT('Ctrl Pts',(29.5647599813841,2.66777854460778,31.5905494329321));
#62460=CARTESIAN_POINT('Ctrl Pts',(29.554906826996,2.6828786313014,31.6070390220085));
#62461=CARTESIAN_POINT('Ctrl Pts',(29.5449325747163,2.69816430208207,31.6237706303625));
#62462=CARTESIAN_POINT('',(29.589548948342,2.67170473125694,31.5905494329235));
#62463=CARTESIAN_POINT('Origin',(29.5762727932907,2.67530826149244,31.5962050315749));
#62464=CARTESIAN_POINT('',(29.5990162172125,2.70673030953627,31.6237706303691));
#62465=CARTESIAN_POINT('Ctrl Pts',(29.5990162172106,2.70673030952925,31.6237706303625));
#62466=CARTESIAN_POINT('Ctrl Pts',(29.5942536716227,2.68911055925274,31.6070390219952));
#62467=CARTESIAN_POINT('Ctrl Pts',(29.589548948337,2.67170473123838,31.5905494329059));
#62468=CARTESIAN_POINT('',(29.7580309269804,2.72555094069491,31.6237706303691));
#62469=CARTESIAN_POINT('Origin',(30.,-1.32966554433622E-14,31.6237706303681));
#62470=CARTESIAN_POINT('',(29.775413173324,2.69370321195775,31.5905494329235));
#62471=CARTESIAN_POINT('Ctrl Pts',(29.7754131733195,2.69370321196601,31.5905494329321));
#62472=CARTESIAN_POINT('Ctrl Pts',(29.7667751320655,2.7095298197151,31.6070390220085));
#62473=CARTESIAN_POINT('Ctrl Pts',(29.7580309269838,2.72555094068851,31.6237706303625));
#62474=CARTESIAN_POINT('',(29.8004337692194,2.69567237556048,31.5905494329235));
#62475=CARTESIAN_POINT('Origin',(29.7874812679388,2.70030645711977,31.5962050602857));
#62476=CARTESIAN_POINT('',(29.8126199288586,2.72984718831658,31.6237706303691));
#62477=CARTESIAN_POINT('Ctrl Pts',(29.8126199288562,2.72984718830972,31.6237706303625));
#62478=CARTESIAN_POINT('Ctrl Pts',(29.8064896349333,2.71265541886322,31.6070390219952));
#62479=CARTESIAN_POINT('Ctrl Pts',(29.800433769213,2.69567237554238,31.5905494329059));
#62480=CARTESIAN_POINT('',(29.9726210990465,2.73613365141461,31.6237706303691));
#62481=CARTESIAN_POINT('Origin',(30.,-1.32966554433622E-14,31.6237706303681));
#62482=CARTESIAN_POINT('',(29.987451017728,2.70302030326666,31.5905494329235));
#62483=CARTESIAN_POINT('Ctrl Pts',(29.9874510177241,2.70302030327525,31.5905494329321));
#62484=CARTESIAN_POINT('Ctrl Pts',(29.9800813460009,2.71947585578017,31.6070390220085));
#62485=CARTESIAN_POINT('Ctrl Pts',(29.9726210990495,2.73613365140797,31.6237706303625));
#62486=CARTESIAN_POINT('Ctrl Pts',(30.,2.69489040503946,31.5823904050395));
#62487=CARTESIAN_POINT('Ctrl Pts',(29.9982996971592,2.69489040503946,31.5823904050395));
#62488=CARTESIAN_POINT('Ctrl Pts',(29.9965490639354,2.69522714758866,31.5827289231894));
#62489=CARTESIAN_POINT('Ctrl Pts',(29.9934248389279,2.69644647069982,31.5839540167345));
#62490=CARTESIAN_POINT('Ctrl Pts',(29.9920523583067,2.69733049287039,31.5848419899159));
#62491=CARTESIAN_POINT('Ctrl Pts',(29.9894391186861,2.6996015700298,31.5871217896387));
#62492=CARTESIAN_POINT('Ctrl Pts',(29.9882404972758,2.70125749446876,31.5887829779419));
#62493=CARTESIAN_POINT('Ctrl Pts',(29.987451017728,2.70302030326666,31.5905494329235));
#62494=CARTESIAN_POINT('',(30.,2.68872936963187,31.5762293696319));
#62495=CARTESIAN_POINT('',(30.,2.68872936963187,31.5762293696319));
#62496=CARTESIAN_POINT('',(30.,-2.68872936963189,31.5762293696319));
#62497=CARTESIAN_POINT('Origin',(30.,-1.32966554433622E-14,31.5762293696319));
#62498=CARTESIAN_POINT('Origin',(30.,-1.32966554433622E-14,31.5762293696319));
#62499=CARTESIAN_POINT('Origin',(30.,-1.32966554433622E-14,31.5430837392638));
#62500=CARTESIAN_POINT('',(30.,-2.67500000000001,31.5430837392638));
#62501=CARTESIAN_POINT('Origin',(30.,-1.32966554433622E-14,31.5430837392638));
#62502=CARTESIAN_POINT('Origin',(30.,-2.72187500000001,31.5430837392638));
#62503=CARTESIAN_POINT('Origin',(30.,-1.32966554433622E-14,16.));
#62504=CARTESIAN_POINT('',(30.,-2.67500000000001,31.06875));
#62505=CARTESIAN_POINT('Origin',(30.,-1.32966554433622E-14,31.06875));
#62506=CARTESIAN_POINT('',(30.,-2.67500000000001,16.));
#62507=CARTESIAN_POINT('Origin',(30.,-1.32966554433622E-14,31.06875));
#62508=CARTESIAN_POINT('',(30.,-2.60625000000001,31.));
#62509=CARTESIAN_POINT('Origin',(30.,-1.32966554433622E-14,31.));
#62510=CARTESIAN_POINT('Origin',(30.,-2.60625000000001,31.06875));
#62511=CARTESIAN_POINT('Origin',(30.,-1.32966554433622E-14,30.85));
#62512=CARTESIAN_POINT('',(30.,-1.65000000000002,31.));
#62513=CARTESIAN_POINT('Origin',(30.,-1.65000000000001,30.85));
#62514=CARTESIAN_POINT('Origin',(30.,-1.32966554433622E-14,31.));
#62515=CARTESIAN_POINT('Origin',(30.,-1.32966554433622E-14,31.6569162607362));
#62516=CARTESIAN_POINT('',(27.4723387620945,1.08324912480478,31.6569162607362));
#62517=CARTESIAN_POINT('Origin',(27.5075595450194,1.04598613791953,31.6570432561871));
#62518=CARTESIAN_POINT('',(27.5347062454699,1.21853465435945,31.6569162607362));
#62519=CARTESIAN_POINT('Origin',(30.,-1.32966554433622E-14,31.6569162607362));
#62520=CARTESIAN_POINT('Origin',(27.5859112932463,1.21595145595199,31.6570220656254));
#62521=CARTESIAN_POINT('Origin',(30.,-1.32966554433622E-14,31.6569162607362));
#62522=CARTESIAN_POINT('',(27.4467007962708,1.0213536000015,31.6569162607362));
#62523=CARTESIAN_POINT('Origin',(27.4979506713832,1.02279586647784,31.6570220656247));
#62524=CARTESIAN_POINT('',(27.3951399513465,0.881591814236737,31.6569162607362));
#62525=CARTESIAN_POINT('Origin',(27.4331757806072,0.847207087483285,31.6570432561871));
#62526=CARTESIAN_POINT('Origin',(30.,-1.32966554433622E-14,31.6569162607362));
#62527=CARTESIAN_POINT('Origin',(30.,-1.32966554433622E-14,31.6569162607362));
#62528=CARTESIAN_POINT('',(27.3744372857209,0.817875561065013,31.6569162607362));
#62529=CARTESIAN_POINT('Origin',(27.4254160156494,0.82333440037271,31.6570220656251));
#62530=CARTESIAN_POINT('',(27.3340009690024,0.674499196974899,31.6569162607362));
#62531=CARTESIAN_POINT('Origin',(27.3746173410621,0.643204723628532,31.6570432561866));
#62532=CARTESIAN_POINT('Origin',(30.,-1.32966554433622E-14,31.6569162607362));
#62533=CARTESIAN_POINT('Origin',(30.,-1.32966554433622E-14,31.6569162607362));
#62534=CARTESIAN_POINT('',(27.3183612423927,0.609355047323335,31.6569162607362));
#62535=CARTESIAN_POINT('Origin',(27.3687545263143,0.61879680390278,31.6570220656251));
#62536=CARTESIAN_POINT('',(27.2892987572189,0.463248067869971,31.6569162607362));
#62537=CARTESIAN_POINT('Origin',(27.3322452586394,0.435236788764015,31.6570432561869));
#62538=CARTESIAN_POINT('Origin',(30.,-1.32966554433622E-14,31.6569162607362));
#62539=CARTESIAN_POINT('Origin',(30.,-1.32966554433622E-14,31.6569162607362));
#62540=CARTESIAN_POINT('',(27.2788183937405,0.397077657083795,31.6569162607362));
#62541=CARTESIAN_POINT('Origin',(27.3283155403022,0.41044411936593,31.6570220656249));
#62542=CARTESIAN_POINT('',(27.2613089199969,0.249140860381007,31.6569162607362));
#62543=CARTESIAN_POINT('Origin',(27.3063207713152,0.224585474366194,31.6570432561871));
#62544=CARTESIAN_POINT('Origin',(30.,-1.32966554433622E-14,31.6569162607362));
#62545=CARTESIAN_POINT('Origin',(30.,-1.32966554433622E-14,31.6569162607362));
#62546=CARTESIAN_POINT('',(27.2560525345756,0.182352151046611,31.6569162607362));
#62547=CARTESIAN_POINT('Origin',(27.3043483774102,0.199560910346922,31.6570220656251));
#62548=CARTESIAN_POINT('',(27.2502040239902,0.0334976166400503,31.6569162607362));
#62549=CARTESIAN_POINT('Origin',(27.2970037121761,0.0125495158363338,31.6570432561875));
#62550=CARTESIAN_POINT('Origin',(30.,-1.32966554433622E-14,31.6569162607362));
#62551=CARTESIAN_POINT('Origin',(30.,-1.32966554433622E-14,31.6569162607362));
#62552=CARTESIAN_POINT('',(27.2502040239902,-0.0334976166400194,31.6569162607362));
#62553=CARTESIAN_POINT('Origin',(27.297000803166,-0.0125526580452972,31.6570220656252));
#62554=CARTESIAN_POINT('',(27.2560525345756,-0.18235215104658,31.6569162607362));
#62555=CARTESIAN_POINT('Origin',(27.3043515239857,-0.199563814630509,31.6570432561868));
#62556=CARTESIAN_POINT('Origin',(30.,-1.32966554433622E-14,31.6569162607362));
#62557=CARTESIAN_POINT('Origin',(30.,-1.32966554433622E-14,31.6569162607362));
#62558=CARTESIAN_POINT('',(27.2613089199969,-0.249140860380976,31.6569162607362));
#62559=CARTESIAN_POINT('Origin',(27.3063181178117,-0.22458883512474,31.6570220656265));
#62560=CARTESIAN_POINT('',(27.2788183937405,-0.397077657083763,31.6569162607362));
#62561=CARTESIAN_POINT('Origin',(27.3283189050458,-0.410446767819208,31.6570432561867));
#62562=CARTESIAN_POINT('Origin',(30.,-1.32966554433622E-14,31.6569162607362));
#62563=CARTESIAN_POINT('Origin',(30.,-1.32966554433622E-14,31.6569162607362));
#62564=CARTESIAN_POINT('',(27.2892987572189,-0.463248067869938,31.6569162607362));
#62565=CARTESIAN_POINT('Origin',(27.3322428769935,-0.4352403473568,31.6570220656245));
#62566=CARTESIAN_POINT('',(27.3183612423927,-0.609355047323306,31.6569162607362));
#62567=CARTESIAN_POINT('Origin',(27.3687580884808,-0.618799180197033,31.6570432561867));
#62568=CARTESIAN_POINT('Origin',(30.,-1.32966554433622E-14,31.6569162607362));
#62569=CARTESIAN_POINT('Origin',(30.,-1.32966554433622E-14,31.6569162607362));
#62570=CARTESIAN_POINT('',(27.3340009690024,-0.674499196974871,31.6569162607362));
#62571=CARTESIAN_POINT('Origin',(27.3746152459701,-0.643208458106799,31.6570220656281));
#62572=CARTESIAN_POINT('',(27.3744372857209,-0.817875561064986,31.6569162607362));
#62573=CARTESIAN_POINT('Origin',(27.4254197532793,-0.823336489857566,31.6570432561877));
#62574=CARTESIAN_POINT('Origin',(30.,-1.32966554433622E-14,31.6569162607362));
#62575=CARTESIAN_POINT('Origin',(30.,-1.32966554433622E-14,31.6569162607362));
#62576=CARTESIAN_POINT('',(27.3951399513465,-0.88159181423671,31.6569162607362));
#62577=CARTESIAN_POINT('Origin',(27.4331739849698,-0.847210974835381,31.6570220656246));
#62578=CARTESIAN_POINT('',(27.4467007962708,-1.02135360000148,31.6569162607362));
#62579=CARTESIAN_POINT('Origin',(27.4979545614299,-1.02279765627042,31.6570432561873));
#62580=CARTESIAN_POINT('Origin',(30.,-1.32966554433622E-14,31.6569162607362));
#62581=CARTESIAN_POINT('Origin',(30.,-1.32966554433622E-14,31.6569162607362));
#62582=CARTESIAN_POINT('',(27.4723387620945,-1.08324912480475,31.6569162607362));
#62583=CARTESIAN_POINT('Origin',(27.5075580599161,-1.04599015417175,31.657022065625));
#62584=CARTESIAN_POINT('',(27.5347062454699,-1.21853465435942,31.6569162607362));
#62585=CARTESIAN_POINT('Origin',(27.5859153117243,-1.21595293501783,31.6570432561869));
#62586=CARTESIAN_POINT('Origin',(30.,-1.32966554433622E-14,31.6569162607362));
#62587=CARTESIAN_POINT('Origin',(30.,-1.32966554433622E-14,31.6569162607362));
#62588=CARTESIAN_POINT('',(27.5651214449068,-1.27822784430149,31.6569162607362));
#62589=CARTESIAN_POINT('Origin',(27.5973088682438,-1.23832045638074,31.6570220656251));
#62590=CARTESIAN_POINT('',(27.637911050459,-1.40820303736935,31.6569162607362));
#62591=CARTESIAN_POINT('Origin',(27.6887596968882,-1.40161145957539,31.6570432561872));
#62592=CARTESIAN_POINT('Origin',(30.,-1.32966554433622E-14,31.6569162607362));
#62593=CARTESIAN_POINT('Origin',(30.,-1.32966554433622E-14,31.6569162607362));
#62594=CARTESIAN_POINT('',(27.6729159636906,-1.46532586408421,31.6569162607362));
#62595=CARTESIAN_POINT('Origin',(27.7018730663766,-1.42301610118967,31.6570220656267));
#62596=CARTESIAN_POINT('',(27.7556789192963,-1.58918938037887,31.6569162607362));
#62597=CARTESIAN_POINT('Origin',(27.8058536470839,-1.57862858340189,31.6570432561867));
#62598=CARTESIAN_POINT('Origin',(30.,-1.32966554433622E-14,31.6569162607362));
#62599=CARTESIAN_POINT('Origin',(30.,-1.32966554433622E-14,31.6569162607362));
#62600=CARTESIAN_POINT('',(27.7950577293922,-1.64338966264456,31.6569162607362));
#62601=CARTESIAN_POINT('Origin',(27.8206059812726,-1.59893837851,31.6570220656387));
#62602=CARTESIAN_POINT('',(27.8872837739086,-1.76037784239926,31.6569162607362));
#62603=CARTESIAN_POINT('Origin',(27.9364752391763,-1.7459129370637,31.6570432561874));
#62604=CARTESIAN_POINT('Origin',(30.,-1.32966554433622E-14,31.6569162607362));
#62605=CARTESIAN_POINT('Origin',(30.,-1.32966554433622E-14,31.6569162607362));
#62606=CARTESIAN_POINT('',(27.9307936974098,-1.81132141745219,31.6569162607362));
#62607=CARTESIAN_POINT('Origin',(27.9527755849842,-1.76500266908356,31.6570220656253));
#62608=CARTESIAN_POINT('',(28.0319142266042,-1.92071298963622,31.6569162607362));
#62609=CARTESIAN_POINT('Origin',(28.0798191476078,-1.90243315689441,31.657043256187));
#62610=CARTESIAN_POINT('Origin',(30.,-1.32966554433622E-14,31.6569162607362));
#62611=CARTESIAN_POINT('Origin',(30.,-1.32966554433622E-14,31.6569162607362));
#62612=CARTESIAN_POINT('',(28.0792870103637,-1.96808577339573,31.6569162607362));
#62613=CARTESIAN_POINT('Origin',(28.097567008002,-1.92018513125043,31.6570220656245));
#62614=CARTESIAN_POINT('',(28.1886785825478,-2.06920630259019,31.6569162607362));
#62615=CARTESIAN_POINT('Origin',(28.2350016095212,-2.0472242436889,31.6570432561873));
#62616=CARTESIAN_POINT('Origin',(30.,-1.32966554433622E-14,31.6569162607362));
#62617=CARTESIAN_POINT('Origin',(30.,-1.32966554433622E-14,31.6569162607362));
#62618=CARTESIAN_POINT('',(28.2396221576007,-2.11271622609136,31.6569162607362));
#62619=CARTESIAN_POINT('Origin',(28.2540875630401,-2.06352901355267,31.6570220656256));
#62620=CARTESIAN_POINT('',(28.3566103373554,-2.20494227060778,31.6569162607362));
#62621=CARTESIAN_POINT('Origin',(28.4010658734316,-2.17939351225073,31.6570432561869));
#62622=CARTESIAN_POINT('Origin',(30.,-1.32966554433622E-14,31.6569162607362));
#62623=CARTESIAN_POINT('Origin',(30.,-1.32966554433622E-14,31.6569162607362));
#62624=CARTESIAN_POINT('',(28.4108106196211,-2.2443210807037,31.6569162607362));
#62625=CARTESIAN_POINT('Origin',(28.4213722488256,-2.19415055329735,31.6570220656249));
#62626=CARTESIAN_POINT('',(28.5346741359157,-2.32708403630936,31.6569162607362));
#62627=CARTESIAN_POINT('Origin',(28.5769880979323,-2.29812609508764,31.6570432561867));
#62628=CARTESIAN_POINT('Origin',(30.,-1.32966554433622E-14,31.6569162607362));
#62629=CARTESIAN_POINT('Origin',(30.,-1.32966554433622E-14,31.6569162607362));
#62630=CARTESIAN_POINT('',(28.5917969626306,-2.362088949541,31.6569162607362));
#62631=CARTESIAN_POINT('Origin',(28.5983896996446,-2.31124442525031,31.6570220656249));
#62632=CARTESIAN_POINT('',(28.7217721556985,-2.43487855509312,31.6569162607362));
#62633=CARTESIAN_POINT('Origin',(28.7616836640096,-2.40268996634326,31.6570432561868));
#62634=CARTESIAN_POINT('Origin',(30.,-1.32966554433622E-14,31.6569162607362));
#62635=CARTESIAN_POINT('Origin',(30.,-1.32966554433622E-14,31.6569162607362));
#62636=CARTESIAN_POINT('',(28.7814653456405,-2.46529375453011,31.6569162607362));
#62637=CARTESIAN_POINT('Origin',(28.784048544048,-2.41408870675338,31.6570220656255));
#62638=CARTESIAN_POINT('',(28.9167508751952,-2.52766123790546,31.6569162607362));
#62639=CARTESIAN_POINT('Origin',(28.9540138620808,-2.49244045498024,31.6570432561872));
#62640=CARTESIAN_POINT('Origin',(30.,-1.32966554433622E-14,31.6569162607362));
#62641=CARTESIAN_POINT('Origin',(30.,-1.32966554433622E-14,31.6569162607362));
#62642=CARTESIAN_POINT('',(28.9786463999985,-2.55329920372917,31.6569162607362));
#62643=CARTESIAN_POINT('Origin',(28.9772041335221,-2.50204932861609,31.657022065625));
#62644=CARTESIAN_POINT('',(29.1184081857632,-2.60486004865345,31.6569162607362));
#62645=CARTESIAN_POINT('Origin',(29.1527929125168,-2.56682421939275,31.6570432561872));
#62646=CARTESIAN_POINT('Origin',(30.,-1.32966554433622E-14,31.6569162607362));
#62647=CARTESIAN_POINT('Origin',(30.,-1.32966554433622E-14,31.6569162607362));
#62648=CARTESIAN_POINT('',(29.182124438935,-2.6255627142791,31.6569162607362));
#62649=CARTESIAN_POINT('Origin',(29.1766655996274,-2.57458398435135,31.6570220656246));
#62650=CARTESIAN_POINT('',(29.3255008030251,-2.66599903099763,31.6569162607362));
#62651=CARTESIAN_POINT('Origin',(29.3567952763715,-2.62538265893786,31.6570432561866));
#62652=CARTESIAN_POINT('Origin',(30.,-1.32966554433622E-14,31.6569162607362));
#62653=CARTESIAN_POINT('Origin',(30.,-1.32966554433622E-14,31.6569162607362));
#62654=CARTESIAN_POINT('',(29.3906449526766,-2.6816387576073,31.6569162607362));
#62655=CARTESIAN_POINT('Origin',(29.3812031960972,-2.63124547368565,31.6570220656251));
#62656=CARTESIAN_POINT('',(29.53675193213,-2.71070124278106,31.6569162607362));
#62657=CARTESIAN_POINT('Origin',(29.5647632112362,-2.66775474136028,31.6570432561871));
#62658=CARTESIAN_POINT('Origin',(30.,-1.32966554433622E-14,31.6569162607362));
#62659=CARTESIAN_POINT('Origin',(30.,-1.32966554433622E-14,31.6569162607362));
#62660=CARTESIAN_POINT('',(29.6029223429162,-2.72118160625948,31.6569162607362));
#62661=CARTESIAN_POINT('Origin',(29.5895558806344,-2.67168445969898,31.6570220656245));
#62662=CARTESIAN_POINT('',(29.750859139619,-2.73869108000313,31.6569162607362));
#62663=CARTESIAN_POINT('Origin',(29.7754145256345,-2.69367922868347,31.6570432561876));
#62664=CARTESIAN_POINT('Origin',(30.,-1.32966554433622E-14,31.6569162607362));
#62665=CARTESIAN_POINT('Origin',(30.,-1.32966554433622E-14,31.6569162607362));
#62666=CARTESIAN_POINT('',(29.8176478489534,-2.74394746542436,31.6569162607362));
#62667=CARTESIAN_POINT('Origin',(29.800439089653,-2.69565162258972,31.6570220656252));
#62668=CARTESIAN_POINT('',(29.9665023833599,-2.74979597600977,31.6569162607362));
#62669=CARTESIAN_POINT('Origin',(29.9874504841626,-2.70299628782621,31.6570432561866));
#62670=CARTESIAN_POINT('Origin',(30.,-1.32966554433622E-14,31.6569162607362));
#62671=CARTESIAN_POINT('Origin',(30.,-1.32966554433622E-14,31.6569162607362));
#62672=CARTESIAN_POINT('',(30.03349761664,-2.74979597600977,31.6569162607362));
#62673=CARTESIAN_POINT('Origin',(30.0125526580435,-2.70299919683014,31.6570220656269));
#62674=CARTESIAN_POINT('',(30.1823521510466,-2.74394746542436,31.6569162607362));
#62675=CARTESIAN_POINT('Origin',(30.1995638146306,-2.69564847601399,31.6570432561868));
#62676=CARTESIAN_POINT('Origin',(30.,-1.32966554433622E-14,31.6569162607362));
#62677=CARTESIAN_POINT('Origin',(30.,-1.32966554433622E-14,31.6569162607362));
#62678=CARTESIAN_POINT('',(30.2491408603809,-2.73869108000313,31.6569162607362));
#62679=CARTESIAN_POINT('Origin',(30.2245888351274,-2.69368188219317,31.6570220656245));
#62680=CARTESIAN_POINT('',(30.3970776570837,-2.72118160625948,31.6569162607362));
#62681=CARTESIAN_POINT('Origin',(30.4104467678196,-2.67168109495285,31.6570432561872));
#62682=CARTESIAN_POINT('Origin',(30.,-1.32966554433622E-14,31.6569162607362));
#62683=CARTESIAN_POINT('Origin',(30.,-1.32966554433622E-14,31.6569162607362));
#62684=CARTESIAN_POINT('',(30.4632480678699,-2.71070124278107,31.6569162607362));
#62685=CARTESIAN_POINT('Origin',(30.4352403473562,-2.66775712300563,31.6570220656249));
#62686=CARTESIAN_POINT('',(30.6093550473233,-2.68163875760731,31.6569162607362));
#62687=CARTESIAN_POINT('Origin',(30.6187991801974,-2.63124191151731,31.6570432561874));
#62688=CARTESIAN_POINT('Origin',(30.,-1.32966554433622E-14,31.6569162607362));
#62689=CARTESIAN_POINT('Origin',(30.,-1.32966554433622E-14,31.6569162607362));
#62690=CARTESIAN_POINT('',(30.6744991969748,-2.66599903099764,31.6569162607362));
#62691=CARTESIAN_POINT('Origin',(30.6432084581108,-2.62538475403506,31.6570220656255));
#62692=CARTESIAN_POINT('',(30.817875561065,-2.62556271427912,31.6569162607362));
#62693=CARTESIAN_POINT('Origin',(30.8233364898573,-2.57458024672293,31.6570432561868));
#62694=CARTESIAN_POINT('Origin',(30.,-1.32966554433622E-14,31.6569162607362));
#62695=CARTESIAN_POINT('Origin',(30.,-1.32966554433622E-14,31.6569162607362));
#62696=CARTESIAN_POINT('',(30.8815918142367,-2.60486004865346,31.6569162607362));
#62697=CARTESIAN_POINT('Origin',(30.8472109748348,-2.56682601502956,31.6570220656249));
#62698=CARTESIAN_POINT('',(31.0213536000014,-2.55329920372919,31.6569162607362));
#62699=CARTESIAN_POINT('Origin',(31.0227976562703,-2.50204543857134,31.6570432561867));
#62700=CARTESIAN_POINT('Origin',(30.,-1.32966554433622E-14,31.6569162607362));
#62701=CARTESIAN_POINT('Origin',(30.,-1.32966554433622E-14,31.6569162607362));
#62702=CARTESIAN_POINT('',(31.0832491248047,-2.52766123790547,31.6569162607362));
#62703=CARTESIAN_POINT('Origin',(31.0459901541642,-2.49244194007693,31.6570220656289));
#62704=CARTESIAN_POINT('',(31.2185346543594,-2.46529375453013,31.6569162607362));
#62705=CARTESIAN_POINT('Origin',(31.2159529350178,-2.41408468827489,31.6570432561872));
#62706=CARTESIAN_POINT('Origin',(30.,-1.32966554433622E-14,31.6569162607362));
#62707=CARTESIAN_POINT('Origin',(30.,-1.32966554433622E-14,31.6569162607362));
#62708=CARTESIAN_POINT('',(31.2782278443015,-2.43487855509314,31.6569162607362));
#62709=CARTESIAN_POINT('Origin',(31.238320456382,-2.40269113175716,31.6570220656245));
#62710=CARTESIAN_POINT('',(31.4082030373693,-2.36208894954102,31.6569162607362));
#62711=CARTESIAN_POINT('Origin',(31.4016114595753,-2.31124030311134,31.6570432561875));
#62712=CARTESIAN_POINT('Origin',(30.,-1.32966554433622E-14,31.6569162607362));
#62713=CARTESIAN_POINT('Origin',(30.,-1.32966554433622E-14,31.6569162607362));
#62714=CARTESIAN_POINT('',(31.4653258640842,-2.32708403630938,31.6569162607362));
#62715=CARTESIAN_POINT('Origin',(31.4230161011935,-2.29812693362589,31.657022065625));
#62716=CARTESIAN_POINT('',(31.5891893803788,-2.24432108070372,31.6569162607362));
#62717=CARTESIAN_POINT('Origin',(31.5786285834021,-2.1941463529175,31.6570432561862));
#62718=CARTESIAN_POINT('Origin',(30.,-1.32966554433622E-14,31.6569162607362));
#62719=CARTESIAN_POINT('Origin',(30.,-1.32966554433622E-14,31.6569162607362));
#62720=CARTESIAN_POINT('',(31.6433896626445,-2.2049422706078,31.6569162607362));
#62721=CARTESIAN_POINT('Origin',(31.5989383785409,-2.17939401874466,31.6570220656252));
#62722=CARTESIAN_POINT('',(31.7603778423992,-2.11271622609138,31.6569162607362));
#62723=CARTESIAN_POINT('Origin',(31.7459129370641,-2.0635247608251,31.6570432561869));
#62724=CARTESIAN_POINT('Origin',(30.,-1.32966554433622E-14,31.6569162607362));
#62725=CARTESIAN_POINT('Origin',(30.,-1.32966554433622E-14,31.6569162607362));
#62726=CARTESIAN_POINT('',(31.8113214174522,-2.06920630259022,31.6569162607362));
#62727=CARTESIAN_POINT('Origin',(31.7650026690826,-2.04722441501533,31.6570220656257));
#62728=CARTESIAN_POINT('',(31.9207129896362,-1.96808577339576,31.6569162607362));
#62729=CARTESIAN_POINT('Origin',(31.9024331568943,-1.92018085239205,31.657043256187));
#62730=CARTESIAN_POINT('Origin',(30.,-1.32966554433622E-14,31.6569162607362));
#62731=CARTESIAN_POINT('Origin',(30.,-1.32966554433622E-14,31.6569162607362));
#62732=CARTESIAN_POINT('',(31.9680857733957,-1.92071298963625,31.6569162607362));
#62733=CARTESIAN_POINT('Origin',(31.9201851312437,-1.90243299199549,31.6570220656273));
#62734=CARTESIAN_POINT('',(32.0692063025902,-1.81132141745222,31.6569162607362));
#62735=CARTESIAN_POINT('Origin',(32.0472242436891,-1.76499839047944,31.6570432561871));
#62736=CARTESIAN_POINT('Origin',(30.,-1.32966554433622E-14,31.6569162607362));
#62737=CARTESIAN_POINT('Origin',(30.,-1.32966554433622E-14,31.6569162607362));
#62738=CARTESIAN_POINT('',(32.1127162260913,-1.76037784239929,31.6569162607362));
#62739=CARTESIAN_POINT('Origin',(32.0635290135546,-1.74591243696045,31.6570220656248));
#62740=CARTESIAN_POINT('',(32.2049422706077,-1.64338966264459,31.6569162607362));
#62741=CARTESIAN_POINT('Origin',(32.1793935122505,-1.59893412656801,31.6570432561871));
#62742=CARTESIAN_POINT('Origin',(30.,-1.32966554433622E-14,31.6569162607362));
#62743=CARTESIAN_POINT('Origin',(30.,-1.32966554433622E-14,31.6569162607362));
#62744=CARTESIAN_POINT('',(32.2443210807037,-1.5891893803789,31.6569162607362));
#62745=CARTESIAN_POINT('Origin',(32.1941505532956,-1.57862775117404,31.6570220656256));
#62746=CARTESIAN_POINT('',(32.3270840363093,-1.46532586408424,31.6569162607362));
#62747=CARTESIAN_POINT('Origin',(32.2981260950875,-1.42301190206755,31.6570432561867));
#62748=CARTESIAN_POINT('Origin',(30.,-1.32966554433622E-14,31.6569162607362));
#62749=CARTESIAN_POINT('Origin',(30.,-1.32966554433622E-14,31.6569162607362));
#62750=CARTESIAN_POINT('',(32.362088949541,-1.40820303736938,31.6569162607362));
#62751=CARTESIAN_POINT('Origin',(32.3112444252322,-1.40161030035328,31.657022065632));
#62752=CARTESIAN_POINT('',(32.4348785550931,-1.27822784430152,31.6569162607362));
#62753=CARTESIAN_POINT('Origin',(32.4026899663432,-1.23831633599041,31.6570432561868));
#62754=CARTESIAN_POINT('Origin',(30.,-1.32966554433622E-14,31.6569162607362));
#62755=CARTESIAN_POINT('Origin',(30.,-1.32966554433622E-14,31.6569162607362));
#62756=CARTESIAN_POINT('',(32.4652937545301,-1.21853465435946,31.6569162607362));
#62757=CARTESIAN_POINT('Origin',(32.414088706754,-1.21595145595202,31.6570220656252));
#62758=CARTESIAN_POINT('',(32.5276612379054,-1.08324912480479,31.6569162607362));
#62759=CARTESIAN_POINT('Origin',(32.4924404549811,-1.04598613792014,31.6570432561868));
#62760=CARTESIAN_POINT('Origin',(30.,-1.32966554433622E-14,31.6569162607362));
#62761=CARTESIAN_POINT('Origin',(30.,-1.32966554433622E-14,31.6569162607362));
#62762=CARTESIAN_POINT('',(32.5532992037291,-1.02135360000151,31.6569162607362));
#62763=CARTESIAN_POINT('Origin',(32.5020493286151,-1.0227958664779,31.6570220656254));
#62764=CARTESIAN_POINT('',(32.6048600486534,-0.881591814236746,31.6569162607362));
#62765=CARTESIAN_POINT('Origin',(32.5668242193914,-0.847207087482045,31.6570432561878));
#62766=CARTESIAN_POINT('Origin',(30.,-1.32966554433622E-14,31.6569162607362));
#62767=CARTESIAN_POINT('Origin',(30.,-1.32966554433622E-14,31.6569162607362));
#62768=CARTESIAN_POINT('',(32.6255627142791,-0.817875561065022,31.6569162607362));
#62769=CARTESIAN_POINT('Origin',(32.5745839843496,-0.82333440037284,31.6570220656255));
#62770=CARTESIAN_POINT('',(32.6659990309976,-0.674499196974908,31.6569162607362));
#62771=CARTESIAN_POINT('Origin',(32.6253826589374,-0.643204723628158,31.6570432561868));
#62772=CARTESIAN_POINT('Origin',(30.,-1.32966554433622E-14,31.6569162607362));
#62773=CARTESIAN_POINT('Origin',(30.,-1.32966554433622E-14,31.6569162607362));
#62774=CARTESIAN_POINT('',(32.6816387576073,-0.609355047323343,31.6569162607362));
#62775=CARTESIAN_POINT('Origin',(32.6312454736857,-0.618796803902764,31.657022065625));
#62776=CARTESIAN_POINT('',(32.710701242781,-0.463248067869977,31.6569162607362));
#62777=CARTESIAN_POINT('Origin',(32.6677547413593,-0.435236788763208,31.6570432561875));
#62778=CARTESIAN_POINT('Origin',(30.,-1.32966554433622E-14,31.6569162607362));
#62779=CARTESIAN_POINT('Origin',(30.,-1.32966554433622E-14,31.6569162607362));
#62780=CARTESIAN_POINT('',(32.7211816062594,-0.397077657083801,31.6569162607362));
#62781=CARTESIAN_POINT('Origin',(32.6716844596186,-0.410444119388296,31.6570220656567));
#62782=CARTESIAN_POINT('',(32.7386910800031,-0.249140860381013,31.6569162607362));
#62783=CARTESIAN_POINT('Origin',(32.6936792286845,-0.224585474366052,31.6570432561872));
#62784=CARTESIAN_POINT('Origin',(30.,-1.32966554433622E-14,31.6569162607362));
#62785=CARTESIAN_POINT('Origin',(30.,-1.32966554433622E-14,31.6569162607362));
#62786=CARTESIAN_POINT('',(32.7439474654243,-0.182352151046618,31.6569162607362));
#62787=CARTESIAN_POINT('Origin',(32.695651622591,-0.19956091034649,31.6570220656247));
#62788=CARTESIAN_POINT('',(32.7497959760097,-0.0334976166400576,31.6569162607362));
#62789=CARTESIAN_POINT('Origin',(32.702996287825,-0.0125495158368562,31.657043256187));
#62790=CARTESIAN_POINT('Origin',(30.,-1.32966554433622E-14,31.6569162607362));
#62791=CARTESIAN_POINT('Origin',(30.,-1.32966554433622E-14,31.6569162607362));
#62792=CARTESIAN_POINT('',(32.7497959760097,0.0334976166400122,31.6569162607362));
#62793=CARTESIAN_POINT('Origin',(32.7029991968315,0.0125526580441019,31.6570220656263));
#62794=CARTESIAN_POINT('',(32.7439474654243,0.182352151046572,31.6569162607362));
#62795=CARTESIAN_POINT('Origin',(32.695648476013,0.199563814630937,31.6570432561873));
#62796=CARTESIAN_POINT('Origin',(30.,-1.32966554433622E-14,31.6569162607362));
#62797=CARTESIAN_POINT('Origin',(30.,-1.32966554433622E-14,31.6569162607362));
#62798=CARTESIAN_POINT('',(32.7386910800031,0.249140860380968,31.6569162607362));
#62799=CARTESIAN_POINT('Origin',(32.6936818821912,0.224588835126342,31.6570220656253));
#62800=CARTESIAN_POINT('',(32.7211816062594,0.397077657083756,31.6569162607362));
#62801=CARTESIAN_POINT('Origin',(32.6716810949533,0.410446767819417,31.657043256187));
#62802=CARTESIAN_POINT('Origin',(30.,-1.32966554433622E-14,31.6569162607362));
#62803=CARTESIAN_POINT('Origin',(30.,-1.32966554433622E-14,31.6569162607362));
#62804=CARTESIAN_POINT('',(32.710701242781,0.463248067869931,31.6569162607362));
#62805=CARTESIAN_POINT('Origin',(32.6677571230054,0.435240347356078,31.6570220656249));
#62806=CARTESIAN_POINT('',(32.6816387576073,0.609355047323298,31.6569162607362));
#62807=CARTESIAN_POINT('Origin',(32.6312419115184,0.618799180197174,31.657043256187));
#62808=CARTESIAN_POINT('Origin',(30.,-1.32966554433622E-14,31.6569162607362));
#62809=CARTESIAN_POINT('Origin',(30.,-1.32966554433622E-14,31.6569162607362));
#62810=CARTESIAN_POINT('',(32.6659990309976,0.674499196974863,31.6569162607362));
#62811=CARTESIAN_POINT('Origin',(32.6253847539863,0.643208458072405,31.6570220656495));
#62812=CARTESIAN_POINT('',(32.6255627142791,0.817875561064977,31.6569162607362));
#62813=CARTESIAN_POINT('Origin',(32.574580246722,0.823336489857403,31.6570432561872));
#62814=CARTESIAN_POINT('Origin',(30.,-1.32966554433622E-14,31.6569162607362));
#62815=CARTESIAN_POINT('Origin',(30.,-1.32966554433622E-14,31.6569162607362));
#62816=CARTESIAN_POINT('',(32.6048600486534,0.881591814236701,31.6569162607362));
#62817=CARTESIAN_POINT('Origin',(32.5668260150295,0.847210974834854,31.6570220656249));
#62818=CARTESIAN_POINT('',(32.5532992037291,1.02135360000147,31.6569162607362));
#62819=CARTESIAN_POINT('Origin',(32.5020454385711,1.02279765627039,31.6570432561869));
#62820=CARTESIAN_POINT('Origin',(30.,-1.32966554433622E-14,31.6569162607362));
#62821=CARTESIAN_POINT('Origin',(30.,-1.32966554433622E-14,31.6569162607362));
#62822=CARTESIAN_POINT('',(32.5276612379054,1.08324912480474,31.6569162607362));
#62823=CARTESIAN_POINT('Origin',(32.4924419400839,1.04599015417185,31.6570220656248));
#62824=CARTESIAN_POINT('',(32.4652937545301,1.21853465435941,31.6569162607362));
#62825=CARTESIAN_POINT('Origin',(32.4140846882753,1.2159529350178,31.657043256187));
#62826=CARTESIAN_POINT('Origin',(30.,-1.32966554433622E-14,31.6569162607362));
#62827=CARTESIAN_POINT('Origin',(30.,-1.32966554433622E-14,31.6569162607362));
#62828=CARTESIAN_POINT('',(32.4348785550931,1.27822784430148,31.6569162607362));
#62829=CARTESIAN_POINT('Origin',(32.4026911317566,1.23832045638126,31.6570220656248));
#62830=CARTESIAN_POINT('',(32.362088949541,1.40820303736934,31.6569162607362));
#62831=CARTESIAN_POINT('Origin',(32.3112403031114,1.40161145957535,31.6570432561874));
#62832=CARTESIAN_POINT('Origin',(30.,-1.32966554433622E-14,31.6569162607362));
#62833=CARTESIAN_POINT('Origin',(30.,-1.32966554433622E-14,31.6569162607362));
#62834=CARTESIAN_POINT('',(32.3270840363093,1.4653258640842,31.6569162607362));
#62835=CARTESIAN_POINT('Origin',(32.2981269336259,1.42301610119356,31.657022065625));
#62836=CARTESIAN_POINT('',(32.2443210807037,1.58918938037886,31.6569162607362));
#62837=CARTESIAN_POINT('Origin',(32.1941463529162,1.57862858340189,31.6570432561866));
#62838=CARTESIAN_POINT('Origin',(30.,-1.32966554433622E-14,31.6569162607362));
#62839=CARTESIAN_POINT('Origin',(30.,-1.32966554433622E-14,31.6569162607362));
#62840=CARTESIAN_POINT('',(32.2049422706078,1.64338966264455,31.6569162607362));
#62841=CARTESIAN_POINT('Origin',(32.1793940187453,1.59893837854221,31.6570220656245));
#62842=CARTESIAN_POINT('',(32.1127162260913,1.76037784239925,31.6569162607362));
#62843=CARTESIAN_POINT('Origin',(32.0635247608241,1.74591293706383,31.6570432561872));
#62844=CARTESIAN_POINT('Origin',(30.,-1.32966554433622E-14,31.6569162607362));
#62845=CARTESIAN_POINT('Origin',(30.,-1.32966554433622E-14,31.6569162607362));
#62846=CARTESIAN_POINT('',(32.0692063025902,1.81132141745218,31.6569162607362));
#62847=CARTESIAN_POINT('Origin',(32.0472244150162,1.76500266908448,31.6570220656248));
#62848=CARTESIAN_POINT('',(31.9680857733957,1.92071298963621,31.6569162607362));
#62849=CARTESIAN_POINT('Origin',(31.9201808523931,1.90243315689474,31.6570432561866));
#62850=CARTESIAN_POINT('Origin',(30.,-1.32966554433622E-14,31.6569162607362));
#62851=CARTESIAN_POINT('Origin',(30.,-1.32966554433622E-14,31.6569162607362));
#62852=CARTESIAN_POINT('',(31.9207129896362,1.96808577339572,31.6569162607362));
#62853=CARTESIAN_POINT('Origin',(31.9024329919958,1.92018513124459,31.657022065627));
#62854=CARTESIAN_POINT('',(31.8113214174522,2.06920630259018,31.6569162607362));
#62855=CARTESIAN_POINT('Origin',(31.7649983904793,2.04722424368911,31.6570432561871));
#62856=CARTESIAN_POINT('Origin',(30.,-1.32966554433622E-14,31.6569162607362));
#62857=CARTESIAN_POINT('Origin',(30.,-1.32966554433622E-14,31.6569162607362));
#62858=CARTESIAN_POINT('',(31.7603778423992,2.11271622609134,31.6569162607362));
#62859=CARTESIAN_POINT('Origin',(31.7459124369604,2.06352901355459,31.6570220656248));
#62860=CARTESIAN_POINT('',(31.6433896626445,2.20494227060776,31.6569162607362));
#62861=CARTESIAN_POINT('Origin',(31.5989341265682,2.17939351225069,31.657043256187));
#62862=CARTESIAN_POINT('Origin',(30.,-1.32966554433622E-14,31.6569162607362));
#62863=CARTESIAN_POINT('Origin',(30.,-1.32966554433622E-14,31.6569162607362));
#62864=CARTESIAN_POINT('',(31.5891893803789,2.24432108070368,31.6569162607362));
#62865=CARTESIAN_POINT('Origin',(31.5786277511742,2.19415055329685,31.6570220656251));
#62866=CARTESIAN_POINT('',(31.4653258640842,2.32708403630934,31.6569162607362));
#62867=CARTESIAN_POINT('Origin',(31.4230119020666,2.29812609508688,31.6570432561872));
#62868=CARTESIAN_POINT('Origin',(30.,-1.32966554433622E-14,31.6569162607362));
#62869=CARTESIAN_POINT('Origin',(30.,-1.32966554433622E-14,31.6569162607362));
#62870=CARTESIAN_POINT('',(31.4082030373693,2.36208894954099,31.6569162607362));
#62871=CARTESIAN_POINT('Origin',(31.4016103003533,2.31124442523252,31.6570220656319));
#62872=CARTESIAN_POINT('',(31.2782278443015,2.4348785550931,31.6569162607362));
#62873=CARTESIAN_POINT('Origin',(31.2383163359906,2.4026899663434,31.6570432561867));
#62874=CARTESIAN_POINT('Origin',(30.,-1.32966554433622E-14,31.6569162607362));
#62875=CARTESIAN_POINT('Origin',(30.,-1.32966554433622E-14,31.6569162607362));
#62876=CARTESIAN_POINT('',(31.2185346543594,2.46529375453009,31.6569162607362));
#62877=CARTESIAN_POINT('Origin',(31.215951455952,2.4140887067551,31.6570220656248));
#62878=CARTESIAN_POINT('',(31.0832491248047,2.52766123790544,31.6569162607362));
#62879=CARTESIAN_POINT('Origin',(31.045986137919,2.49244045498011,31.6570432561873));
#62880=CARTESIAN_POINT('Origin',(30.,-1.32966554433622E-14,31.6569162607362));
#62881=CARTESIAN_POINT('Origin',(30.,-1.32966554433622E-14,31.6569162607362));
#62882=CARTESIAN_POINT('',(31.0213536000015,2.55329920372915,31.6569162607362));
#62883=CARTESIAN_POINT('Origin',(31.0227958664779,2.50204932861496,31.6570220656254));
#62884=CARTESIAN_POINT('',(30.8815918142367,2.60486004865343,31.6569162607362));
#62885=CARTESIAN_POINT('Origin',(30.8472070874836,2.56682421939316,31.6570432561869));
#62886=CARTESIAN_POINT('Origin',(30.,-1.32966554433622E-14,31.6569162607362));
#62887=CARTESIAN_POINT('Origin',(30.,-1.32966554433622E-14,31.6569162607362));
#62888=CARTESIAN_POINT('',(30.817875561065,2.62556271427908,31.6569162607362));
#62889=CARTESIAN_POINT('Origin',(30.8233344003728,2.5745839843498,31.6570220656254));
#62890=CARTESIAN_POINT('',(30.6744991969749,2.6659990309976,31.6569162607362));
#62891=CARTESIAN_POINT('Origin',(30.6432047236281,2.62538265893739,31.6570432561868));
#62892=CARTESIAN_POINT('Origin',(30.,-1.32966554433622E-14,31.6569162607362));
#62893=CARTESIAN_POINT('Origin',(30.,-1.32966554433622E-14,31.6569162607362));
#62894=CARTESIAN_POINT('',(30.6093550473233,2.68163875760728,31.6569162607362));
#62895=CARTESIAN_POINT('Origin',(30.6187968039028,2.63124547368537,31.6570220656252));
#62896=CARTESIAN_POINT('',(30.4632480678699,2.71070124278104,31.6569162607362));
#62897=CARTESIAN_POINT('Origin',(30.4352367887645,2.66775474136143,31.6570432561865));
#62898=CARTESIAN_POINT('Origin',(30.,-1.32966554433622E-14,31.6569162607362));
#62899=CARTESIAN_POINT('Origin',(30.,-1.32966554433622E-14,31.6569162607362));
#62900=CARTESIAN_POINT('',(27.5651214449069,1.27822784430151,31.6569162607362));
#62901=CARTESIAN_POINT('Origin',(27.5973100336575,1.23831633598946,31.6570432561873));
#62902=CARTESIAN_POINT('',(27.637911050459,1.40820303736937,31.6569162607362));
#62903=CARTESIAN_POINT('Origin',(30.,-1.32966554433622E-14,31.6569162607362));
#62904=CARTESIAN_POINT('Origin',(27.6887555747495,1.40161030035545,31.6570220656248));
#62905=CARTESIAN_POINT('Origin',(30.,-1.32966554433622E-14,31.6569162607362));
#62906=CARTESIAN_POINT('',(27.6729159636906,1.46532586408423,31.6569162607362));
#62907=CARTESIAN_POINT('Origin',(27.7018739049127,1.42301190206727,31.6570432561868));
#62908=CARTESIAN_POINT('',(27.7556789192963,1.58918938037889,31.6569162607362));
#62909=CARTESIAN_POINT('Origin',(30.,-1.32966554433622E-14,31.6569162607362));
#62910=CARTESIAN_POINT('Origin',(27.805849446702,1.5786277511745,31.6570220656247));
#62911=CARTESIAN_POINT('Origin',(30.,-1.32966554433622E-14,31.6569162607362));
#62912=CARTESIAN_POINT('',(27.7950577293922,1.64338966264458,31.6569162607362));
#62913=CARTESIAN_POINT('Origin',(27.8206064877494,1.59893412656804,31.6570432561871));
#62914=CARTESIAN_POINT('',(27.8872837739086,1.76037784239928,31.6569162607362));
#62915=CARTESIAN_POINT('Origin',(30.,-1.32966554433622E-14,31.6569162607362));
#62916=CARTESIAN_POINT('Origin',(27.936470986445,1.74591243696058,31.6570220656246));
#62917=CARTESIAN_POINT('Origin',(30.,-1.32966554433622E-14,31.6569162607362));
#62918=CARTESIAN_POINT('',(27.9307936974098,1.81132141745221,31.6569162607362));
#62919=CARTESIAN_POINT('Origin',(27.9527757563104,1.76499839048029,31.6570432561867));
#62920=CARTESIAN_POINT('',(28.0319142266043,1.92071298963623,31.6569162607362));
#62921=CARTESIAN_POINT('Origin',(30.,-1.32966554433622E-14,31.6569162607362));
#62922=CARTESIAN_POINT('Origin',(28.0798148687497,1.90243299199796,31.6570220656246));
#62923=CARTESIAN_POINT('Origin',(30.,-1.32966554433622E-14,31.6569162607362));
#62924=CARTESIAN_POINT('',(28.0792870103638,1.96808577339574,31.6569162607362));
#62925=CARTESIAN_POINT('Origin',(28.0975668431059,1.92018085239124,31.6570432561874));
#62926=CARTESIAN_POINT('',(28.1886785825478,2.0692063025902,31.6569162607362));
#62927=CARTESIAN_POINT('Origin',(30.,-1.32966554433622E-14,31.6569162607362));
#62928=CARTESIAN_POINT('Origin',(28.2349973309159,2.04722441501599,31.657022065625));
#62929=CARTESIAN_POINT('Origin',(30.,-1.32966554433622E-14,31.6569162607362));
#62930=CARTESIAN_POINT('',(28.2396221576007,2.11271622609137,31.6569162607362));
#62931=CARTESIAN_POINT('Origin',(28.2540870629359,2.06352476082518,31.6570432561869));
#62932=CARTESIAN_POINT('',(28.3566103373554,2.20494227060779,31.6569162607362));
#62933=CARTESIAN_POINT('Origin',(30.,-1.32966554433622E-14,31.6569162607362));
#62934=CARTESIAN_POINT('Origin',(28.4010616214895,2.17939401872761,31.6570220656385));
#62935=CARTESIAN_POINT('Origin',(30.,-1.32966554433622E-14,31.6569162607362));
#62936=CARTESIAN_POINT('',(28.4108106196211,2.2443210807037,31.6569162607362));
#62937=CARTESIAN_POINT('Origin',(28.4213714165984,2.19414635291463,31.6570432561873));
#62938=CARTESIAN_POINT('',(28.5346741359158,2.32708403630936,31.6569162607362));
#62939=CARTESIAN_POINT('Origin',(30.,-1.32966554433622E-14,31.6569162607362));
#62940=CARTESIAN_POINT('Origin',(28.5769838988101,2.29812693362349,31.6570220656266));
#62941=CARTESIAN_POINT('Origin',(30.,-1.32966554433622E-14,31.6569162607362));
#62942=CARTESIAN_POINT('',(28.5917969626306,2.36208894954101,31.6569162607362));
#62943=CARTESIAN_POINT('Origin',(28.5983885404246,2.31124030311217,31.6570432561871));
#62944=CARTESIAN_POINT('',(28.7217721556985,2.43487855509312,31.6569162607362));
#62945=CARTESIAN_POINT('Origin',(30.,-1.32966554433622E-14,31.6569162607362));
#62946=CARTESIAN_POINT('Origin',(28.7616795436181,2.40269113175706,31.6570220656245));
#62947=CARTESIAN_POINT('Origin',(30.,-1.32966554433622E-14,31.6569162607362));
#62948=CARTESIAN_POINT('',(28.7814653456406,2.46529375453011,31.6569162607362));
#62949=CARTESIAN_POINT('Origin',(28.7840470649822,2.41408468827519,31.6570432561871));
#62950=CARTESIAN_POINT('',(28.9167508751953,2.52766123790545,31.6569162607362));
#62951=CARTESIAN_POINT('Origin',(30.,-1.32966554433622E-14,31.6569162607362));
#62952=CARTESIAN_POINT('Origin',(28.9540098458282,2.49244194008388,31.6570220656249));
#62953=CARTESIAN_POINT('Origin',(30.,-1.32966554433622E-14,31.6569162607362));
#62954=CARTESIAN_POINT('',(28.9786463999985,2.55329920372917,31.6569162607362));
#62955=CARTESIAN_POINT('Origin',(28.9772023437296,2.50204543857058,31.657043256187));
#62956=CARTESIAN_POINT('',(29.1184081857633,2.60486004865344,31.6569162607362));
#62957=CARTESIAN_POINT('Origin',(30.,-1.32966554433622E-14,31.6569162607362));
#62958=CARTESIAN_POINT('Origin',(29.1527890251647,2.56682601503002,31.6570220656247));
#62959=CARTESIAN_POINT('Origin',(30.,-1.32966554433622E-14,31.6569162607362));
#62960=CARTESIAN_POINT('',(29.182124438935,2.62556271427909,31.6569162607362));
#62961=CARTESIAN_POINT('Origin',(29.1766635101426,2.57458024672254,31.657043256187));
#62962=CARTESIAN_POINT('',(29.3255008030251,2.66599903099761,31.6569162607362));
#62963=CARTESIAN_POINT('Origin',(30.,-1.32966554433622E-14,31.6569162607362));
#62964=CARTESIAN_POINT('Origin',(29.356791541893,2.62538475403008,31.657022065628));
#62965=CARTESIAN_POINT('Origin',(30.,-1.32966554433622E-14,31.6569162607362));
#62966=CARTESIAN_POINT('',(29.3906449526767,2.68163875760729,31.6569162607362));
#62967=CARTESIAN_POINT('Origin',(29.3812008198028,2.6312419115181,31.6570432561872));
#62968=CARTESIAN_POINT('',(29.5367519321301,2.71070124278105,31.6569162607362));
#62969=CARTESIAN_POINT('Origin',(30.,-1.32966554433622E-14,31.6569162607362));
#62970=CARTESIAN_POINT('Origin',(29.5647596526443,2.66775712300484,31.6570220656252));
#62971=CARTESIAN_POINT('Origin',(30.,-1.32966554433622E-14,31.6569162607362));
#62972=CARTESIAN_POINT('',(29.6029223429162,2.72118160625946,31.6569162607362));
#62973=CARTESIAN_POINT('Origin',(29.5895532321803,2.67168109495224,31.6570432561874));
#62974=CARTESIAN_POINT('',(29.750859139619,2.7386910800031,31.6569162607362));
#62975=CARTESIAN_POINT('Origin',(30.,-1.32966554433622E-14,31.6569162607362));
#62976=CARTESIAN_POINT('Origin',(29.7754111648735,2.69368188219135,31.6570220656252));
#62977=CARTESIAN_POINT('Origin',(30.,-1.32966554433622E-14,31.6569162607362));
#62978=CARTESIAN_POINT('',(29.8176478489534,2.74394746542433,31.6569162607362));
#62979=CARTESIAN_POINT('Origin',(29.8004361853695,2.6956484760142,31.6570432561868));
#62980=CARTESIAN_POINT('',(29.9665023833599,2.74979597600974,31.6569162607362));
#62981=CARTESIAN_POINT('Origin',(30.,-1.32966554433622E-14,31.6569162607362));
#62982=CARTESIAN_POINT('Origin',(29.9874473419551,2.70299919683309,31.6570220656256));
#62983=CARTESIAN_POINT('Origin',(30.,-1.32966554433622E-14,31.6569162607362));
#62984=CARTESIAN_POINT('',(30.3970776570838,2.72118160625945,31.6569162607362));
#62985=CARTESIAN_POINT('Origin',(30.4104441193885,2.67168445961759,31.6570220656571));
#62986=CARTESIAN_POINT('',(30.249140860381,2.7386910800031,31.6569162607362));
#62987=CARTESIAN_POINT('Origin',(30.2245854743662,2.69367922868485,31.657043256187));
#62988=CARTESIAN_POINT('Origin',(30.,-1.32966554433622E-14,31.6569162607362));
#62989=CARTESIAN_POINT('Origin',(30.,-1.32966554433622E-14,16.));
#62990=CARTESIAN_POINT('',(27.4723387620945,1.08324912480478,33.8305837392638));
#62991=CARTESIAN_POINT('',(27.4723387620945,1.08324912480478,16.));
#62992=CARTESIAN_POINT('',(27.5347062454699,1.21853465435945,33.8305837392638));
#62993=CARTESIAN_POINT('Origin',(30.,-1.32966554433622E-14,33.8305837392638));
#62994=CARTESIAN_POINT('',(27.5347062454699,1.21853465435945,16.));
#62995=CARTESIAN_POINT('Origin',(30.,-1.32966554433622E-14,16.));
#62996=CARTESIAN_POINT('',(27.4467007962708,1.0213536000015,33.8305837392638));
#62997=CARTESIAN_POINT('',(27.4467007962708,1.0213536000015,16.));
#62998=CARTESIAN_POINT('',(27.3951399513465,0.881591814236741,33.8305837392638));
#62999=CARTESIAN_POINT('',(27.3951399513465,0.881591814236737,16.));
#63000=CARTESIAN_POINT('Origin',(30.,-1.32966554433622E-14,33.8305837392638));
#63001=CARTESIAN_POINT('Origin',(30.,-1.32966554433622E-14,16.));
#63002=CARTESIAN_POINT('',(27.3744372857209,0.817875561065013,33.8305837392638));
#63003=CARTESIAN_POINT('',(27.3744372857209,0.817875561065013,16.));
#63004=CARTESIAN_POINT('',(27.3340009690024,0.674499196974903,33.8305837392638));
#63005=CARTESIAN_POINT('',(27.3340009690024,0.674499196974899,16.));
#63006=CARTESIAN_POINT('Origin',(30.,-1.32966554433622E-14,33.8305837392638));
#63007=CARTESIAN_POINT('Origin',(30.,-1.32966554433622E-14,16.));
#63008=CARTESIAN_POINT('',(27.3183612423927,0.609355047323334,33.8305837392638));
#63009=CARTESIAN_POINT('',(27.3183612423927,0.609355047323335,16.));
#63010=CARTESIAN_POINT('',(27.2892987572189,0.463248067869974,33.8305837392638));
#63011=CARTESIAN_POINT('',(27.2892987572189,0.463248067869971,16.));
#63012=CARTESIAN_POINT('Origin',(30.,-1.32966554433622E-14,33.8305837392638));
#63013=CARTESIAN_POINT('Origin',(30.,-1.32966554433622E-14,16.));
#63014=CARTESIAN_POINT('',(27.2788183937405,0.397077657083793,33.8305837392638));
#63015=CARTESIAN_POINT('',(27.2788183937405,0.397077657083795,16.));
#63016=CARTESIAN_POINT('',(27.2613089199969,0.24914086038101,33.8305837392638));
#63017=CARTESIAN_POINT('',(27.2613089199969,0.249140860381007,16.));
#63018=CARTESIAN_POINT('Origin',(30.,-1.32966554433622E-14,33.8305837392638));
#63019=CARTESIAN_POINT('Origin',(30.,-1.32966554433622E-14,16.));
#63020=CARTESIAN_POINT('',(27.2560525345756,0.182352151046609,33.8305837392638));
#63021=CARTESIAN_POINT('',(27.2560525345756,0.182352151046611,16.));
#63022=CARTESIAN_POINT('',(27.2502040239902,0.0334976166400525,33.8305837392638));
#63023=CARTESIAN_POINT('',(27.2502040239902,0.0334976166400503,16.));
#63024=CARTESIAN_POINT('Origin',(30.,-1.32966554433622E-14,33.8305837392638));
#63025=CARTESIAN_POINT('Origin',(30.,-1.32966554433622E-14,16.));
#63026=CARTESIAN_POINT('',(27.2502040239902,-0.0334976166400219,33.8305837392638));
#63027=CARTESIAN_POINT('',(27.2502040239902,-0.0334976166400194,16.));
#63028=CARTESIAN_POINT('',(27.2560525345756,-0.182352151046578,33.8305837392638));
#63029=CARTESIAN_POINT('',(27.2560525345756,-0.18235215104658,16.));
#63030=CARTESIAN_POINT('Origin',(30.,-1.32966554433622E-14,33.8305837392638));
#63031=CARTESIAN_POINT('Origin',(30.,-1.32966554433622E-14,16.));
#63032=CARTESIAN_POINT('',(27.2613089199969,-0.249140860380979,33.8305837392638));
#63033=CARTESIAN_POINT('',(27.2613089199969,-0.249140860380976,16.));
#63034=CARTESIAN_POINT('',(27.2788183937405,-0.397077657083761,33.8305837392638));
#63035=CARTESIAN_POINT('',(27.2788183937405,-0.397077657083763,16.));
#63036=CARTESIAN_POINT('Origin',(30.,-1.32966554433622E-14,33.8305837392638));
#63037=CARTESIAN_POINT('Origin',(30.,-1.32966554433622E-14,16.));
#63038=CARTESIAN_POINT('',(27.2892987572189,-0.463248067869942,33.8305837392638));
#63039=CARTESIAN_POINT('',(27.2892987572189,-0.463248067869938,16.));
#63040=CARTESIAN_POINT('',(27.3183612423927,-0.609355047323305,33.8305837392638));
#63041=CARTESIAN_POINT('',(27.3183612423927,-0.609355047323306,16.));
#63042=CARTESIAN_POINT('Origin',(30.,-1.32966554433622E-14,33.8305837392638));
#63043=CARTESIAN_POINT('Origin',(30.,-1.32966554433622E-14,16.));
#63044=CARTESIAN_POINT('',(27.3340009690023,-0.674499196974875,33.8305837392638));
#63045=CARTESIAN_POINT('',(27.3340009690024,-0.674499196974871,16.));
#63046=CARTESIAN_POINT('',(27.3744372857209,-0.817875561064985,33.8305837392638));
#63047=CARTESIAN_POINT('',(27.3744372857209,-0.817875561064986,16.));
#63048=CARTESIAN_POINT('Origin',(30.,-1.32966554433622E-14,33.8305837392638));
#63049=CARTESIAN_POINT('Origin',(30.,-1.32966554433622E-14,16.));
#63050=CARTESIAN_POINT('',(27.3951399513465,-0.881591814236714,33.8305837392638));
#63051=CARTESIAN_POINT('',(27.3951399513465,-0.88159181423671,16.));
#63052=CARTESIAN_POINT('',(27.4467007962708,-1.02135360000148,33.8305837392638));
#63053=CARTESIAN_POINT('',(27.4467007962708,-1.02135360000148,16.));
#63054=CARTESIAN_POINT('Origin',(30.,-1.32966554433622E-14,33.8305837392638));
#63055=CARTESIAN_POINT('Origin',(30.,-1.32966554433622E-14,16.));
#63056=CARTESIAN_POINT('',(27.4723387620945,-1.08324912480476,33.8305837392638));
#63057=CARTESIAN_POINT('',(27.4723387620945,-1.08324912480475,16.));
#63058=CARTESIAN_POINT('',(27.5347062454699,-1.21853465435942,33.8305837392638));
#63059=CARTESIAN_POINT('',(27.5347062454699,-1.21853465435942,16.));
#63060=CARTESIAN_POINT('Origin',(30.,-1.32966554433622E-14,33.8305837392638));
#63061=CARTESIAN_POINT('Origin',(30.,-1.32966554433622E-14,16.));
#63062=CARTESIAN_POINT('',(27.5651214449068,-1.27822784430149,33.8305837392638));
#63063=CARTESIAN_POINT('',(27.5651214449068,-1.27822784430149,16.));
#63064=CARTESIAN_POINT('',(27.637911050459,-1.40820303736935,33.8305837392638));
#63065=CARTESIAN_POINT('',(27.637911050459,-1.40820303736935,16.));
#63066=CARTESIAN_POINT('Origin',(30.,-1.32966554433622E-14,33.8305837392638));
#63067=CARTESIAN_POINT('Origin',(30.,-1.32966554433622E-14,16.));
#63068=CARTESIAN_POINT('',(27.6729159636906,-1.46532586408422,33.8305837392638));
#63069=CARTESIAN_POINT('',(27.6729159636906,-1.46532586408421,16.));
#63070=CARTESIAN_POINT('',(27.7556789192963,-1.58918938037887,33.8305837392638));
#63071=CARTESIAN_POINT('',(27.7556789192963,-1.58918938037887,16.));
#63072=CARTESIAN_POINT('Origin',(30.,-1.32966554433622E-14,33.8305837392638));
#63073=CARTESIAN_POINT('Origin',(30.,-1.32966554433622E-14,16.));
#63074=CARTESIAN_POINT('',(27.7950577293922,-1.64338966264456,33.8305837392638));
#63075=CARTESIAN_POINT('',(27.7950577293922,-1.64338966264456,16.));
#63076=CARTESIAN_POINT('',(27.8872837739086,-1.76037784239926,33.8305837392638));
#63077=CARTESIAN_POINT('',(27.8872837739086,-1.76037784239926,16.));
#63078=CARTESIAN_POINT('Origin',(30.,-1.32966554433622E-14,33.8305837392638));
#63079=CARTESIAN_POINT('Origin',(30.,-1.32966554433622E-14,16.));
#63080=CARTESIAN_POINT('',(27.9307936974098,-1.81132141745219,33.8305837392638));
#63081=CARTESIAN_POINT('',(27.9307936974098,-1.81132141745219,16.));
#63082=CARTESIAN_POINT('',(28.0319142266042,-1.92071298963622,33.8305837392638));
#63083=CARTESIAN_POINT('',(28.0319142266042,-1.92071298963622,16.));
#63084=CARTESIAN_POINT('Origin',(30.,-1.32966554433622E-14,33.8305837392638));
#63085=CARTESIAN_POINT('Origin',(30.,-1.32966554433622E-14,16.));
#63086=CARTESIAN_POINT('',(28.0792870103637,-1.96808577339574,33.8305837392638));
#63087=CARTESIAN_POINT('',(28.0792870103637,-1.96808577339573,16.));
#63088=CARTESIAN_POINT('',(28.1886785825478,-2.06920630259019,33.8305837392638));
#63089=CARTESIAN_POINT('',(28.1886785825478,-2.06920630259019,16.));
#63090=CARTESIAN_POINT('Origin',(30.,-1.32966554433622E-14,33.8305837392638));
#63091=CARTESIAN_POINT('Origin',(30.,-1.32966554433622E-14,16.));
#63092=CARTESIAN_POINT('',(28.2396221576007,-2.11271622609136,33.8305837392638));
#63093=CARTESIAN_POINT('',(28.2396221576007,-2.11271622609136,16.));
#63094=CARTESIAN_POINT('',(28.3566103373554,-2.20494227060778,33.8305837392638));
#63095=CARTESIAN_POINT('',(28.3566103373554,-2.20494227060778,16.));
#63096=CARTESIAN_POINT('Origin',(30.,-1.32966554433622E-14,33.8305837392638));
#63097=CARTESIAN_POINT('Origin',(30.,-1.32966554433622E-14,16.));
#63098=CARTESIAN_POINT('',(28.4108106196211,-2.2443210807037,33.8305837392638));
#63099=CARTESIAN_POINT('',(28.4108106196211,-2.2443210807037,16.));
#63100=CARTESIAN_POINT('',(28.5346741359157,-2.32708403630936,33.8305837392638));
#63101=CARTESIAN_POINT('',(28.5346741359157,-2.32708403630936,16.));
#63102=CARTESIAN_POINT('Origin',(30.,-1.32966554433622E-14,33.8305837392638));
#63103=CARTESIAN_POINT('Origin',(30.,-1.32966554433622E-14,16.));
#63104=CARTESIAN_POINT('',(28.5917969626306,-2.36208894954101,33.8305837392638));
#63105=CARTESIAN_POINT('',(28.5917969626306,-2.362088949541,16.));
#63106=CARTESIAN_POINT('',(28.7217721556985,-2.43487855509313,33.8305837392638));
#63107=CARTESIAN_POINT('',(28.7217721556985,-2.43487855509312,16.));
#63108=CARTESIAN_POINT('Origin',(30.,-1.32966554433622E-14,33.8305837392638));
#63109=CARTESIAN_POINT('Origin',(30.,-1.32966554433622E-14,16.));
#63110=CARTESIAN_POINT('',(28.7814653456405,-2.46529375453011,33.8305837392638));
#63111=CARTESIAN_POINT('',(28.7814653456405,-2.46529375453011,16.));
#63112=CARTESIAN_POINT('',(28.9167508751952,-2.52766123790546,33.8305837392638));
#63113=CARTESIAN_POINT('',(28.9167508751952,-2.52766123790546,16.));
#63114=CARTESIAN_POINT('Origin',(30.,-1.32966554433622E-14,33.8305837392638));
#63115=CARTESIAN_POINT('Origin',(30.,-1.32966554433622E-14,16.));
#63116=CARTESIAN_POINT('',(28.9786463999985,-2.55329920372918,33.8305837392638));
#63117=CARTESIAN_POINT('',(28.9786463999985,-2.55329920372917,16.));
#63118=CARTESIAN_POINT('',(29.1184081857632,-2.60486004865345,33.8305837392638));
#63119=CARTESIAN_POINT('',(29.1184081857632,-2.60486004865345,16.));
#63120=CARTESIAN_POINT('Origin',(30.,-1.32966554433622E-14,33.8305837392638));
#63121=CARTESIAN_POINT('Origin',(30.,-1.32966554433622E-14,16.));
#63122=CARTESIAN_POINT('',(29.182124438935,-2.62556271427911,33.8305837392638));
#63123=CARTESIAN_POINT('',(29.182124438935,-2.6255627142791,16.));
#63124=CARTESIAN_POINT('',(29.3255008030251,-2.66599903099763,33.8305837392638));
#63125=CARTESIAN_POINT('',(29.3255008030251,-2.66599903099763,16.));
#63126=CARTESIAN_POINT('Origin',(30.,-1.32966554433622E-14,33.8305837392638));
#63127=CARTESIAN_POINT('Origin',(30.,-1.32966554433622E-14,16.));
#63128=CARTESIAN_POINT('',(29.3906449526766,-2.68163875760731,33.8305837392638));
#63129=CARTESIAN_POINT('',(29.3906449526766,-2.6816387576073,16.));
#63130=CARTESIAN_POINT('',(29.53675193213,-2.71070124278107,33.8305837392638));
#63131=CARTESIAN_POINT('',(29.53675193213,-2.71070124278106,16.));
#63132=CARTESIAN_POINT('Origin',(30.,-1.32966554433622E-14,33.8305837392638));
#63133=CARTESIAN_POINT('Origin',(30.,-1.32966554433622E-14,16.));
#63134=CARTESIAN_POINT('',(29.6029223429162,-2.72118160625948,33.8305837392638));
#63135=CARTESIAN_POINT('',(29.6029223429162,-2.72118160625948,16.));
#63136=CARTESIAN_POINT('',(29.750859139619,-2.73869108000313,33.8305837392638));
#63137=CARTESIAN_POINT('',(29.750859139619,-2.73869108000313,16.));
#63138=CARTESIAN_POINT('Origin',(30.,-1.32966554433622E-14,33.8305837392638));
#63139=CARTESIAN_POINT('Origin',(30.,-1.32966554433622E-14,16.));
#63140=CARTESIAN_POINT('',(29.8176478489534,-2.74394746542436,33.8305837392638));
#63141=CARTESIAN_POINT('',(29.8176478489534,-2.74394746542436,16.));
#63142=CARTESIAN_POINT('',(29.9665023833599,-2.74979597600977,33.8305837392638));
#63143=CARTESIAN_POINT('',(29.9665023833599,-2.74979597600977,16.));
#63144=CARTESIAN_POINT('Origin',(30.,-1.32966554433622E-14,33.8305837392638));
#63145=CARTESIAN_POINT('Origin',(30.,-1.32966554433622E-14,16.));
#63146=CARTESIAN_POINT('',(30.03349761664,-2.74979597600977,33.8305837392638));
#63147=CARTESIAN_POINT('',(30.03349761664,-2.74979597600977,16.));
#63148=CARTESIAN_POINT('',(30.1823521510466,-2.74394746542436,33.8305837392638));
#63149=CARTESIAN_POINT('',(30.1823521510466,-2.74394746542436,16.));
#63150=CARTESIAN_POINT('Origin',(30.,-1.32966554433622E-14,33.8305837392638));
#63151=CARTESIAN_POINT('Origin',(30.,-1.32966554433622E-14,16.));
#63152=CARTESIAN_POINT('',(30.249140860381,-2.73869108000313,33.8305837392638));
#63153=CARTESIAN_POINT('',(30.2491408603809,-2.73869108000313,16.));
#63154=CARTESIAN_POINT('',(30.3970776570837,-2.72118160625949,33.8305837392638));
#63155=CARTESIAN_POINT('',(30.3970776570837,-2.72118160625948,16.));
#63156=CARTESIAN_POINT('Origin',(30.,-1.32966554433622E-14,33.8305837392638));
#63157=CARTESIAN_POINT('Origin',(30.,-1.32966554433622E-14,16.));
#63158=CARTESIAN_POINT('',(30.4632480678699,-2.71070124278108,33.8305837392638));
#63159=CARTESIAN_POINT('',(30.4632480678699,-2.71070124278107,16.));
#63160=CARTESIAN_POINT('',(30.6093550473233,-2.68163875760732,33.8305837392638));
#63161=CARTESIAN_POINT('',(30.6093550473233,-2.68163875760731,16.));
#63162=CARTESIAN_POINT('Origin',(30.,-1.32966554433622E-14,33.8305837392638));
#63163=CARTESIAN_POINT('Origin',(30.,-1.32966554433622E-14,16.));
#63164=CARTESIAN_POINT('',(30.6744991969748,-2.66599903099764,33.8305837392638));
#63165=CARTESIAN_POINT('',(30.6744991969748,-2.66599903099764,16.));
#63166=CARTESIAN_POINT('',(30.817875561065,-2.62556271427912,33.8305837392638));
#63167=CARTESIAN_POINT('',(30.817875561065,-2.62556271427912,16.));
#63168=CARTESIAN_POINT('Origin',(30.,-1.32966554433622E-14,33.8305837392638));
#63169=CARTESIAN_POINT('Origin',(30.,-1.32966554433622E-14,16.));
#63170=CARTESIAN_POINT('',(30.8815918142367,-2.60486004865346,33.8305837392638));
#63171=CARTESIAN_POINT('',(30.8815918142367,-2.60486004865346,16.));
#63172=CARTESIAN_POINT('',(31.0213536000014,-2.55329920372919,33.8305837392638));
#63173=CARTESIAN_POINT('',(31.0213536000014,-2.55329920372919,16.));
#63174=CARTESIAN_POINT('Origin',(30.,-1.32966554433622E-14,33.8305837392638));
#63175=CARTESIAN_POINT('Origin',(30.,-1.32966554433622E-14,16.));
#63176=CARTESIAN_POINT('',(31.0832491248047,-2.52766123790547,33.8305837392638));
#63177=CARTESIAN_POINT('',(31.0832491248047,-2.52766123790547,16.));
#63178=CARTESIAN_POINT('',(31.2185346543594,-2.46529375453013,33.8305837392638));
#63179=CARTESIAN_POINT('',(31.2185346543594,-2.46529375453013,16.));
#63180=CARTESIAN_POINT('Origin',(30.,-1.32966554433622E-14,33.8305837392638));
#63181=CARTESIAN_POINT('Origin',(30.,-1.32966554433622E-14,16.));
#63182=CARTESIAN_POINT('',(31.2782278443015,-2.43487855509314,33.8305837392638));
#63183=CARTESIAN_POINT('',(31.2782278443015,-2.43487855509314,16.));
#63184=CARTESIAN_POINT('',(31.4082030373693,-2.36208894954103,33.8305837392638));
#63185=CARTESIAN_POINT('',(31.4082030373693,-2.36208894954102,16.));
#63186=CARTESIAN_POINT('Origin',(30.,-1.32966554433622E-14,33.8305837392638));
#63187=CARTESIAN_POINT('Origin',(30.,-1.32966554433622E-14,16.));
#63188=CARTESIAN_POINT('',(31.4653258640842,-2.32708403630938,33.8305837392638));
#63189=CARTESIAN_POINT('',(31.4653258640842,-2.32708403630938,16.));
#63190=CARTESIAN_POINT('',(31.5891893803788,-2.24432108070372,33.8305837392638));
#63191=CARTESIAN_POINT('',(31.5891893803788,-2.24432108070372,16.));
#63192=CARTESIAN_POINT('Origin',(30.,-1.32966554433622E-14,33.8305837392638));
#63193=CARTESIAN_POINT('Origin',(30.,-1.32966554433622E-14,16.));
#63194=CARTESIAN_POINT('',(31.6433896626445,-2.2049422706078,33.8305837392638));
#63195=CARTESIAN_POINT('',(31.6433896626445,-2.2049422706078,16.));
#63196=CARTESIAN_POINT('',(31.7603778423992,-2.11271622609139,33.8305837392638));
#63197=CARTESIAN_POINT('',(31.7603778423992,-2.11271622609138,16.));
#63198=CARTESIAN_POINT('Origin',(30.,-1.32966554433622E-14,33.8305837392638));
#63199=CARTESIAN_POINT('Origin',(30.,-1.32966554433622E-14,16.));
#63200=CARTESIAN_POINT('',(31.8113214174522,-2.06920630259022,33.8305837392638));
#63201=CARTESIAN_POINT('',(31.8113214174522,-2.06920630259022,16.));
#63202=CARTESIAN_POINT('',(31.9207129896362,-1.96808577339576,33.8305837392638));
#63203=CARTESIAN_POINT('',(31.9207129896362,-1.96808577339576,16.));
#63204=CARTESIAN_POINT('Origin',(30.,-1.32966554433622E-14,33.8305837392638));
#63205=CARTESIAN_POINT('Origin',(30.,-1.32966554433622E-14,16.));
#63206=CARTESIAN_POINT('',(31.9680857733957,-1.92071298963625,33.8305837392638));
#63207=CARTESIAN_POINT('',(31.9680857733957,-1.92071298963625,16.));
#63208=CARTESIAN_POINT('',(32.0692063025902,-1.81132141745222,33.8305837392638));
#63209=CARTESIAN_POINT('',(32.0692063025902,-1.81132141745222,16.));
#63210=CARTESIAN_POINT('Origin',(30.,-1.32966554433622E-14,33.8305837392638));
#63211=CARTESIAN_POINT('Origin',(30.,-1.32966554433622E-14,16.));
#63212=CARTESIAN_POINT('',(32.1127162260913,-1.76037784239929,33.8305837392638));
#63213=CARTESIAN_POINT('',(32.1127162260913,-1.76037784239929,16.));
#63214=CARTESIAN_POINT('',(32.2049422706078,-1.6433896626446,33.8305837392638));
#63215=CARTESIAN_POINT('',(32.2049422706077,-1.64338966264459,16.));
#63216=CARTESIAN_POINT('Origin',(30.,-1.32966554433622E-14,33.8305837392638));
#63217=CARTESIAN_POINT('Origin',(30.,-1.32966554433622E-14,16.));
#63218=CARTESIAN_POINT('',(32.2443210807037,-1.5891893803789,33.8305837392638));
#63219=CARTESIAN_POINT('',(32.2443210807037,-1.5891893803789,16.));
#63220=CARTESIAN_POINT('',(32.3270840363093,-1.46532586408425,33.8305837392638));
#63221=CARTESIAN_POINT('',(32.3270840363093,-1.46532586408424,16.));
#63222=CARTESIAN_POINT('Origin',(30.,-1.32966554433622E-14,33.8305837392638));
#63223=CARTESIAN_POINT('Origin',(30.,-1.32966554433622E-14,16.));
#63224=CARTESIAN_POINT('',(32.362088949541,-1.40820303736938,33.8305837392638));
#63225=CARTESIAN_POINT('',(32.362088949541,-1.40820303736938,16.));
#63226=CARTESIAN_POINT('',(32.4348785550931,-1.27822784430152,33.8305837392638));
#63227=CARTESIAN_POINT('',(32.4348785550931,-1.27822784430152,16.));
#63228=CARTESIAN_POINT('Origin',(30.,-1.32966554433622E-14,33.8305837392638));
#63229=CARTESIAN_POINT('Origin',(30.,-1.32966554433622E-14,16.));
#63230=CARTESIAN_POINT('',(32.4652937545301,-1.21853465435946,33.8305837392638));
#63231=CARTESIAN_POINT('',(32.4652937545301,-1.21853465435946,16.));
#63232=CARTESIAN_POINT('',(32.5276612379054,-1.08324912480479,33.8305837392638));
#63233=CARTESIAN_POINT('',(32.5276612379054,-1.08324912480479,16.));
#63234=CARTESIAN_POINT('Origin',(30.,-1.32966554433622E-14,33.8305837392638));
#63235=CARTESIAN_POINT('Origin',(30.,-1.32966554433622E-14,16.));
#63236=CARTESIAN_POINT('',(32.5532992037291,-1.02135360000151,33.8305837392638));
#63237=CARTESIAN_POINT('',(32.5532992037291,-1.02135360000151,16.));
#63238=CARTESIAN_POINT('',(32.6048600486534,-0.88159181423675,33.8305837392638));
#63239=CARTESIAN_POINT('',(32.6048600486534,-0.881591814236746,16.));
#63240=CARTESIAN_POINT('Origin',(30.,-1.32966554433622E-14,33.8305837392638));
#63241=CARTESIAN_POINT('Origin',(30.,-1.32966554433622E-14,16.));
#63242=CARTESIAN_POINT('',(32.6255627142791,-0.817875561065022,33.8305837392638));
#63243=CARTESIAN_POINT('',(32.6255627142791,-0.817875561065022,16.));
#63244=CARTESIAN_POINT('',(32.6659990309976,-0.674499196974912,33.8305837392638));
#63245=CARTESIAN_POINT('',(32.6659990309976,-0.674499196974908,16.));
#63246=CARTESIAN_POINT('Origin',(30.,-1.32966554433622E-14,33.8305837392638));
#63247=CARTESIAN_POINT('Origin',(30.,-1.32966554433622E-14,16.));
#63248=CARTESIAN_POINT('',(32.6816387576073,-0.609355047323342,33.8305837392638));
#63249=CARTESIAN_POINT('',(32.6816387576073,-0.609355047323343,16.));
#63250=CARTESIAN_POINT('',(32.710701242781,-0.463248067869981,33.8305837392638));
#63251=CARTESIAN_POINT('',(32.710701242781,-0.463248067869977,16.));
#63252=CARTESIAN_POINT('Origin',(30.,-1.32966554433622E-14,33.8305837392638));
#63253=CARTESIAN_POINT('Origin',(30.,-1.32966554433622E-14,16.));
#63254=CARTESIAN_POINT('',(32.7211816062594,-0.3970776570838,33.8305837392638));
#63255=CARTESIAN_POINT('',(32.7211816062594,-0.397077657083801,16.));
#63256=CARTESIAN_POINT('',(32.7386910800031,-0.249140860381016,33.8305837392638));
#63257=CARTESIAN_POINT('',(32.7386910800031,-0.249140860381013,16.));
#63258=CARTESIAN_POINT('Origin',(30.,-1.32966554433622E-14,33.8305837392638));
#63259=CARTESIAN_POINT('Origin',(30.,-1.32966554433622E-14,16.));
#63260=CARTESIAN_POINT('',(32.7439474654243,-0.182352151046616,33.8305837392638));
#63261=CARTESIAN_POINT('',(32.7439474654243,-0.182352151046618,16.));
#63262=CARTESIAN_POINT('',(32.7497959760097,-0.03349761664006,33.8305837392638));
#63263=CARTESIAN_POINT('',(32.7497959760097,-0.0334976166400576,16.));
#63264=CARTESIAN_POINT('Origin',(30.,-1.32966554433622E-14,33.8305837392638));
#63265=CARTESIAN_POINT('Origin',(30.,-1.32966554433622E-14,16.));
#63266=CARTESIAN_POINT('',(32.7497959760097,0.0334976166400146,33.8305837392638));
#63267=CARTESIAN_POINT('',(32.7497959760097,0.0334976166400122,16.));
#63268=CARTESIAN_POINT('',(32.7439474654243,0.18235215104657,33.8305837392638));
#63269=CARTESIAN_POINT('',(32.7439474654243,0.182352151046572,16.));
#63270=CARTESIAN_POINT('Origin',(30.,-1.32966554433622E-14,33.8305837392638));
#63271=CARTESIAN_POINT('Origin',(30.,-1.32966554433622E-14,16.));
#63272=CARTESIAN_POINT('',(32.7386910800031,0.249140860380971,33.8305837392638));
#63273=CARTESIAN_POINT('',(32.7386910800031,0.249140860380968,16.));
#63274=CARTESIAN_POINT('',(32.7211816062594,0.397077657083754,33.8305837392638));
#63275=CARTESIAN_POINT('',(32.7211816062594,0.397077657083756,16.));
#63276=CARTESIAN_POINT('Origin',(30.,-1.32966554433622E-14,33.8305837392638));
#63277=CARTESIAN_POINT('Origin',(30.,-1.32966554433622E-14,16.));
#63278=CARTESIAN_POINT('',(32.710701242781,0.463248067869934,33.8305837392638));
#63279=CARTESIAN_POINT('',(32.710701242781,0.463248067869931,16.));
#63280=CARTESIAN_POINT('',(32.6816387576073,0.609355047323297,33.8305837392638));
#63281=CARTESIAN_POINT('',(32.6816387576073,0.609355047323298,16.));
#63282=CARTESIAN_POINT('Origin',(30.,-1.32966554433622E-14,33.8305837392638));
#63283=CARTESIAN_POINT('Origin',(30.,-1.32966554433622E-14,16.));
#63284=CARTESIAN_POINT('',(32.6659990309976,0.674499196974867,33.8305837392638));
#63285=CARTESIAN_POINT('',(32.6659990309976,0.674499196974863,16.));
#63286=CARTESIAN_POINT('',(32.6255627142791,0.817875561064977,33.8305837392638));
#63287=CARTESIAN_POINT('',(32.6255627142791,0.817875561064977,16.));
#63288=CARTESIAN_POINT('Origin',(30.,-1.32966554433622E-14,33.8305837392638));
#63289=CARTESIAN_POINT('Origin',(30.,-1.32966554433622E-14,16.));
#63290=CARTESIAN_POINT('',(32.6048600486534,0.881591814236705,33.8305837392638));
#63291=CARTESIAN_POINT('',(32.6048600486534,0.881591814236701,16.));
#63292=CARTESIAN_POINT('',(32.5532992037292,1.02135360000147,33.8305837392638));
#63293=CARTESIAN_POINT('',(32.5532992037291,1.02135360000147,16.));
#63294=CARTESIAN_POINT('Origin',(30.,-1.32966554433622E-14,33.8305837392638));
#63295=CARTESIAN_POINT('Origin',(30.,-1.32966554433622E-14,16.));
#63296=CARTESIAN_POINT('',(32.5276612379054,1.08324912480475,33.8305837392638));
#63297=CARTESIAN_POINT('',(32.5276612379054,1.08324912480474,16.));
#63298=CARTESIAN_POINT('',(32.4652937545301,1.21853465435941,33.8305837392638));
#63299=CARTESIAN_POINT('',(32.4652937545301,1.21853465435941,16.));
#63300=CARTESIAN_POINT('Origin',(30.,-1.32966554433622E-14,33.8305837392638));
#63301=CARTESIAN_POINT('Origin',(30.,-1.32966554433622E-14,16.));
#63302=CARTESIAN_POINT('',(32.4348785550931,1.27822784430148,33.8305837392638));
#63303=CARTESIAN_POINT('',(32.4348785550931,1.27822784430148,16.));
#63304=CARTESIAN_POINT('',(32.362088949541,1.40820303736934,33.8305837392638));
#63305=CARTESIAN_POINT('',(32.362088949541,1.40820303736934,16.));
#63306=CARTESIAN_POINT('Origin',(30.,-1.32966554433622E-14,33.8305837392638));
#63307=CARTESIAN_POINT('Origin',(30.,-1.32966554433622E-14,16.));
#63308=CARTESIAN_POINT('',(32.3270840363093,1.4653258640842,33.8305837392638));
#63309=CARTESIAN_POINT('',(32.3270840363093,1.4653258640842,16.));
#63310=CARTESIAN_POINT('',(32.2443210807037,1.58918938037886,33.8305837392638));
#63311=CARTESIAN_POINT('',(32.2443210807037,1.58918938037886,16.));
#63312=CARTESIAN_POINT('Origin',(30.,-1.32966554433622E-14,33.8305837392638));
#63313=CARTESIAN_POINT('Origin',(30.,-1.32966554433622E-14,16.));
#63314=CARTESIAN_POINT('',(32.2049422706078,1.64338966264455,33.8305837392638));
#63315=CARTESIAN_POINT('',(32.2049422706078,1.64338966264455,16.));
#63316=CARTESIAN_POINT('',(32.1127162260914,1.76037784239925,33.8305837392638));
#63317=CARTESIAN_POINT('',(32.1127162260913,1.76037784239925,16.));
#63318=CARTESIAN_POINT('Origin',(30.,-1.32966554433622E-14,33.8305837392638));
#63319=CARTESIAN_POINT('Origin',(30.,-1.32966554433622E-14,16.));
#63320=CARTESIAN_POINT('',(32.0692063025902,1.81132141745218,33.8305837392638));
#63321=CARTESIAN_POINT('',(32.0692063025902,1.81132141745218,16.));
#63322=CARTESIAN_POINT('',(31.9680857733957,1.92071298963621,33.8305837392638));
#63323=CARTESIAN_POINT('',(31.9680857733957,1.92071298963621,16.));
#63324=CARTESIAN_POINT('Origin',(30.,-1.32966554433622E-14,33.8305837392638));
#63325=CARTESIAN_POINT('Origin',(30.,-1.32966554433622E-14,16.));
#63326=CARTESIAN_POINT('',(31.9207129896362,1.96808577339572,33.8305837392638));
#63327=CARTESIAN_POINT('',(31.9207129896362,1.96808577339572,16.));
#63328=CARTESIAN_POINT('',(31.8113214174522,2.06920630259018,33.8305837392638));
#63329=CARTESIAN_POINT('',(31.8113214174522,2.06920630259018,16.));
#63330=CARTESIAN_POINT('Origin',(30.,-1.32966554433622E-14,33.8305837392638));
#63331=CARTESIAN_POINT('Origin',(30.,-1.32966554433622E-14,16.));
#63332=CARTESIAN_POINT('',(31.7603778423992,2.11271622609135,33.8305837392638));
#63333=CARTESIAN_POINT('',(31.7603778423992,2.11271622609134,16.));
#63334=CARTESIAN_POINT('',(31.6433896626446,2.20494227060777,33.8305837392638));
#63335=CARTESIAN_POINT('',(31.6433896626445,2.20494227060776,16.));
#63336=CARTESIAN_POINT('Origin',(30.,-1.32966554433622E-14,33.8305837392638));
#63337=CARTESIAN_POINT('Origin',(30.,-1.32966554433622E-14,16.));
#63338=CARTESIAN_POINT('',(31.5891893803789,2.24432108070369,33.8305837392638));
#63339=CARTESIAN_POINT('',(31.5891893803789,2.24432108070368,16.));
#63340=CARTESIAN_POINT('',(31.4653258640842,2.32708403630934,33.8305837392638));
#63341=CARTESIAN_POINT('',(31.4653258640842,2.32708403630934,16.));
#63342=CARTESIAN_POINT('Origin',(30.,-1.32966554433622E-14,33.8305837392638));
#63343=CARTESIAN_POINT('Origin',(30.,-1.32966554433622E-14,16.));
#63344=CARTESIAN_POINT('',(31.4082030373693,2.36208894954099,33.8305837392638));
#63345=CARTESIAN_POINT('',(31.4082030373693,2.36208894954099,16.));
#63346=CARTESIAN_POINT('',(31.2782278443015,2.43487855509311,33.8305837392638));
#63347=CARTESIAN_POINT('',(31.2782278443015,2.4348785550931,16.));
#63348=CARTESIAN_POINT('Origin',(30.,-1.32966554433622E-14,33.8305837392638));
#63349=CARTESIAN_POINT('Origin',(30.,-1.32966554433622E-14,16.));
#63350=CARTESIAN_POINT('',(31.2185346543594,2.4652937545301,33.8305837392638));
#63351=CARTESIAN_POINT('',(31.2185346543594,2.46529375453009,16.));
#63352=CARTESIAN_POINT('',(31.0832491248047,2.52766123790544,33.8305837392638));
#63353=CARTESIAN_POINT('',(31.0832491248047,2.52766123790544,16.));
#63354=CARTESIAN_POINT('Origin',(30.,-1.32966554433622E-14,33.8305837392638));
#63355=CARTESIAN_POINT('Origin',(30.,-1.32966554433622E-14,16.));
#63356=CARTESIAN_POINT('',(31.0213536000015,2.55329920372916,33.8305837392638));
#63357=CARTESIAN_POINT('',(31.0213536000015,2.55329920372915,16.));
#63358=CARTESIAN_POINT('',(30.8815918142367,2.60486004865343,33.8305837392638));
#63359=CARTESIAN_POINT('',(30.8815918142367,2.60486004865343,16.));
#63360=CARTESIAN_POINT('Origin',(30.,-1.32966554433622E-14,33.8305837392638));
#63361=CARTESIAN_POINT('Origin',(30.,-1.32966554433622E-14,16.));
#63362=CARTESIAN_POINT('',(30.817875561065,2.62556271427909,33.8305837392638));
#63363=CARTESIAN_POINT('',(30.817875561065,2.62556271427908,16.));
#63364=CARTESIAN_POINT('',(30.6744991969749,2.66599903099761,33.8305837392638));
#63365=CARTESIAN_POINT('',(30.6744991969749,2.6659990309976,16.));
#63366=CARTESIAN_POINT('Origin',(30.,-1.32966554433622E-14,33.8305837392638));
#63367=CARTESIAN_POINT('Origin',(30.,-1.32966554433622E-14,16.));
#63368=CARTESIAN_POINT('',(30.6093550473233,2.68163875760729,33.8305837392638));
#63369=CARTESIAN_POINT('',(30.6093550473233,2.68163875760728,16.));
#63370=CARTESIAN_POINT('',(30.4632480678699,2.71070124278105,33.8305837392638));
#63371=CARTESIAN_POINT('',(30.4632480678699,2.71070124278104,16.));
#63372=CARTESIAN_POINT('Origin',(30.,-1.32966554433622E-14,33.8305837392638));
#63373=CARTESIAN_POINT('Origin',(30.,-1.32966554433622E-14,16.));
#63374=CARTESIAN_POINT('',(27.5651214449069,1.27822784430151,33.8305837392638));
#63375=CARTESIAN_POINT('',(27.5651214449069,1.27822784430151,16.));
#63376=CARTESIAN_POINT('',(27.637911050459,1.40820303736937,33.8305837392638));
#63377=CARTESIAN_POINT('Origin',(30.,-1.32966554433622E-14,33.8305837392638));
#63378=CARTESIAN_POINT('',(27.637911050459,1.40820303736937,16.));
#63379=CARTESIAN_POINT('Origin',(30.,-1.32966554433622E-14,16.));
#63380=CARTESIAN_POINT('',(27.6729159636906,1.46532586408424,33.8305837392638));
#63381=CARTESIAN_POINT('',(27.6729159636906,1.46532586408423,16.));
#63382=CARTESIAN_POINT('',(27.7556789192963,1.58918938037889,33.8305837392638));
#63383=CARTESIAN_POINT('Origin',(30.,-1.32966554433622E-14,33.8305837392638));
#63384=CARTESIAN_POINT('',(27.7556789192963,1.58918938037889,16.));
#63385=CARTESIAN_POINT('Origin',(30.,-1.32966554433622E-14,16.));
#63386=CARTESIAN_POINT('',(27.7950577293922,1.64338966264458,33.8305837392638));
#63387=CARTESIAN_POINT('',(27.7950577293922,1.64338966264458,16.));
#63388=CARTESIAN_POINT('',(27.8872837739086,1.76037784239928,33.8305837392638));
#63389=CARTESIAN_POINT('Origin',(30.,-1.32966554433622E-14,33.8305837392638));
#63390=CARTESIAN_POINT('',(27.8872837739086,1.76037784239928,16.));
#63391=CARTESIAN_POINT('Origin',(30.,-1.32966554433622E-14,16.));
#63392=CARTESIAN_POINT('',(27.9307936974098,1.81132141745221,33.8305837392638));
#63393=CARTESIAN_POINT('',(27.9307936974098,1.81132141745221,16.));
#63394=CARTESIAN_POINT('',(28.0319142266043,1.92071298963624,33.8305837392638));
#63395=CARTESIAN_POINT('Origin',(30.,-1.32966554433622E-14,33.8305837392638));
#63396=CARTESIAN_POINT('',(28.0319142266043,1.92071298963623,16.));
#63397=CARTESIAN_POINT('Origin',(30.,-1.32966554433622E-14,16.));
#63398=CARTESIAN_POINT('',(28.0792870103638,1.96808577339575,33.8305837392638));
#63399=CARTESIAN_POINT('',(28.0792870103638,1.96808577339574,16.));
#63400=CARTESIAN_POINT('',(28.1886785825478,2.06920630259021,33.8305837392638));
#63401=CARTESIAN_POINT('Origin',(30.,-1.32966554433622E-14,33.8305837392638));
#63402=CARTESIAN_POINT('',(28.1886785825478,2.0692063025902,16.));
#63403=CARTESIAN_POINT('Origin',(30.,-1.32966554433622E-14,16.));
#63404=CARTESIAN_POINT('',(28.2396221576007,2.11271622609138,33.8305837392638));
#63405=CARTESIAN_POINT('',(28.2396221576007,2.11271622609137,16.));
#63406=CARTESIAN_POINT('',(28.3566103373554,2.20494227060779,33.8305837392638));
#63407=CARTESIAN_POINT('Origin',(30.,-1.32966554433622E-14,33.8305837392638));
#63408=CARTESIAN_POINT('',(28.3566103373554,2.20494227060779,16.));
#63409=CARTESIAN_POINT('Origin',(30.,-1.32966554433622E-14,16.));
#63410=CARTESIAN_POINT('',(28.4108106196211,2.24432108070371,33.8305837392638));
#63411=CARTESIAN_POINT('',(28.4108106196211,2.2443210807037,16.));
#63412=CARTESIAN_POINT('',(28.5346741359158,2.32708403630936,33.8305837392638));
#63413=CARTESIAN_POINT('Origin',(30.,-1.32966554433622E-14,33.8305837392638));
#63414=CARTESIAN_POINT('',(28.5346741359158,2.32708403630936,16.));
#63415=CARTESIAN_POINT('Origin',(30.,-1.32966554433622E-14,16.));
#63416=CARTESIAN_POINT('',(28.5917969626306,2.36208894954101,33.8305837392638));
#63417=CARTESIAN_POINT('',(28.5917969626306,2.36208894954101,16.));
#63418=CARTESIAN_POINT('',(28.7217721556985,2.43487855509313,33.8305837392638));
#63419=CARTESIAN_POINT('Origin',(30.,-1.32966554433622E-14,33.8305837392638));
#63420=CARTESIAN_POINT('',(28.7217721556985,2.43487855509312,16.));
#63421=CARTESIAN_POINT('Origin',(30.,-1.32966554433622E-14,16.));
#63422=CARTESIAN_POINT('',(28.7814653456406,2.46529375453011,33.8305837392638));
#63423=CARTESIAN_POINT('',(28.7814653456406,2.46529375453011,16.));
#63424=CARTESIAN_POINT('',(28.9167508751952,2.52766123790546,33.8305837392638));
#63425=CARTESIAN_POINT('Origin',(30.,-1.32966554433622E-14,33.8305837392638));
#63426=CARTESIAN_POINT('',(28.9167508751953,2.52766123790545,16.));
#63427=CARTESIAN_POINT('Origin',(30.,-1.32966554433622E-14,16.));
#63428=CARTESIAN_POINT('',(28.9786463999985,2.55329920372917,33.8305837392638));
#63429=CARTESIAN_POINT('',(28.9786463999985,2.55329920372917,16.));
#63430=CARTESIAN_POINT('',(29.1184081857633,2.60486004865344,33.8305837392638));
#63431=CARTESIAN_POINT('Origin',(30.,-1.32966554433622E-14,33.8305837392638));
#63432=CARTESIAN_POINT('',(29.1184081857633,2.60486004865344,16.));
#63433=CARTESIAN_POINT('Origin',(30.,-1.32966554433622E-14,16.));
#63434=CARTESIAN_POINT('',(29.182124438935,2.6255627142791,33.8305837392638));
#63435=CARTESIAN_POINT('',(29.182124438935,2.62556271427909,16.));
#63436=CARTESIAN_POINT('',(29.3255008030251,2.66599903099762,33.8305837392638));
#63437=CARTESIAN_POINT('Origin',(30.,-1.32966554433622E-14,33.8305837392638));
#63438=CARTESIAN_POINT('',(29.3255008030251,2.66599903099761,16.));
#63439=CARTESIAN_POINT('Origin',(30.,-1.32966554433622E-14,16.));
#63440=CARTESIAN_POINT('',(29.3906449526767,2.6816387576073,33.8305837392638));
#63441=CARTESIAN_POINT('',(29.3906449526767,2.68163875760729,16.));
#63442=CARTESIAN_POINT('',(29.5367519321301,2.71070124278105,33.8305837392638));
#63443=CARTESIAN_POINT('Origin',(30.,-1.32966554433622E-14,33.8305837392638));
#63444=CARTESIAN_POINT('',(29.5367519321301,2.71070124278105,16.));
#63445=CARTESIAN_POINT('Origin',(30.,-1.32966554433622E-14,16.));
#63446=CARTESIAN_POINT('',(29.6029223429162,2.72118160625947,33.8305837392638));
#63447=CARTESIAN_POINT('',(29.6029223429162,2.72118160625946,16.));
#63448=CARTESIAN_POINT('',(29.750859139619,2.73869108000311,33.8305837392638));
#63449=CARTESIAN_POINT('Origin',(30.,-1.32966554433622E-14,33.8305837392638));
#63450=CARTESIAN_POINT('',(29.750859139619,2.7386910800031,16.));
#63451=CARTESIAN_POINT('Origin',(30.,-1.32966554433622E-14,16.));
#63452=CARTESIAN_POINT('',(29.8176478489534,2.74394746542434,33.8305837392638));
#63453=CARTESIAN_POINT('',(29.8176478489534,2.74394746542433,16.));
#63454=CARTESIAN_POINT('',(29.9665023833599,2.74979597600975,33.8305837392638));
#63455=CARTESIAN_POINT('Origin',(30.,-1.32966554433622E-14,33.8305837392638));
#63456=CARTESIAN_POINT('',(29.9665023833599,2.74979597600974,16.));
#63457=CARTESIAN_POINT('Origin',(30.,-1.32966554433622E-14,16.));
#63458=CARTESIAN_POINT('',(30.3970776570838,2.72118160625946,33.8305837392638));
#63459=CARTESIAN_POINT('',(30.3970776570838,2.72118160625945,16.));
#63460=CARTESIAN_POINT('',(30.249140860381,2.73869108000311,33.8305837392638));
#63461=CARTESIAN_POINT('',(30.249140860381,2.7386910800031,16.));
#63462=CARTESIAN_POINT('Origin',(30.,-1.32966554433622E-14,33.8305837392638));
#63463=CARTESIAN_POINT('Origin',(30.,-1.32966554433622E-14,33.8305837392638));
#63464=CARTESIAN_POINT('Origin',(27.5075580599235,1.0459901541636,33.8304779343707));
#63465=CARTESIAN_POINT('Origin',(27.5859153117241,1.21595293501799,33.830456743813));
#63466=CARTESIAN_POINT('Origin',(30.,-1.32966554433622E-14,33.8305837392638));
#63467=CARTESIAN_POINT('Origin',(27.4979545614264,1.02279765627048,33.8304567438139));
#63468=CARTESIAN_POINT('Origin',(27.4331739849704,0.847210974834779,33.830477934375));
#63469=CARTESIAN_POINT('Origin',(30.,-1.32966554433622E-14,33.8305837392638));
#63470=CARTESIAN_POINT('Origin',(27.4254197532764,0.823336489857381,33.8304567438132));
#63471=CARTESIAN_POINT('Origin',(27.3746152459633,0.643208458112014,33.8304779343751));
#63472=CARTESIAN_POINT('Origin',(30.,-1.32966554433622E-14,33.8305837392638));
#63473=CARTESIAN_POINT('Origin',(27.368758088479,0.618799180196873,33.8304567438137));
#63474=CARTESIAN_POINT('Origin',(27.3322428769935,0.435240347356666,33.8304779343754));
#63475=CARTESIAN_POINT('Origin',(30.,-1.32966554433622E-14,33.8305837392638));
#63476=CARTESIAN_POINT('Origin',(27.3283189050469,0.410446767819665,33.8304567438127));
#63477=CARTESIAN_POINT('Origin',(27.3063181178076,0.224588835126915,33.8304779343751));
#63478=CARTESIAN_POINT('Origin',(30.,-1.32966554433622E-14,33.8305837392638));
#63479=CARTESIAN_POINT('Origin',(27.3043515239852,0.199563814630461,33.8304567438133));
#63480=CARTESIAN_POINT('Origin',(27.2970008031678,0.0125526580442922,33.8304779343738));
#63481=CARTESIAN_POINT('Origin',(30.,-1.32966554433622E-14,33.8305837392638));
#63482=CARTESIAN_POINT('Origin',(27.2970037121732,-0.012549515837469,33.8304567438135));
#63483=CARTESIAN_POINT('Origin',(27.3043483774083,-0.199560910346332,33.8304779343754));
#63484=CARTESIAN_POINT('Origin',(30.,-1.32966554433622E-14,33.8305837392638));
#63485=CARTESIAN_POINT('Origin',(27.3063207713147,-0.224585474366301,33.8304567438129));
#63486=CARTESIAN_POINT('Origin',(27.3283155403039,-0.410444119366497,33.8304779343742));
#63487=CARTESIAN_POINT('Origin',(30.,-1.32966554433622E-14,33.8305837392638));
#63488=CARTESIAN_POINT('Origin',(27.3322452586388,-0.435236788764194,33.8304567438132));
#63489=CARTESIAN_POINT('Origin',(27.3687545263134,-0.618796803902706,33.8304779343752));
#63490=CARTESIAN_POINT('Origin',(30.,-1.32966554433622E-14,33.8305837392638));
#63491=CARTESIAN_POINT('Origin',(27.3746173410614,-0.643204723628853,33.8304567438136));
#63492=CARTESIAN_POINT('Origin',(27.4254160156486,-0.823334400372707,33.8304779343751));
#63493=CARTESIAN_POINT('Origin',(30.,-1.32966554433622E-14,33.8305837392638));
#63494=CARTESIAN_POINT('Origin',(27.433175780606,-0.847207087484101,33.8304567438133));
#63495=CARTESIAN_POINT('Origin',(27.4979506713824,-1.02279586647791,33.8304779343754));
#63496=CARTESIAN_POINT('Origin',(30.,-1.32966554433622E-14,33.8305837392638));
#63497=CARTESIAN_POINT('Origin',(27.5075595450189,-1.04598613791989,33.830456743813));
#63498=CARTESIAN_POINT('Origin',(27.5859112932449,-1.21595145595217,33.830477934375));
#63499=CARTESIAN_POINT('Origin',(30.,-1.32966554433622E-14,33.8305837392638));
#63500=CARTESIAN_POINT('Origin',(27.5973100336554,-1.23831633599182,33.8304567438138));
#63501=CARTESIAN_POINT('Origin',(27.6887555747498,-1.40161030035549,33.8304779343749));
#63502=CARTESIAN_POINT('Origin',(30.,-1.32966554433622E-14,33.8305837392638));
#63503=CARTESIAN_POINT('Origin',(27.7018739049122,-1.42301190206769,33.8304567438132));
#63504=CARTESIAN_POINT('Origin',(27.8058494467036,-1.57862775117429,33.8304779343746));
#63505=CARTESIAN_POINT('Origin',(30.,-1.32966554433622E-14,33.8305837392638));
#63506=CARTESIAN_POINT('Origin',(27.8206064877493,-1.59893412656796,33.8304567438128));
#63507=CARTESIAN_POINT('Origin',(27.9364709864456,-1.74591243696051,33.830477934375));
#63508=CARTESIAN_POINT('Origin',(30.,-1.32966554433622E-14,33.8305837392638));
#63509=CARTESIAN_POINT('Origin',(27.9527757563098,-1.76499839048126,33.8304567438135));
#63510=CARTESIAN_POINT('Origin',(28.0798148687495,-1.90243299199812,33.8304779343753));
#63511=CARTESIAN_POINT('Origin',(30.,-1.32966554433622E-14,33.8305837392638));
#63512=CARTESIAN_POINT('Origin',(28.0975668431045,-1.92018085239454,33.8304567438138));
#63513=CARTESIAN_POINT('Origin',(28.234997330915,-2.04722441501659,33.8304779343752));
#63514=CARTESIAN_POINT('Origin',(30.,-1.32966554433622E-14,33.8305837392638));
#63515=CARTESIAN_POINT('Origin',(28.2540870629355,-2.06352476082575,33.8304567438132));
#63516=CARTESIAN_POINT('Origin',(28.4010616214883,-2.1793940187284,33.8304779343619));
#63517=CARTESIAN_POINT('Origin',(30.,-1.32966554433622E-14,33.8305837392638));
#63518=CARTESIAN_POINT('Origin',(28.4213714165976,-2.19414635291788,33.8304567438138));
#63519=CARTESIAN_POINT('Origin',(28.5769838988107,-2.29812693362319,33.8304779343729));
#63520=CARTESIAN_POINT('Origin',(30.,-1.32966554433622E-14,33.8305837392638));
#63521=CARTESIAN_POINT('Origin',(28.5983885404242,-2.31124030311337,33.8304567438133));
#63522=CARTESIAN_POINT('Origin',(28.7616795436178,-2.40269113175742,33.8304779343754));
#63523=CARTESIAN_POINT('Origin',(30.,-1.32966554433622E-14,33.8305837392638));
#63524=CARTESIAN_POINT('Origin',(28.7840470649819,-2.41408468827727,33.8304567438135));
#63525=CARTESIAN_POINT('Origin',(28.9540098458287,-2.49244194008352,33.8304779343747));
#63526=CARTESIAN_POINT('Origin',(30.,-1.32966554433622E-14,33.8305837392638));
#63527=CARTESIAN_POINT('Origin',(28.9772023437295,-2.50204543857419,33.8304567438141));
#63528=CARTESIAN_POINT('Origin',(29.1527890251654,-2.5668260150294,33.8304779343748));
#63529=CARTESIAN_POINT('Origin',(30.,-1.32966554433622E-14,33.8305837392638));
#63530=CARTESIAN_POINT('Origin',(29.1766635101425,-2.57458024672298,33.8304567438129));
#63531=CARTESIAN_POINT('Origin',(29.3567915418921,-2.62538475403142,33.8304779343725));
#63532=CARTESIAN_POINT('Origin',(30.,-1.32966554433622E-14,33.8305837392638));
#63533=CARTESIAN_POINT('Origin',(29.3812008198029,-2.63124191151983,33.8304567438133));
#63534=CARTESIAN_POINT('Origin',(29.5647596526443,-2.66775712300496,33.8304779343746));
#63535=CARTESIAN_POINT('Origin',(30.,-1.32966554433622E-14,33.8305837392638));
#63536=CARTESIAN_POINT('Origin',(29.589553232181,-2.67168109495555,33.8304567438136));
#63537=CARTESIAN_POINT('Origin',(29.7754111648755,-2.69368188218804,33.8304779343731));
#63538=CARTESIAN_POINT('Origin',(30.,-1.32966554433622E-14,33.8305837392638));
#63539=CARTESIAN_POINT('Origin',(29.8004361853699,-2.69564847601571,33.8304567438137));
#63540=CARTESIAN_POINT('Origin',(29.9874473419542,-2.70299919683539,33.8304779343752));
#63541=CARTESIAN_POINT('Origin',(30.,-1.32966554433622E-14,33.8305837392638));
#63542=CARTESIAN_POINT('Origin',(30.0125495158367,-2.70299628782517,33.8304567438128));
#63543=CARTESIAN_POINT('Origin',(30.199560910346,-2.6956516225925,33.8304779343757));
#63544=CARTESIAN_POINT('Origin',(30.,-1.32966554433622E-14,33.8305837392638));
#63545=CARTESIAN_POINT('Origin',(30.2245854743665,-2.69367922868563,33.8304567438131));
#63546=CARTESIAN_POINT('Origin',(30.4104441193657,-2.67168445969903,33.8304779343754));
#63547=CARTESIAN_POINT('Origin',(30.,-1.32966554433622E-14,33.8305837392638));
#63548=CARTESIAN_POINT('Origin',(30.4352367887642,-2.66775474136125,33.8304567438132));
#63549=CARTESIAN_POINT('Origin',(30.6187968039027,-2.63124547368644,33.8304779343751));
#63550=CARTESIAN_POINT('Origin',(30.,-1.32966554433622E-14,33.8305837392638));
#63551=CARTESIAN_POINT('Origin',(30.6432047236274,-2.6253826589367,33.8304567438126));
#63552=CARTESIAN_POINT('Origin',(30.8233344003726,-2.57458398435223,33.8304779343755));
#63553=CARTESIAN_POINT('Origin',(30.,-1.32966554433622E-14,33.8305837392638));
#63554=CARTESIAN_POINT('Origin',(30.8472070874839,-2.5668242193938,33.8304567438132));
#63555=CARTESIAN_POINT('Origin',(31.0227958664778,-2.50204932861793,33.8304779343756));
#63556=CARTESIAN_POINT('Origin',(30.,-1.32966554433622E-14,33.8305837392638));
#63557=CARTESIAN_POINT('Origin',(31.0459861379201,-2.49244045498134,33.8304567438131));
#63558=CARTESIAN_POINT('Origin',(31.2159514559521,-2.41408870675381,33.8304779343746));
#63559=CARTESIAN_POINT('Origin',(30.,-1.32966554433622E-14,33.8305837392638));
#63560=CARTESIAN_POINT('Origin',(31.2383163359911,-2.402689966344,33.8304567438135));
#63561=CARTESIAN_POINT('Origin',(31.4016103003557,-2.3112444252517,33.8304779343755));
#63562=CARTESIAN_POINT('Origin',(30.,-1.32966554433622E-14,33.8305837392638));
#63563=CARTESIAN_POINT('Origin',(31.4230119020685,-2.29812609508837,33.8304567438136));
#63564=CARTESIAN_POINT('Origin',(31.5786277511746,-2.19415055329817,33.8304779343753));
#63565=CARTESIAN_POINT('Origin',(30.,-1.32966554433622E-14,33.8305837392638));
#63566=CARTESIAN_POINT('Origin',(31.5989341265715,-2.17939351225268,33.8304567438143));
#63567=CARTESIAN_POINT('Origin',(31.7459124369605,-2.06352901355452,33.8304779343751));
#63568=CARTESIAN_POINT('Origin',(30.,-1.32966554433622E-14,33.8305837392638));
#63569=CARTESIAN_POINT('Origin',(31.764998390482,-2.04722424369058,33.8304567438139));
#63570=CARTESIAN_POINT('Origin',(31.9024329919978,-1.92018513124985,33.8304779343751));
#63571=CARTESIAN_POINT('Origin',(30.,-1.32966554433622E-14,33.8305837392638));
#63572=CARTESIAN_POINT('Origin',(31.9201808523926,-1.90243315689474,33.8304567438131));
#63573=CARTESIAN_POINT('Origin',(32.0472244150163,-1.76500266908446,33.830477934375));
#63574=CARTESIAN_POINT('Origin',(30.,-1.32966554433622E-14,33.8305837392638));
#63575=CARTESIAN_POINT('Origin',(32.0635247608254,-1.74591293706441,33.8304567438131));
#63576=CARTESIAN_POINT('Origin',(32.1793940187282,-1.59893837851134,33.8304779343617));
#63577=CARTESIAN_POINT('Origin',(30.,-1.32966554433622E-14,33.8305837392638));
#63578=CARTESIAN_POINT('Origin',(32.1941463529172,-1.57862858340229,33.8304567438136));
#63579=CARTESIAN_POINT('Origin',(32.2981269336233,-1.42301610118952,33.830477934373));
#63580=CARTESIAN_POINT('Origin',(30.,-1.32966554433622E-14,33.8305837392638));
#63581=CARTESIAN_POINT('Origin',(32.311240303114,-1.40161145957583,33.8304567438134));
#63582=CARTESIAN_POINT('Origin',(32.4026911317571,-1.23832045638176,33.8304779343753));
#63583=CARTESIAN_POINT('Origin',(30.,-1.32966554433622E-14,33.8305837392638));
#63584=CARTESIAN_POINT('Origin',(32.4140846882749,-1.21595293501797,33.8304567438127));
#63585=CARTESIAN_POINT('Origin',(32.4924419400838,-1.04599015417152,33.8304779343749));
#63586=CARTESIAN_POINT('Origin',(30.,-1.32966554433622E-14,33.8305837392638));
#63587=CARTESIAN_POINT('Origin',(32.5020454385714,-1.02279765627054,33.8304567438132));
#63588=CARTESIAN_POINT('Origin',(32.56682601503,-0.847210974835106,33.8304779343751));
#63589=CARTESIAN_POINT('Origin',(30.,-1.32966554433622E-14,33.8305837392638));
#63590=CARTESIAN_POINT('Origin',(32.5745802467237,-0.823336489857386,33.8304567438133));
#63591=CARTESIAN_POINT('Origin',(32.6253847540299,-0.643208458106727,33.8304779343718));
#63592=CARTESIAN_POINT('Origin',(30.,-1.32966554433622E-14,33.8305837392638));
#63593=CARTESIAN_POINT('Origin',(32.6312419115182,-0.618799180197391,33.8304567438127));
#63594=CARTESIAN_POINT('Origin',(32.6677571230055,-0.435240347356057,33.830477934375));
#63595=CARTESIAN_POINT('Origin',(30.,-1.32966554433622E-14,33.8305837392638));
#63596=CARTESIAN_POINT('Origin',(32.6716810949544,-0.410446767819313,33.8304567438133));
#63597=CARTESIAN_POINT('Origin',(32.6936818821919,-0.224588835126652,33.8304779343749));
#63598=CARTESIAN_POINT('Origin',(30.,-1.32966554433622E-14,33.8305837392638));
#63599=CARTESIAN_POINT('Origin',(32.6956484760151,-0.199563814630355,33.8304567438134));
#63600=CARTESIAN_POINT('Origin',(32.7029991968333,-0.0125526580448477,33.8304779343743));
#63601=CARTESIAN_POINT('Origin',(30.,-1.32966554433622E-14,33.8305837392638));
#63602=CARTESIAN_POINT('Origin',(32.7029962878262,0.0125495158371826,33.8304567438133));
#63603=CARTESIAN_POINT('Origin',(32.6956516225903,0.19956091034681,33.8304779343749));
#63604=CARTESIAN_POINT('Origin',(30.,-1.32966554433622E-14,33.8305837392638));
#63605=CARTESIAN_POINT('Origin',(32.6936792286859,0.22458547436666,33.8304567438133));
#63606=CARTESIAN_POINT('Origin',(32.6716844596177,0.410444119388619,33.8304779343428));
#63607=CARTESIAN_POINT('Origin',(30.,-1.32966554433622E-14,33.8305837392638));
#63608=CARTESIAN_POINT('Origin',(32.6677547413622,0.435236788764869,33.8304567438136));
#63609=CARTESIAN_POINT('Origin',(32.6312454736863,0.618796803902747,33.8304779343751));
#63610=CARTESIAN_POINT('Origin',(30.,-1.32966554433622E-14,33.8305837392638));
#63611=CARTESIAN_POINT('Origin',(32.625382658939,0.643204723629168,33.8304567438138));
#63612=CARTESIAN_POINT('Origin',(32.5745839843506,0.823334400372804,33.8304779343749));
#63613=CARTESIAN_POINT('Origin',(30.,-1.32966554433622E-14,33.8305837392638));
#63614=CARTESIAN_POINT('Origin',(32.5668242193939,0.847207087484111,33.8304567438133));
#63615=CARTESIAN_POINT('Origin',(32.5020493286164,1.02279586647793,33.830477934375));
#63616=CARTESIAN_POINT('Origin',(30.,-1.32966554433622E-14,33.8305837392638));
#63617=CARTESIAN_POINT('Origin',(32.4924404549818,1.04598613792066,33.8304567438134));
#63618=CARTESIAN_POINT('Origin',(32.4140887067556,1.21595145595219,33.8304779343752));
#63619=CARTESIAN_POINT('Origin',(30.,-1.32966554433622E-14,33.8305837392638));
#63620=CARTESIAN_POINT('Origin',(32.4026899663445,1.2383163359917,33.8304567438137));
#63621=CARTESIAN_POINT('Origin',(32.3112444252326,1.40161030035344,33.830477934368));
#63622=CARTESIAN_POINT('Origin',(30.,-1.32966554433622E-14,33.8305837392638));
#63623=CARTESIAN_POINT('Origin',(32.2981260950878,1.42301190206775,33.8304567438133));
#63624=CARTESIAN_POINT('Origin',(32.1941505532983,1.57862775117468,33.8304779343753));
#63625=CARTESIAN_POINT('Origin',(30.,-1.32966554433622E-14,33.8305837392638));
#63626=CARTESIAN_POINT('Origin',(32.1793935122518,1.59893412656992,33.8304567438136));
#63627=CARTESIAN_POINT('Origin',(32.0635290135536,1.74591243696026,33.8304779343747));
#63628=CARTESIAN_POINT('Origin',(30.,-1.32966554433622E-14,33.8305837392638));
#63629=CARTESIAN_POINT('Origin',(32.04722424369,1.76499839048088,33.8304567438134));
#63630=CARTESIAN_POINT('Origin',(31.9201851312459,1.90243299199643,33.8304779343734));
#63631=CARTESIAN_POINT('Origin',(30.,-1.32966554433622E-14,33.8305837392638));
#63632=CARTESIAN_POINT('Origin',(31.9024331568948,1.92018085239292,33.8304567438132));
#63633=CARTESIAN_POINT('Origin',(31.7650026690842,2.0472244150162,33.8304779343749));
#63634=CARTESIAN_POINT('Origin',(30.,-1.32966554433622E-14,33.8305837392638));
#63635=CARTESIAN_POINT('Origin',(31.7459129370645,2.06352476082576,33.8304567438132));
#63636=CARTESIAN_POINT('Origin',(31.5989383785419,2.17939401874533,33.8304779343753));
#63637=CARTESIAN_POINT('Origin',(30.,-1.32966554433622E-14,33.8305837392638));
#63638=CARTESIAN_POINT('Origin',(31.5786285834019,2.1941463529156,33.830456743813));
#63639=CARTESIAN_POINT('Origin',(31.4230161011941,2.29812693362645,33.8304779343752));
#63640=CARTESIAN_POINT('Origin',(30.,-1.32966554433622E-14,33.8305837392638));
#63641=CARTESIAN_POINT('Origin',(31.4016114595758,2.31124030311394,33.8304567438134));
#63642=CARTESIAN_POINT('Origin',(31.2383204563814,2.40269113175683,33.8304779343751));
#63643=CARTESIAN_POINT('Origin',(30.,-1.32966554433622E-14,33.8305837392638));
#63644=CARTESIAN_POINT('Origin',(31.215952935018,2.41408468827632,33.8304567438131));
#63645=CARTESIAN_POINT('Origin',(31.0459901541714,2.49244194008366,33.8304779343748));
#63646=CARTESIAN_POINT('Origin',(30.,-1.32966554433622E-14,33.8305837392638));
#63647=CARTESIAN_POINT('Origin',(31.0227976562705,2.50204543857161,33.8304567438132));
#63648=CARTESIAN_POINT('Origin',(30.8472109748356,2.56682601503055,33.8304779343754));
#63649=CARTESIAN_POINT('Origin',(30.,-1.32966554433622E-14,33.8305837392638));
#63650=CARTESIAN_POINT('Origin',(30.8233364898573,2.574580246724,33.8304567438134));
#63651=CARTESIAN_POINT('Origin',(30.6432084580721,2.62538475398616,33.8304779343503));
#63652=CARTESIAN_POINT('Origin',(30.,-1.32966554433622E-14,33.8305837392638));
#63653=CARTESIAN_POINT('Origin',(30.6187991801972,2.63124191151918,33.8304567438131));
#63654=CARTESIAN_POINT('Origin',(30.4352403473569,2.66775712300684,33.8304779343755));
#63655=CARTESIAN_POINT('Origin',(30.,-1.32966554433622E-14,33.8305837392638));
#63656=CARTESIAN_POINT('Origin',(27.5973088682432,1.23832045638137,33.8304779343751));
#63657=CARTESIAN_POINT('Origin',(27.6887596968862,1.40161145957579,33.8304567438134));
#63658=CARTESIAN_POINT('Origin',(30.,-1.32966554433622E-14,33.8305837392638));
#63659=CARTESIAN_POINT('Origin',(27.7018730663741,1.4230161011934,33.8304779343749));
#63660=CARTESIAN_POINT('Origin',(27.8058536470835,1.57862858340213,33.8304567438133));
#63661=CARTESIAN_POINT('Origin',(30.,-1.32966554433622E-14,33.8305837392638));
#63662=CARTESIAN_POINT('Origin',(27.8206059812548,1.59893837854177,33.8304779343751));
#63663=CARTESIAN_POINT('Origin',(27.9364752391745,1.7459129370644,33.8304567438132));
#63664=CARTESIAN_POINT('Origin',(30.,-1.32966554433622E-14,33.8305837392638));
#63665=CARTESIAN_POINT('Origin',(27.952775584984,1.76500266908388,33.8304779343747));
#63666=CARTESIAN_POINT('Origin',(28.0798191476065,1.90243315689505,33.8304567438134));
#63667=CARTESIAN_POINT('Origin',(30.,-1.32966554433622E-14,33.8305837392638));
#63668=CARTESIAN_POINT('Origin',(28.0975670080041,1.92018513124447,33.8304779343728));
#63669=CARTESIAN_POINT('Origin',(28.23500160952,2.04722424368963,33.830456743813));
#63670=CARTESIAN_POINT('Origin',(30.,-1.32966554433622E-14,33.8305837392638));
#63671=CARTESIAN_POINT('Origin',(28.2540875630398,2.06352901355343,33.8304779343746));
#63672=CARTESIAN_POINT('Origin',(28.4010658734306,2.17939351225149,33.8304567438134));
#63673=CARTESIAN_POINT('Origin',(30.,-1.32966554433622E-14,33.8305837392638));
#63674=CARTESIAN_POINT('Origin',(28.4213722488255,2.19415055329726,33.8304779343749));
#63675=CARTESIAN_POINT('Origin',(28.5769880979325,2.29812609508769,33.8304567438131));
#63676=CARTESIAN_POINT('Origin',(30.,-1.32966554433622E-14,33.8305837392638));
#63677=CARTESIAN_POINT('Origin',(28.5983896996467,2.31124442523142,33.8304779343677));
#63678=CARTESIAN_POINT('Origin',(28.7616836640084,2.40268996634441,33.8304567438137));
#63679=CARTESIAN_POINT('Origin',(30.,-1.32966554433622E-14,33.8305837392638));
#63680=CARTESIAN_POINT('Origin',(28.7840485440478,2.41408870675589,33.8304779343753));
#63681=CARTESIAN_POINT('Origin',(28.9540138620795,2.49244045498167,33.8304567438133));
#63682=CARTESIAN_POINT('Origin',(30.,-1.32966554433622E-14,33.8305837392638));
#63683=CARTESIAN_POINT('Origin',(28.9772041335221,2.50204932861683,33.8304779343752));
#63684=CARTESIAN_POINT('Origin',(29.1527929125161,2.56682421939371,33.8304567438132));
#63685=CARTESIAN_POINT('Origin',(30.,-1.32966554433622E-14,33.8305837392638));
#63686=CARTESIAN_POINT('Origin',(29.1766655996273,2.57458398435145,33.8304779343752));
#63687=CARTESIAN_POINT('Origin',(29.3567952763716,2.62538265893797,33.8304567438133));
#63688=CARTESIAN_POINT('Origin',(30.,-1.32966554433622E-14,33.8305837392638));
#63689=CARTESIAN_POINT('Origin',(29.3812031960975,2.63124547368767,33.8304779343756));
#63690=CARTESIAN_POINT('Origin',(29.5647632112354,2.66775474136179,33.8304567438135));
#63691=CARTESIAN_POINT('Origin',(30.,-1.32966554433622E-14,33.8305837392638));
#63692=CARTESIAN_POINT('Origin',(29.5895558806117,2.67168445961877,33.8304779343432));
#63693=CARTESIAN_POINT('Origin',(29.775414525633,2.69367922868643,33.8304567438135));
#63694=CARTESIAN_POINT('Origin',(30.,-1.32966554433622E-14,33.8305837392638));
#63695=CARTESIAN_POINT('Origin',(29.8004390896529,2.69565162258947,33.8304779343745));
#63696=CARTESIAN_POINT('Origin',(29.9874504841622,2.70299628782743,33.8304567438137));
#63697=CARTESIAN_POINT('Origin',(30.,-1.32966554433622E-14,33.8305837392638));
#63698=CARTESIAN_POINT('Origin',(30.4104467678198,2.67168109495229,33.8304567438124));
#63699=CARTESIAN_POINT('Origin',(30.2245888351268,2.69368188219228,33.830477934375));
#63700=CARTESIAN_POINT('Origin',(30.,1.17524047358083,16.));
#63701=CARTESIAN_POINT('Origin',(30.,2.60624999999999,31.));
#63702=CARTESIAN_POINT('Origin',(30.,-1.32966554433622E-14,31.6569162607362));
#63703=CARTESIAN_POINT('',(30.1823521510466,2.74394746542433,31.6569162607362));
#63704=CARTESIAN_POINT('Origin',(30.1995609103462,2.69565162259179,31.6570220656244));
#63705=CARTESIAN_POINT('',(30.03349761664,2.74979597600974,31.6569162607362));
#63706=CARTESIAN_POINT('Origin',(30.0125495158372,2.70299628782596,31.6570432561867));
#63707=CARTESIAN_POINT('Origin',(30.,-1.32966554433622E-14,31.6569162607362));
#63708=CARTESIAN_POINT('Origin',(30.,-1.32966554433622E-14,16.));
#63709=CARTESIAN_POINT('',(30.1823521510466,2.74394746542434,33.8305837392638));
#63710=CARTESIAN_POINT('',(30.1823521510466,2.74394746542433,16.));
#63711=CARTESIAN_POINT('',(30.03349761664,2.74979597600975,33.8305837392638));
#63712=CARTESIAN_POINT('',(30.03349761664,2.74979597600974,16.));
#63713=CARTESIAN_POINT('Origin',(30.,-1.32966554433622E-14,33.8305837392638));
#63714=CARTESIAN_POINT('Origin',(30.,-1.32966554433622E-14,33.8305837392638));
#63715=CARTESIAN_POINT('Origin',(30.1995638146302,2.69564847601544,33.8304567438135));
#63716=CARTESIAN_POINT('Origin',(30.0125526580447,2.70299919683307,33.8304779343742));
#63717=CARTESIAN_POINT('Origin',(30.,-1.32966554433622E-14,34.));
#63718=CARTESIAN_POINT('Origin',(30.,-1.32966554433622E-14,32.5));
#63719=CARTESIAN_POINT('',(30.,-1.44337567297407,32.5));
#63720=CARTESIAN_POINT('',(31.25,-0.72168783648704,32.5));
#63721=CARTESIAN_POINT('',(30.,-1.44337567297407,32.5));
#63722=CARTESIAN_POINT('',(31.25,0.721687836487017,32.5));
#63723=CARTESIAN_POINT('',(31.25,-0.72168783648704,32.5));
#63724=CARTESIAN_POINT('',(30.,1.44337567297405,32.5));
#63725=CARTESIAN_POINT('',(31.25,0.721687836487017,32.5));
#63726=CARTESIAN_POINT('',(28.75,0.721687836487017,32.5));
#63727=CARTESIAN_POINT('',(30.,1.44337567297405,32.5));
#63728=CARTESIAN_POINT('',(28.75,-0.721687836487044,32.5));
#63729=CARTESIAN_POINT('',(28.75,0.721687836487017,32.5));
#63730=CARTESIAN_POINT('',(28.75,-0.721687836487044,32.5));
#63731=CARTESIAN_POINT('Origin',(31.25,-0.72168783648704,32.5));
#63732=CARTESIAN_POINT('',(31.25,-0.72168783648704,32.5));
#63733=CARTESIAN_POINT('',(31.25,0.721687836487017,32.5));
#63734=CARTESIAN_POINT('Origin',(31.25,0.721687836487017,32.5));
#63735=CARTESIAN_POINT('',(30.,1.44337567297405,32.5));
#63736=CARTESIAN_POINT('Origin',(30.,1.44337567297405,32.5));
#63737=CARTESIAN_POINT('',(28.75,0.721687836487017,32.5));
#63738=CARTESIAN_POINT('Origin',(28.75,0.721687836487017,32.5));
#63739=CARTESIAN_POINT('',(28.75,-0.721687836487044,32.5));
#63740=CARTESIAN_POINT('Origin',(28.75,-0.721687836487044,32.5));
#63741=CARTESIAN_POINT('',(30.,-1.44337567297407,32.5));
#63742=CARTESIAN_POINT('Origin',(30.,-1.44337567297407,32.5));
#63743=CARTESIAN_POINT('Ctrl Pts',(30.,1.17523237272422,15.7500046770317));
#63744=CARTESIAN_POINT('Ctrl Pts',(29.3214792732473,1.17523237272422,15.7916713436984));
#63745=CARTESIAN_POINT('Ctrl Pts',(28.9822189098709,0.587616186362105,15.8333380103651));
#63746=CARTESIAN_POINT('Ctrl Pts',(28.6429585464946,-1.32141491426617E-14,
15.8750046770317));
#63747=CARTESIAN_POINT('Ctrl Pts',(28.9822189098709,-0.587616186362132,
15.9166713436984));
#63748=CARTESIAN_POINT('Ctrl Pts',(29.3214792732473,-1.17523237272425,15.9583380103651));
#63749=CARTESIAN_POINT('Ctrl Pts',(30.,-1.17523237272425,16.0000046770317));
#63750=CARTESIAN_POINT('Ctrl Pts',(30.6785207267527,-1.17523237272425,16.0416713436984));
#63751=CARTESIAN_POINT('Ctrl Pts',(31.017781090129,-0.587616186362132,16.0833380103651));
#63752=CARTESIAN_POINT('Ctrl Pts',(31.3570414535054,-1.35453513912972E-14,
16.1250046770317));
#63753=CARTESIAN_POINT('Ctrl Pts',(31.017781090129,0.587616186362104,16.1666713436984));
#63754=CARTESIAN_POINT('Ctrl Pts',(30.6785207267527,1.17523237272422,16.2083380103651));
#63755=CARTESIAN_POINT('Ctrl Pts',(30.,1.17523237272422,16.2500046770317));
#63756=CARTESIAN_POINT('Ctrl Pts',(29.3214792732473,1.17523237272422,16.2916713436984));
#63757=CARTESIAN_POINT('Ctrl Pts',(28.9822189098709,0.587616186362105,16.3333380103651));
#63758=CARTESIAN_POINT('Ctrl Pts',(28.6429585464946,-1.32141491426617E-14,
16.3750046770317));
#63759=CARTESIAN_POINT('Ctrl Pts',(28.9822189098709,-0.587616186362132,
16.4166713436984));
#63760=CARTESIAN_POINT('Ctrl Pts',(29.3214792732473,-1.17523237272425,16.4583380103651));
#63761=CARTESIAN_POINT('Ctrl Pts',(30.,-1.17523237272425,16.5000046770317));
#63762=CARTESIAN_POINT('Ctrl Pts',(30.6785207267527,-1.17523237272425,16.5416713436984));
#63763=CARTESIAN_POINT('Ctrl Pts',(31.017781090129,-0.587616186362132,16.5833380103651));
#63764=CARTESIAN_POINT('Ctrl Pts',(31.3570414535054,-1.35453513912972E-14,
16.6250046770317));
#63765=CARTESIAN_POINT('Ctrl Pts',(31.017781090129,0.587616186362104,16.6666713436984));
#63766=CARTESIAN_POINT('Ctrl Pts',(30.6785207267527,1.17523237272422,16.7083380103651));
#63767=CARTESIAN_POINT('Ctrl Pts',(30.,1.17523237272422,16.7500046770317));
#63768=CARTESIAN_POINT('Ctrl Pts',(29.3214792732473,1.17523237272422,16.7916713436984));
#63769=CARTESIAN_POINT('Ctrl Pts',(28.9822189098709,0.587616186362105,16.8333380103651));
#63770=CARTESIAN_POINT('Ctrl Pts',(28.6429585464946,-1.32141491426617E-14,
16.8750046770317));
#63771=CARTESIAN_POINT('Ctrl Pts',(28.9822189098709,-0.587616186362132,
16.9166713436984));
#63772=CARTESIAN_POINT('Ctrl Pts',(29.3214792732473,-1.17523237272425,16.9583380103651));
#63773=CARTESIAN_POINT('Ctrl Pts',(30.,-1.17523237272425,17.0000046770317));
#63774=CARTESIAN_POINT('Ctrl Pts',(30.6785207267527,-1.17523237272425,17.0416713436984));
#63775=CARTESIAN_POINT('Ctrl Pts',(31.017781090129,-0.587616186362132,17.0833380103651));
#63776=CARTESIAN_POINT('Ctrl Pts',(31.3570414535054,-1.35453513912972E-14,
17.1250046770317));
#63777=CARTESIAN_POINT('Ctrl Pts',(31.017781090129,0.587616186362104,17.1666713436984));
#63778=CARTESIAN_POINT('Ctrl Pts',(30.6785207267527,1.17523237272422,17.2083380103651));
#63779=CARTESIAN_POINT('Ctrl Pts',(30.,1.17523237272422,17.2500046770317));
#63780=CARTESIAN_POINT('Ctrl Pts',(29.3214792732473,1.17523237272422,17.2916713436984));
#63781=CARTESIAN_POINT('Ctrl Pts',(28.9822189098709,0.587616186362105,17.3333380103651));
#63782=CARTESIAN_POINT('Ctrl Pts',(28.6429585464946,-1.32141491426617E-14,
17.3750046770317));
#63783=CARTESIAN_POINT('Ctrl Pts',(28.9822189098709,-0.587616186362132,
17.4166713436984));
#63784=CARTESIAN_POINT('Ctrl Pts',(29.3214792732473,-1.17523237272425,17.4583380103651));
#63785=CARTESIAN_POINT('Ctrl Pts',(30.,-1.17523237272425,17.5000046770317));
#63786=CARTESIAN_POINT('Ctrl Pts',(30.6785207267527,-1.17523237272425,17.5416713436984));
#63787=CARTESIAN_POINT('Ctrl Pts',(31.017781090129,-0.587616186362132,17.5833380103651));
#63788=CARTESIAN_POINT('Ctrl Pts',(31.3570414535054,-1.35453513912972E-14,
17.6250046770317));
#63789=CARTESIAN_POINT('Ctrl Pts',(31.017781090129,0.587616186362104,17.6666713436984));
#63790=CARTESIAN_POINT('Ctrl Pts',(30.6785207267527,1.17523237272422,17.7083380103651));
#63791=CARTESIAN_POINT('Ctrl Pts',(30.,1.17523237272422,17.7500046770317));
#63792=CARTESIAN_POINT('Ctrl Pts',(29.3214792732473,1.17523237272422,17.7916713436984));
#63793=CARTESIAN_POINT('Ctrl Pts',(28.9822189098709,0.587616186362105,17.8333380103651));
#63794=CARTESIAN_POINT('Ctrl Pts',(28.6429585464946,-1.32141491426617E-14,
17.8750046770317));
#63795=CARTESIAN_POINT('Ctrl Pts',(28.9822189098709,-0.587616186362132,
17.9166713436984));
#63796=CARTESIAN_POINT('Ctrl Pts',(29.3214792732473,-1.17523237272425,17.9583380103651));
#63797=CARTESIAN_POINT('Ctrl Pts',(30.,-1.17523237272425,18.0000046770317));
#63798=CARTESIAN_POINT('Ctrl Pts',(30.6785207267527,-1.17523237272425,18.0416713436984));
#63799=CARTESIAN_POINT('Ctrl Pts',(31.017781090129,-0.587616186362132,18.0833380103651));
#63800=CARTESIAN_POINT('Ctrl Pts',(31.3570414535054,-1.35453513912972E-14,
18.1250046770317));
#63801=CARTESIAN_POINT('Ctrl Pts',(31.017781090129,0.587616186362104,18.1666713436984));
#63802=CARTESIAN_POINT('Ctrl Pts',(30.6785207267527,1.17523237272422,18.2083380103651));
#63803=CARTESIAN_POINT('Ctrl Pts',(30.,1.17523237272422,18.2500046770317));
#63804=CARTESIAN_POINT('Ctrl Pts',(29.3214792732473,1.17523237272422,18.2916713436984));
#63805=CARTESIAN_POINT('Ctrl Pts',(28.9822189098709,0.587616186362105,18.3333380103651));
#63806=CARTESIAN_POINT('Ctrl Pts',(28.6429585464946,-1.32141491426617E-14,
18.3750046770317));
#63807=CARTESIAN_POINT('Ctrl Pts',(28.9822189098709,-0.587616186362132,
18.4166713436984));
#63808=CARTESIAN_POINT('Ctrl Pts',(29.3214792732473,-1.17523237272425,18.4583380103651));
#63809=CARTESIAN_POINT('Ctrl Pts',(30.,-1.17523237272425,18.5000046770317));
#63810=CARTESIAN_POINT('Ctrl Pts',(30.6785207267527,-1.17523237272425,18.5416713436984));
#63811=CARTESIAN_POINT('Ctrl Pts',(31.017781090129,-0.587616186362132,18.5833380103651));
#63812=CARTESIAN_POINT('Ctrl Pts',(31.3570414535054,-1.35453513912972E-14,
18.6250046770317));
#63813=CARTESIAN_POINT('Ctrl Pts',(31.017781090129,0.587616186362104,18.6666713436984));
#63814=CARTESIAN_POINT('Ctrl Pts',(30.6785207267527,1.17523237272422,18.7083380103651));
#63815=CARTESIAN_POINT('Ctrl Pts',(30.,1.17523237272422,18.7500046770317));
#63816=CARTESIAN_POINT('Ctrl Pts',(29.3214792732473,1.17523237272422,18.7916713436984));
#63817=CARTESIAN_POINT('Ctrl Pts',(28.9822189098709,0.587616186362105,18.8333380103651));
#63818=CARTESIAN_POINT('Ctrl Pts',(28.6429585464946,-1.32141491426617E-14,
18.8750046770317));
#63819=CARTESIAN_POINT('Ctrl Pts',(28.9822189098709,-0.587616186362132,
18.9166713436984));
#63820=CARTESIAN_POINT('Ctrl Pts',(29.3214792732473,-1.17523237272425,18.9583380103651));
#63821=CARTESIAN_POINT('Ctrl Pts',(30.,-1.17523237272425,19.0000046770317));
#63822=CARTESIAN_POINT('Ctrl Pts',(30.6785207267527,-1.17523237272425,19.0416713436984));
#63823=CARTESIAN_POINT('Ctrl Pts',(31.017781090129,-0.587616186362132,19.0833380103651));
#63824=CARTESIAN_POINT('Ctrl Pts',(31.3570414535054,-1.35453513912972E-14,
19.1250046770317));
#63825=CARTESIAN_POINT('Ctrl Pts',(31.017781090129,0.587616186362104,19.1666713436984));
#63826=CARTESIAN_POINT('Ctrl Pts',(30.6785207267527,1.17523237272422,19.2083380103651));
#63827=CARTESIAN_POINT('Ctrl Pts',(30.,1.17523237272422,19.2500046770317));
#63828=CARTESIAN_POINT('Ctrl Pts',(29.3214792732473,1.17523237272422,19.2916713436984));
#63829=CARTESIAN_POINT('Ctrl Pts',(28.9822189098709,0.587616186362105,19.3333380103651));
#63830=CARTESIAN_POINT('Ctrl Pts',(28.6429585464946,-1.32141491426617E-14,
19.3750046770317));
#63831=CARTESIAN_POINT('Ctrl Pts',(28.9822189098709,-0.587616186362132,
19.4166713436984));
#63832=CARTESIAN_POINT('Ctrl Pts',(29.3214792732473,-1.17523237272425,19.4583380103651));
#63833=CARTESIAN_POINT('Ctrl Pts',(30.,-1.17523237272425,19.5000046770317));
#63834=CARTESIAN_POINT('Ctrl Pts',(30.6785207267527,-1.17523237272425,19.5416713436984));
#63835=CARTESIAN_POINT('Ctrl Pts',(31.017781090129,-0.587616186362132,19.5833380103651));
#63836=CARTESIAN_POINT('Ctrl Pts',(31.3570414535054,-1.35453513912972E-14,
19.6250046770317));
#63837=CARTESIAN_POINT('Ctrl Pts',(31.017781090129,0.587616186362104,19.6666713436984));
#63838=CARTESIAN_POINT('Ctrl Pts',(30.6785207267527,1.17523237272422,19.7083380103651));
#63839=CARTESIAN_POINT('Ctrl Pts',(30.,1.17523237272422,19.7500046770317));
#63840=CARTESIAN_POINT('Ctrl Pts',(29.3214792732473,1.17523237272422,19.7916713436984));
#63841=CARTESIAN_POINT('Ctrl Pts',(28.9822189098709,0.587616186362105,19.8333380103651));
#63842=CARTESIAN_POINT('Ctrl Pts',(28.6429585464946,-1.32141491426617E-14,
19.8750046770317));
#63843=CARTESIAN_POINT('Ctrl Pts',(28.9822189098709,-0.587616186362132,
19.9166713436984));
#63844=CARTESIAN_POINT('Ctrl Pts',(29.3214792732473,-1.17523237272425,19.9583380103651));
#63845=CARTESIAN_POINT('Ctrl Pts',(30.,-1.17523237272425,20.0000046770317));
#63846=CARTESIAN_POINT('Ctrl Pts',(30.6785207267527,-1.17523237272425,20.0416713436984));
#63847=CARTESIAN_POINT('Ctrl Pts',(31.017781090129,-0.587616186362132,20.0833380103651));
#63848=CARTESIAN_POINT('Ctrl Pts',(31.3570414535054,-1.35453513912972E-14,
20.1250046770317));
#63849=CARTESIAN_POINT('Ctrl Pts',(31.017781090129,0.587616186362104,20.1666713436984));
#63850=CARTESIAN_POINT('Ctrl Pts',(30.6785207267527,1.17523237272422,20.2083380103651));
#63851=CARTESIAN_POINT('Ctrl Pts',(30.,1.17523237272422,20.2500046770317));
#63852=CARTESIAN_POINT('Ctrl Pts',(29.3214792732473,1.17523237272422,20.2916713436984));
#63853=CARTESIAN_POINT('Ctrl Pts',(28.9822189098709,0.587616186362105,20.3333380103651));
#63854=CARTESIAN_POINT('Ctrl Pts',(28.6429585464946,-1.32141491426617E-14,
20.3750046770317));
#63855=CARTESIAN_POINT('Ctrl Pts',(28.9822189098709,-0.587616186362132,
20.4166713436984));
#63856=CARTESIAN_POINT('Ctrl Pts',(29.3214792732473,-1.17523237272425,20.4583380103651));
#63857=CARTESIAN_POINT('Ctrl Pts',(30.,-1.17523237272425,20.5000046770317));
#63858=CARTESIAN_POINT('Ctrl Pts',(30.6785207267527,-1.17523237272425,20.5416713436984));
#63859=CARTESIAN_POINT('Ctrl Pts',(31.017781090129,-0.587616186362132,20.5833380103651));
#63860=CARTESIAN_POINT('Ctrl Pts',(31.3570414535054,-1.35453513912972E-14,
20.6250046770317));
#63861=CARTESIAN_POINT('Ctrl Pts',(31.017781090129,0.587616186362104,20.6666713436984));
#63862=CARTESIAN_POINT('Ctrl Pts',(30.6785207267527,1.17523237272422,20.7083380103651));
#63863=CARTESIAN_POINT('Ctrl Pts',(30.,1.17523237272422,20.7500046770317));
#63864=CARTESIAN_POINT('Ctrl Pts',(29.3214792732473,1.17523237272422,20.7916713436984));
#63865=CARTESIAN_POINT('Ctrl Pts',(28.9822189098709,0.587616186362105,20.8333380103651));
#63866=CARTESIAN_POINT('Ctrl Pts',(28.6429585464946,-1.32141491426617E-14,
20.8750046770317));
#63867=CARTESIAN_POINT('Ctrl Pts',(28.9822189098709,-0.587616186362132,
20.9166713436984));
#63868=CARTESIAN_POINT('Ctrl Pts',(29.3214792732473,-1.17523237272425,20.9583380103651));
#63869=CARTESIAN_POINT('Ctrl Pts',(30.,-1.17523237272425,21.0000046770317));
#63870=CARTESIAN_POINT('Ctrl Pts',(30.6785207267527,-1.17523237272425,21.0416713436984));
#63871=CARTESIAN_POINT('Ctrl Pts',(31.017781090129,-0.587616186362132,21.0833380103651));
#63872=CARTESIAN_POINT('Ctrl Pts',(31.3570414535054,-1.35453513912972E-14,
21.1250046770317));
#63873=CARTESIAN_POINT('Ctrl Pts',(31.017781090129,0.587616186362104,21.1666713436984));
#63874=CARTESIAN_POINT('Ctrl Pts',(30.6785207267527,1.17523237272422,21.2083380103651));
#63875=CARTESIAN_POINT('Ctrl Pts',(30.,1.17523237272422,21.2500046770317));
#63876=CARTESIAN_POINT('Ctrl Pts',(29.3214792732473,1.17523237272422,21.2916713436984));
#63877=CARTESIAN_POINT('Ctrl Pts',(28.9822189098709,0.587616186362105,21.3333380103651));
#63878=CARTESIAN_POINT('Ctrl Pts',(28.6429585464946,-1.32141491426617E-14,
21.3750046770317));
#63879=CARTESIAN_POINT('Ctrl Pts',(28.9822189098709,-0.587616186362132,
21.4166713436984));
#63880=CARTESIAN_POINT('Ctrl Pts',(29.3214792732473,-1.17523237272425,21.4583380103651));
#63881=CARTESIAN_POINT('Ctrl Pts',(30.,-1.17523237272425,21.5000046770317));
#63882=CARTESIAN_POINT('Ctrl Pts',(30.6785207267527,-1.17523237272425,21.5416713436984));
#63883=CARTESIAN_POINT('Ctrl Pts',(31.017781090129,-0.587616186362132,21.5833380103651));
#63884=CARTESIAN_POINT('Ctrl Pts',(31.3570414535054,-1.35453513912972E-14,
21.6250046770317));
#63885=CARTESIAN_POINT('Ctrl Pts',(31.017781090129,0.587616186362104,21.6666713436984));
#63886=CARTESIAN_POINT('Ctrl Pts',(30.6785207267527,1.17523237272422,21.7083380103651));
#63887=CARTESIAN_POINT('Ctrl Pts',(30.,1.17523237272422,21.7500046770317));
#63888=CARTESIAN_POINT('Ctrl Pts',(29.3214792732473,1.17523237272422,21.7916713436984));
#63889=CARTESIAN_POINT('Ctrl Pts',(28.9822189098709,0.587616186362105,21.8333380103651));
#63890=CARTESIAN_POINT('Ctrl Pts',(28.6429585464946,-1.32141491426617E-14,
21.8750046770317));
#63891=CARTESIAN_POINT('Ctrl Pts',(28.9822189098709,-0.587616186362132,
21.9166713436984));
#63892=CARTESIAN_POINT('Ctrl Pts',(29.3214792732473,-1.17523237272425,21.9583380103651));
#63893=CARTESIAN_POINT('Ctrl Pts',(30.,-1.17523237272425,22.0000046770317));
#63894=CARTESIAN_POINT('Ctrl Pts',(30.6785207267527,-1.17523237272425,22.0416713436984));
#63895=CARTESIAN_POINT('Ctrl Pts',(31.017781090129,-0.587616186362132,22.0833380103651));
#63896=CARTESIAN_POINT('Ctrl Pts',(31.3570414535054,-1.35453513912972E-14,
22.1250046770317));
#63897=CARTESIAN_POINT('Ctrl Pts',(31.017781090129,0.587616186362104,22.1666713436984));
#63898=CARTESIAN_POINT('Ctrl Pts',(30.6785207267527,1.17523237272422,22.2083380103651));
#63899=CARTESIAN_POINT('Ctrl Pts',(30.,1.17523237272422,22.2500046770317));
#63900=CARTESIAN_POINT('Ctrl Pts',(29.3214792732473,1.17523237272422,22.2916713436984));
#63901=CARTESIAN_POINT('Ctrl Pts',(28.9822189098709,0.587616186362105,22.3333380103651));
#63902=CARTESIAN_POINT('Ctrl Pts',(28.6429585464946,-1.32141491426617E-14,
22.3750046770317));
#63903=CARTESIAN_POINT('Ctrl Pts',(28.9822189098709,-0.587616186362132,
22.4166713436984));
#63904=CARTESIAN_POINT('Ctrl Pts',(29.3214792732473,-1.17523237272425,22.4583380103651));
#63905=CARTESIAN_POINT('Ctrl Pts',(30.,-1.17523237272425,22.5000046770317));
#63906=CARTESIAN_POINT('Ctrl Pts',(30.6785207267527,-1.17523237272425,22.5416713436984));
#63907=CARTESIAN_POINT('Ctrl Pts',(31.017781090129,-0.587616186362132,22.5833380103651));
#63908=CARTESIAN_POINT('Ctrl Pts',(31.3570414535054,-1.35453513912972E-14,
22.6250046770317));
#63909=CARTESIAN_POINT('Ctrl Pts',(31.017781090129,0.587616186362104,22.6666713436984));
#63910=CARTESIAN_POINT('Ctrl Pts',(30.6785207267527,1.17523237272422,22.7083380103651));
#63911=CARTESIAN_POINT('Ctrl Pts',(30.,1.17523237272422,22.7500046770317));
#63912=CARTESIAN_POINT('Ctrl Pts',(29.3214792732473,1.17523237272422,22.7916713436984));
#63913=CARTESIAN_POINT('Ctrl Pts',(28.9822189098709,0.587616186362105,22.8333380103651));
#63914=CARTESIAN_POINT('Ctrl Pts',(28.6429585464946,-1.32141491426617E-14,
22.8750046770317));
#63915=CARTESIAN_POINT('Ctrl Pts',(28.9822189098709,-0.587616186362132,
22.9166713436984));
#63916=CARTESIAN_POINT('Ctrl Pts',(29.3214792732473,-1.17523237272425,22.9583380103651));
#63917=CARTESIAN_POINT('Ctrl Pts',(30.,-1.17523237272425,23.0000046770317));
#63918=CARTESIAN_POINT('Ctrl Pts',(30.6785207267527,-1.17523237272425,23.0416713436984));
#63919=CARTESIAN_POINT('Ctrl Pts',(31.017781090129,-0.587616186362132,23.0833380103651));
#63920=CARTESIAN_POINT('Ctrl Pts',(31.3570414535054,-1.35453513912972E-14,
23.1250046770317));
#63921=CARTESIAN_POINT('Ctrl Pts',(31.017781090129,0.587616186362104,23.1666713436984));
#63922=CARTESIAN_POINT('Ctrl Pts',(30.6785207267527,1.17523237272422,23.2083380103651));
#63923=CARTESIAN_POINT('Ctrl Pts',(30.,1.17523237272422,23.2500046770317));
#63924=CARTESIAN_POINT('Ctrl Pts',(29.3214792732473,1.17523237272422,23.2916713436984));
#63925=CARTESIAN_POINT('Ctrl Pts',(28.9822189098709,0.587616186362105,23.3333380103651));
#63926=CARTESIAN_POINT('Ctrl Pts',(28.6429585464946,-1.32141491426617E-14,
23.3750046770317));
#63927=CARTESIAN_POINT('Ctrl Pts',(28.9822189098709,-0.587616186362132,
23.4166713436984));
#63928=CARTESIAN_POINT('Ctrl Pts',(29.3214792732473,-1.17523237272425,23.4583380103651));
#63929=CARTESIAN_POINT('Ctrl Pts',(30.,-1.17523237272425,23.5000046770317));
#63930=CARTESIAN_POINT('Ctrl Pts',(30.6785207267527,-1.17523237272425,23.5416713436984));
#63931=CARTESIAN_POINT('Ctrl Pts',(31.017781090129,-0.587616186362132,23.5833380103651));
#63932=CARTESIAN_POINT('Ctrl Pts',(31.3570414535054,-1.35453513912972E-14,
23.6250046770317));
#63933=CARTESIAN_POINT('Ctrl Pts',(31.017781090129,0.587616186362104,23.6666713436984));
#63934=CARTESIAN_POINT('Ctrl Pts',(30.6785207267527,1.17523237272422,23.7083380103651));
#63935=CARTESIAN_POINT('Ctrl Pts',(30.,1.17523237272422,23.7500046770317));
#63936=CARTESIAN_POINT('Ctrl Pts',(29.3214792732473,1.17523237272422,23.7916713436984));
#63937=CARTESIAN_POINT('Ctrl Pts',(28.9822189098709,0.587616186362105,23.8333380103651));
#63938=CARTESIAN_POINT('Ctrl Pts',(28.6429585464946,-1.32141491426617E-14,
23.8750046770317));
#63939=CARTESIAN_POINT('Ctrl Pts',(28.9822189098709,-0.587616186362132,
23.9166713436984));
#63940=CARTESIAN_POINT('Ctrl Pts',(29.3214792732473,-1.17523237272425,23.9583380103651));
#63941=CARTESIAN_POINT('Ctrl Pts',(30.,-1.17523237272425,24.0000046770317));
#63942=CARTESIAN_POINT('Ctrl Pts',(30.6785207267527,-1.17523237272425,24.0416713436984));
#63943=CARTESIAN_POINT('Ctrl Pts',(31.017781090129,-0.587616186362132,24.0833380103651));
#63944=CARTESIAN_POINT('Ctrl Pts',(31.3570414535054,-1.35453513912972E-14,
24.1250046770317));
#63945=CARTESIAN_POINT('Ctrl Pts',(31.017781090129,0.587616186362104,24.1666713436984));
#63946=CARTESIAN_POINT('Ctrl Pts',(30.6785207267527,1.17523237272422,24.2083380103651));
#63947=CARTESIAN_POINT('Ctrl Pts',(30.,1.17523237272422,24.2500046770317));
#63948=CARTESIAN_POINT('Ctrl Pts',(29.3214792732473,1.17523237272422,24.2916713436984));
#63949=CARTESIAN_POINT('Ctrl Pts',(28.9822189098709,0.587616186362105,24.3333380103651));
#63950=CARTESIAN_POINT('Ctrl Pts',(28.6429585464946,-1.32141491426617E-14,
24.3750046770317));
#63951=CARTESIAN_POINT('Ctrl Pts',(28.9822189098709,-0.587616186362132,
24.4166713436984));
#63952=CARTESIAN_POINT('Ctrl Pts',(29.3214792732473,-1.17523237272425,24.4583380103651));
#63953=CARTESIAN_POINT('Ctrl Pts',(30.,-1.17523237272425,24.5000046770317));
#63954=CARTESIAN_POINT('Ctrl Pts',(30.6785207267527,-1.17523237272425,24.5416713436984));
#63955=CARTESIAN_POINT('Ctrl Pts',(31.017781090129,-0.587616186362132,24.5833380103651));
#63956=CARTESIAN_POINT('Ctrl Pts',(31.3570414535054,-1.35453513912972E-14,
24.6250046770317));
#63957=CARTESIAN_POINT('Ctrl Pts',(31.017781090129,0.587616186362104,24.6666713436984));
#63958=CARTESIAN_POINT('Ctrl Pts',(30.6785207267527,1.17523237272422,24.7083380103651));
#63959=CARTESIAN_POINT('Ctrl Pts',(30.,1.17523237272422,24.7500046770317));
#63960=CARTESIAN_POINT('Ctrl Pts',(29.3214792732473,1.17523237272422,24.7916713436984));
#63961=CARTESIAN_POINT('Ctrl Pts',(28.9822189098709,0.587616186362105,24.8333380103651));
#63962=CARTESIAN_POINT('Ctrl Pts',(28.6429585464946,-1.32141491426617E-14,
24.8750046770317));
#63963=CARTESIAN_POINT('Ctrl Pts',(28.9822189098709,-0.587616186362132,
24.9166713436984));
#63964=CARTESIAN_POINT('Ctrl Pts',(29.3214792732473,-1.17523237272425,24.9583380103651));
#63965=CARTESIAN_POINT('Ctrl Pts',(30.,-1.17523237272425,25.0000046770317));
#63966=CARTESIAN_POINT('Ctrl Pts',(30.6785207267527,-1.17523237272425,25.0416713436984));
#63967=CARTESIAN_POINT('Ctrl Pts',(31.017781090129,-0.587616186362132,25.0833380103651));
#63968=CARTESIAN_POINT('Ctrl Pts',(31.3570414535054,-1.35453513912972E-14,
25.1250046770317));
#63969=CARTESIAN_POINT('Ctrl Pts',(31.017781090129,0.587616186362104,25.1666713436984));
#63970=CARTESIAN_POINT('Ctrl Pts',(30.6785207267527,1.17523237272422,25.2083380103651));
#63971=CARTESIAN_POINT('Ctrl Pts',(30.,1.17523237272422,25.2500046770317));
#63972=CARTESIAN_POINT('Ctrl Pts',(29.3214792732473,1.17523237272422,25.2916713436984));
#63973=CARTESIAN_POINT('Ctrl Pts',(28.9822189098709,0.587616186362105,25.3333380103651));
#63974=CARTESIAN_POINT('Ctrl Pts',(28.6429585464946,-1.32141491426617E-14,
25.3750046770317));
#63975=CARTESIAN_POINT('Ctrl Pts',(28.9822189098709,-0.587616186362132,
25.4166713436984));
#63976=CARTESIAN_POINT('Ctrl Pts',(29.3214792732473,-1.17523237272425,25.4583380103651));
#63977=CARTESIAN_POINT('Ctrl Pts',(30.,-1.17523237272425,25.5000046770317));
#63978=CARTESIAN_POINT('Ctrl Pts',(30.6785207267527,-1.17523237272425,25.5416713436984));
#63979=CARTESIAN_POINT('Ctrl Pts',(31.017781090129,-0.587616186362132,25.5833380103651));
#63980=CARTESIAN_POINT('Ctrl Pts',(31.3570414535054,-1.35453513912972E-14,
25.6250046770317));
#63981=CARTESIAN_POINT('Ctrl Pts',(31.017781090129,0.587616186362104,25.6666713436984));
#63982=CARTESIAN_POINT('Ctrl Pts',(30.6785207267527,1.17523237272422,25.7083380103651));
#63983=CARTESIAN_POINT('Ctrl Pts',(30.,1.17523237272422,25.7500046770317));
#63984=CARTESIAN_POINT('Ctrl Pts',(29.3214792732473,1.17523237272422,25.7916713436984));
#63985=CARTESIAN_POINT('Ctrl Pts',(28.9822189098709,0.587616186362105,25.8333380103651));
#63986=CARTESIAN_POINT('Ctrl Pts',(28.6429585464946,-1.32141491426617E-14,
25.8750046770317));
#63987=CARTESIAN_POINT('Ctrl Pts',(28.9822189098709,-0.587616186362132,
25.9166713436984));
#63988=CARTESIAN_POINT('Ctrl Pts',(29.3214792732473,-1.17523237272425,25.9583380103651));
#63989=CARTESIAN_POINT('Ctrl Pts',(30.,-1.17523237272425,26.0000046770317));
#63990=CARTESIAN_POINT('Ctrl Pts',(30.6785207267527,-1.17523237272425,26.0416713436984));
#63991=CARTESIAN_POINT('Ctrl Pts',(31.017781090129,-0.587616186362132,26.0833380103651));
#63992=CARTESIAN_POINT('Ctrl Pts',(31.3570414535054,-1.35453513912972E-14,
26.1250046770317));
#63993=CARTESIAN_POINT('Ctrl Pts',(31.017781090129,0.587616186362104,26.1666713436984));
#63994=CARTESIAN_POINT('Ctrl Pts',(30.6785207267527,1.17523237272422,26.2083380103651));
#63995=CARTESIAN_POINT('Ctrl Pts',(30.,1.17523237272422,26.2500046770317));
#63996=CARTESIAN_POINT('Ctrl Pts',(29.3214792732473,1.17523237272422,26.2916713436984));
#63997=CARTESIAN_POINT('Ctrl Pts',(28.9822189098709,0.587616186362105,26.3333380103651));
#63998=CARTESIAN_POINT('Ctrl Pts',(28.6429585464946,-1.32141491426617E-14,
26.3750046770317));
#63999=CARTESIAN_POINT('Ctrl Pts',(28.9822189098709,-0.587616186362132,
26.4166713436984));
#64000=CARTESIAN_POINT('Ctrl Pts',(29.3214792732473,-1.17523237272425,26.4583380103651));
#64001=CARTESIAN_POINT('Ctrl Pts',(30.,-1.17523237272425,26.5000046770317));
#64002=CARTESIAN_POINT('Ctrl Pts',(30.6785207267527,-1.17523237272425,26.5416713436984));
#64003=CARTESIAN_POINT('Ctrl Pts',(31.017781090129,-0.587616186362132,26.5833380103651));
#64004=CARTESIAN_POINT('Ctrl Pts',(31.3570414535054,-1.35453513912972E-14,
26.6250046770317));
#64005=CARTESIAN_POINT('Ctrl Pts',(31.017781090129,0.587616186362104,26.6666713436984));
#64006=CARTESIAN_POINT('Ctrl Pts',(30.6785207267527,1.17523237272422,26.7083380103651));
#64007=CARTESIAN_POINT('Ctrl Pts',(30.,1.17523237272422,26.7500046770317));
#64008=CARTESIAN_POINT('Ctrl Pts',(29.3214792732473,1.17523237272422,26.7916713436984));
#64009=CARTESIAN_POINT('Ctrl Pts',(28.9822189098709,0.587616186362105,26.8333380103651));
#64010=CARTESIAN_POINT('Ctrl Pts',(28.6429585464946,-1.32141491426617E-14,
26.8750046770317));
#64011=CARTESIAN_POINT('Ctrl Pts',(28.9822189098709,-0.587616186362132,
26.9166713436984));
#64012=CARTESIAN_POINT('Ctrl Pts',(29.3214792732473,-1.17523237272425,26.9583380103651));
#64013=CARTESIAN_POINT('Ctrl Pts',(30.,-1.17523237272425,27.0000046770317));
#64014=CARTESIAN_POINT('Ctrl Pts',(30.6785207267527,-1.17523237272425,27.0416713436984));
#64015=CARTESIAN_POINT('Ctrl Pts',(31.017781090129,-0.587616186362132,27.0833380103651));
#64016=CARTESIAN_POINT('Ctrl Pts',(31.3570414535054,-1.35453513912972E-14,
27.1250046770317));
#64017=CARTESIAN_POINT('Ctrl Pts',(31.017781090129,0.587616186362104,27.1666713436984));
#64018=CARTESIAN_POINT('Ctrl Pts',(30.6785207267527,1.17523237272422,27.2083380103651));
#64019=CARTESIAN_POINT('Ctrl Pts',(30.,1.17523237272422,27.2500046770317));
#64020=CARTESIAN_POINT('Ctrl Pts',(29.3214792732473,1.17523237272422,27.2916713436984));
#64021=CARTESIAN_POINT('Ctrl Pts',(28.9822189098709,0.587616186362105,27.3333380103651));
#64022=CARTESIAN_POINT('Ctrl Pts',(28.6429585464946,-1.32141491426617E-14,
27.3750046770317));
#64023=CARTESIAN_POINT('Ctrl Pts',(28.9822189098709,-0.587616186362132,
27.4166713436984));
#64024=CARTESIAN_POINT('Ctrl Pts',(29.3214792732473,-1.17523237272425,27.4583380103651));
#64025=CARTESIAN_POINT('Ctrl Pts',(30.,-1.17523237272425,27.5000046770317));
#64026=CARTESIAN_POINT('Ctrl Pts',(30.6785207267527,-1.17523237272425,27.5416713436984));
#64027=CARTESIAN_POINT('Ctrl Pts',(31.017781090129,-0.587616186362132,27.5833380103651));
#64028=CARTESIAN_POINT('Ctrl Pts',(31.3570414535054,-1.35453513912972E-14,
27.6250046770317));
#64029=CARTESIAN_POINT('Ctrl Pts',(31.017781090129,0.587616186362104,27.6666713436984));
#64030=CARTESIAN_POINT('Ctrl Pts',(30.6785207267527,1.17523237272422,27.7083380103651));
#64031=CARTESIAN_POINT('Ctrl Pts',(30.,1.17523237272422,27.7500046770317));
#64032=CARTESIAN_POINT('Ctrl Pts',(29.3214792732473,1.17523237272422,27.7916713436984));
#64033=CARTESIAN_POINT('Ctrl Pts',(28.9822189098709,0.587616186362105,27.8333380103651));
#64034=CARTESIAN_POINT('Ctrl Pts',(28.6429585464946,-1.32141491426617E-14,
27.8750046770317));
#64035=CARTESIAN_POINT('Ctrl Pts',(28.9822189098709,-0.587616186362132,
27.9166713436984));
#64036=CARTESIAN_POINT('Ctrl Pts',(29.3214792732473,-1.17523237272425,27.9583380103651));
#64037=CARTESIAN_POINT('Ctrl Pts',(30.,-1.17523237272425,28.0000046770317));
#64038=CARTESIAN_POINT('Ctrl Pts',(30.6785207267527,-1.17523237272425,28.0416713436984));
#64039=CARTESIAN_POINT('Ctrl Pts',(31.017781090129,-0.587616186362132,28.0833380103651));
#64040=CARTESIAN_POINT('Ctrl Pts',(31.3570414535054,-1.35453513912972E-14,
28.1250046770317));
#64041=CARTESIAN_POINT('Ctrl Pts',(31.017781090129,0.587616186362104,28.1666713436984));
#64042=CARTESIAN_POINT('Ctrl Pts',(30.6785207267527,1.17523237272422,28.2083380103651));
#64043=CARTESIAN_POINT('Ctrl Pts',(30.,1.17523237272422,28.2500046770317));
#64044=CARTESIAN_POINT('Ctrl Pts',(29.3214792732473,1.17523237272422,28.2916713436984));
#64045=CARTESIAN_POINT('Ctrl Pts',(28.9822189098709,0.587616186362105,28.3333380103651));
#64046=CARTESIAN_POINT('Ctrl Pts',(28.6429585464946,-1.32141491426617E-14,
28.3750046770317));
#64047=CARTESIAN_POINT('Ctrl Pts',(28.9822189098709,-0.587616186362132,
28.4166713436984));
#64048=CARTESIAN_POINT('Ctrl Pts',(29.3214792732473,-1.17523237272425,28.4583380103651));
#64049=CARTESIAN_POINT('Ctrl Pts',(30.,-1.17523237272425,28.5000046770317));
#64050=CARTESIAN_POINT('Ctrl Pts',(30.6785207267527,-1.17523237272425,28.5416713436984));
#64051=CARTESIAN_POINT('Ctrl Pts',(31.017781090129,-0.587616186362132,28.5833380103651));
#64052=CARTESIAN_POINT('Ctrl Pts',(31.3570414535054,-1.35453513912972E-14,
28.6250046770317));
#64053=CARTESIAN_POINT('Ctrl Pts',(31.017781090129,0.587616186362104,28.6666713436984));
#64054=CARTESIAN_POINT('Ctrl Pts',(30.6785207267527,1.17523237272422,28.7083380103651));
#64055=CARTESIAN_POINT('Ctrl Pts',(30.,1.17523237272422,28.7500046770317));
#64056=CARTESIAN_POINT('Ctrl Pts',(29.3214792732473,1.17523237272422,28.7916713436984));
#64057=CARTESIAN_POINT('Ctrl Pts',(28.9822189098709,0.587616186362105,28.8333380103651));
#64058=CARTESIAN_POINT('Ctrl Pts',(28.6429585464946,-1.32141491426617E-14,
28.8750046770317));
#64059=CARTESIAN_POINT('Ctrl Pts',(28.9822189098709,-0.587616186362132,
28.9166713436984));
#64060=CARTESIAN_POINT('Ctrl Pts',(29.3214792732473,-1.17523237272425,28.9583380103651));
#64061=CARTESIAN_POINT('Ctrl Pts',(30.,-1.17523237272425,29.0000046770317));
#64062=CARTESIAN_POINT('Ctrl Pts',(30.6785207267527,-1.17523237272425,29.0416713436984));
#64063=CARTESIAN_POINT('Ctrl Pts',(31.017781090129,-0.587616186362132,29.0833380103651));
#64064=CARTESIAN_POINT('Ctrl Pts',(31.3570414535054,-1.35453513912972E-14,
29.1250046770317));
#64065=CARTESIAN_POINT('Ctrl Pts',(31.017781090129,0.587616186362104,29.1666713436984));
#64066=CARTESIAN_POINT('Ctrl Pts',(30.6785207267527,1.17523237272422,29.2083380103651));
#64067=CARTESIAN_POINT('Ctrl Pts',(30.,1.17523237272422,29.2500046770317));
#64068=CARTESIAN_POINT('Ctrl Pts',(29.3214792732473,1.17523237272422,29.2916713436984));
#64069=CARTESIAN_POINT('Ctrl Pts',(28.9822189098709,0.587616186362105,29.3333380103651));
#64070=CARTESIAN_POINT('Ctrl Pts',(28.6429585464946,-1.32141491426617E-14,
29.3750046770317));
#64071=CARTESIAN_POINT('Ctrl Pts',(28.9822189098709,-0.587616186362132,
29.4166713436984));
#64072=CARTESIAN_POINT('Ctrl Pts',(29.3214792732473,-1.17523237272425,29.4583380103651));
#64073=CARTESIAN_POINT('Ctrl Pts',(30.,-1.17523237272425,29.5000046770317));
#64074=CARTESIAN_POINT('Ctrl Pts',(30.6785207267527,-1.17523237272425,29.5416713436984));
#64075=CARTESIAN_POINT('Ctrl Pts',(31.017781090129,-0.587616186362132,29.5833380103651));
#64076=CARTESIAN_POINT('Ctrl Pts',(31.3570414535054,-1.35453513912972E-14,
29.6250046770317));
#64077=CARTESIAN_POINT('Ctrl Pts',(31.017781090129,0.587616186362104,29.6666713436984));
#64078=CARTESIAN_POINT('Ctrl Pts',(30.6785207267527,1.17523237272422,29.7083380103651));
#64079=CARTESIAN_POINT('Ctrl Pts',(30.,1.17523237272422,29.7500046770317));
#64080=CARTESIAN_POINT('Ctrl Pts',(29.3214792732473,1.17523237272422,29.7916713436984));
#64081=CARTESIAN_POINT('Ctrl Pts',(28.9822189098709,0.587616186362105,29.8333380103651));
#64082=CARTESIAN_POINT('Ctrl Pts',(28.6429585464946,-1.32141491426617E-14,
29.8750046770317));
#64083=CARTESIAN_POINT('Ctrl Pts',(28.9822189098709,-0.587616186362132,
29.9166713436984));
#64084=CARTESIAN_POINT('Ctrl Pts',(29.3214792732473,-1.17523237272425,29.9583380103651));
#64085=CARTESIAN_POINT('Ctrl Pts',(30.,-1.17523237272425,30.0000046770317));
#64086=CARTESIAN_POINT('Ctrl Pts',(30.6785207267527,-1.17523237272425,30.0416713436984));
#64087=CARTESIAN_POINT('Ctrl Pts',(31.017781090129,-0.587616186362132,30.0833380103651));
#64088=CARTESIAN_POINT('Ctrl Pts',(31.3570414535054,-1.35453513912972E-14,
30.1250046770317));
#64089=CARTESIAN_POINT('Ctrl Pts',(31.017781090129,0.587616186362104,30.1666713436984));
#64090=CARTESIAN_POINT('Ctrl Pts',(30.6785207267527,1.17523237272422,30.2083380103651));
#64091=CARTESIAN_POINT('Ctrl Pts',(30.,1.17523237272422,30.2500046770317));
#64092=CARTESIAN_POINT('Ctrl Pts',(29.3214792732473,1.17523237272422,30.2916713436984));
#64093=CARTESIAN_POINT('Ctrl Pts',(28.9822189098709,0.587616186362105,30.3333380103651));
#64094=CARTESIAN_POINT('Ctrl Pts',(28.6429585464946,-1.32141491426617E-14,
30.3750046770317));
#64095=CARTESIAN_POINT('Ctrl Pts',(28.9822189098709,-0.587616186362132,
30.4166713436984));
#64096=CARTESIAN_POINT('Ctrl Pts',(29.3214792732473,-1.17523237272425,30.4583380103651));
#64097=CARTESIAN_POINT('Ctrl Pts',(30.,-1.17523237272425,30.5000046770317));
#64098=CARTESIAN_POINT('Ctrl Pts',(30.6785207267527,-1.17523237272425,30.5416713436984));
#64099=CARTESIAN_POINT('Ctrl Pts',(31.017781090129,-0.587616186362132,30.5833380103651));
#64100=CARTESIAN_POINT('Ctrl Pts',(31.3570414535054,-1.35453513912972E-14,
30.6250046770317));
#64101=CARTESIAN_POINT('Ctrl Pts',(31.017781090129,0.587616186362104,30.6666713436984));
#64102=CARTESIAN_POINT('Ctrl Pts',(30.6785207267527,1.17523237272422,30.7083380103651));
#64103=CARTESIAN_POINT('Ctrl Pts',(30.,1.17523237272422,30.7500046770317));
#64104=CARTESIAN_POINT('Ctrl Pts',(29.3214792732473,1.17523237272422,30.7916713436984));
#64105=CARTESIAN_POINT('Ctrl Pts',(28.9822189098709,0.587616186362105,30.8333380103651));
#64106=CARTESIAN_POINT('Ctrl Pts',(28.6429585464946,-1.32141491426617E-14,
30.8750046770317));
#64107=CARTESIAN_POINT('Ctrl Pts',(28.9822189098709,-0.587616186362132,
30.9166713436984));
#64108=CARTESIAN_POINT('Ctrl Pts',(29.3214792732473,-1.17523237272425,30.9583380103651));
#64109=CARTESIAN_POINT('Ctrl Pts',(30.,-1.17523237272425,31.0000046770317));
#64110=CARTESIAN_POINT('Ctrl Pts',(30.6785207267527,-1.17523237272425,31.0416713436984));
#64111=CARTESIAN_POINT('Ctrl Pts',(31.017781090129,-0.587616186362132,31.0833380103651));
#64112=CARTESIAN_POINT('Ctrl Pts',(31.3570414535054,-1.35453513912972E-14,
31.1250046770317));
#64113=CARTESIAN_POINT('Ctrl Pts',(31.017781090129,0.587616186362104,31.1666713436984));
#64114=CARTESIAN_POINT('Ctrl Pts',(30.6785207267527,1.17523237272422,31.2083380103651));
#64115=CARTESIAN_POINT('Ctrl Pts',(30.,1.17523237272422,31.2500046770317));
#64116=CARTESIAN_POINT('Ctrl Pts',(30.,1.52706329386825,15.546875));
#64117=CARTESIAN_POINT('Ctrl Pts',(29.1183495962155,1.52706329386825,15.5885416666667));
#64118=CARTESIAN_POINT('Ctrl Pts',(28.6775243943233,0.76353164693412,15.6302083333334));
#64119=CARTESIAN_POINT('Ctrl Pts',(28.2366991924311,-1.31894491186926E-14,
15.671875));
#64120=CARTESIAN_POINT('Ctrl Pts',(28.6775243943233,-0.763531646934146,
15.7135416666667));
#64121=CARTESIAN_POINT('Ctrl Pts',(29.1183495962155,-1.52706329386828,15.7552083333334));
#64122=CARTESIAN_POINT('Ctrl Pts',(30.,-1.52706329386828,15.796875));
#64123=CARTESIAN_POINT('Ctrl Pts',(30.8816504037844,-1.52706329386828,15.8385416666667));
#64124=CARTESIAN_POINT('Ctrl Pts',(31.3224756056766,-0.763531646934147,
15.8802083333334));
#64125=CARTESIAN_POINT('Ctrl Pts',(31.7633008075689,-1.36198038370242E-14,
15.921875));
#64126=CARTESIAN_POINT('Ctrl Pts',(31.3224756056766,0.763531646934118,15.9635416666667));
#64127=CARTESIAN_POINT('Ctrl Pts',(30.8816504037844,1.52706329386825,16.0052083333334));
#64128=CARTESIAN_POINT('Ctrl Pts',(30.,1.52706329386825,16.046875));
#64129=CARTESIAN_POINT('Ctrl Pts',(29.1183495962155,1.52706329386825,16.0885416666667));
#64130=CARTESIAN_POINT('Ctrl Pts',(28.6775243943233,0.76353164693412,16.1302083333334));
#64131=CARTESIAN_POINT('Ctrl Pts',(28.2366991924311,-1.31894491186926E-14,
16.171875));
#64132=CARTESIAN_POINT('Ctrl Pts',(28.6775243943233,-0.763531646934146,
16.2135416666667));
#64133=CARTESIAN_POINT('Ctrl Pts',(29.1183495962155,-1.52706329386828,16.2552083333334));
#64134=CARTESIAN_POINT('Ctrl Pts',(30.,-1.52706329386828,16.296875));
#64135=CARTESIAN_POINT('Ctrl Pts',(30.8816504037844,-1.52706329386828,16.3385416666667));
#64136=CARTESIAN_POINT('Ctrl Pts',(31.3224756056766,-0.763531646934147,
16.3802083333334));
#64137=CARTESIAN_POINT('Ctrl Pts',(31.7633008075689,-1.36198038370242E-14,
16.421875));
#64138=CARTESIAN_POINT('Ctrl Pts',(31.3224756056766,0.763531646934118,16.4635416666667));
#64139=CARTESIAN_POINT('Ctrl Pts',(30.8816504037844,1.52706329386825,16.5052083333334));
#64140=CARTESIAN_POINT('Ctrl Pts',(30.,1.52706329386825,16.546875));
#64141=CARTESIAN_POINT('Ctrl Pts',(29.1183495962155,1.52706329386825,16.5885416666667));
#64142=CARTESIAN_POINT('Ctrl Pts',(28.6775243943233,0.76353164693412,16.6302083333334));
#64143=CARTESIAN_POINT('Ctrl Pts',(28.2366991924311,-1.31894491186926E-14,
16.671875));
#64144=CARTESIAN_POINT('Ctrl Pts',(28.6775243943233,-0.763531646934146,
16.7135416666667));
#64145=CARTESIAN_POINT('Ctrl Pts',(29.1183495962155,-1.52706329386828,16.7552083333334));
#64146=CARTESIAN_POINT('Ctrl Pts',(30.,-1.52706329386828,16.796875));
#64147=CARTESIAN_POINT('Ctrl Pts',(30.8816504037844,-1.52706329386828,16.8385416666667));
#64148=CARTESIAN_POINT('Ctrl Pts',(31.3224756056766,-0.763531646934147,
16.8802083333334));
#64149=CARTESIAN_POINT('Ctrl Pts',(31.7633008075689,-1.36198038370242E-14,
16.921875));
#64150=CARTESIAN_POINT('Ctrl Pts',(31.3224756056766,0.763531646934118,16.9635416666667));
#64151=CARTESIAN_POINT('Ctrl Pts',(30.8816504037844,1.52706329386825,17.0052083333334));
#64152=CARTESIAN_POINT('Ctrl Pts',(30.,1.52706329386825,17.046875));
#64153=CARTESIAN_POINT('Ctrl Pts',(29.1183495962155,1.52706329386825,17.0885416666667));
#64154=CARTESIAN_POINT('Ctrl Pts',(28.6775243943233,0.76353164693412,17.1302083333334));
#64155=CARTESIAN_POINT('Ctrl Pts',(28.2366991924311,-1.31894491186926E-14,
17.171875));
#64156=CARTESIAN_POINT('Ctrl Pts',(28.6775243943233,-0.763531646934146,
17.2135416666667));
#64157=CARTESIAN_POINT('Ctrl Pts',(29.1183495962155,-1.52706329386828,17.2552083333334));
#64158=CARTESIAN_POINT('Ctrl Pts',(30.,-1.52706329386828,17.296875));
#64159=CARTESIAN_POINT('Ctrl Pts',(30.8816504037844,-1.52706329386828,17.3385416666667));
#64160=CARTESIAN_POINT('Ctrl Pts',(31.3224756056766,-0.763531646934147,
17.3802083333334));
#64161=CARTESIAN_POINT('Ctrl Pts',(31.7633008075689,-1.36198038370242E-14,
17.421875));
#64162=CARTESIAN_POINT('Ctrl Pts',(31.3224756056766,0.763531646934118,17.4635416666667));
#64163=CARTESIAN_POINT('Ctrl Pts',(30.8816504037844,1.52706329386825,17.5052083333334));
#64164=CARTESIAN_POINT('Ctrl Pts',(30.,1.52706329386825,17.546875));
#64165=CARTESIAN_POINT('Ctrl Pts',(29.1183495962155,1.52706329386825,17.5885416666667));
#64166=CARTESIAN_POINT('Ctrl Pts',(28.6775243943233,0.76353164693412,17.6302083333334));
#64167=CARTESIAN_POINT('Ctrl Pts',(28.2366991924311,-1.31894491186926E-14,
17.671875));
#64168=CARTESIAN_POINT('Ctrl Pts',(28.6775243943233,-0.763531646934146,
17.7135416666667));
#64169=CARTESIAN_POINT('Ctrl Pts',(29.1183495962155,-1.52706329386828,17.7552083333334));
#64170=CARTESIAN_POINT('Ctrl Pts',(30.,-1.52706329386828,17.796875));
#64171=CARTESIAN_POINT('Ctrl Pts',(30.8816504037844,-1.52706329386828,17.8385416666667));
#64172=CARTESIAN_POINT('Ctrl Pts',(31.3224756056766,-0.763531646934147,
17.8802083333334));
#64173=CARTESIAN_POINT('Ctrl Pts',(31.7633008075689,-1.36198038370242E-14,
17.921875));
#64174=CARTESIAN_POINT('Ctrl Pts',(31.3224756056766,0.763531646934118,17.9635416666667));
#64175=CARTESIAN_POINT('Ctrl Pts',(30.8816504037844,1.52706329386825,18.0052083333334));
#64176=CARTESIAN_POINT('Ctrl Pts',(30.,1.52706329386825,18.046875));
#64177=CARTESIAN_POINT('Ctrl Pts',(29.1183495962155,1.52706329386825,18.0885416666667));
#64178=CARTESIAN_POINT('Ctrl Pts',(28.6775243943233,0.76353164693412,18.1302083333334));
#64179=CARTESIAN_POINT('Ctrl Pts',(28.2366991924311,-1.31894491186926E-14,
18.171875));
#64180=CARTESIAN_POINT('Ctrl Pts',(28.6775243943233,-0.763531646934146,
18.2135416666667));
#64181=CARTESIAN_POINT('Ctrl Pts',(29.1183495962155,-1.52706329386828,18.2552083333334));
#64182=CARTESIAN_POINT('Ctrl Pts',(30.,-1.52706329386828,18.296875));
#64183=CARTESIAN_POINT('Ctrl Pts',(30.8816504037844,-1.52706329386828,18.3385416666667));
#64184=CARTESIAN_POINT('Ctrl Pts',(31.3224756056766,-0.763531646934147,
18.3802083333334));
#64185=CARTESIAN_POINT('Ctrl Pts',(31.7633008075689,-1.36198038370242E-14,
18.421875));
#64186=CARTESIAN_POINT('Ctrl Pts',(31.3224756056766,0.763531646934118,18.4635416666667));
#64187=CARTESIAN_POINT('Ctrl Pts',(30.8816504037844,1.52706329386825,18.5052083333334));
#64188=CARTESIAN_POINT('Ctrl Pts',(30.,1.52706329386825,18.546875));
#64189=CARTESIAN_POINT('Ctrl Pts',(29.1183495962155,1.52706329386825,18.5885416666667));
#64190=CARTESIAN_POINT('Ctrl Pts',(28.6775243943233,0.76353164693412,18.6302083333334));
#64191=CARTESIAN_POINT('Ctrl Pts',(28.2366991924311,-1.31894491186926E-14,
18.671875));
#64192=CARTESIAN_POINT('Ctrl Pts',(28.6775243943233,-0.763531646934146,
18.7135416666667));
#64193=CARTESIAN_POINT('Ctrl Pts',(29.1183495962155,-1.52706329386828,18.7552083333334));
#64194=CARTESIAN_POINT('Ctrl Pts',(30.,-1.52706329386828,18.796875));
#64195=CARTESIAN_POINT('Ctrl Pts',(30.8816504037844,-1.52706329386828,18.8385416666667));
#64196=CARTESIAN_POINT('Ctrl Pts',(31.3224756056766,-0.763531646934147,
18.8802083333334));
#64197=CARTESIAN_POINT('Ctrl Pts',(31.7633008075689,-1.36198038370242E-14,
18.921875));
#64198=CARTESIAN_POINT('Ctrl Pts',(31.3224756056766,0.763531646934118,18.9635416666667));
#64199=CARTESIAN_POINT('Ctrl Pts',(30.8816504037844,1.52706329386825,19.0052083333334));
#64200=CARTESIAN_POINT('Ctrl Pts',(30.,1.52706329386825,19.046875));
#64201=CARTESIAN_POINT('Ctrl Pts',(29.1183495962155,1.52706329386825,19.0885416666667));
#64202=CARTESIAN_POINT('Ctrl Pts',(28.6775243943233,0.76353164693412,19.1302083333334));
#64203=CARTESIAN_POINT('Ctrl Pts',(28.2366991924311,-1.31894491186926E-14,
19.171875));
#64204=CARTESIAN_POINT('Ctrl Pts',(28.6775243943233,-0.763531646934146,
19.2135416666667));
#64205=CARTESIAN_POINT('Ctrl Pts',(29.1183495962155,-1.52706329386828,19.2552083333334));
#64206=CARTESIAN_POINT('Ctrl Pts',(30.,-1.52706329386828,19.296875));
#64207=CARTESIAN_POINT('Ctrl Pts',(30.8816504037844,-1.52706329386828,19.3385416666667));
#64208=CARTESIAN_POINT('Ctrl Pts',(31.3224756056766,-0.763531646934147,
19.3802083333334));
#64209=CARTESIAN_POINT('Ctrl Pts',(31.7633008075689,-1.36198038370242E-14,
19.421875));
#64210=CARTESIAN_POINT('Ctrl Pts',(31.3224756056766,0.763531646934118,19.4635416666667));
#64211=CARTESIAN_POINT('Ctrl Pts',(30.8816504037844,1.52706329386825,19.5052083333334));
#64212=CARTESIAN_POINT('Ctrl Pts',(30.,1.52706329386825,19.546875));
#64213=CARTESIAN_POINT('Ctrl Pts',(29.1183495962155,1.52706329386825,19.5885416666667));
#64214=CARTESIAN_POINT('Ctrl Pts',(28.6775243943233,0.76353164693412,19.6302083333334));
#64215=CARTESIAN_POINT('Ctrl Pts',(28.2366991924311,-1.31894491186926E-14,
19.671875));
#64216=CARTESIAN_POINT('Ctrl Pts',(28.6775243943233,-0.763531646934146,
19.7135416666667));
#64217=CARTESIAN_POINT('Ctrl Pts',(29.1183495962155,-1.52706329386828,19.7552083333334));
#64218=CARTESIAN_POINT('Ctrl Pts',(30.,-1.52706329386828,19.796875));
#64219=CARTESIAN_POINT('Ctrl Pts',(30.8816504037844,-1.52706329386828,19.8385416666667));
#64220=CARTESIAN_POINT('Ctrl Pts',(31.3224756056766,-0.763531646934147,
19.8802083333334));
#64221=CARTESIAN_POINT('Ctrl Pts',(31.7633008075689,-1.36198038370242E-14,
19.921875));
#64222=CARTESIAN_POINT('Ctrl Pts',(31.3224756056766,0.763531646934118,19.9635416666667));
#64223=CARTESIAN_POINT('Ctrl Pts',(30.8816504037844,1.52706329386825,20.0052083333334));
#64224=CARTESIAN_POINT('Ctrl Pts',(30.,1.52706329386825,20.046875));
#64225=CARTESIAN_POINT('Ctrl Pts',(29.1183495962155,1.52706329386825,20.0885416666667));
#64226=CARTESIAN_POINT('Ctrl Pts',(28.6775243943233,0.76353164693412,20.1302083333334));
#64227=CARTESIAN_POINT('Ctrl Pts',(28.2366991924311,-1.31894491186926E-14,
20.171875));
#64228=CARTESIAN_POINT('Ctrl Pts',(28.6775243943233,-0.763531646934146,
20.2135416666667));
#64229=CARTESIAN_POINT('Ctrl Pts',(29.1183495962155,-1.52706329386828,20.2552083333334));
#64230=CARTESIAN_POINT('Ctrl Pts',(30.,-1.52706329386828,20.296875));
#64231=CARTESIAN_POINT('Ctrl Pts',(30.8816504037844,-1.52706329386828,20.3385416666667));
#64232=CARTESIAN_POINT('Ctrl Pts',(31.3224756056766,-0.763531646934147,
20.3802083333334));
#64233=CARTESIAN_POINT('Ctrl Pts',(31.7633008075689,-1.36198038370242E-14,
20.421875));
#64234=CARTESIAN_POINT('Ctrl Pts',(31.3224756056766,0.763531646934118,20.4635416666667));
#64235=CARTESIAN_POINT('Ctrl Pts',(30.8816504037844,1.52706329386825,20.5052083333334));
#64236=CARTESIAN_POINT('Ctrl Pts',(30.,1.52706329386825,20.546875));
#64237=CARTESIAN_POINT('Ctrl Pts',(29.1183495962155,1.52706329386825,20.5885416666667));
#64238=CARTESIAN_POINT('Ctrl Pts',(28.6775243943233,0.76353164693412,20.6302083333334));
#64239=CARTESIAN_POINT('Ctrl Pts',(28.2366991924311,-1.31894491186926E-14,
20.671875));
#64240=CARTESIAN_POINT('Ctrl Pts',(28.6775243943233,-0.763531646934146,
20.7135416666667));
#64241=CARTESIAN_POINT('Ctrl Pts',(29.1183495962155,-1.52706329386828,20.7552083333334));
#64242=CARTESIAN_POINT('Ctrl Pts',(30.,-1.52706329386828,20.796875));
#64243=CARTESIAN_POINT('Ctrl Pts',(30.8816504037844,-1.52706329386828,20.8385416666667));
#64244=CARTESIAN_POINT('Ctrl Pts',(31.3224756056766,-0.763531646934147,
20.8802083333334));
#64245=CARTESIAN_POINT('Ctrl Pts',(31.7633008075689,-1.36198038370242E-14,
20.921875));
#64246=CARTESIAN_POINT('Ctrl Pts',(31.3224756056766,0.763531646934118,20.9635416666667));
#64247=CARTESIAN_POINT('Ctrl Pts',(30.8816504037844,1.52706329386825,21.0052083333334));
#64248=CARTESIAN_POINT('Ctrl Pts',(30.,1.52706329386825,21.046875));
#64249=CARTESIAN_POINT('Ctrl Pts',(29.1183495962155,1.52706329386825,21.0885416666667));
#64250=CARTESIAN_POINT('Ctrl Pts',(28.6775243943233,0.76353164693412,21.1302083333334));
#64251=CARTESIAN_POINT('Ctrl Pts',(28.2366991924311,-1.31894491186926E-14,
21.171875));
#64252=CARTESIAN_POINT('Ctrl Pts',(28.6775243943233,-0.763531646934146,
21.2135416666667));
#64253=CARTESIAN_POINT('Ctrl Pts',(29.1183495962155,-1.52706329386828,21.2552083333334));
#64254=CARTESIAN_POINT('Ctrl Pts',(30.,-1.52706329386828,21.296875));
#64255=CARTESIAN_POINT('Ctrl Pts',(30.8816504037844,-1.52706329386828,21.3385416666667));
#64256=CARTESIAN_POINT('Ctrl Pts',(31.3224756056766,-0.763531646934147,
21.3802083333334));
#64257=CARTESIAN_POINT('Ctrl Pts',(31.7633008075689,-1.36198038370242E-14,
21.421875));
#64258=CARTESIAN_POINT('Ctrl Pts',(31.3224756056766,0.763531646934118,21.4635416666667));
#64259=CARTESIAN_POINT('Ctrl Pts',(30.8816504037844,1.52706329386825,21.5052083333334));
#64260=CARTESIAN_POINT('Ctrl Pts',(30.,1.52706329386825,21.546875));
#64261=CARTESIAN_POINT('Ctrl Pts',(29.1183495962155,1.52706329386825,21.5885416666667));
#64262=CARTESIAN_POINT('Ctrl Pts',(28.6775243943233,0.76353164693412,21.6302083333334));
#64263=CARTESIAN_POINT('Ctrl Pts',(28.2366991924311,-1.31894491186926E-14,
21.671875));
#64264=CARTESIAN_POINT('Ctrl Pts',(28.6775243943233,-0.763531646934146,
21.7135416666667));
#64265=CARTESIAN_POINT('Ctrl Pts',(29.1183495962155,-1.52706329386828,21.7552083333334));
#64266=CARTESIAN_POINT('Ctrl Pts',(30.,-1.52706329386828,21.796875));
#64267=CARTESIAN_POINT('Ctrl Pts',(30.8816504037844,-1.52706329386828,21.8385416666667));
#64268=CARTESIAN_POINT('Ctrl Pts',(31.3224756056766,-0.763531646934147,
21.8802083333334));
#64269=CARTESIAN_POINT('Ctrl Pts',(31.7633008075689,-1.36198038370242E-14,
21.921875));
#64270=CARTESIAN_POINT('Ctrl Pts',(31.3224756056766,0.763531646934118,21.9635416666667));
#64271=CARTESIAN_POINT('Ctrl Pts',(30.8816504037844,1.52706329386825,22.0052083333334));
#64272=CARTESIAN_POINT('Ctrl Pts',(30.,1.52706329386825,22.046875));
#64273=CARTESIAN_POINT('Ctrl Pts',(29.1183495962155,1.52706329386825,22.0885416666667));
#64274=CARTESIAN_POINT('Ctrl Pts',(28.6775243943233,0.76353164693412,22.1302083333334));
#64275=CARTESIAN_POINT('Ctrl Pts',(28.2366991924311,-1.31894491186926E-14,
22.171875));
#64276=CARTESIAN_POINT('Ctrl Pts',(28.6775243943233,-0.763531646934146,
22.2135416666667));
#64277=CARTESIAN_POINT('Ctrl Pts',(29.1183495962155,-1.52706329386828,22.2552083333334));
#64278=CARTESIAN_POINT('Ctrl Pts',(30.,-1.52706329386828,22.296875));
#64279=CARTESIAN_POINT('Ctrl Pts',(30.8816504037844,-1.52706329386828,22.3385416666667));
#64280=CARTESIAN_POINT('Ctrl Pts',(31.3224756056766,-0.763531646934147,
22.3802083333334));
#64281=CARTESIAN_POINT('Ctrl Pts',(31.7633008075689,-1.36198038370242E-14,
22.421875));
#64282=CARTESIAN_POINT('Ctrl Pts',(31.3224756056766,0.763531646934118,22.4635416666667));
#64283=CARTESIAN_POINT('Ctrl Pts',(30.8816504037844,1.52706329386825,22.5052083333334));
#64284=CARTESIAN_POINT('Ctrl Pts',(30.,1.52706329386825,22.546875));
#64285=CARTESIAN_POINT('Ctrl Pts',(29.1183495962155,1.52706329386825,22.5885416666667));
#64286=CARTESIAN_POINT('Ctrl Pts',(28.6775243943233,0.76353164693412,22.6302083333334));
#64287=CARTESIAN_POINT('Ctrl Pts',(28.2366991924311,-1.31894491186926E-14,
22.671875));
#64288=CARTESIAN_POINT('Ctrl Pts',(28.6775243943233,-0.763531646934146,
22.7135416666667));
#64289=CARTESIAN_POINT('Ctrl Pts',(29.1183495962155,-1.52706329386828,22.7552083333334));
#64290=CARTESIAN_POINT('Ctrl Pts',(30.,-1.52706329386828,22.796875));
#64291=CARTESIAN_POINT('Ctrl Pts',(30.8816504037844,-1.52706329386828,22.8385416666667));
#64292=CARTESIAN_POINT('Ctrl Pts',(31.3224756056766,-0.763531646934147,
22.8802083333334));
#64293=CARTESIAN_POINT('Ctrl Pts',(31.7633008075689,-1.36198038370242E-14,
22.921875));
#64294=CARTESIAN_POINT('Ctrl Pts',(31.3224756056766,0.763531646934118,22.9635416666667));
#64295=CARTESIAN_POINT('Ctrl Pts',(30.8816504037844,1.52706329386825,23.0052083333334));
#64296=CARTESIAN_POINT('Ctrl Pts',(30.,1.52706329386825,23.046875));
#64297=CARTESIAN_POINT('Ctrl Pts',(29.1183495962155,1.52706329386825,23.0885416666667));
#64298=CARTESIAN_POINT('Ctrl Pts',(28.6775243943233,0.76353164693412,23.1302083333334));
#64299=CARTESIAN_POINT('Ctrl Pts',(28.2366991924311,-1.31894491186926E-14,
23.171875));
#64300=CARTESIAN_POINT('Ctrl Pts',(28.6775243943233,-0.763531646934146,
23.2135416666667));
#64301=CARTESIAN_POINT('Ctrl Pts',(29.1183495962155,-1.52706329386828,23.2552083333334));
#64302=CARTESIAN_POINT('Ctrl Pts',(30.,-1.52706329386828,23.296875));
#64303=CARTESIAN_POINT('Ctrl Pts',(30.8816504037844,-1.52706329386828,23.3385416666667));
#64304=CARTESIAN_POINT('Ctrl Pts',(31.3224756056766,-0.763531646934147,
23.3802083333334));
#64305=CARTESIAN_POINT('Ctrl Pts',(31.7633008075689,-1.36198038370242E-14,
23.421875));
#64306=CARTESIAN_POINT('Ctrl Pts',(31.3224756056766,0.763531646934118,23.4635416666667));
#64307=CARTESIAN_POINT('Ctrl Pts',(30.8816504037844,1.52706329386825,23.5052083333334));
#64308=CARTESIAN_POINT('Ctrl Pts',(30.,1.52706329386825,23.546875));
#64309=CARTESIAN_POINT('Ctrl Pts',(29.1183495962155,1.52706329386825,23.5885416666667));
#64310=CARTESIAN_POINT('Ctrl Pts',(28.6775243943233,0.76353164693412,23.6302083333334));
#64311=CARTESIAN_POINT('Ctrl Pts',(28.2366991924311,-1.31894491186926E-14,
23.671875));
#64312=CARTESIAN_POINT('Ctrl Pts',(28.6775243943233,-0.763531646934146,
23.7135416666667));
#64313=CARTESIAN_POINT('Ctrl Pts',(29.1183495962155,-1.52706329386828,23.7552083333334));
#64314=CARTESIAN_POINT('Ctrl Pts',(30.,-1.52706329386828,23.796875));
#64315=CARTESIAN_POINT('Ctrl Pts',(30.8816504037844,-1.52706329386828,23.8385416666667));
#64316=CARTESIAN_POINT('Ctrl Pts',(31.3224756056766,-0.763531646934147,
23.8802083333334));
#64317=CARTESIAN_POINT('Ctrl Pts',(31.7633008075689,-1.36198038370242E-14,
23.921875));
#64318=CARTESIAN_POINT('Ctrl Pts',(31.3224756056766,0.763531646934118,23.9635416666667));
#64319=CARTESIAN_POINT('Ctrl Pts',(30.8816504037844,1.52706329386825,24.0052083333334));
#64320=CARTESIAN_POINT('Ctrl Pts',(30.,1.52706329386825,24.046875));
#64321=CARTESIAN_POINT('Ctrl Pts',(29.1183495962155,1.52706329386825,24.0885416666667));
#64322=CARTESIAN_POINT('Ctrl Pts',(28.6775243943233,0.76353164693412,24.1302083333334));
#64323=CARTESIAN_POINT('Ctrl Pts',(28.2366991924311,-1.31894491186926E-14,
24.171875));
#64324=CARTESIAN_POINT('Ctrl Pts',(28.6775243943233,-0.763531646934146,
24.2135416666667));
#64325=CARTESIAN_POINT('Ctrl Pts',(29.1183495962155,-1.52706329386828,24.2552083333334));
#64326=CARTESIAN_POINT('Ctrl Pts',(30.,-1.52706329386828,24.296875));
#64327=CARTESIAN_POINT('Ctrl Pts',(30.8816504037844,-1.52706329386828,24.3385416666667));
#64328=CARTESIAN_POINT('Ctrl Pts',(31.3224756056766,-0.763531646934147,
24.3802083333334));
#64329=CARTESIAN_POINT('Ctrl Pts',(31.7633008075689,-1.36198038370242E-14,
24.421875));
#64330=CARTESIAN_POINT('Ctrl Pts',(31.3224756056766,0.763531646934118,24.4635416666667));
#64331=CARTESIAN_POINT('Ctrl Pts',(30.8816504037844,1.52706329386825,24.5052083333334));
#64332=CARTESIAN_POINT('Ctrl Pts',(30.,1.52706329386825,24.546875));
#64333=CARTESIAN_POINT('Ctrl Pts',(29.1183495962155,1.52706329386825,24.5885416666667));
#64334=CARTESIAN_POINT('Ctrl Pts',(28.6775243943233,0.76353164693412,24.6302083333334));
#64335=CARTESIAN_POINT('Ctrl Pts',(28.2366991924311,-1.31894491186926E-14,
24.671875));
#64336=CARTESIAN_POINT('Ctrl Pts',(28.6775243943233,-0.763531646934146,
24.7135416666667));
#64337=CARTESIAN_POINT('Ctrl Pts',(29.1183495962155,-1.52706329386828,24.7552083333334));
#64338=CARTESIAN_POINT('Ctrl Pts',(30.,-1.52706329386828,24.796875));
#64339=CARTESIAN_POINT('Ctrl Pts',(30.8816504037844,-1.52706329386828,24.8385416666667));
#64340=CARTESIAN_POINT('Ctrl Pts',(31.3224756056766,-0.763531646934147,
24.8802083333334));
#64341=CARTESIAN_POINT('Ctrl Pts',(31.7633008075689,-1.36198038370242E-14,
24.921875));
#64342=CARTESIAN_POINT('Ctrl Pts',(31.3224756056766,0.763531646934118,24.9635416666667));
#64343=CARTESIAN_POINT('Ctrl Pts',(30.8816504037844,1.52706329386825,25.0052083333334));
#64344=CARTESIAN_POINT('Ctrl Pts',(30.,1.52706329386825,25.046875));
#64345=CARTESIAN_POINT('Ctrl Pts',(29.1183495962155,1.52706329386825,25.0885416666667));
#64346=CARTESIAN_POINT('Ctrl Pts',(28.6775243943233,0.76353164693412,25.1302083333334));
#64347=CARTESIAN_POINT('Ctrl Pts',(28.2366991924311,-1.31894491186926E-14,
25.171875));
#64348=CARTESIAN_POINT('Ctrl Pts',(28.6775243943233,-0.763531646934146,
25.2135416666667));
#64349=CARTESIAN_POINT('Ctrl Pts',(29.1183495962155,-1.52706329386828,25.2552083333334));
#64350=CARTESIAN_POINT('Ctrl Pts',(30.,-1.52706329386828,25.296875));
#64351=CARTESIAN_POINT('Ctrl Pts',(30.8816504037844,-1.52706329386828,25.3385416666667));
#64352=CARTESIAN_POINT('Ctrl Pts',(31.3224756056766,-0.763531646934147,
25.3802083333334));
#64353=CARTESIAN_POINT('Ctrl Pts',(31.7633008075689,-1.36198038370242E-14,
25.421875));
#64354=CARTESIAN_POINT('Ctrl Pts',(31.3224756056766,0.763531646934118,25.4635416666667));
#64355=CARTESIAN_POINT('Ctrl Pts',(30.8816504037844,1.52706329386825,25.5052083333334));
#64356=CARTESIAN_POINT('Ctrl Pts',(30.,1.52706329386825,25.546875));
#64357=CARTESIAN_POINT('Ctrl Pts',(29.1183495962155,1.52706329386825,25.5885416666667));
#64358=CARTESIAN_POINT('Ctrl Pts',(28.6775243943233,0.76353164693412,25.6302083333334));
#64359=CARTESIAN_POINT('Ctrl Pts',(28.2366991924311,-1.31894491186926E-14,
25.671875));
#64360=CARTESIAN_POINT('Ctrl Pts',(28.6775243943233,-0.763531646934146,
25.7135416666667));
#64361=CARTESIAN_POINT('Ctrl Pts',(29.1183495962155,-1.52706329386828,25.7552083333334));
#64362=CARTESIAN_POINT('Ctrl Pts',(30.,-1.52706329386828,25.796875));
#64363=CARTESIAN_POINT('Ctrl Pts',(30.8816504037844,-1.52706329386828,25.8385416666667));
#64364=CARTESIAN_POINT('Ctrl Pts',(31.3224756056766,-0.763531646934147,
25.8802083333334));
#64365=CARTESIAN_POINT('Ctrl Pts',(31.7633008075689,-1.36198038370242E-14,
25.921875));
#64366=CARTESIAN_POINT('Ctrl Pts',(31.3224756056766,0.763531646934118,25.9635416666667));
#64367=CARTESIAN_POINT('Ctrl Pts',(30.8816504037844,1.52706329386825,26.0052083333334));
#64368=CARTESIAN_POINT('Ctrl Pts',(30.,1.52706329386825,26.046875));
#64369=CARTESIAN_POINT('Ctrl Pts',(29.1183495962155,1.52706329386825,26.0885416666667));
#64370=CARTESIAN_POINT('Ctrl Pts',(28.6775243943233,0.76353164693412,26.1302083333334));
#64371=CARTESIAN_POINT('Ctrl Pts',(28.2366991924311,-1.31894491186926E-14,
26.171875));
#64372=CARTESIAN_POINT('Ctrl Pts',(28.6775243943233,-0.763531646934146,
26.2135416666667));
#64373=CARTESIAN_POINT('Ctrl Pts',(29.1183495962155,-1.52706329386828,26.2552083333334));
#64374=CARTESIAN_POINT('Ctrl Pts',(30.,-1.52706329386828,26.296875));
#64375=CARTESIAN_POINT('Ctrl Pts',(30.8816504037844,-1.52706329386828,26.3385416666667));
#64376=CARTESIAN_POINT('Ctrl Pts',(31.3224756056766,-0.763531646934147,
26.3802083333334));
#64377=CARTESIAN_POINT('Ctrl Pts',(31.7633008075689,-1.36198038370242E-14,
26.421875));
#64378=CARTESIAN_POINT('Ctrl Pts',(31.3224756056766,0.763531646934118,26.4635416666667));
#64379=CARTESIAN_POINT('Ctrl Pts',(30.8816504037844,1.52706329386825,26.5052083333334));
#64380=CARTESIAN_POINT('Ctrl Pts',(30.,1.52706329386825,26.546875));
#64381=CARTESIAN_POINT('Ctrl Pts',(29.1183495962155,1.52706329386825,26.5885416666667));
#64382=CARTESIAN_POINT('Ctrl Pts',(28.6775243943233,0.76353164693412,26.6302083333334));
#64383=CARTESIAN_POINT('Ctrl Pts',(28.2366991924311,-1.31894491186926E-14,
26.671875));
#64384=CARTESIAN_POINT('Ctrl Pts',(28.6775243943233,-0.763531646934146,
26.7135416666667));
#64385=CARTESIAN_POINT('Ctrl Pts',(29.1183495962155,-1.52706329386828,26.7552083333334));
#64386=CARTESIAN_POINT('Ctrl Pts',(30.,-1.52706329386828,26.796875));
#64387=CARTESIAN_POINT('Ctrl Pts',(30.8816504037844,-1.52706329386828,26.8385416666667));
#64388=CARTESIAN_POINT('Ctrl Pts',(31.3224756056766,-0.763531646934147,
26.8802083333334));
#64389=CARTESIAN_POINT('Ctrl Pts',(31.7633008075689,-1.36198038370242E-14,
26.921875));
#64390=CARTESIAN_POINT('Ctrl Pts',(31.3224756056766,0.763531646934118,26.9635416666667));
#64391=CARTESIAN_POINT('Ctrl Pts',(30.8816504037844,1.52706329386825,27.0052083333334));
#64392=CARTESIAN_POINT('Ctrl Pts',(30.,1.52706329386825,27.046875));
#64393=CARTESIAN_POINT('Ctrl Pts',(29.1183495962155,1.52706329386825,27.0885416666667));
#64394=CARTESIAN_POINT('Ctrl Pts',(28.6775243943233,0.76353164693412,27.1302083333334));
#64395=CARTESIAN_POINT('Ctrl Pts',(28.2366991924311,-1.31894491186926E-14,
27.171875));
#64396=CARTESIAN_POINT('Ctrl Pts',(28.6775243943233,-0.763531646934146,
27.2135416666667));
#64397=CARTESIAN_POINT('Ctrl Pts',(29.1183495962155,-1.52706329386828,27.2552083333334));
#64398=CARTESIAN_POINT('Ctrl Pts',(30.,-1.52706329386828,27.296875));
#64399=CARTESIAN_POINT('Ctrl Pts',(30.8816504037844,-1.52706329386828,27.3385416666667));
#64400=CARTESIAN_POINT('Ctrl Pts',(31.3224756056766,-0.763531646934147,
27.3802083333334));
#64401=CARTESIAN_POINT('Ctrl Pts',(31.7633008075689,-1.36198038370242E-14,
27.421875));
#64402=CARTESIAN_POINT('Ctrl Pts',(31.3224756056766,0.763531646934118,27.4635416666667));
#64403=CARTESIAN_POINT('Ctrl Pts',(30.8816504037844,1.52706329386825,27.5052083333334));
#64404=CARTESIAN_POINT('Ctrl Pts',(30.,1.52706329386825,27.546875));
#64405=CARTESIAN_POINT('Ctrl Pts',(29.1183495962155,1.52706329386825,27.5885416666667));
#64406=CARTESIAN_POINT('Ctrl Pts',(28.6775243943233,0.76353164693412,27.6302083333334));
#64407=CARTESIAN_POINT('Ctrl Pts',(28.2366991924311,-1.31894491186926E-14,
27.671875));
#64408=CARTESIAN_POINT('Ctrl Pts',(28.6775243943233,-0.763531646934146,
27.7135416666667));
#64409=CARTESIAN_POINT('Ctrl Pts',(29.1183495962155,-1.52706329386828,27.7552083333334));
#64410=CARTESIAN_POINT('Ctrl Pts',(30.,-1.52706329386828,27.796875));
#64411=CARTESIAN_POINT('Ctrl Pts',(30.8816504037844,-1.52706329386828,27.8385416666667));
#64412=CARTESIAN_POINT('Ctrl Pts',(31.3224756056766,-0.763531646934147,
27.8802083333334));
#64413=CARTESIAN_POINT('Ctrl Pts',(31.7633008075689,-1.36198038370242E-14,
27.921875));
#64414=CARTESIAN_POINT('Ctrl Pts',(31.3224756056766,0.763531646934118,27.9635416666667));
#64415=CARTESIAN_POINT('Ctrl Pts',(30.8816504037844,1.52706329386825,28.0052083333334));
#64416=CARTESIAN_POINT('Ctrl Pts',(30.,1.52706329386825,28.046875));
#64417=CARTESIAN_POINT('Ctrl Pts',(29.1183495962155,1.52706329386825,28.0885416666667));
#64418=CARTESIAN_POINT('Ctrl Pts',(28.6775243943233,0.76353164693412,28.1302083333334));
#64419=CARTESIAN_POINT('Ctrl Pts',(28.2366991924311,-1.31894491186926E-14,
28.171875));
#64420=CARTESIAN_POINT('Ctrl Pts',(28.6775243943233,-0.763531646934146,
28.2135416666667));
#64421=CARTESIAN_POINT('Ctrl Pts',(29.1183495962155,-1.52706329386828,28.2552083333334));
#64422=CARTESIAN_POINT('Ctrl Pts',(30.,-1.52706329386828,28.296875));
#64423=CARTESIAN_POINT('Ctrl Pts',(30.8816504037844,-1.52706329386828,28.3385416666667));
#64424=CARTESIAN_POINT('Ctrl Pts',(31.3224756056766,-0.763531646934147,
28.3802083333334));
#64425=CARTESIAN_POINT('Ctrl Pts',(31.7633008075689,-1.36198038370242E-14,
28.421875));
#64426=CARTESIAN_POINT('Ctrl Pts',(31.3224756056766,0.763531646934118,28.4635416666667));
#64427=CARTESIAN_POINT('Ctrl Pts',(30.8816504037844,1.52706329386825,28.5052083333334));
#64428=CARTESIAN_POINT('Ctrl Pts',(30.,1.52706329386825,28.546875));
#64429=CARTESIAN_POINT('Ctrl Pts',(29.1183495962155,1.52706329386825,28.5885416666667));
#64430=CARTESIAN_POINT('Ctrl Pts',(28.6775243943233,0.76353164693412,28.6302083333334));
#64431=CARTESIAN_POINT('Ctrl Pts',(28.2366991924311,-1.31894491186926E-14,
28.671875));
#64432=CARTESIAN_POINT('Ctrl Pts',(28.6775243943233,-0.763531646934146,
28.7135416666667));
#64433=CARTESIAN_POINT('Ctrl Pts',(29.1183495962155,-1.52706329386828,28.7552083333334));
#64434=CARTESIAN_POINT('Ctrl Pts',(30.,-1.52706329386828,28.796875));
#64435=CARTESIAN_POINT('Ctrl Pts',(30.8816504037844,-1.52706329386828,28.8385416666667));
#64436=CARTESIAN_POINT('Ctrl Pts',(31.3224756056766,-0.763531646934147,
28.8802083333334));
#64437=CARTESIAN_POINT('Ctrl Pts',(31.7633008075689,-1.36198038370242E-14,
28.921875));
#64438=CARTESIAN_POINT('Ctrl Pts',(31.3224756056766,0.763531646934118,28.9635416666667));
#64439=CARTESIAN_POINT('Ctrl Pts',(30.8816504037844,1.52706329386825,29.0052083333334));
#64440=CARTESIAN_POINT('Ctrl Pts',(30.,1.52706329386825,29.046875));
#64441=CARTESIAN_POINT('Ctrl Pts',(29.1183495962155,1.52706329386825,29.0885416666667));
#64442=CARTESIAN_POINT('Ctrl Pts',(28.6775243943233,0.76353164693412,29.1302083333334));
#64443=CARTESIAN_POINT('Ctrl Pts',(28.2366991924311,-1.31894491186926E-14,
29.171875));
#64444=CARTESIAN_POINT('Ctrl Pts',(28.6775243943233,-0.763531646934146,
29.2135416666667));
#64445=CARTESIAN_POINT('Ctrl Pts',(29.1183495962155,-1.52706329386828,29.2552083333334));
#64446=CARTESIAN_POINT('Ctrl Pts',(30.,-1.52706329386828,29.296875));
#64447=CARTESIAN_POINT('Ctrl Pts',(30.8816504037844,-1.52706329386828,29.3385416666667));
#64448=CARTESIAN_POINT('Ctrl Pts',(31.3224756056766,-0.763531646934147,
29.3802083333334));
#64449=CARTESIAN_POINT('Ctrl Pts',(31.7633008075689,-1.36198038370242E-14,
29.421875));
#64450=CARTESIAN_POINT('Ctrl Pts',(31.3224756056766,0.763531646934118,29.4635416666667));
#64451=CARTESIAN_POINT('Ctrl Pts',(30.8816504037844,1.52706329386825,29.5052083333334));
#64452=CARTESIAN_POINT('Ctrl Pts',(30.,1.52706329386825,29.546875));
#64453=CARTESIAN_POINT('Ctrl Pts',(29.1183495962155,1.52706329386825,29.5885416666667));
#64454=CARTESIAN_POINT('Ctrl Pts',(28.6775243943233,0.76353164693412,29.6302083333334));
#64455=CARTESIAN_POINT('Ctrl Pts',(28.2366991924311,-1.31894491186926E-14,
29.671875));
#64456=CARTESIAN_POINT('Ctrl Pts',(28.6775243943233,-0.763531646934146,
29.7135416666667));
#64457=CARTESIAN_POINT('Ctrl Pts',(29.1183495962155,-1.52706329386828,29.7552083333334));
#64458=CARTESIAN_POINT('Ctrl Pts',(30.,-1.52706329386828,29.796875));
#64459=CARTESIAN_POINT('Ctrl Pts',(30.8816504037844,-1.52706329386828,29.8385416666667));
#64460=CARTESIAN_POINT('Ctrl Pts',(31.3224756056766,-0.763531646934147,
29.8802083333334));
#64461=CARTESIAN_POINT('Ctrl Pts',(31.7633008075689,-1.36198038370242E-14,
29.921875));
#64462=CARTESIAN_POINT('Ctrl Pts',(31.3224756056766,0.763531646934118,29.9635416666667));
#64463=CARTESIAN_POINT('Ctrl Pts',(30.8816504037844,1.52706329386825,30.0052083333334));
#64464=CARTESIAN_POINT('Ctrl Pts',(30.,1.52706329386825,30.046875));
#64465=CARTESIAN_POINT('Ctrl Pts',(29.1183495962155,1.52706329386825,30.0885416666667));
#64466=CARTESIAN_POINT('Ctrl Pts',(28.6775243943233,0.76353164693412,30.1302083333334));
#64467=CARTESIAN_POINT('Ctrl Pts',(28.2366991924311,-1.31894491186926E-14,
30.171875));
#64468=CARTESIAN_POINT('Ctrl Pts',(28.6775243943233,-0.763531646934146,
30.2135416666667));
#64469=CARTESIAN_POINT('Ctrl Pts',(29.1183495962155,-1.52706329386828,30.2552083333334));
#64470=CARTESIAN_POINT('Ctrl Pts',(30.,-1.52706329386828,30.296875));
#64471=CARTESIAN_POINT('Ctrl Pts',(30.8816504037844,-1.52706329386828,30.3385416666667));
#64472=CARTESIAN_POINT('Ctrl Pts',(31.3224756056766,-0.763531646934147,
30.3802083333334));
#64473=CARTESIAN_POINT('Ctrl Pts',(31.7633008075689,-1.36198038370242E-14,
30.421875));
#64474=CARTESIAN_POINT('Ctrl Pts',(31.3224756056766,0.763531646934118,30.4635416666667));
#64475=CARTESIAN_POINT('Ctrl Pts',(30.8816504037844,1.52706329386825,30.5052083333334));
#64476=CARTESIAN_POINT('Ctrl Pts',(30.,1.52706329386825,30.546875));
#64477=CARTESIAN_POINT('Ctrl Pts',(29.1183495962155,1.52706329386825,30.5885416666667));
#64478=CARTESIAN_POINT('Ctrl Pts',(28.6775243943233,0.76353164693412,30.6302083333334));
#64479=CARTESIAN_POINT('Ctrl Pts',(28.2366991924311,-1.31894491186926E-14,
30.671875));
#64480=CARTESIAN_POINT('Ctrl Pts',(28.6775243943233,-0.763531646934146,
30.7135416666667));
#64481=CARTESIAN_POINT('Ctrl Pts',(29.1183495962155,-1.52706329386828,30.7552083333334));
#64482=CARTESIAN_POINT('Ctrl Pts',(30.,-1.52706329386828,30.796875));
#64483=CARTESIAN_POINT('Ctrl Pts',(30.8816504037844,-1.52706329386828,30.8385416666667));
#64484=CARTESIAN_POINT('Ctrl Pts',(31.3224756056766,-0.763531646934147,
30.8802083333334));
#64485=CARTESIAN_POINT('Ctrl Pts',(31.7633008075689,-1.36198038370242E-14,
30.921875));
#64486=CARTESIAN_POINT('Ctrl Pts',(31.3224756056766,0.763531646934118,30.9635416666667));
#64487=CARTESIAN_POINT('Ctrl Pts',(30.8816504037844,1.52706329386825,31.0052083333334));
#64488=CARTESIAN_POINT('Ctrl Pts',(30.,1.52706329386825,31.046875));
#64489=CARTESIAN_POINT('Ctrl Pts',(30.8234003400376,-0.838570603170131,
30.5624996575278));
#64490=CARTESIAN_POINT('Ctrl Pts',(30.9252409219315,-0.749808119816165,
30.5671289662449));
#64491=CARTESIAN_POINT('Ctrl Pts',(31.0094069192668,-0.645130506686946,
30.571193014068));
#64492=CARTESIAN_POINT('Ctrl Pts',(31.1396529784097,-0.412074319923831,
30.5795221820465));
#64493=CARTESIAN_POINT('Ctrl Pts',(31.1849584507844,-0.287685440765051,
30.5838904393726));
#64494=CARTESIAN_POINT('Ctrl Pts',(31.2386945750578,-0.00655181811616603,
30.5935664195233));
#64495=CARTESIAN_POINT('Ctrl Pts',(31.2387490550162,0.149503133824081,30.5988162542928));
#64496=CARTESIAN_POINT('Ctrl Pts',(31.1719223736106,0.500568259068406,30.610386374166));
#64497=CARTESIAN_POINT('Ctrl Pts',(31.0923154827319,0.652496494934345,30.6150433766711));
#64498=CARTESIAN_POINT('Ctrl Pts',(30.9283336729762,0.900293879400657,30.6239504439807));
#64499=CARTESIAN_POINT('Ctrl Pts',(30.8055598520391,1.02369588322745,30.6294622341334));
#64500=CARTESIAN_POINT('Ctrl Pts',(30.5288337282237,1.20882504193349,30.6401101417162));
#64501=CARTESIAN_POINT('Ctrl Pts',(30.3799906896905,1.27260041719159,30.6451552807199));
#64502=CARTESIAN_POINT('Ctrl Pts',(30.0014927028803,1.35728019461807,30.6565651904367));
#64503=CARTESIAN_POINT('Ctrl Pts',(29.8132785668206,1.33887636851719,30.6613880776071));
#64504=CARTESIAN_POINT('Ctrl Pts',(29.5198061598154,1.28660005614596,30.6701589170659));
#64505=CARTESIAN_POINT('Ctrl Pts',(29.3521505621284,1.22147978200258,30.6756096035631));
#64506=CARTESIAN_POINT('Ctrl Pts',(29.0485837866741,1.02916361274227,30.6863949411503));
#64507=CARTESIAN_POINT('Ctrl Pts',(28.9162494293832,0.902843317652004,30.6916208752244));
#64508=CARTESIAN_POINT('Ctrl Pts',(28.7272437086822,0.633185410868888,30.7002552651022));
#64509=CARTESIAN_POINT('Ctrl Pts',(28.6461891944724,0.476094037694283,30.7048351996635));
#64510=CARTESIAN_POINT('Ctrl Pts',(28.551105022901,0.105569064666544,30.715730913862));
#64511=CARTESIAN_POINT('Ctrl Pts',(28.5402826505383,-0.0831493783931786,
30.7211721595761));
#64512=CARTESIAN_POINT('Ctrl Pts',(28.5859138822382,-0.415083694084825,
30.7305650693331));
#64513=CARTESIAN_POINT('Ctrl Pts',(28.6283908398168,-0.557537406078615,
30.7345346397522));
#64514=CARTESIAN_POINT('Ctrl Pts',(28.7447696187018,-0.802908073480822,
30.7412906353098));
#64515=CARTESIAN_POINT('Ctrl Pts',(28.8264704242263,-0.938163811130005,
30.7451577422722));
#64516=CARTESIAN_POINT('Ctrl Pts',(28.9490560961683,-1.07028823734174,30.7500000000014));
#64517=CARTESIAN_POINT('Ctrl Pts',(30.,1.52706329386825,16.015625));
#64518=CARTESIAN_POINT('Ctrl Pts',(29.1183495962155,1.52706329386825,16.0572916666666));
#64519=CARTESIAN_POINT('Ctrl Pts',(28.6775243943233,0.76353164693412,16.0989583333333));
#64520=CARTESIAN_POINT('Ctrl Pts',(28.2366991924311,-1.31894491186926E-14,
16.140625));
#64521=CARTESIAN_POINT('Ctrl Pts',(28.6775243943233,-0.763531646934146,
16.1822916666666));
#64522=CARTESIAN_POINT('Ctrl Pts',(29.1183495962155,-1.52706329386828,16.2239583333333));
#64523=CARTESIAN_POINT('Ctrl Pts',(30.,-1.52706329386828,16.265625));
#64524=CARTESIAN_POINT('Ctrl Pts',(30.8816504037844,-1.52706329386828,16.3072916666666));
#64525=CARTESIAN_POINT('Ctrl Pts',(31.3224756056766,-0.763531646934147,
16.3489583333333));
#64526=CARTESIAN_POINT('Ctrl Pts',(31.7633008075689,-1.36198038370242E-14,
16.390625));
#64527=CARTESIAN_POINT('Ctrl Pts',(31.3224756056766,0.763531646934118,16.4322916666666));
#64528=CARTESIAN_POINT('Ctrl Pts',(30.8816504037844,1.52706329386825,16.4739583333333));
#64529=CARTESIAN_POINT('Ctrl Pts',(30.,1.52706329386825,16.515625));
#64530=CARTESIAN_POINT('Ctrl Pts',(29.1183495962155,1.52706329386825,16.5572916666666));
#64531=CARTESIAN_POINT('Ctrl Pts',(28.6775243943233,0.76353164693412,16.5989583333333));
#64532=CARTESIAN_POINT('Ctrl Pts',(28.2366991924311,-1.31894491186926E-14,
16.640625));
#64533=CARTESIAN_POINT('Ctrl Pts',(28.6775243943233,-0.763531646934146,
16.6822916666666));
#64534=CARTESIAN_POINT('Ctrl Pts',(29.1183495962155,-1.52706329386828,16.7239583333333));
#64535=CARTESIAN_POINT('Ctrl Pts',(30.,-1.52706329386828,16.765625));
#64536=CARTESIAN_POINT('Ctrl Pts',(30.8816504037844,-1.52706329386828,16.8072916666666));
#64537=CARTESIAN_POINT('Ctrl Pts',(31.3224756056766,-0.763531646934147,
16.8489583333333));
#64538=CARTESIAN_POINT('Ctrl Pts',(31.7633008075689,-1.36198038370242E-14,
16.890625));
#64539=CARTESIAN_POINT('Ctrl Pts',(31.3224756056766,0.763531646934118,16.9322916666666));
#64540=CARTESIAN_POINT('Ctrl Pts',(30.8816504037844,1.52706329386825,16.9739583333333));
#64541=CARTESIAN_POINT('Ctrl Pts',(30.,1.52706329386825,17.015625));
#64542=CARTESIAN_POINT('Ctrl Pts',(29.1183495962155,1.52706329386825,17.0572916666666));
#64543=CARTESIAN_POINT('Ctrl Pts',(28.6775243943233,0.76353164693412,17.0989583333333));
#64544=CARTESIAN_POINT('Ctrl Pts',(28.2366991924311,-1.31894491186926E-14,
17.140625));
#64545=CARTESIAN_POINT('Ctrl Pts',(28.6775243943233,-0.763531646934146,
17.1822916666666));
#64546=CARTESIAN_POINT('Ctrl Pts',(29.1183495962155,-1.52706329386828,17.2239583333333));
#64547=CARTESIAN_POINT('Ctrl Pts',(30.,-1.52706329386828,17.265625));
#64548=CARTESIAN_POINT('Ctrl Pts',(30.8816504037844,-1.52706329386828,17.3072916666666));
#64549=CARTESIAN_POINT('Ctrl Pts',(31.3224756056766,-0.763531646934147,
17.3489583333333));
#64550=CARTESIAN_POINT('Ctrl Pts',(31.7633008075689,-1.36198038370242E-14,
17.390625));
#64551=CARTESIAN_POINT('Ctrl Pts',(31.3224756056766,0.763531646934118,17.4322916666666));
#64552=CARTESIAN_POINT('Ctrl Pts',(30.8816504037844,1.52706329386825,17.4739583333333));
#64553=CARTESIAN_POINT('Ctrl Pts',(30.,1.52706329386825,17.515625));
#64554=CARTESIAN_POINT('Ctrl Pts',(29.1183495962155,1.52706329386825,17.5572916666666));
#64555=CARTESIAN_POINT('Ctrl Pts',(28.6775243943233,0.76353164693412,17.5989583333333));
#64556=CARTESIAN_POINT('Ctrl Pts',(28.2366991924311,-1.31894491186926E-14,
17.640625));
#64557=CARTESIAN_POINT('Ctrl Pts',(28.6775243943233,-0.763531646934146,
17.6822916666666));
#64558=CARTESIAN_POINT('Ctrl Pts',(29.1183495962155,-1.52706329386828,17.7239583333333));
#64559=CARTESIAN_POINT('Ctrl Pts',(30.,-1.52706329386828,17.765625));
#64560=CARTESIAN_POINT('Ctrl Pts',(30.8816504037844,-1.52706329386828,17.8072916666666));
#64561=CARTESIAN_POINT('Ctrl Pts',(31.3224756056766,-0.763531646934147,
17.8489583333333));
#64562=CARTESIAN_POINT('Ctrl Pts',(31.7633008075689,-1.36198038370242E-14,
17.890625));
#64563=CARTESIAN_POINT('Ctrl Pts',(31.3224756056766,0.763531646934118,17.9322916666666));
#64564=CARTESIAN_POINT('Ctrl Pts',(30.8816504037844,1.52706329386825,17.9739583333333));
#64565=CARTESIAN_POINT('Ctrl Pts',(30.,1.52706329386825,18.015625));
#64566=CARTESIAN_POINT('Ctrl Pts',(29.1183495962155,1.52706329386825,18.0572916666666));
#64567=CARTESIAN_POINT('Ctrl Pts',(28.6775243943233,0.76353164693412,18.0989583333333));
#64568=CARTESIAN_POINT('Ctrl Pts',(28.2366991924311,-1.31894491186926E-14,
18.140625));
#64569=CARTESIAN_POINT('Ctrl Pts',(28.6775243943233,-0.763531646934146,
18.1822916666666));
#64570=CARTESIAN_POINT('Ctrl Pts',(29.1183495962155,-1.52706329386828,18.2239583333333));
#64571=CARTESIAN_POINT('Ctrl Pts',(30.,-1.52706329386828,18.265625));
#64572=CARTESIAN_POINT('Ctrl Pts',(30.8816504037844,-1.52706329386828,18.3072916666666));
#64573=CARTESIAN_POINT('Ctrl Pts',(31.3224756056766,-0.763531646934147,
18.3489583333333));
#64574=CARTESIAN_POINT('Ctrl Pts',(31.7633008075689,-1.36198038370242E-14,
18.390625));
#64575=CARTESIAN_POINT('Ctrl Pts',(31.3224756056766,0.763531646934118,18.4322916666666));
#64576=CARTESIAN_POINT('Ctrl Pts',(30.8816504037844,1.52706329386825,18.4739583333333));
#64577=CARTESIAN_POINT('Ctrl Pts',(30.,1.52706329386825,18.515625));
#64578=CARTESIAN_POINT('Ctrl Pts',(29.1183495962155,1.52706329386825,18.5572916666666));
#64579=CARTESIAN_POINT('Ctrl Pts',(28.6775243943233,0.76353164693412,18.5989583333333));
#64580=CARTESIAN_POINT('Ctrl Pts',(28.2366991924311,-1.31894491186926E-14,
18.640625));
#64581=CARTESIAN_POINT('Ctrl Pts',(28.6775243943233,-0.763531646934146,
18.6822916666666));
#64582=CARTESIAN_POINT('Ctrl Pts',(29.1183495962155,-1.52706329386828,18.7239583333333));
#64583=CARTESIAN_POINT('Ctrl Pts',(30.,-1.52706329386828,18.765625));
#64584=CARTESIAN_POINT('Ctrl Pts',(30.8816504037844,-1.52706329386828,18.8072916666666));
#64585=CARTESIAN_POINT('Ctrl Pts',(31.3224756056766,-0.763531646934147,
18.8489583333333));
#64586=CARTESIAN_POINT('Ctrl Pts',(31.7633008075689,-1.36198038370242E-14,
18.890625));
#64587=CARTESIAN_POINT('Ctrl Pts',(31.3224756056766,0.763531646934118,18.9322916666666));
#64588=CARTESIAN_POINT('Ctrl Pts',(30.8816504037844,1.52706329386825,18.9739583333333));
#64589=CARTESIAN_POINT('Ctrl Pts',(30.,1.52706329386825,19.015625));
#64590=CARTESIAN_POINT('Ctrl Pts',(29.1183495962155,1.52706329386825,19.0572916666666));
#64591=CARTESIAN_POINT('Ctrl Pts',(28.6775243943233,0.76353164693412,19.0989583333333));
#64592=CARTESIAN_POINT('Ctrl Pts',(28.2366991924311,-1.31894491186926E-14,
19.140625));
#64593=CARTESIAN_POINT('Ctrl Pts',(28.6775243943233,-0.763531646934146,
19.1822916666666));
#64594=CARTESIAN_POINT('Ctrl Pts',(29.1183495962155,-1.52706329386828,19.2239583333333));
#64595=CARTESIAN_POINT('Ctrl Pts',(30.,-1.52706329386828,19.265625));
#64596=CARTESIAN_POINT('Ctrl Pts',(30.8816504037844,-1.52706329386828,19.3072916666666));
#64597=CARTESIAN_POINT('Ctrl Pts',(31.3224756056766,-0.763531646934147,
19.3489583333333));
#64598=CARTESIAN_POINT('Ctrl Pts',(31.7633008075689,-1.36198038370242E-14,
19.390625));
#64599=CARTESIAN_POINT('Ctrl Pts',(31.3224756056766,0.763531646934118,19.4322916666666));
#64600=CARTESIAN_POINT('Ctrl Pts',(30.8816504037844,1.52706329386825,19.4739583333333));
#64601=CARTESIAN_POINT('Ctrl Pts',(30.,1.52706329386825,19.515625));
#64602=CARTESIAN_POINT('Ctrl Pts',(29.1183495962155,1.52706329386825,19.5572916666666));
#64603=CARTESIAN_POINT('Ctrl Pts',(28.6775243943233,0.76353164693412,19.5989583333333));
#64604=CARTESIAN_POINT('Ctrl Pts',(28.2366991924311,-1.31894491186926E-14,
19.640625));
#64605=CARTESIAN_POINT('Ctrl Pts',(28.6775243943233,-0.763531646934146,
19.6822916666666));
#64606=CARTESIAN_POINT('Ctrl Pts',(29.1183495962155,-1.52706329386828,19.7239583333333));
#64607=CARTESIAN_POINT('Ctrl Pts',(30.,-1.52706329386828,19.765625));
#64608=CARTESIAN_POINT('Ctrl Pts',(30.8816504037844,-1.52706329386828,19.8072916666666));
#64609=CARTESIAN_POINT('Ctrl Pts',(31.3224756056766,-0.763531646934147,
19.8489583333333));
#64610=CARTESIAN_POINT('Ctrl Pts',(31.7633008075689,-1.36198038370242E-14,
19.890625));
#64611=CARTESIAN_POINT('Ctrl Pts',(31.3224756056766,0.763531646934118,19.9322916666666));
#64612=CARTESIAN_POINT('Ctrl Pts',(30.8816504037844,1.52706329386825,19.9739583333333));
#64613=CARTESIAN_POINT('Ctrl Pts',(30.,1.52706329386825,20.015625));
#64614=CARTESIAN_POINT('Ctrl Pts',(29.1183495962155,1.52706329386825,20.0572916666666));
#64615=CARTESIAN_POINT('Ctrl Pts',(28.6775243943233,0.76353164693412,20.0989583333333));
#64616=CARTESIAN_POINT('Ctrl Pts',(28.2366991924311,-1.31894491186926E-14,
20.140625));
#64617=CARTESIAN_POINT('Ctrl Pts',(28.6775243943233,-0.763531646934146,
20.1822916666666));
#64618=CARTESIAN_POINT('Ctrl Pts',(29.1183495962155,-1.52706329386828,20.2239583333333));
#64619=CARTESIAN_POINT('Ctrl Pts',(30.,-1.52706329386828,20.265625));
#64620=CARTESIAN_POINT('Ctrl Pts',(30.8816504037844,-1.52706329386828,20.3072916666666));
#64621=CARTESIAN_POINT('Ctrl Pts',(31.3224756056766,-0.763531646934147,
20.3489583333333));
#64622=CARTESIAN_POINT('Ctrl Pts',(31.7633008075689,-1.36198038370242E-14,
20.390625));
#64623=CARTESIAN_POINT('Ctrl Pts',(31.3224756056766,0.763531646934118,20.4322916666666));
#64624=CARTESIAN_POINT('Ctrl Pts',(30.8816504037844,1.52706329386825,20.4739583333333));
#64625=CARTESIAN_POINT('Ctrl Pts',(30.,1.52706329386825,20.515625));
#64626=CARTESIAN_POINT('Ctrl Pts',(29.1183495962155,1.52706329386825,20.5572916666666));
#64627=CARTESIAN_POINT('Ctrl Pts',(28.6775243943233,0.76353164693412,20.5989583333333));
#64628=CARTESIAN_POINT('Ctrl Pts',(28.2366991924311,-1.31894491186926E-14,
20.640625));
#64629=CARTESIAN_POINT('Ctrl Pts',(28.6775243943233,-0.763531646934146,
20.6822916666666));
#64630=CARTESIAN_POINT('Ctrl Pts',(29.1183495962155,-1.52706329386828,20.7239583333333));
#64631=CARTESIAN_POINT('Ctrl Pts',(30.,-1.52706329386828,20.765625));
#64632=CARTESIAN_POINT('Ctrl Pts',(30.8816504037844,-1.52706329386828,20.8072916666666));
#64633=CARTESIAN_POINT('Ctrl Pts',(31.3224756056766,-0.763531646934147,
20.8489583333333));
#64634=CARTESIAN_POINT('Ctrl Pts',(31.7633008075689,-1.36198038370242E-14,
20.890625));
#64635=CARTESIAN_POINT('Ctrl Pts',(31.3224756056766,0.763531646934118,20.9322916666666));
#64636=CARTESIAN_POINT('Ctrl Pts',(30.8816504037844,1.52706329386825,20.9739583333333));
#64637=CARTESIAN_POINT('Ctrl Pts',(30.,1.52706329386825,21.015625));
#64638=CARTESIAN_POINT('Ctrl Pts',(29.1183495962155,1.52706329386825,21.0572916666666));
#64639=CARTESIAN_POINT('Ctrl Pts',(28.6775243943233,0.76353164693412,21.0989583333333));
#64640=CARTESIAN_POINT('Ctrl Pts',(28.2366991924311,-1.31894491186926E-14,
21.140625));
#64641=CARTESIAN_POINT('Ctrl Pts',(28.6775243943233,-0.763531646934146,
21.1822916666666));
#64642=CARTESIAN_POINT('Ctrl Pts',(29.1183495962155,-1.52706329386828,21.2239583333333));
#64643=CARTESIAN_POINT('Ctrl Pts',(30.,-1.52706329386828,21.265625));
#64644=CARTESIAN_POINT('Ctrl Pts',(30.8816504037844,-1.52706329386828,21.3072916666666));
#64645=CARTESIAN_POINT('Ctrl Pts',(31.3224756056766,-0.763531646934147,
21.3489583333333));
#64646=CARTESIAN_POINT('Ctrl Pts',(31.7633008075689,-1.36198038370242E-14,
21.390625));
#64647=CARTESIAN_POINT('Ctrl Pts',(31.3224756056766,0.763531646934118,21.4322916666666));
#64648=CARTESIAN_POINT('Ctrl Pts',(30.8816504037844,1.52706329386825,21.4739583333333));
#64649=CARTESIAN_POINT('Ctrl Pts',(30.,1.52706329386825,21.515625));
#64650=CARTESIAN_POINT('Ctrl Pts',(29.1183495962155,1.52706329386825,21.5572916666666));
#64651=CARTESIAN_POINT('Ctrl Pts',(28.6775243943233,0.76353164693412,21.5989583333333));
#64652=CARTESIAN_POINT('Ctrl Pts',(28.2366991924311,-1.31894491186926E-14,
21.640625));
#64653=CARTESIAN_POINT('Ctrl Pts',(28.6775243943233,-0.763531646934146,
21.6822916666666));
#64654=CARTESIAN_POINT('Ctrl Pts',(29.1183495962155,-1.52706329386828,21.7239583333333));
#64655=CARTESIAN_POINT('Ctrl Pts',(30.,-1.52706329386828,21.765625));
#64656=CARTESIAN_POINT('Ctrl Pts',(30.8816504037844,-1.52706329386828,21.8072916666666));
#64657=CARTESIAN_POINT('Ctrl Pts',(31.3224756056766,-0.763531646934147,
21.8489583333333));
#64658=CARTESIAN_POINT('Ctrl Pts',(31.7633008075689,-1.36198038370242E-14,
21.890625));
#64659=CARTESIAN_POINT('Ctrl Pts',(31.3224756056766,0.763531646934118,21.9322916666666));
#64660=CARTESIAN_POINT('Ctrl Pts',(30.8816504037844,1.52706329386825,21.9739583333333));
#64661=CARTESIAN_POINT('Ctrl Pts',(30.,1.52706329386825,22.015625));
#64662=CARTESIAN_POINT('Ctrl Pts',(29.1183495962155,1.52706329386825,22.0572916666666));
#64663=CARTESIAN_POINT('Ctrl Pts',(28.6775243943233,0.76353164693412,22.0989583333333));
#64664=CARTESIAN_POINT('Ctrl Pts',(28.2366991924311,-1.31894491186926E-14,
22.140625));
#64665=CARTESIAN_POINT('Ctrl Pts',(28.6775243943233,-0.763531646934146,
22.1822916666666));
#64666=CARTESIAN_POINT('Ctrl Pts',(29.1183495962155,-1.52706329386828,22.2239583333333));
#64667=CARTESIAN_POINT('Ctrl Pts',(30.,-1.52706329386828,22.265625));
#64668=CARTESIAN_POINT('Ctrl Pts',(30.8816504037844,-1.52706329386828,22.3072916666666));
#64669=CARTESIAN_POINT('Ctrl Pts',(31.3224756056766,-0.763531646934147,
22.3489583333333));
#64670=CARTESIAN_POINT('Ctrl Pts',(31.7633008075689,-1.36198038370242E-14,
22.390625));
#64671=CARTESIAN_POINT('Ctrl Pts',(31.3224756056766,0.763531646934118,22.4322916666666));
#64672=CARTESIAN_POINT('Ctrl Pts',(30.8816504037844,1.52706329386825,22.4739583333333));
#64673=CARTESIAN_POINT('Ctrl Pts',(30.,1.52706329386825,22.515625));
#64674=CARTESIAN_POINT('Ctrl Pts',(29.1183495962155,1.52706329386825,22.5572916666666));
#64675=CARTESIAN_POINT('Ctrl Pts',(28.6775243943233,0.76353164693412,22.5989583333333));
#64676=CARTESIAN_POINT('Ctrl Pts',(28.2366991924311,-1.31894491186926E-14,
22.640625));
#64677=CARTESIAN_POINT('Ctrl Pts',(28.6775243943233,-0.763531646934146,
22.6822916666666));
#64678=CARTESIAN_POINT('Ctrl Pts',(29.1183495962155,-1.52706329386828,22.7239583333333));
#64679=CARTESIAN_POINT('Ctrl Pts',(30.,-1.52706329386828,22.765625));
#64680=CARTESIAN_POINT('Ctrl Pts',(30.8816504037844,-1.52706329386828,22.8072916666666));
#64681=CARTESIAN_POINT('Ctrl Pts',(31.3224756056766,-0.763531646934147,
22.8489583333333));
#64682=CARTESIAN_POINT('Ctrl Pts',(31.7633008075689,-1.36198038370242E-14,
22.890625));
#64683=CARTESIAN_POINT('Ctrl Pts',(31.3224756056766,0.763531646934118,22.9322916666666));
#64684=CARTESIAN_POINT('Ctrl Pts',(30.8816504037844,1.52706329386825,22.9739583333333));
#64685=CARTESIAN_POINT('Ctrl Pts',(30.,1.52706329386825,23.015625));
#64686=CARTESIAN_POINT('Ctrl Pts',(29.1183495962155,1.52706329386825,23.0572916666666));
#64687=CARTESIAN_POINT('Ctrl Pts',(28.6775243943233,0.76353164693412,23.0989583333333));
#64688=CARTESIAN_POINT('Ctrl Pts',(28.2366991924311,-1.31894491186926E-14,
23.140625));
#64689=CARTESIAN_POINT('Ctrl Pts',(28.6775243943233,-0.763531646934146,
23.1822916666666));
#64690=CARTESIAN_POINT('Ctrl Pts',(29.1183495962155,-1.52706329386828,23.2239583333333));
#64691=CARTESIAN_POINT('Ctrl Pts',(30.,-1.52706329386828,23.265625));
#64692=CARTESIAN_POINT('Ctrl Pts',(30.8816504037844,-1.52706329386828,23.3072916666666));
#64693=CARTESIAN_POINT('Ctrl Pts',(31.3224756056766,-0.763531646934147,
23.3489583333333));
#64694=CARTESIAN_POINT('Ctrl Pts',(31.7633008075689,-1.36198038370242E-14,
23.390625));
#64695=CARTESIAN_POINT('Ctrl Pts',(31.3224756056766,0.763531646934118,23.4322916666666));
#64696=CARTESIAN_POINT('Ctrl Pts',(30.8816504037844,1.52706329386825,23.4739583333333));
#64697=CARTESIAN_POINT('Ctrl Pts',(30.,1.52706329386825,23.515625));
#64698=CARTESIAN_POINT('Ctrl Pts',(29.1183495962155,1.52706329386825,23.5572916666666));
#64699=CARTESIAN_POINT('Ctrl Pts',(28.6775243943233,0.76353164693412,23.5989583333333));
#64700=CARTESIAN_POINT('Ctrl Pts',(28.2366991924311,-1.31894491186926E-14,
23.640625));
#64701=CARTESIAN_POINT('Ctrl Pts',(28.6775243943233,-0.763531646934146,
23.6822916666666));
#64702=CARTESIAN_POINT('Ctrl Pts',(29.1183495962155,-1.52706329386828,23.7239583333333));
#64703=CARTESIAN_POINT('Ctrl Pts',(30.,-1.52706329386828,23.765625));
#64704=CARTESIAN_POINT('Ctrl Pts',(30.8816504037844,-1.52706329386828,23.8072916666666));
#64705=CARTESIAN_POINT('Ctrl Pts',(31.3224756056766,-0.763531646934147,
23.8489583333333));
#64706=CARTESIAN_POINT('Ctrl Pts',(31.7633008075689,-1.36198038370242E-14,
23.890625));
#64707=CARTESIAN_POINT('Ctrl Pts',(31.3224756056766,0.763531646934118,23.9322916666666));
#64708=CARTESIAN_POINT('Ctrl Pts',(30.8816504037844,1.52706329386825,23.9739583333333));
#64709=CARTESIAN_POINT('Ctrl Pts',(30.,1.52706329386825,24.015625));
#64710=CARTESIAN_POINT('Ctrl Pts',(29.1183495962155,1.52706329386825,24.0572916666666));
#64711=CARTESIAN_POINT('Ctrl Pts',(28.6775243943233,0.76353164693412,24.0989583333333));
#64712=CARTESIAN_POINT('Ctrl Pts',(28.2366991924311,-1.31894491186926E-14,
24.140625));
#64713=CARTESIAN_POINT('Ctrl Pts',(28.6775243943233,-0.763531646934146,
24.1822916666666));
#64714=CARTESIAN_POINT('Ctrl Pts',(29.1183495962155,-1.52706329386828,24.2239583333333));
#64715=CARTESIAN_POINT('Ctrl Pts',(30.,-1.52706329386828,24.265625));
#64716=CARTESIAN_POINT('Ctrl Pts',(30.8816504037844,-1.52706329386828,24.3072916666666));
#64717=CARTESIAN_POINT('Ctrl Pts',(31.3224756056766,-0.763531646934147,
24.3489583333333));
#64718=CARTESIAN_POINT('Ctrl Pts',(31.7633008075689,-1.36198038370242E-14,
24.390625));
#64719=CARTESIAN_POINT('Ctrl Pts',(31.3224756056766,0.763531646934118,24.4322916666666));
#64720=CARTESIAN_POINT('Ctrl Pts',(30.8816504037844,1.52706329386825,24.4739583333333));
#64721=CARTESIAN_POINT('Ctrl Pts',(30.,1.52706329386825,24.515625));
#64722=CARTESIAN_POINT('Ctrl Pts',(29.1183495962155,1.52706329386825,24.5572916666666));
#64723=CARTESIAN_POINT('Ctrl Pts',(28.6775243943233,0.76353164693412,24.5989583333333));
#64724=CARTESIAN_POINT('Ctrl Pts',(28.2366991924311,-1.31894491186926E-14,
24.640625));
#64725=CARTESIAN_POINT('Ctrl Pts',(28.6775243943233,-0.763531646934146,
24.6822916666666));
#64726=CARTESIAN_POINT('Ctrl Pts',(29.1183495962155,-1.52706329386828,24.7239583333333));
#64727=CARTESIAN_POINT('Ctrl Pts',(30.,-1.52706329386828,24.765625));
#64728=CARTESIAN_POINT('Ctrl Pts',(30.8816504037844,-1.52706329386828,24.8072916666666));
#64729=CARTESIAN_POINT('Ctrl Pts',(31.3224756056766,-0.763531646934147,
24.8489583333333));
#64730=CARTESIAN_POINT('Ctrl Pts',(31.7633008075689,-1.36198038370242E-14,
24.890625));
#64731=CARTESIAN_POINT('Ctrl Pts',(31.3224756056766,0.763531646934118,24.9322916666666));
#64732=CARTESIAN_POINT('Ctrl Pts',(30.8816504037844,1.52706329386825,24.9739583333333));
#64733=CARTESIAN_POINT('Ctrl Pts',(30.,1.52706329386825,25.015625));
#64734=CARTESIAN_POINT('Ctrl Pts',(29.1183495962155,1.52706329386825,25.0572916666666));
#64735=CARTESIAN_POINT('Ctrl Pts',(28.6775243943233,0.76353164693412,25.0989583333333));
#64736=CARTESIAN_POINT('Ctrl Pts',(28.2366991924311,-1.31894491186926E-14,
25.140625));
#64737=CARTESIAN_POINT('Ctrl Pts',(28.6775243943233,-0.763531646934146,
25.1822916666666));
#64738=CARTESIAN_POINT('Ctrl Pts',(29.1183495962155,-1.52706329386828,25.2239583333333));
#64739=CARTESIAN_POINT('Ctrl Pts',(30.,-1.52706329386828,25.265625));
#64740=CARTESIAN_POINT('Ctrl Pts',(30.8816504037844,-1.52706329386828,25.3072916666666));
#64741=CARTESIAN_POINT('Ctrl Pts',(31.3224756056766,-0.763531646934147,
25.3489583333333));
#64742=CARTESIAN_POINT('Ctrl Pts',(31.7633008075689,-1.36198038370242E-14,
25.390625));
#64743=CARTESIAN_POINT('Ctrl Pts',(31.3224756056766,0.763531646934118,25.4322916666666));
#64744=CARTESIAN_POINT('Ctrl Pts',(30.8816504037844,1.52706329386825,25.4739583333333));
#64745=CARTESIAN_POINT('Ctrl Pts',(30.,1.52706329386825,25.515625));
#64746=CARTESIAN_POINT('Ctrl Pts',(29.1183495962155,1.52706329386825,25.5572916666666));
#64747=CARTESIAN_POINT('Ctrl Pts',(28.6775243943233,0.76353164693412,25.5989583333333));
#64748=CARTESIAN_POINT('Ctrl Pts',(28.2366991924311,-1.31894491186926E-14,
25.640625));
#64749=CARTESIAN_POINT('Ctrl Pts',(28.6775243943233,-0.763531646934146,
25.6822916666666));
#64750=CARTESIAN_POINT('Ctrl Pts',(29.1183495962155,-1.52706329386828,25.7239583333333));
#64751=CARTESIAN_POINT('Ctrl Pts',(30.,-1.52706329386828,25.765625));
#64752=CARTESIAN_POINT('Ctrl Pts',(30.8816504037844,-1.52706329386828,25.8072916666666));
#64753=CARTESIAN_POINT('Ctrl Pts',(31.3224756056766,-0.763531646934147,
25.8489583333333));
#64754=CARTESIAN_POINT('Ctrl Pts',(31.7633008075689,-1.36198038370242E-14,
25.890625));
#64755=CARTESIAN_POINT('Ctrl Pts',(31.3224756056766,0.763531646934118,25.9322916666666));
#64756=CARTESIAN_POINT('Ctrl Pts',(30.8816504037844,1.52706329386825,25.9739583333333));
#64757=CARTESIAN_POINT('Ctrl Pts',(30.,1.52706329386825,26.015625));
#64758=CARTESIAN_POINT('Ctrl Pts',(29.1183495962155,1.52706329386825,26.0572916666666));
#64759=CARTESIAN_POINT('Ctrl Pts',(28.6775243943233,0.76353164693412,26.0989583333333));
#64760=CARTESIAN_POINT('Ctrl Pts',(28.2366991924311,-1.31894491186926E-14,
26.140625));
#64761=CARTESIAN_POINT('Ctrl Pts',(28.6775243943233,-0.763531646934146,
26.1822916666666));
#64762=CARTESIAN_POINT('Ctrl Pts',(29.1183495962155,-1.52706329386828,26.2239583333333));
#64763=CARTESIAN_POINT('Ctrl Pts',(30.,-1.52706329386828,26.265625));
#64764=CARTESIAN_POINT('Ctrl Pts',(30.8816504037844,-1.52706329386828,26.3072916666666));
#64765=CARTESIAN_POINT('Ctrl Pts',(31.3224756056766,-0.763531646934147,
26.3489583333333));
#64766=CARTESIAN_POINT('Ctrl Pts',(31.7633008075689,-1.36198038370242E-14,
26.390625));
#64767=CARTESIAN_POINT('Ctrl Pts',(31.3224756056766,0.763531646934118,26.4322916666666));
#64768=CARTESIAN_POINT('Ctrl Pts',(30.8816504037844,1.52706329386825,26.4739583333333));
#64769=CARTESIAN_POINT('Ctrl Pts',(30.,1.52706329386825,26.515625));
#64770=CARTESIAN_POINT('Ctrl Pts',(29.1183495962155,1.52706329386825,26.5572916666666));
#64771=CARTESIAN_POINT('Ctrl Pts',(28.6775243943233,0.76353164693412,26.5989583333333));
#64772=CARTESIAN_POINT('Ctrl Pts',(28.2366991924311,-1.31894491186926E-14,
26.640625));
#64773=CARTESIAN_POINT('Ctrl Pts',(28.6775243943233,-0.763531646934146,
26.6822916666666));
#64774=CARTESIAN_POINT('Ctrl Pts',(29.1183495962155,-1.52706329386828,26.7239583333333));
#64775=CARTESIAN_POINT('Ctrl Pts',(30.,-1.52706329386828,26.765625));
#64776=CARTESIAN_POINT('Ctrl Pts',(30.8816504037844,-1.52706329386828,26.8072916666666));
#64777=CARTESIAN_POINT('Ctrl Pts',(31.3224756056766,-0.763531646934147,
26.8489583333333));
#64778=CARTESIAN_POINT('Ctrl Pts',(31.7633008075689,-1.36198038370242E-14,
26.890625));
#64779=CARTESIAN_POINT('Ctrl Pts',(31.3224756056766,0.763531646934118,26.9322916666666));
#64780=CARTESIAN_POINT('Ctrl Pts',(30.8816504037844,1.52706329386825,26.9739583333333));
#64781=CARTESIAN_POINT('Ctrl Pts',(30.,1.52706329386825,27.015625));
#64782=CARTESIAN_POINT('Ctrl Pts',(29.1183495962155,1.52706329386825,27.0572916666666));
#64783=CARTESIAN_POINT('Ctrl Pts',(28.6775243943233,0.76353164693412,27.0989583333333));
#64784=CARTESIAN_POINT('Ctrl Pts',(28.2366991924311,-1.31894491186926E-14,
27.140625));
#64785=CARTESIAN_POINT('Ctrl Pts',(28.6775243943233,-0.763531646934146,
27.1822916666666));
#64786=CARTESIAN_POINT('Ctrl Pts',(29.1183495962155,-1.52706329386828,27.2239583333333));
#64787=CARTESIAN_POINT('Ctrl Pts',(30.,-1.52706329386828,27.265625));
#64788=CARTESIAN_POINT('Ctrl Pts',(30.8816504037844,-1.52706329386828,27.3072916666666));
#64789=CARTESIAN_POINT('Ctrl Pts',(31.3224756056766,-0.763531646934147,
27.3489583333333));
#64790=CARTESIAN_POINT('Ctrl Pts',(31.7633008075689,-1.36198038370242E-14,
27.390625));
#64791=CARTESIAN_POINT('Ctrl Pts',(31.3224756056766,0.763531646934118,27.4322916666666));
#64792=CARTESIAN_POINT('Ctrl Pts',(30.8816504037844,1.52706329386825,27.4739583333333));
#64793=CARTESIAN_POINT('Ctrl Pts',(30.,1.52706329386825,27.515625));
#64794=CARTESIAN_POINT('Ctrl Pts',(29.1183495962155,1.52706329386825,27.5572916666666));
#64795=CARTESIAN_POINT('Ctrl Pts',(28.6775243943233,0.76353164693412,27.5989583333333));
#64796=CARTESIAN_POINT('Ctrl Pts',(28.2366991924311,-1.31894491186926E-14,
27.640625));
#64797=CARTESIAN_POINT('Ctrl Pts',(28.6775243943233,-0.763531646934146,
27.6822916666666));
#64798=CARTESIAN_POINT('Ctrl Pts',(29.1183495962155,-1.52706329386828,27.7239583333333));
#64799=CARTESIAN_POINT('Ctrl Pts',(30.,-1.52706329386828,27.765625));
#64800=CARTESIAN_POINT('Ctrl Pts',(30.8816504037844,-1.52706329386828,27.8072916666666));
#64801=CARTESIAN_POINT('Ctrl Pts',(31.3224756056766,-0.763531646934147,
27.8489583333333));
#64802=CARTESIAN_POINT('Ctrl Pts',(31.7633008075689,-1.36198038370242E-14,
27.890625));
#64803=CARTESIAN_POINT('Ctrl Pts',(31.3224756056766,0.763531646934118,27.9322916666666));
#64804=CARTESIAN_POINT('Ctrl Pts',(30.8816504037844,1.52706329386825,27.9739583333333));
#64805=CARTESIAN_POINT('Ctrl Pts',(30.,1.52706329386825,28.015625));
#64806=CARTESIAN_POINT('Ctrl Pts',(29.1183495962155,1.52706329386825,28.0572916666666));
#64807=CARTESIAN_POINT('Ctrl Pts',(28.6775243943233,0.76353164693412,28.0989583333333));
#64808=CARTESIAN_POINT('Ctrl Pts',(28.2366991924311,-1.31894491186926E-14,
28.140625));
#64809=CARTESIAN_POINT('Ctrl Pts',(28.6775243943233,-0.763531646934146,
28.1822916666666));
#64810=CARTESIAN_POINT('Ctrl Pts',(29.1183495962155,-1.52706329386828,28.2239583333333));
#64811=CARTESIAN_POINT('Ctrl Pts',(30.,-1.52706329386828,28.265625));
#64812=CARTESIAN_POINT('Ctrl Pts',(30.8816504037844,-1.52706329386828,28.3072916666666));
#64813=CARTESIAN_POINT('Ctrl Pts',(31.3224756056766,-0.763531646934147,
28.3489583333333));
#64814=CARTESIAN_POINT('Ctrl Pts',(31.7633008075689,-1.36198038370242E-14,
28.390625));
#64815=CARTESIAN_POINT('Ctrl Pts',(31.3224756056766,0.763531646934118,28.4322916666666));
#64816=CARTESIAN_POINT('Ctrl Pts',(30.8816504037844,1.52706329386825,28.4739583333333));
#64817=CARTESIAN_POINT('Ctrl Pts',(30.,1.52706329386825,28.515625));
#64818=CARTESIAN_POINT('Ctrl Pts',(29.1183495962155,1.52706329386825,28.5572916666666));
#64819=CARTESIAN_POINT('Ctrl Pts',(28.6775243943233,0.76353164693412,28.5989583333333));
#64820=CARTESIAN_POINT('Ctrl Pts',(28.2366991924311,-1.31894491186926E-14,
28.640625));
#64821=CARTESIAN_POINT('Ctrl Pts',(28.6775243943233,-0.763531646934146,
28.6822916666666));
#64822=CARTESIAN_POINT('Ctrl Pts',(29.1183495962155,-1.52706329386828,28.7239583333333));
#64823=CARTESIAN_POINT('Ctrl Pts',(30.,-1.52706329386828,28.765625));
#64824=CARTESIAN_POINT('Ctrl Pts',(30.8816504037844,-1.52706329386828,28.8072916666666));
#64825=CARTESIAN_POINT('Ctrl Pts',(31.3224756056766,-0.763531646934147,
28.8489583333333));
#64826=CARTESIAN_POINT('Ctrl Pts',(31.7633008075689,-1.36198038370242E-14,
28.890625));
#64827=CARTESIAN_POINT('Ctrl Pts',(31.3224756056766,0.763531646934118,28.9322916666666));
#64828=CARTESIAN_POINT('Ctrl Pts',(30.8816504037844,1.52706329386825,28.9739583333333));
#64829=CARTESIAN_POINT('Ctrl Pts',(30.,1.52706329386825,29.015625));
#64830=CARTESIAN_POINT('Ctrl Pts',(29.1183495962155,1.52706329386825,29.0572916666666));
#64831=CARTESIAN_POINT('Ctrl Pts',(28.6775243943233,0.76353164693412,29.0989583333333));
#64832=CARTESIAN_POINT('Ctrl Pts',(28.2366991924311,-1.31894491186926E-14,
29.140625));
#64833=CARTESIAN_POINT('Ctrl Pts',(28.6775243943233,-0.763531646934146,
29.1822916666666));
#64834=CARTESIAN_POINT('Ctrl Pts',(29.1183495962155,-1.52706329386828,29.2239583333333));
#64835=CARTESIAN_POINT('Ctrl Pts',(30.,-1.52706329386828,29.265625));
#64836=CARTESIAN_POINT('Ctrl Pts',(30.8816504037844,-1.52706329386828,29.3072916666666));
#64837=CARTESIAN_POINT('Ctrl Pts',(31.3224756056766,-0.763531646934147,
29.3489583333333));
#64838=CARTESIAN_POINT('Ctrl Pts',(31.7633008075689,-1.36198038370242E-14,
29.390625));
#64839=CARTESIAN_POINT('Ctrl Pts',(31.3224756056766,0.763531646934118,29.4322916666666));
#64840=CARTESIAN_POINT('Ctrl Pts',(30.8816504037844,1.52706329386825,29.4739583333333));
#64841=CARTESIAN_POINT('Ctrl Pts',(30.,1.52706329386825,29.515625));
#64842=CARTESIAN_POINT('Ctrl Pts',(29.1183495962155,1.52706329386825,29.5572916666666));
#64843=CARTESIAN_POINT('Ctrl Pts',(28.6775243943233,0.76353164693412,29.5989583333333));
#64844=CARTESIAN_POINT('Ctrl Pts',(28.2366991924311,-1.31894491186926E-14,
29.640625));
#64845=CARTESIAN_POINT('Ctrl Pts',(28.6775243943233,-0.763531646934146,
29.6822916666666));
#64846=CARTESIAN_POINT('Ctrl Pts',(29.1183495962155,-1.52706329386828,29.7239583333333));
#64847=CARTESIAN_POINT('Ctrl Pts',(30.,-1.52706329386828,29.765625));
#64848=CARTESIAN_POINT('Ctrl Pts',(30.8816504037844,-1.52706329386828,29.8072916666666));
#64849=CARTESIAN_POINT('Ctrl Pts',(31.3224756056766,-0.763531646934147,
29.8489583333333));
#64850=CARTESIAN_POINT('Ctrl Pts',(31.7633008075689,-1.36198038370242E-14,
29.890625));
#64851=CARTESIAN_POINT('Ctrl Pts',(31.3224756056766,0.763531646934118,29.9322916666666));
#64852=CARTESIAN_POINT('Ctrl Pts',(30.8816504037844,1.52706329386825,29.9739583333333));
#64853=CARTESIAN_POINT('Ctrl Pts',(30.,1.52706329386825,30.015625));
#64854=CARTESIAN_POINT('Ctrl Pts',(29.1183495962155,1.52706329386825,30.0572916666666));
#64855=CARTESIAN_POINT('Ctrl Pts',(28.6775243943233,0.76353164693412,30.0989583333333));
#64856=CARTESIAN_POINT('Ctrl Pts',(28.2366991924311,-1.31894491186926E-14,
30.140625));
#64857=CARTESIAN_POINT('Ctrl Pts',(28.6775243943233,-0.763531646934146,
30.1822916666666));
#64858=CARTESIAN_POINT('Ctrl Pts',(29.1183495962155,-1.52706329386828,30.2239583333333));
#64859=CARTESIAN_POINT('Ctrl Pts',(30.,-1.52706329386828,30.265625));
#64860=CARTESIAN_POINT('Ctrl Pts',(30.8816504037844,-1.52706329386828,30.3072916666666));
#64861=CARTESIAN_POINT('Ctrl Pts',(31.3224756056766,-0.763531646934147,
30.3489583333333));
#64862=CARTESIAN_POINT('Ctrl Pts',(31.7633008075689,-1.36198038370242E-14,
30.390625));
#64863=CARTESIAN_POINT('Ctrl Pts',(31.3224756056766,0.763531646934118,30.4322916666666));
#64864=CARTESIAN_POINT('Ctrl Pts',(30.8816504037844,1.52706329386825,30.4739583333333));
#64865=CARTESIAN_POINT('Ctrl Pts',(30.,1.52706329386825,30.515625));
#64866=CARTESIAN_POINT('Ctrl Pts',(29.1183495962155,1.52706329386825,30.5572916666666));
#64867=CARTESIAN_POINT('Ctrl Pts',(28.6775243943233,0.76353164693412,30.5989583333333));
#64868=CARTESIAN_POINT('Ctrl Pts',(28.2366991924311,-1.31894491186926E-14,
30.640625));
#64869=CARTESIAN_POINT('Ctrl Pts',(28.6775243943233,-0.763531646934146,
30.6822916666666));
#64870=CARTESIAN_POINT('Ctrl Pts',(29.1183495962155,-1.52706329386828,30.7239583333333));
#64871=CARTESIAN_POINT('Ctrl Pts',(30.,-1.52706329386828,30.765625));
#64872=CARTESIAN_POINT('Ctrl Pts',(30.8816504037844,-1.52706329386828,30.8072916666666));
#64873=CARTESIAN_POINT('Ctrl Pts',(31.3224756056766,-0.763531646934147,
30.8489583333333));
#64874=CARTESIAN_POINT('Ctrl Pts',(31.7633008075689,-1.36198038370242E-14,
30.890625));
#64875=CARTESIAN_POINT('Ctrl Pts',(31.3224756056766,0.763531646934118,30.9322916666666));
#64876=CARTESIAN_POINT('Ctrl Pts',(30.8816504037844,1.52706329386825,30.9739583333333));
#64877=CARTESIAN_POINT('Ctrl Pts',(30.,1.52706329386825,31.015625));
#64878=CARTESIAN_POINT('Ctrl Pts',(29.1183495962155,1.52706329386825,31.0572916666666));
#64879=CARTESIAN_POINT('Ctrl Pts',(28.6775243943233,0.76353164693412,31.0989583333333));
#64880=CARTESIAN_POINT('Ctrl Pts',(28.2366991924311,-1.31894491186926E-14,
31.140625));
#64881=CARTESIAN_POINT('Ctrl Pts',(28.6775243943233,-0.763531646934146,
31.1822916666666));
#64882=CARTESIAN_POINT('Ctrl Pts',(29.1183495962155,-1.52706329386828,31.2239583333333));
#64883=CARTESIAN_POINT('Ctrl Pts',(30.,-1.52706329386828,31.265625));
#64884=CARTESIAN_POINT('Ctrl Pts',(30.8816504037844,-1.52706329386828,31.3072916666666));
#64885=CARTESIAN_POINT('Ctrl Pts',(31.3224756056766,-0.763531646934147,
31.3489583333333));
#64886=CARTESIAN_POINT('Ctrl Pts',(31.7633008075689,-1.36198038370242E-14,
31.390625));
#64887=CARTESIAN_POINT('Ctrl Pts',(31.3224756056766,0.763531646934118,31.4322916666666));
#64888=CARTESIAN_POINT('Ctrl Pts',(30.8816504037844,1.52706329386825,31.4739583333333));
#64889=CARTESIAN_POINT('Ctrl Pts',(30.,1.52706329386825,31.515625));
#64890=CARTESIAN_POINT('Ctrl Pts',(30.,1.17523507120987,15.8124968809397));
#64891=CARTESIAN_POINT('Ctrl Pts',(29.3214777152758,1.17523507120987,15.8541635476064));
#64892=CARTESIAN_POINT('Ctrl Pts',(28.9822165729138,0.587617535604928,15.895830214273));
#64893=CARTESIAN_POINT('Ctrl Pts',(28.6429554305518,-1.32141489532166E-14,
15.9374968809397));
#64894=CARTESIAN_POINT('Ctrl Pts',(28.9822165729138,-0.587617535604954,
15.9791635476064));
#64895=CARTESIAN_POINT('Ctrl Pts',(29.3214777152758,-1.17523507120989,16.020830214273));
#64896=CARTESIAN_POINT('Ctrl Pts',(30.,-1.17523507120989,16.0624968809397));
#64897=CARTESIAN_POINT('Ctrl Pts',(30.6785222847241,-1.17523507120989,16.1041635476064));
#64898=CARTESIAN_POINT('Ctrl Pts',(31.0177834270861,-0.587617535604955,
16.145830214273));
#64899=CARTESIAN_POINT('Ctrl Pts',(31.3570445694482,-1.35453519623354E-14,
16.1874968809397));
#64900=CARTESIAN_POINT('Ctrl Pts',(31.0177834270861,0.587617535604927,16.2291635476064));
#64901=CARTESIAN_POINT('Ctrl Pts',(30.6785222847241,1.17523507120987,16.270830214273));
#64902=CARTESIAN_POINT('Ctrl Pts',(30.,1.17523507120987,16.3124968809397));
#64903=CARTESIAN_POINT('Ctrl Pts',(29.3214777152758,1.17523507120987,16.3541635476064));
#64904=CARTESIAN_POINT('Ctrl Pts',(28.9822165729138,0.587617535604928,16.395830214273));
#64905=CARTESIAN_POINT('Ctrl Pts',(28.6429554305518,-1.32141489532166E-14,
16.4374968809397));
#64906=CARTESIAN_POINT('Ctrl Pts',(28.9822165729138,-0.587617535604954,
16.4791635476064));
#64907=CARTESIAN_POINT('Ctrl Pts',(29.3214777152758,-1.17523507120989,16.520830214273));
#64908=CARTESIAN_POINT('Ctrl Pts',(30.,-1.17523507120989,16.5624968809397));
#64909=CARTESIAN_POINT('Ctrl Pts',(30.6785222847241,-1.17523507120989,16.6041635476064));
#64910=CARTESIAN_POINT('Ctrl Pts',(31.0177834270861,-0.587617535604955,
16.645830214273));
#64911=CARTESIAN_POINT('Ctrl Pts',(31.3570445694482,-1.35453519623354E-14,
16.6874968809397));
#64912=CARTESIAN_POINT('Ctrl Pts',(31.0177834270861,0.587617535604927,16.7291635476064));
#64913=CARTESIAN_POINT('Ctrl Pts',(30.6785222847241,1.17523507120987,16.770830214273));
#64914=CARTESIAN_POINT('Ctrl Pts',(30.,1.17523507120987,16.8124968809397));
#64915=CARTESIAN_POINT('Ctrl Pts',(29.3214777152758,1.17523507120987,16.8541635476064));
#64916=CARTESIAN_POINT('Ctrl Pts',(28.9822165729138,0.587617535604928,16.895830214273));
#64917=CARTESIAN_POINT('Ctrl Pts',(28.6429554305518,-1.32141489532166E-14,
16.9374968809397));
#64918=CARTESIAN_POINT('Ctrl Pts',(28.9822165729138,-0.587617535604954,
16.9791635476064));
#64919=CARTESIAN_POINT('Ctrl Pts',(29.3214777152758,-1.17523507120989,17.020830214273));
#64920=CARTESIAN_POINT('Ctrl Pts',(30.,-1.17523507120989,17.0624968809397));
#64921=CARTESIAN_POINT('Ctrl Pts',(30.6785222847241,-1.17523507120989,17.1041635476064));
#64922=CARTESIAN_POINT('Ctrl Pts',(31.0177834270861,-0.587617535604955,
17.145830214273));
#64923=CARTESIAN_POINT('Ctrl Pts',(31.3570445694482,-1.35453519623354E-14,
17.1874968809397));
#64924=CARTESIAN_POINT('Ctrl Pts',(31.0177834270861,0.587617535604927,17.2291635476064));
#64925=CARTESIAN_POINT('Ctrl Pts',(30.6785222847241,1.17523507120987,17.270830214273));
#64926=CARTESIAN_POINT('Ctrl Pts',(30.,1.17523507120987,17.3124968809397));
#64927=CARTESIAN_POINT('Ctrl Pts',(29.3214777152758,1.17523507120987,17.3541635476064));
#64928=CARTESIAN_POINT('Ctrl Pts',(28.9822165729138,0.587617535604928,17.395830214273));
#64929=CARTESIAN_POINT('Ctrl Pts',(28.6429554305518,-1.32141489532166E-14,
17.4374968809397));
#64930=CARTESIAN_POINT('Ctrl Pts',(28.9822165729138,-0.587617535604954,
17.4791635476064));
#64931=CARTESIAN_POINT('Ctrl Pts',(29.3214777152758,-1.17523507120989,17.520830214273));
#64932=CARTESIAN_POINT('Ctrl Pts',(30.,-1.17523507120989,17.5624968809397));
#64933=CARTESIAN_POINT('Ctrl Pts',(30.6785222847241,-1.17523507120989,17.6041635476064));
#64934=CARTESIAN_POINT('Ctrl Pts',(31.0177834270861,-0.587617535604955,
17.645830214273));
#64935=CARTESIAN_POINT('Ctrl Pts',(31.3570445694482,-1.35453519623354E-14,
17.6874968809397));
#64936=CARTESIAN_POINT('Ctrl Pts',(31.0177834270861,0.587617535604927,17.7291635476064));
#64937=CARTESIAN_POINT('Ctrl Pts',(30.6785222847241,1.17523507120987,17.770830214273));
#64938=CARTESIAN_POINT('Ctrl Pts',(30.,1.17523507120987,17.8124968809397));
#64939=CARTESIAN_POINT('Ctrl Pts',(29.3214777152758,1.17523507120987,17.8541635476064));
#64940=CARTESIAN_POINT('Ctrl Pts',(28.9822165729138,0.587617535604928,17.895830214273));
#64941=CARTESIAN_POINT('Ctrl Pts',(28.6429554305518,-1.32141489532166E-14,
17.9374968809397));
#64942=CARTESIAN_POINT('Ctrl Pts',(28.9822165729138,-0.587617535604954,
17.9791635476064));
#64943=CARTESIAN_POINT('Ctrl Pts',(29.3214777152758,-1.17523507120989,18.020830214273));
#64944=CARTESIAN_POINT('Ctrl Pts',(30.,-1.17523507120989,18.0624968809397));
#64945=CARTESIAN_POINT('Ctrl Pts',(30.6785222847241,-1.17523507120989,18.1041635476064));
#64946=CARTESIAN_POINT('Ctrl Pts',(31.0177834270861,-0.587617535604955,
18.145830214273));
#64947=CARTESIAN_POINT('Ctrl Pts',(31.3570445694482,-1.35453519623354E-14,
18.1874968809397));
#64948=CARTESIAN_POINT('Ctrl Pts',(31.0177834270861,0.587617535604927,18.2291635476064));
#64949=CARTESIAN_POINT('Ctrl Pts',(30.6785222847241,1.17523507120987,18.270830214273));
#64950=CARTESIAN_POINT('Ctrl Pts',(30.,1.17523507120987,18.3124968809397));
#64951=CARTESIAN_POINT('Ctrl Pts',(29.3214777152758,1.17523507120987,18.3541635476064));
#64952=CARTESIAN_POINT('Ctrl Pts',(28.9822165729138,0.587617535604928,18.395830214273));
#64953=CARTESIAN_POINT('Ctrl Pts',(28.6429554305518,-1.32141489532166E-14,
18.4374968809397));
#64954=CARTESIAN_POINT('Ctrl Pts',(28.9822165729138,-0.587617535604954,
18.4791635476064));
#64955=CARTESIAN_POINT('Ctrl Pts',(29.3214777152758,-1.17523507120989,18.520830214273));
#64956=CARTESIAN_POINT('Ctrl Pts',(30.,-1.17523507120989,18.5624968809397));
#64957=CARTESIAN_POINT('Ctrl Pts',(30.6785222847241,-1.17523507120989,18.6041635476064));
#64958=CARTESIAN_POINT('Ctrl Pts',(31.0177834270861,-0.587617535604955,
18.645830214273));
#64959=CARTESIAN_POINT('Ctrl Pts',(31.3570445694482,-1.35453519623354E-14,
18.6874968809397));
#64960=CARTESIAN_POINT('Ctrl Pts',(31.0177834270861,0.587617535604927,18.7291635476064));
#64961=CARTESIAN_POINT('Ctrl Pts',(30.6785222847241,1.17523507120987,18.770830214273));
#64962=CARTESIAN_POINT('Ctrl Pts',(30.,1.17523507120987,18.8124968809397));
#64963=CARTESIAN_POINT('Ctrl Pts',(29.3214777152758,1.17523507120987,18.8541635476064));
#64964=CARTESIAN_POINT('Ctrl Pts',(28.9822165729138,0.587617535604928,18.895830214273));
#64965=CARTESIAN_POINT('Ctrl Pts',(28.6429554305518,-1.32141489532166E-14,
18.9374968809397));
#64966=CARTESIAN_POINT('Ctrl Pts',(28.9822165729138,-0.587617535604954,
18.9791635476064));
#64967=CARTESIAN_POINT('Ctrl Pts',(29.3214777152758,-1.17523507120989,19.020830214273));
#64968=CARTESIAN_POINT('Ctrl Pts',(30.,-1.17523507120989,19.0624968809397));
#64969=CARTESIAN_POINT('Ctrl Pts',(30.6785222847241,-1.17523507120989,19.1041635476064));
#64970=CARTESIAN_POINT('Ctrl Pts',(31.0177834270861,-0.587617535604955,
19.145830214273));
#64971=CARTESIAN_POINT('Ctrl Pts',(31.3570445694482,-1.35453519623354E-14,
19.1874968809397));
#64972=CARTESIAN_POINT('Ctrl Pts',(31.0177834270861,0.587617535604927,19.2291635476064));
#64973=CARTESIAN_POINT('Ctrl Pts',(30.6785222847241,1.17523507120987,19.270830214273));
#64974=CARTESIAN_POINT('Ctrl Pts',(30.,1.17523507120987,19.3124968809397));
#64975=CARTESIAN_POINT('Ctrl Pts',(29.3214777152758,1.17523507120987,19.3541635476064));
#64976=CARTESIAN_POINT('Ctrl Pts',(28.9822165729138,0.587617535604928,19.395830214273));
#64977=CARTESIAN_POINT('Ctrl Pts',(28.6429554305518,-1.32141489532166E-14,
19.4374968809397));
#64978=CARTESIAN_POINT('Ctrl Pts',(28.9822165729138,-0.587617535604954,
19.4791635476064));
#64979=CARTESIAN_POINT('Ctrl Pts',(29.3214777152758,-1.17523507120989,19.520830214273));
#64980=CARTESIAN_POINT('Ctrl Pts',(30.,-1.17523507120989,19.5624968809397));
#64981=CARTESIAN_POINT('Ctrl Pts',(30.6785222847241,-1.17523507120989,19.6041635476064));
#64982=CARTESIAN_POINT('Ctrl Pts',(31.0177834270861,-0.587617535604955,
19.645830214273));
#64983=CARTESIAN_POINT('Ctrl Pts',(31.3570445694482,-1.35453519623354E-14,
19.6874968809397));
#64984=CARTESIAN_POINT('Ctrl Pts',(31.0177834270861,0.587617535604927,19.7291635476064));
#64985=CARTESIAN_POINT('Ctrl Pts',(30.6785222847241,1.17523507120987,19.770830214273));
#64986=CARTESIAN_POINT('Ctrl Pts',(30.,1.17523507120987,19.8124968809397));
#64987=CARTESIAN_POINT('Ctrl Pts',(29.3214777152758,1.17523507120987,19.8541635476064));
#64988=CARTESIAN_POINT('Ctrl Pts',(28.9822165729138,0.587617535604928,19.895830214273));
#64989=CARTESIAN_POINT('Ctrl Pts',(28.6429554305518,-1.32141489532166E-14,
19.9374968809397));
#64990=CARTESIAN_POINT('Ctrl Pts',(28.9822165729138,-0.587617535604954,
19.9791635476064));
#64991=CARTESIAN_POINT('Ctrl Pts',(29.3214777152758,-1.17523507120989,20.020830214273));
#64992=CARTESIAN_POINT('Ctrl Pts',(30.,-1.17523507120989,20.0624968809397));
#64993=CARTESIAN_POINT('Ctrl Pts',(30.6785222847241,-1.17523507120989,20.1041635476064));
#64994=CARTESIAN_POINT('Ctrl Pts',(31.0177834270861,-0.587617535604955,
20.145830214273));
#64995=CARTESIAN_POINT('Ctrl Pts',(31.3570445694482,-1.35453519623354E-14,
20.1874968809397));
#64996=CARTESIAN_POINT('Ctrl Pts',(31.0177834270861,0.587617535604927,20.2291635476064));
#64997=CARTESIAN_POINT('Ctrl Pts',(30.6785222847241,1.17523507120987,20.270830214273));
#64998=CARTESIAN_POINT('Ctrl Pts',(30.,1.17523507120987,20.3124968809397));
#64999=CARTESIAN_POINT('Ctrl Pts',(29.3214777152758,1.17523507120987,20.3541635476064));
#65000=CARTESIAN_POINT('Ctrl Pts',(28.9822165729138,0.587617535604928,20.395830214273));
#65001=CARTESIAN_POINT('Ctrl Pts',(28.6429554305518,-1.32141489532166E-14,
20.4374968809397));
#65002=CARTESIAN_POINT('Ctrl Pts',(28.9822165729138,-0.587617535604954,
20.4791635476064));
#65003=CARTESIAN_POINT('Ctrl Pts',(29.3214777152758,-1.17523507120989,20.520830214273));
#65004=CARTESIAN_POINT('Ctrl Pts',(30.,-1.17523507120989,20.5624968809397));
#65005=CARTESIAN_POINT('Ctrl Pts',(30.6785222847241,-1.17523507120989,20.6041635476064));
#65006=CARTESIAN_POINT('Ctrl Pts',(31.0177834270861,-0.587617535604955,
20.645830214273));
#65007=CARTESIAN_POINT('Ctrl Pts',(31.3570445694482,-1.35453519623354E-14,
20.6874968809397));
#65008=CARTESIAN_POINT('Ctrl Pts',(31.0177834270861,0.587617535604927,20.7291635476064));
#65009=CARTESIAN_POINT('Ctrl Pts',(30.6785222847241,1.17523507120987,20.770830214273));
#65010=CARTESIAN_POINT('Ctrl Pts',(30.,1.17523507120987,20.8124968809397));
#65011=CARTESIAN_POINT('Ctrl Pts',(29.3214777152758,1.17523507120987,20.8541635476064));
#65012=CARTESIAN_POINT('Ctrl Pts',(28.9822165729138,0.587617535604928,20.895830214273));
#65013=CARTESIAN_POINT('Ctrl Pts',(28.6429554305518,-1.32141489532166E-14,
20.9374968809397));
#65014=CARTESIAN_POINT('Ctrl Pts',(28.9822165729138,-0.587617535604954,
20.9791635476064));
#65015=CARTESIAN_POINT('Ctrl Pts',(29.3214777152758,-1.17523507120989,21.020830214273));
#65016=CARTESIAN_POINT('Ctrl Pts',(30.,-1.17523507120989,21.0624968809397));
#65017=CARTESIAN_POINT('Ctrl Pts',(30.6785222847241,-1.17523507120989,21.1041635476064));
#65018=CARTESIAN_POINT('Ctrl Pts',(31.0177834270861,-0.587617535604955,
21.145830214273));
#65019=CARTESIAN_POINT('Ctrl Pts',(31.3570445694482,-1.35453519623354E-14,
21.1874968809397));
#65020=CARTESIAN_POINT('Ctrl Pts',(31.0177834270861,0.587617535604927,21.2291635476064));
#65021=CARTESIAN_POINT('Ctrl Pts',(30.6785222847241,1.17523507120987,21.270830214273));
#65022=CARTESIAN_POINT('Ctrl Pts',(30.,1.17523507120987,21.3124968809397));
#65023=CARTESIAN_POINT('Ctrl Pts',(29.3214777152758,1.17523507120987,21.3541635476064));
#65024=CARTESIAN_POINT('Ctrl Pts',(28.9822165729138,0.587617535604928,21.395830214273));
#65025=CARTESIAN_POINT('Ctrl Pts',(28.6429554305518,-1.32141489532166E-14,
21.4374968809397));
#65026=CARTESIAN_POINT('Ctrl Pts',(28.9822165729138,-0.587617535604954,
21.4791635476064));
#65027=CARTESIAN_POINT('Ctrl Pts',(29.3214777152758,-1.17523507120989,21.520830214273));
#65028=CARTESIAN_POINT('Ctrl Pts',(30.,-1.17523507120989,21.5624968809397));
#65029=CARTESIAN_POINT('Ctrl Pts',(30.6785222847241,-1.17523507120989,21.6041635476064));
#65030=CARTESIAN_POINT('Ctrl Pts',(31.0177834270861,-0.587617535604955,
21.645830214273));
#65031=CARTESIAN_POINT('Ctrl Pts',(31.3570445694482,-1.35453519623354E-14,
21.6874968809397));
#65032=CARTESIAN_POINT('Ctrl Pts',(31.0177834270861,0.587617535604927,21.7291635476064));
#65033=CARTESIAN_POINT('Ctrl Pts',(30.6785222847241,1.17523507120987,21.770830214273));
#65034=CARTESIAN_POINT('Ctrl Pts',(30.,1.17523507120987,21.8124968809397));
#65035=CARTESIAN_POINT('Ctrl Pts',(29.3214777152758,1.17523507120987,21.8541635476064));
#65036=CARTESIAN_POINT('Ctrl Pts',(28.9822165729138,0.587617535604928,21.895830214273));
#65037=CARTESIAN_POINT('Ctrl Pts',(28.6429554305518,-1.32141489532166E-14,
21.9374968809397));
#65038=CARTESIAN_POINT('Ctrl Pts',(28.9822165729138,-0.587617535604954,
21.9791635476064));
#65039=CARTESIAN_POINT('Ctrl Pts',(29.3214777152758,-1.17523507120989,22.020830214273));
#65040=CARTESIAN_POINT('Ctrl Pts',(30.,-1.17523507120989,22.0624968809397));
#65041=CARTESIAN_POINT('Ctrl Pts',(30.6785222847241,-1.17523507120989,22.1041635476064));
#65042=CARTESIAN_POINT('Ctrl Pts',(31.0177834270861,-0.587617535604955,
22.145830214273));
#65043=CARTESIAN_POINT('Ctrl Pts',(31.3570445694482,-1.35453519623354E-14,
22.1874968809397));
#65044=CARTESIAN_POINT('Ctrl Pts',(31.0177834270861,0.587617535604927,22.2291635476064));
#65045=CARTESIAN_POINT('Ctrl Pts',(30.6785222847241,1.17523507120987,22.270830214273));
#65046=CARTESIAN_POINT('Ctrl Pts',(30.,1.17523507120987,22.3124968809397));
#65047=CARTESIAN_POINT('Ctrl Pts',(29.3214777152758,1.17523507120987,22.3541635476064));
#65048=CARTESIAN_POINT('Ctrl Pts',(28.9822165729138,0.587617535604928,22.395830214273));
#65049=CARTESIAN_POINT('Ctrl Pts',(28.6429554305518,-1.32141489532166E-14,
22.4374968809397));
#65050=CARTESIAN_POINT('Ctrl Pts',(28.9822165729138,-0.587617535604954,
22.4791635476064));
#65051=CARTESIAN_POINT('Ctrl Pts',(29.3214777152758,-1.17523507120989,22.520830214273));
#65052=CARTESIAN_POINT('Ctrl Pts',(30.,-1.17523507120989,22.5624968809397));
#65053=CARTESIAN_POINT('Ctrl Pts',(30.6785222847241,-1.17523507120989,22.6041635476064));
#65054=CARTESIAN_POINT('Ctrl Pts',(31.0177834270861,-0.587617535604955,
22.645830214273));
#65055=CARTESIAN_POINT('Ctrl Pts',(31.3570445694482,-1.35453519623354E-14,
22.6874968809397));
#65056=CARTESIAN_POINT('Ctrl Pts',(31.0177834270861,0.587617535604927,22.7291635476064));
#65057=CARTESIAN_POINT('Ctrl Pts',(30.6785222847241,1.17523507120987,22.770830214273));
#65058=CARTESIAN_POINT('Ctrl Pts',(30.,1.17523507120987,22.8124968809397));
#65059=CARTESIAN_POINT('Ctrl Pts',(29.3214777152758,1.17523507120987,22.8541635476064));
#65060=CARTESIAN_POINT('Ctrl Pts',(28.9822165729138,0.587617535604928,22.895830214273));
#65061=CARTESIAN_POINT('Ctrl Pts',(28.6429554305518,-1.32141489532166E-14,
22.9374968809397));
#65062=CARTESIAN_POINT('Ctrl Pts',(28.9822165729138,-0.587617535604954,
22.9791635476064));
#65063=CARTESIAN_POINT('Ctrl Pts',(29.3214777152758,-1.17523507120989,23.020830214273));
#65064=CARTESIAN_POINT('Ctrl Pts',(30.,-1.17523507120989,23.0624968809397));
#65065=CARTESIAN_POINT('Ctrl Pts',(30.6785222847241,-1.17523507120989,23.1041635476064));
#65066=CARTESIAN_POINT('Ctrl Pts',(31.0177834270861,-0.587617535604955,
23.145830214273));
#65067=CARTESIAN_POINT('Ctrl Pts',(31.3570445694482,-1.35453519623354E-14,
23.1874968809397));
#65068=CARTESIAN_POINT('Ctrl Pts',(31.0177834270861,0.587617535604927,23.2291635476064));
#65069=CARTESIAN_POINT('Ctrl Pts',(30.6785222847241,1.17523507120987,23.270830214273));
#65070=CARTESIAN_POINT('Ctrl Pts',(30.,1.17523507120987,23.3124968809397));
#65071=CARTESIAN_POINT('Ctrl Pts',(29.3214777152758,1.17523507120987,23.3541635476064));
#65072=CARTESIAN_POINT('Ctrl Pts',(28.9822165729138,0.587617535604928,23.395830214273));
#65073=CARTESIAN_POINT('Ctrl Pts',(28.6429554305518,-1.32141489532166E-14,
23.4374968809397));
#65074=CARTESIAN_POINT('Ctrl Pts',(28.9822165729138,-0.587617535604954,
23.4791635476064));
#65075=CARTESIAN_POINT('Ctrl Pts',(29.3214777152758,-1.17523507120989,23.520830214273));
#65076=CARTESIAN_POINT('Ctrl Pts',(30.,-1.17523507120989,23.5624968809397));
#65077=CARTESIAN_POINT('Ctrl Pts',(30.6785222847241,-1.17523507120989,23.6041635476064));
#65078=CARTESIAN_POINT('Ctrl Pts',(31.0177834270861,-0.587617535604955,
23.645830214273));
#65079=CARTESIAN_POINT('Ctrl Pts',(31.3570445694482,-1.35453519623354E-14,
23.6874968809397));
#65080=CARTESIAN_POINT('Ctrl Pts',(31.0177834270861,0.587617535604927,23.7291635476064));
#65081=CARTESIAN_POINT('Ctrl Pts',(30.6785222847241,1.17523507120987,23.770830214273));
#65082=CARTESIAN_POINT('Ctrl Pts',(30.,1.17523507120987,23.8124968809397));
#65083=CARTESIAN_POINT('Ctrl Pts',(29.3214777152758,1.17523507120987,23.8541635476064));
#65084=CARTESIAN_POINT('Ctrl Pts',(28.9822165729138,0.587617535604928,23.895830214273));
#65085=CARTESIAN_POINT('Ctrl Pts',(28.6429554305518,-1.32141489532166E-14,
23.9374968809397));
#65086=CARTESIAN_POINT('Ctrl Pts',(28.9822165729138,-0.587617535604954,
23.9791635476064));
#65087=CARTESIAN_POINT('Ctrl Pts',(29.3214777152758,-1.17523507120989,24.020830214273));
#65088=CARTESIAN_POINT('Ctrl Pts',(30.,-1.17523507120989,24.0624968809397));
#65089=CARTESIAN_POINT('Ctrl Pts',(30.6785222847241,-1.17523507120989,24.1041635476064));
#65090=CARTESIAN_POINT('Ctrl Pts',(31.0177834270861,-0.587617535604955,
24.145830214273));
#65091=CARTESIAN_POINT('Ctrl Pts',(31.3570445694482,-1.35453519623354E-14,
24.1874968809397));
#65092=CARTESIAN_POINT('Ctrl Pts',(31.0177834270861,0.587617535604927,24.2291635476064));
#65093=CARTESIAN_POINT('Ctrl Pts',(30.6785222847241,1.17523507120987,24.270830214273));
#65094=CARTESIAN_POINT('Ctrl Pts',(30.,1.17523507120987,24.3124968809397));
#65095=CARTESIAN_POINT('Ctrl Pts',(29.3214777152758,1.17523507120987,24.3541635476064));
#65096=CARTESIAN_POINT('Ctrl Pts',(28.9822165729138,0.587617535604928,24.395830214273));
#65097=CARTESIAN_POINT('Ctrl Pts',(28.6429554305518,-1.32141489532166E-14,
24.4374968809397));
#65098=CARTESIAN_POINT('Ctrl Pts',(28.9822165729138,-0.587617535604954,
24.4791635476064));
#65099=CARTESIAN_POINT('Ctrl Pts',(29.3214777152758,-1.17523507120989,24.520830214273));
#65100=CARTESIAN_POINT('Ctrl Pts',(30.,-1.17523507120989,24.5624968809397));
#65101=CARTESIAN_POINT('Ctrl Pts',(30.6785222847241,-1.17523507120989,24.6041635476064));
#65102=CARTESIAN_POINT('Ctrl Pts',(31.0177834270861,-0.587617535604955,
24.645830214273));
#65103=CARTESIAN_POINT('Ctrl Pts',(31.3570445694482,-1.35453519623354E-14,
24.6874968809397));
#65104=CARTESIAN_POINT('Ctrl Pts',(31.0177834270861,0.587617535604927,24.7291635476064));
#65105=CARTESIAN_POINT('Ctrl Pts',(30.6785222847241,1.17523507120987,24.770830214273));
#65106=CARTESIAN_POINT('Ctrl Pts',(30.,1.17523507120987,24.8124968809397));
#65107=CARTESIAN_POINT('Ctrl Pts',(29.3214777152758,1.17523507120987,24.8541635476064));
#65108=CARTESIAN_POINT('Ctrl Pts',(28.9822165729138,0.587617535604928,24.895830214273));
#65109=CARTESIAN_POINT('Ctrl Pts',(28.6429554305518,-1.32141489532166E-14,
24.9374968809397));
#65110=CARTESIAN_POINT('Ctrl Pts',(28.9822165729138,-0.587617535604954,
24.9791635476064));
#65111=CARTESIAN_POINT('Ctrl Pts',(29.3214777152758,-1.17523507120989,25.020830214273));
#65112=CARTESIAN_POINT('Ctrl Pts',(30.,-1.17523507120989,25.0624968809397));
#65113=CARTESIAN_POINT('Ctrl Pts',(30.6785222847241,-1.17523507120989,25.1041635476064));
#65114=CARTESIAN_POINT('Ctrl Pts',(31.0177834270861,-0.587617535604955,
25.145830214273));
#65115=CARTESIAN_POINT('Ctrl Pts',(31.3570445694482,-1.35453519623354E-14,
25.1874968809397));
#65116=CARTESIAN_POINT('Ctrl Pts',(31.0177834270861,0.587617535604927,25.2291635476064));
#65117=CARTESIAN_POINT('Ctrl Pts',(30.6785222847241,1.17523507120987,25.270830214273));
#65118=CARTESIAN_POINT('Ctrl Pts',(30.,1.17523507120987,25.3124968809397));
#65119=CARTESIAN_POINT('Ctrl Pts',(29.3214777152758,1.17523507120987,25.3541635476064));
#65120=CARTESIAN_POINT('Ctrl Pts',(28.9822165729138,0.587617535604928,25.395830214273));
#65121=CARTESIAN_POINT('Ctrl Pts',(28.6429554305518,-1.32141489532166E-14,
25.4374968809397));
#65122=CARTESIAN_POINT('Ctrl Pts',(28.9822165729138,-0.587617535604954,
25.4791635476064));
#65123=CARTESIAN_POINT('Ctrl Pts',(29.3214777152758,-1.17523507120989,25.520830214273));
#65124=CARTESIAN_POINT('Ctrl Pts',(30.,-1.17523507120989,25.5624968809397));
#65125=CARTESIAN_POINT('Ctrl Pts',(30.6785222847241,-1.17523507120989,25.6041635476064));
#65126=CARTESIAN_POINT('Ctrl Pts',(31.0177834270861,-0.587617535604955,
25.645830214273));
#65127=CARTESIAN_POINT('Ctrl Pts',(31.3570445694482,-1.35453519623354E-14,
25.6874968809397));
#65128=CARTESIAN_POINT('Ctrl Pts',(31.0177834270861,0.587617535604927,25.7291635476064));
#65129=CARTESIAN_POINT('Ctrl Pts',(30.6785222847241,1.17523507120987,25.770830214273));
#65130=CARTESIAN_POINT('Ctrl Pts',(30.,1.17523507120987,25.8124968809397));
#65131=CARTESIAN_POINT('Ctrl Pts',(29.3214777152758,1.17523507120987,25.8541635476064));
#65132=CARTESIAN_POINT('Ctrl Pts',(28.9822165729138,0.587617535604928,25.895830214273));
#65133=CARTESIAN_POINT('Ctrl Pts',(28.6429554305518,-1.32141489532166E-14,
25.9374968809397));
#65134=CARTESIAN_POINT('Ctrl Pts',(28.9822165729138,-0.587617535604954,
25.9791635476064));
#65135=CARTESIAN_POINT('Ctrl Pts',(29.3214777152758,-1.17523507120989,26.020830214273));
#65136=CARTESIAN_POINT('Ctrl Pts',(30.,-1.17523507120989,26.0624968809397));
#65137=CARTESIAN_POINT('Ctrl Pts',(30.6785222847241,-1.17523507120989,26.1041635476064));
#65138=CARTESIAN_POINT('Ctrl Pts',(31.0177834270861,-0.587617535604955,
26.145830214273));
#65139=CARTESIAN_POINT('Ctrl Pts',(31.3570445694482,-1.35453519623354E-14,
26.1874968809397));
#65140=CARTESIAN_POINT('Ctrl Pts',(31.0177834270861,0.587617535604927,26.2291635476064));
#65141=CARTESIAN_POINT('Ctrl Pts',(30.6785222847241,1.17523507120987,26.270830214273));
#65142=CARTESIAN_POINT('Ctrl Pts',(30.,1.17523507120987,26.3124968809397));
#65143=CARTESIAN_POINT('Ctrl Pts',(29.3214777152758,1.17523507120987,26.3541635476064));
#65144=CARTESIAN_POINT('Ctrl Pts',(28.9822165729138,0.587617535604928,26.395830214273));
#65145=CARTESIAN_POINT('Ctrl Pts',(28.6429554305518,-1.32141489532166E-14,
26.4374968809397));
#65146=CARTESIAN_POINT('Ctrl Pts',(28.9822165729138,-0.587617535604954,
26.4791635476064));
#65147=CARTESIAN_POINT('Ctrl Pts',(29.3214777152758,-1.17523507120989,26.520830214273));
#65148=CARTESIAN_POINT('Ctrl Pts',(30.,-1.17523507120989,26.5624968809397));
#65149=CARTESIAN_POINT('Ctrl Pts',(30.6785222847241,-1.17523507120989,26.6041635476064));
#65150=CARTESIAN_POINT('Ctrl Pts',(31.0177834270861,-0.587617535604955,
26.645830214273));
#65151=CARTESIAN_POINT('Ctrl Pts',(31.3570445694482,-1.35453519623354E-14,
26.6874968809397));
#65152=CARTESIAN_POINT('Ctrl Pts',(31.0177834270861,0.587617535604927,26.7291635476064));
#65153=CARTESIAN_POINT('Ctrl Pts',(30.6785222847241,1.17523507120987,26.770830214273));
#65154=CARTESIAN_POINT('Ctrl Pts',(30.,1.17523507120987,26.8124968809397));
#65155=CARTESIAN_POINT('Ctrl Pts',(29.3214777152758,1.17523507120987,26.8541635476064));
#65156=CARTESIAN_POINT('Ctrl Pts',(28.9822165729138,0.587617535604928,26.895830214273));
#65157=CARTESIAN_POINT('Ctrl Pts',(28.6429554305518,-1.32141489532166E-14,
26.9374968809397));
#65158=CARTESIAN_POINT('Ctrl Pts',(28.9822165729138,-0.587617535604954,
26.9791635476064));
#65159=CARTESIAN_POINT('Ctrl Pts',(29.3214777152758,-1.17523507120989,27.020830214273));
#65160=CARTESIAN_POINT('Ctrl Pts',(30.,-1.17523507120989,27.0624968809397));
#65161=CARTESIAN_POINT('Ctrl Pts',(30.6785222847241,-1.17523507120989,27.1041635476064));
#65162=CARTESIAN_POINT('Ctrl Pts',(31.0177834270861,-0.587617535604955,
27.145830214273));
#65163=CARTESIAN_POINT('Ctrl Pts',(31.3570445694482,-1.35453519623354E-14,
27.1874968809397));
#65164=CARTESIAN_POINT('Ctrl Pts',(31.0177834270861,0.587617535604927,27.2291635476064));
#65165=CARTESIAN_POINT('Ctrl Pts',(30.6785222847241,1.17523507120987,27.270830214273));
#65166=CARTESIAN_POINT('Ctrl Pts',(30.,1.17523507120987,27.3124968809397));
#65167=CARTESIAN_POINT('Ctrl Pts',(29.3214777152758,1.17523507120987,27.3541635476064));
#65168=CARTESIAN_POINT('Ctrl Pts',(28.9822165729138,0.587617535604928,27.395830214273));
#65169=CARTESIAN_POINT('Ctrl Pts',(28.6429554305518,-1.32141489532166E-14,
27.4374968809397));
#65170=CARTESIAN_POINT('Ctrl Pts',(28.9822165729138,-0.587617535604954,
27.4791635476064));
#65171=CARTESIAN_POINT('Ctrl Pts',(29.3214777152758,-1.17523507120989,27.520830214273));
#65172=CARTESIAN_POINT('Ctrl Pts',(30.,-1.17523507120989,27.5624968809397));
#65173=CARTESIAN_POINT('Ctrl Pts',(30.6785222847241,-1.17523507120989,27.6041635476064));
#65174=CARTESIAN_POINT('Ctrl Pts',(31.0177834270861,-0.587617535604955,
27.645830214273));
#65175=CARTESIAN_POINT('Ctrl Pts',(31.3570445694482,-1.35453519623354E-14,
27.6874968809397));
#65176=CARTESIAN_POINT('Ctrl Pts',(31.0177834270861,0.587617535604927,27.7291635476064));
#65177=CARTESIAN_POINT('Ctrl Pts',(30.6785222847241,1.17523507120987,27.770830214273));
#65178=CARTESIAN_POINT('Ctrl Pts',(30.,1.17523507120987,27.8124968809397));
#65179=CARTESIAN_POINT('Ctrl Pts',(29.3214777152758,1.17523507120987,27.8541635476064));
#65180=CARTESIAN_POINT('Ctrl Pts',(28.9822165729138,0.587617535604928,27.895830214273));
#65181=CARTESIAN_POINT('Ctrl Pts',(28.6429554305518,-1.32141489532166E-14,
27.9374968809397));
#65182=CARTESIAN_POINT('Ctrl Pts',(28.9822165729138,-0.587617535604954,
27.9791635476064));
#65183=CARTESIAN_POINT('Ctrl Pts',(29.3214777152758,-1.17523507120989,28.020830214273));
#65184=CARTESIAN_POINT('Ctrl Pts',(30.,-1.17523507120989,28.0624968809397));
#65185=CARTESIAN_POINT('Ctrl Pts',(30.6785222847241,-1.17523507120989,28.1041635476064));
#65186=CARTESIAN_POINT('Ctrl Pts',(31.0177834270861,-0.587617535604955,
28.145830214273));
#65187=CARTESIAN_POINT('Ctrl Pts',(31.3570445694482,-1.35453519623354E-14,
28.1874968809397));
#65188=CARTESIAN_POINT('Ctrl Pts',(31.0177834270861,0.587617535604927,28.2291635476064));
#65189=CARTESIAN_POINT('Ctrl Pts',(30.6785222847241,1.17523507120987,28.270830214273));
#65190=CARTESIAN_POINT('Ctrl Pts',(30.,1.17523507120987,28.3124968809397));
#65191=CARTESIAN_POINT('Ctrl Pts',(29.3214777152758,1.17523507120987,28.3541635476064));
#65192=CARTESIAN_POINT('Ctrl Pts',(28.9822165729138,0.587617535604928,28.395830214273));
#65193=CARTESIAN_POINT('Ctrl Pts',(28.6429554305518,-1.32141489532166E-14,
28.4374968809397));
#65194=CARTESIAN_POINT('Ctrl Pts',(28.9822165729138,-0.587617535604954,
28.4791635476064));
#65195=CARTESIAN_POINT('Ctrl Pts',(29.3214777152758,-1.17523507120989,28.520830214273));
#65196=CARTESIAN_POINT('Ctrl Pts',(30.,-1.17523507120989,28.5624968809397));
#65197=CARTESIAN_POINT('Ctrl Pts',(30.6785222847241,-1.17523507120989,28.6041635476064));
#65198=CARTESIAN_POINT('Ctrl Pts',(31.0177834270861,-0.587617535604955,
28.645830214273));
#65199=CARTESIAN_POINT('Ctrl Pts',(31.3570445694482,-1.35453519623354E-14,
28.6874968809397));
#65200=CARTESIAN_POINT('Ctrl Pts',(31.0177834270861,0.587617535604927,28.7291635476064));
#65201=CARTESIAN_POINT('Ctrl Pts',(30.6785222847241,1.17523507120987,28.770830214273));
#65202=CARTESIAN_POINT('Ctrl Pts',(30.,1.17523507120987,28.8124968809397));
#65203=CARTESIAN_POINT('Ctrl Pts',(29.3214777152758,1.17523507120987,28.8541635476064));
#65204=CARTESIAN_POINT('Ctrl Pts',(28.9822165729138,0.587617535604928,28.895830214273));
#65205=CARTESIAN_POINT('Ctrl Pts',(28.6429554305518,-1.32141489532166E-14,
28.9374968809397));
#65206=CARTESIAN_POINT('Ctrl Pts',(28.9822165729138,-0.587617535604954,
28.9791635476064));
#65207=CARTESIAN_POINT('Ctrl Pts',(29.3214777152758,-1.17523507120989,29.020830214273));
#65208=CARTESIAN_POINT('Ctrl Pts',(30.,-1.17523507120989,29.0624968809397));
#65209=CARTESIAN_POINT('Ctrl Pts',(30.6785222847241,-1.17523507120989,29.1041635476064));
#65210=CARTESIAN_POINT('Ctrl Pts',(31.0177834270861,-0.587617535604955,
29.145830214273));
#65211=CARTESIAN_POINT('Ctrl Pts',(31.3570445694482,-1.35453519623354E-14,
29.1874968809397));
#65212=CARTESIAN_POINT('Ctrl Pts',(31.0177834270861,0.587617535604927,29.2291635476064));
#65213=CARTESIAN_POINT('Ctrl Pts',(30.6785222847241,1.17523507120987,29.270830214273));
#65214=CARTESIAN_POINT('Ctrl Pts',(30.,1.17523507120987,29.3124968809397));
#65215=CARTESIAN_POINT('Ctrl Pts',(29.3214777152758,1.17523507120987,29.3541635476064));
#65216=CARTESIAN_POINT('Ctrl Pts',(28.9822165729138,0.587617535604928,29.395830214273));
#65217=CARTESIAN_POINT('Ctrl Pts',(28.6429554305518,-1.32141489532166E-14,
29.4374968809397));
#65218=CARTESIAN_POINT('Ctrl Pts',(28.9822165729138,-0.587617535604954,
29.4791635476064));
#65219=CARTESIAN_POINT('Ctrl Pts',(29.3214777152758,-1.17523507120989,29.520830214273));
#65220=CARTESIAN_POINT('Ctrl Pts',(30.,-1.17523507120989,29.5624968809397));
#65221=CARTESIAN_POINT('Ctrl Pts',(30.6785222847241,-1.17523507120989,29.6041635476064));
#65222=CARTESIAN_POINT('Ctrl Pts',(31.0177834270861,-0.587617535604955,
29.645830214273));
#65223=CARTESIAN_POINT('Ctrl Pts',(31.3570445694482,-1.35453519623354E-14,
29.6874968809397));
#65224=CARTESIAN_POINT('Ctrl Pts',(31.0177834270861,0.587617535604927,29.7291635476064));
#65225=CARTESIAN_POINT('Ctrl Pts',(30.6785222847241,1.17523507120987,29.770830214273));
#65226=CARTESIAN_POINT('Ctrl Pts',(30.,1.17523507120987,29.8124968809397));
#65227=CARTESIAN_POINT('Ctrl Pts',(29.3214777152758,1.17523507120987,29.8541635476064));
#65228=CARTESIAN_POINT('Ctrl Pts',(28.9822165729138,0.587617535604928,29.895830214273));
#65229=CARTESIAN_POINT('Ctrl Pts',(28.6429554305518,-1.32141489532166E-14,
29.9374968809397));
#65230=CARTESIAN_POINT('Ctrl Pts',(28.9822165729138,-0.587617535604954,
29.9791635476064));
#65231=CARTESIAN_POINT('Ctrl Pts',(29.3214777152758,-1.17523507120989,30.020830214273));
#65232=CARTESIAN_POINT('Ctrl Pts',(30.,-1.17523507120989,30.0624968809397));
#65233=CARTESIAN_POINT('Ctrl Pts',(30.6785222847241,-1.17523507120989,30.1041635476064));
#65234=CARTESIAN_POINT('Ctrl Pts',(31.0177834270861,-0.587617535604955,
30.145830214273));
#65235=CARTESIAN_POINT('Ctrl Pts',(31.3570445694482,-1.35453519623354E-14,
30.1874968809397));
#65236=CARTESIAN_POINT('Ctrl Pts',(31.0177834270861,0.587617535604927,30.2291635476064));
#65237=CARTESIAN_POINT('Ctrl Pts',(30.6785222847241,1.17523507120987,30.270830214273));
#65238=CARTESIAN_POINT('Ctrl Pts',(30.,1.17523507120987,30.3124968809397));
#65239=CARTESIAN_POINT('Ctrl Pts',(29.3214777152758,1.17523507120987,30.3541635476064));
#65240=CARTESIAN_POINT('Ctrl Pts',(28.9822165729138,0.587617535604928,30.395830214273));
#65241=CARTESIAN_POINT('Ctrl Pts',(28.6429554305518,-1.32141489532166E-14,
30.4374968809397));
#65242=CARTESIAN_POINT('Ctrl Pts',(28.9822165729138,-0.587617535604954,
30.4791635476064));
#65243=CARTESIAN_POINT('Ctrl Pts',(29.3214777152758,-1.17523507120989,30.520830214273));
#65244=CARTESIAN_POINT('Ctrl Pts',(30.,-1.17523507120989,30.5624968809397));
#65245=CARTESIAN_POINT('Ctrl Pts',(30.6785222847241,-1.17523507120989,30.6041635476064));
#65246=CARTESIAN_POINT('Ctrl Pts',(31.0177834270861,-0.587617535604955,
30.645830214273));
#65247=CARTESIAN_POINT('Ctrl Pts',(31.3570445694482,-1.35453519623354E-14,
30.6874968809397));
#65248=CARTESIAN_POINT('Ctrl Pts',(31.0177834270861,0.587617535604927,30.7291635476064));
#65249=CARTESIAN_POINT('Ctrl Pts',(30.6785222847241,1.17523507120987,30.770830214273));
#65250=CARTESIAN_POINT('Ctrl Pts',(30.,1.17523507120987,30.8124968809397));
#65251=CARTESIAN_POINT('Ctrl Pts',(29.3214777152758,1.17523507120987,30.8541635476064));
#65252=CARTESIAN_POINT('Ctrl Pts',(28.9822165729138,0.587617535604928,30.895830214273));
#65253=CARTESIAN_POINT('Ctrl Pts',(28.6429554305518,-1.32141489532166E-14,
30.9374968809397));
#65254=CARTESIAN_POINT('Ctrl Pts',(28.9822165729138,-0.587617535604954,
30.9791635476064));
#65255=CARTESIAN_POINT('Ctrl Pts',(29.3214777152758,-1.17523507120989,31.020830214273));
#65256=CARTESIAN_POINT('Ctrl Pts',(30.,-1.17523507120989,31.0624968809397));
#65257=CARTESIAN_POINT('Ctrl Pts',(30.6785222847241,-1.17523507120989,31.1041635476064));
#65258=CARTESIAN_POINT('Ctrl Pts',(31.0177834270861,-0.587617535604955,
31.145830214273));
#65259=CARTESIAN_POINT('Ctrl Pts',(31.3570445694482,-1.35453519623354E-14,
31.1874968809397));
#65260=CARTESIAN_POINT('Ctrl Pts',(31.0177834270861,0.587617535604927,31.2291635476064));
#65261=CARTESIAN_POINT('Ctrl Pts',(30.6785222847241,1.17523507120987,31.270830214273));
#65262=CARTESIAN_POINT('Ctrl Pts',(30.,1.17523507120987,31.3124968809397));
#65263=CARTESIAN_POINT('',(30.,-1.50000000000002,30.75));
#65264=CARTESIAN_POINT('Origin',(30.,-1.24258096838242E-13,1029.88397459622));
#65265=CARTESIAN_POINT('Origin',(30.06875,2.82851012598683,15.7235432561772));
#65266=CARTESIAN_POINT('',(30.012548982272,2.70302030326666,15.7235432561772));
#65267=CARTESIAN_POINT('Origin',(30.,2.70864040503946,15.7235432561772));
#65268=CARTESIAN_POINT('',(29.987451017728,2.70302030326666,15.7235432561772));
#65269=CARTESIAN_POINT('Origin',(29.987451017728,2.70302030326666,15.7235432561772));
#65270=CARTESIAN_POINT('Origin',(30.2904604134361,2.81439671040465,15.7235432561772));
#65271=CARTESIAN_POINT('',(30.224586826676,2.69370321195774,15.7235432561772));
#65272=CARTESIAN_POINT('Origin',(30.2125174768313,2.70029057063376,15.7235432561772));
#65273=CARTESIAN_POINT('',(30.1995662307806,2.69567237556048,15.7235432561772));
#65274=CARTESIAN_POINT('Origin',(30.1995662307806,2.69567237556048,15.7235432561772));
#65275=CARTESIAN_POINT('Origin',(29.8466157199522,2.82518483606723,15.7235432561772));
#65276=CARTESIAN_POINT('',(29.8004337692194,2.69567237556048,15.7235432561772));
#65277=CARTESIAN_POINT('Origin',(29.7874825231687,2.70029057063376,15.7235432561772));
#65278=CARTESIAN_POINT('',(29.775413173324,2.69370321195775,15.7235432561772));
#65279=CARTESIAN_POINT('Origin',(29.775413173324,2.69370321195775,15.7235432561772));
#65280=CARTESIAN_POINT('Origin',(29.6254271049963,2.804441342164,15.7235432561772));
#65281=CARTESIAN_POINT('',(29.589548948342,2.67170473125694,15.7235432561772));
#65282=CARTESIAN_POINT('Origin',(29.5762752872513,2.67529254692237,15.7235432561772));
#65283=CARTESIAN_POINT('',(29.5647599813892,2.6677785445999,15.7235432561772));
#65284=CARTESIAN_POINT('Origin',(29.5647599813892,2.6677785445999,15.7235432561772));
#65285=CARTESIAN_POINT('Origin',(29.4065478564962,2.76640753481494,15.7235432561772));
#65286=CARTESIAN_POINT('',(29.3811946946869,2.63126513885323,15.7235432561772));
#65287=CARTESIAN_POINT('Origin',(29.3676804550908,2.63380045503416,15.7235432561772));
#65288=CARTESIAN_POINT('',(29.3567901889011,2.6254061353882,15.7235432561772));
#65289=CARTESIAN_POINT('Origin',(29.3567901889011,2.6254061353882,15.7235432561772));
#65290=CARTESIAN_POINT('Origin',(29.1913274378037,2.71131790508989,15.7235432561772));
#65291=CARTESIAN_POINT('',(29.1766555815128,2.57460292188403,15.7235432561772));
#65292=CARTESIAN_POINT('Origin',(29.1629840831922,2.57607010751313,15.7235432561772));
#65293=CARTESIAN_POINT('',(29.1527859987874,2.56684722431571,15.7235432561772));
#65294=CARTESIAN_POINT('Origin',(29.1527859987874,2.56684722431571,15.7235432561772));
#65295=CARTESIAN_POINT('Origin',(28.9810927543681,2.63951209887526,15.7235432561772));
#65296=CARTESIAN_POINT('',(28.9771926604684,2.50206742175908,15.7235432561772));
#65297=CARTESIAN_POINT('Origin',(28.9634481927567,2.50245743114905,15.7235432561772));
#65298=CARTESIAN_POINT('',(28.9540051647184,2.49246284654199,15.7235432561772));
#65299=CARTESIAN_POINT('Origin',(28.9540051647184,2.49246284654199,15.7235432561772));
#65300=CARTESIAN_POINT('Origin',(28.7771399729228,2.55143282284423,15.7235432561772));
#65301=CARTESIAN_POINT('Origin',(28.7616732366375,2.40271160649133,15.7235432561772));
#65302=CARTESIAN_POINT('Origin',(28.5807265301867,2.44762311502286,15.7235432561772));
#65303=CARTESIAN_POINT('Origin',(28.5769760048382,2.29814685040398,15.7235432561772));
#65304=CARTESIAN_POINT('Origin',(28.3930633803483,2.32872299678009,15.7235432561772));
#65305=CARTESIAN_POINT('Origin',(28.4010521891726,2.1794132547725,15.7235432561772));
#65306=CARTESIAN_POINT('Origin',(28.2153075291307,2.1954655268832,15.7235432561772));
#65307=CARTESIAN_POINT('Origin',(28.2349864184648,2.0472428516969,15.7235432561772));
#65308=CARTESIAN_POINT('Origin',(28.0485549004665,2.0486722819467,15.7235432561772));
#65309=CARTESIAN_POINT('Origin',(28.0798025434137,1.90245051566326,15.7235432561772));
#65310=CARTESIAN_POINT('Origin',(27.8938335797622,1.88924829113933,15.7235432561772));
#65311=CARTESIAN_POINT('Origin',(27.9364573242129,1.74592893957157,15.7235432561772));
#65312=CARTESIAN_POINT('Origin',(27.7520974754101,1.71817645637828,15.7235432561772));
#65313=CARTESIAN_POINT('Origin',(27.805834531806,1.57864313098712,15.7235432561772));
#65314=CARTESIAN_POINT('Origin',(27.6242204376256,1.53651149241201,15.7235432561772));
#65315=CARTESIAN_POINT('Origin',(27.6887394991445,1.40162446254803,15.7235432561772));
#65316=CARTESIAN_POINT('Origin',(27.5109908708699,1.3453734241531,15.7235432561772));
#65317=CARTESIAN_POINT('Origin',(27.5858941560429,1.2159643132099,15.7235432561772));
#65318=CARTESIAN_POINT('Origin',(30.5103800418355,2.78293160322096,15.7235432561772));
#65319=CARTESIAN_POINT('',(30.4352400186108,2.66777854459989,15.7235432561772));
#65320=CARTESIAN_POINT('Origin',(30.4237247127487,2.67529254692237,15.7235432561772));
#65321=CARTESIAN_POINT('',(30.410451051658,2.67170473125694,15.7235432561772));
#65322=CARTESIAN_POINT('Origin',(30.410451051658,2.67170473125694,15.7235432561772));
#65323=CARTESIAN_POINT('Origin',(30.7271530075584,2.73430879728474,15.7235432561772));
#65324=CARTESIAN_POINT('',(30.6432098110989,2.62540613538819,15.7235432561772));
#65325=CARTESIAN_POINT('Origin',(30.6323195449092,2.63380045503415,15.7235432561772));
#65326=CARTESIAN_POINT('',(30.6188053053131,2.63126513885322,15.7235432561772));
#65327=CARTESIAN_POINT('Origin',(30.6188053053131,2.63126513885322,15.7235432561772));
#65328=CARTESIAN_POINT('Origin',(30.9394428331868,2.66882806836332,15.7235432561772));
#65329=CARTESIAN_POINT('',(30.8472140012126,2.5668472243157,15.7235432561772));
#65330=CARTESIAN_POINT('Origin',(30.8370159168078,2.57607010751312,15.7235432561772));
#65331=CARTESIAN_POINT('',(30.8233444184872,2.57460292188402,15.7235432561772));
#65332=CARTESIAN_POINT('Origin',(30.8233444184872,2.57460292188402,15.7235432561772));
#65333=CARTESIAN_POINT('Origin',(31.1459406813522,2.58689312692505,15.7235432561772));
#65334=CARTESIAN_POINT('',(31.0459948352816,2.49246284654197,15.7235432561772));
#65335=CARTESIAN_POINT('Origin',(31.0365518072432,2.50245743114904,15.7235432561772));
#65336=CARTESIAN_POINT('',(31.0228073395316,2.50206742175906,15.7235432561772));
#65337=CARTESIAN_POINT('Origin',(31.0228073395316,2.50206742175906,15.7235432561772));
#65338=CARTESIAN_POINT('Origin',(31.3453734241531,2.48900912913003,15.7235432561772));
#65339=CARTESIAN_POINT('',(31.2383267633625,2.40271160649132,15.7235432561772));
#65340=CARTESIAN_POINT('Origin',(31.2296970110986,2.41341627257038,15.7235432561772));
#65341=CARTESIAN_POINT('',(31.2159643132099,2.41410584395711,15.7235432561772));
#65342=CARTESIAN_POINT('Origin',(31.2159643132099,2.41410584395711,15.7235432561772));
#65343=CARTESIAN_POINT('Origin',(31.536511492412,2.3757795623744,15.7235432561772));
#65344=CARTESIAN_POINT('',(31.4230239951618,2.29814685040396,15.7235432561772));
#65345=CARTESIAN_POINT('Origin',(31.4152607239647,2.30949560012898,15.7235432561772));
#65346=CARTESIAN_POINT('',(31.401624462548,2.3112605008555,15.7235432561772));
#65347=CARTESIAN_POINT('Origin',(31.401624462548,2.3112605008555,15.7235432561772));
#65348=CARTESIAN_POINT('Origin',(31.7181764563782,2.24790252458986,15.7235432561772));
#65349=CARTESIAN_POINT('',(31.5989478108274,2.17941325477248,15.7235432561772));
#65350=CARTESIAN_POINT('Origin',(31.5920988838457,2.19133611932756,15.7235432561772));
#65351=CARTESIAN_POINT('',(31.5786431309871,2.19416546819402,15.7235432561772));
#65352=CARTESIAN_POINT('Origin',(31.5786431309871,2.19416546819402,15.7235432561772));
#65353=CARTESIAN_POINT('Origin',(31.8892482911393,2.10616642023777,15.7235432561772));
#65354=CARTESIAN_POINT('',(31.7650135815352,2.04724285169688,15.7235432561772));
#65355=CARTESIAN_POINT('Origin',(31.7591212246811,2.05966632265728,15.7235432561772));
#65356=CARTESIAN_POINT('',(31.7459289395715,2.06354267578706,15.7235432561772));
#65357=CARTESIAN_POINT('Origin',(31.7459289395715,2.06354267578706,15.7235432561772));
#65358=CARTESIAN_POINT('Origin',(32.0486722819467,1.95144509953352,15.7235432561772));
#65359=CARTESIAN_POINT('',(31.9201974565863,1.90245051566323,15.7235432561772));
#65360=CARTESIAN_POINT('Origin',(31.9152979981993,1.91529799819927,15.7235432561772));
#65361=CARTESIAN_POINT('',(31.9024505156632,1.9201974565863,15.7235432561772));
#65362=CARTESIAN_POINT('Origin',(31.9024505156632,1.9201974565863,15.7235432561772));
#65363=CARTESIAN_POINT('Origin',(32.1954655268832,1.7846924708693,15.7235432561772));
#65364=CARTESIAN_POINT('',(32.0635426757871,1.74592893957153,15.7235432561772));
#65365=CARTESIAN_POINT('Origin',(32.0596663226573,1.75912122468115,15.7235432561772));
#65366=CARTESIAN_POINT('',(32.0472428516969,1.76501358153524,15.7235432561772));
#65367=CARTESIAN_POINT('Origin',(32.0472428516969,1.76501358153524,15.7235432561772));
#65368=CARTESIAN_POINT('Origin',(32.3287229967801,1.6069366196517,15.7235432561772));
#65369=CARTESIAN_POINT('',(32.194165468194,1.57864313098709,15.7235432561772));
#65370=CARTESIAN_POINT('Origin',(32.1913361193276,1.59209888384569,15.7235432561772));
#65371=CARTESIAN_POINT('',(32.1794132547725,1.59894781082743,15.7235432561772));
#65372=CARTESIAN_POINT('Origin',(32.1794132547725,1.59894781082743,15.7235432561772));
#65373=CARTESIAN_POINT('Origin',(32.4476231150228,1.41927346981329,15.7235432561772));
#65374=CARTESIAN_POINT('',(32.3112605008555,1.401624462548,15.7235432561772));
#65375=CARTESIAN_POINT('Origin',(32.309495600129,1.41526072396473,15.7235432561772));
#65376=CARTESIAN_POINT('',(32.298146850404,1.42302399516178,15.7235432561772));
#65377=CARTESIAN_POINT('Origin',(32.298146850404,1.42302399516178,15.7235432561772));
#65378=CARTESIAN_POINT('Origin',(32.5514328228442,1.22286002707717,15.7235432561772));
#65379=CARTESIAN_POINT('',(32.4141058439571,1.21596431320987,15.7235432561772));
#65380=CARTESIAN_POINT('Origin',(32.4134162725704,1.22969701109858,15.7235432561772));
#65381=CARTESIAN_POINT('',(32.4027116064913,1.23832676336245,15.7235432561772));
#65382=CARTESIAN_POINT('Origin',(32.4027116064913,1.23832676336245,15.7235432561772));
#65383=CARTESIAN_POINT('Origin',(32.6395120988752,1.01890724563189,15.7235432561772));
#65384=CARTESIAN_POINT('',(32.5020674217591,1.02280733953163,15.7235432561772));
#65385=CARTESIAN_POINT('Origin',(32.502457431149,1.03655180724325,15.7235432561772));
#65386=CARTESIAN_POINT('',(32.492462846542,1.04599483528156,15.7235432561772));
#65387=CARTESIAN_POINT('Origin',(32.492462846542,1.04599483528156,15.7235432561772));
#65388=CARTESIAN_POINT('Origin',(32.7113179050899,0.808672562196245,15.7235432561772));
#65389=CARTESIAN_POINT('',(32.574602921884,0.823344418487232,15.7235432561772));
#65390=CARTESIAN_POINT('Origin',(32.5760701075131,0.837015916807817,15.7235432561772));
#65391=CARTESIAN_POINT('',(32.5668472243157,0.84721400121258,15.7235432561772));
#65392=CARTESIAN_POINT('Origin',(32.5668472243157,0.84721400121258,15.7235432561772));
#65393=CARTESIAN_POINT('Origin',(32.7664075348149,0.593452143503749,15.7235432561772));
#65394=CARTESIAN_POINT('',(32.6312651388532,0.618805305313054,15.7235432561772));
#65395=CARTESIAN_POINT('Origin',(32.6338004550341,0.632319544909225,15.7235432561772));
#65396=CARTESIAN_POINT('',(32.6254061353882,0.64320981109888,15.7235432561772));
#65397=CARTESIAN_POINT('Origin',(32.6254061353882,0.64320981109888,15.7235432561772));
#65398=CARTESIAN_POINT('Origin',(32.804441342164,0.37457289500369,15.7235432561772));
#65399=CARTESIAN_POINT('',(32.6717047312569,0.410451051657977,15.7235432561772));
#65400=CARTESIAN_POINT('Origin',(32.6752925469224,0.423724712748682,15.7235432561772));
#65401=CARTESIAN_POINT('',(32.6677785445999,0.435240018610789,15.7235432561772));
#65402=CARTESIAN_POINT('Origin',(32.6677785445999,0.435240018610789,15.7235432561772));
#65403=CARTESIAN_POINT('Origin',(32.8251848360672,0.153384280047806,15.7235432561772));
#65404=CARTESIAN_POINT('',(32.6956723755605,0.199566230780603,15.7235432561772));
#65405=CARTESIAN_POINT('Origin',(32.7002905706337,0.212517476831278,15.7235432561772));
#65406=CARTESIAN_POINT('',(32.6937032119577,0.224586826675969,15.7235432561772));
#65407=CARTESIAN_POINT('Origin',(32.6937032119577,0.224586826675969,15.7235432561772));
#65408=CARTESIAN_POINT('Origin',(32.8285101259868,-0.0687500000000229,15.7235432561772));
#65409=CARTESIAN_POINT('',(32.7030203032667,-0.0125489822720396,15.7235432561772));
#65410=CARTESIAN_POINT('Origin',(32.7086404050395,-2.31188656783185E-14,
15.7235432561772));
#65411=CARTESIAN_POINT('',(32.7030203032667,0.0125489822719939,15.7235432561772));
#65412=CARTESIAN_POINT('Origin',(32.7030203032667,0.0125489822719939,15.7235432561772));
#65413=CARTESIAN_POINT('Origin',(32.8143967104046,-0.290460413436156,15.7235432561772));
#65414=CARTESIAN_POINT('',(32.6937032119577,-0.224586826676015,15.7235432561772));
#65415=CARTESIAN_POINT('Origin',(32.7002905706337,-0.212517476831324,15.7235432561772));
#65416=CARTESIAN_POINT('',(32.6956723755605,-0.199566230780649,15.7235432561772));
#65417=CARTESIAN_POINT('Origin',(32.6956723755605,-0.199566230780649,15.7235432561772));
#65418=CARTESIAN_POINT('Origin',(32.7829316032209,-0.510380041835567,15.7235432561772));
#65419=CARTESIAN_POINT('',(32.6677785445999,-0.435240018610835,15.7235432561772));
#65420=CARTESIAN_POINT('Origin',(32.6752925469224,-0.423724712748728,15.7235432561772));
#65421=CARTESIAN_POINT('',(32.6717047312569,-0.410451051658023,15.7235432561772));
#65422=CARTESIAN_POINT('Origin',(32.6717047312569,-0.410451051658023,15.7235432561772));
#65423=CARTESIAN_POINT('Origin',(32.7343087972847,-0.727153007558476,15.7235432561772));
#65424=CARTESIAN_POINT('',(32.6254061353882,-0.643209811098926,15.7235432561772));
#65425=CARTESIAN_POINT('Origin',(32.6338004550341,-0.632319544909271,15.7235432561772));
#65426=CARTESIAN_POINT('',(32.6312651388532,-0.6188053053131,15.7235432561772));
#65427=CARTESIAN_POINT('Origin',(32.6312651388532,-0.6188053053131,15.7235432561772));
#65428=CARTESIAN_POINT('Origin',(32.6688280683633,-0.939442833186874,15.7235432561772));
#65429=CARTESIAN_POINT('',(32.5668472243157,-0.847214001212625,15.7235432561772));
#65430=CARTESIAN_POINT('Origin',(32.5760701075131,-0.837015916807863,15.7235432561772));
#65431=CARTESIAN_POINT('',(32.574602921884,-0.823344418487278,15.7235432561772));
#65432=CARTESIAN_POINT('Origin',(32.574602921884,-0.823344418487278,15.7235432561772));
#65433=CARTESIAN_POINT('Origin',(32.586893126925,-1.14594068135223,15.7235432561772));
#65434=CARTESIAN_POINT('',(32.492462846542,-1.0459948352816,15.7235432561772));
#65435=CARTESIAN_POINT('Origin',(32.502457431149,-1.0365518072433,15.7235432561772));
#65436=CARTESIAN_POINT('',(32.5020674217591,-1.02280733953168,15.7235432561772));
#65437=CARTESIAN_POINT('Origin',(32.5020674217591,-1.02280733953168,15.7235432561772));
#65438=CARTESIAN_POINT('Origin',(32.48900912913,-1.34537342415311,15.7235432561772));
#65439=CARTESIAN_POINT('',(32.4027116064913,-1.2383267633625,15.7235432561772));
#65440=CARTESIAN_POINT('Origin',(32.4134162725704,-1.22969701109862,15.7235432561772));
#65441=CARTESIAN_POINT('',(32.4141058439571,-1.21596431320991,15.7235432561772));
#65442=CARTESIAN_POINT('Origin',(32.4141058439571,-1.21596431320991,15.7235432561772));
#65443=CARTESIAN_POINT('Origin',(32.3757795623744,-1.53651149241202,15.7235432561772));
#65444=CARTESIAN_POINT('',(32.2981468504039,-1.42302399516182,15.7235432561772));
#65445=CARTESIAN_POINT('Origin',(32.309495600129,-1.41526072396478,15.7235432561772));
#65446=CARTESIAN_POINT('',(32.3112605008555,-1.40162446254804,15.7235432561772));
#65447=CARTESIAN_POINT('Origin',(32.3112605008555,-1.40162446254804,15.7235432561772));
#65448=CARTESIAN_POINT('Origin',(32.2479025245898,-1.71817645637829,15.7235432561772));
#65449=CARTESIAN_POINT('',(32.1794132547725,-1.59894781082747,15.7235432561772));
#65450=CARTESIAN_POINT('Origin',(32.1913361193275,-1.59209888384574,15.7235432561772));
#65451=CARTESIAN_POINT('',(32.194165468194,-1.57864313098713,15.7235432561772));
#65452=CARTESIAN_POINT('Origin',(32.194165468194,-1.57864313098713,15.7235432561772));
#65453=CARTESIAN_POINT('Origin',(32.1061664202378,-1.88924829113934,15.7235432561772));
#65454=CARTESIAN_POINT('',(32.0472428516969,-1.76501358153528,15.7235432561772));
#65455=CARTESIAN_POINT('Origin',(32.0596663226573,-1.75912122468119,15.7235432561772));
#65456=CARTESIAN_POINT('',(32.063542675787,-1.74592893957158,15.7235432561772));
#65457=CARTESIAN_POINT('Origin',(32.063542675787,-1.74592893957158,15.7235432561772));
#65458=CARTESIAN_POINT('Origin',(31.9514450995335,-2.04867228194671,15.7235432561772));
#65459=CARTESIAN_POINT('',(31.9024505156632,-1.92019745658634,15.7235432561772));
#65460=CARTESIAN_POINT('Origin',(31.9152979981993,-1.91529799819931,15.7235432561772));
#65461=CARTESIAN_POINT('',(31.9201974565863,-1.90245051566327,15.7235432561772));
#65462=CARTESIAN_POINT('Origin',(31.9201974565863,-1.90245051566327,15.7235432561772));
#65463=CARTESIAN_POINT('Origin',(31.7846924708693,-2.19546552688321,15.7235432561772));
#65464=CARTESIAN_POINT('',(31.7459289395715,-2.0635426757871,15.7235432561772));
#65465=CARTESIAN_POINT('Origin',(31.7591212246811,-2.05966632265732,15.7235432561772));
#65466=CARTESIAN_POINT('',(31.7650135815352,-2.04724285169692,15.7235432561772));
#65467=CARTESIAN_POINT('Origin',(31.7650135815352,-2.04724285169692,15.7235432561772));
#65468=CARTESIAN_POINT('Origin',(31.6069366196517,-2.32872299678011,15.7235432561772));
#65469=CARTESIAN_POINT('',(31.5786431309871,-2.19416546819406,15.7235432561772));
#65470=CARTESIAN_POINT('Origin',(31.5920988838457,-2.1913361193276,15.7235432561772));
#65471=CARTESIAN_POINT('',(31.5989478108274,-2.17941325477251,15.7235432561772));
#65472=CARTESIAN_POINT('Origin',(31.5989478108274,-2.17941325477251,15.7235432561772));
#65473=CARTESIAN_POINT('Origin',(31.4192734698133,-2.44762311502288,15.7235432561772));
#65474=CARTESIAN_POINT('',(31.401624462548,-2.31126050085554,15.7235432561772));
#65475=CARTESIAN_POINT('Origin',(31.4152607239647,-2.30949560012901,15.7235432561772));
#65476=CARTESIAN_POINT('',(31.4230239951618,-2.29814685040399,15.7235432561772));
#65477=CARTESIAN_POINT('Origin',(31.4230239951618,-2.29814685040399,15.7235432561772));
#65478=CARTESIAN_POINT('Origin',(31.2228600270771,-2.55143282284425,15.7235432561772));
#65479=CARTESIAN_POINT('',(31.2159643132098,-2.41410584395714,15.7235432561772));
#65480=CARTESIAN_POINT('Origin',(31.2296970110986,-2.41341627257041,15.7235432561772));
#65481=CARTESIAN_POINT('',(31.2383267633624,-2.40271160649135,15.7235432561772));
#65482=CARTESIAN_POINT('Origin',(31.2383267633624,-2.40271160649135,15.7235432561772));
#65483=CARTESIAN_POINT('Origin',(31.0189072456319,-2.63951209887528,15.7235432561772));
#65484=CARTESIAN_POINT('',(31.0228073395316,-2.5020674217591,15.7235432561772));
#65485=CARTESIAN_POINT('Origin',(31.0365518072432,-2.50245743114907,15.7235432561772));
#65486=CARTESIAN_POINT('',(31.0459948352815,-2.49246284654201,15.7235432561772));
#65487=CARTESIAN_POINT('Origin',(31.0459948352815,-2.49246284654201,15.7235432561772));
#65488=CARTESIAN_POINT('Origin',(30.8086725621962,-2.71131790508991,15.7235432561772));
#65489=CARTESIAN_POINT('',(30.8233444184872,-2.57460292188405,15.7235432561772));
#65490=CARTESIAN_POINT('Origin',(30.8370159168078,-2.57607010751315,15.7235432561772));
#65491=CARTESIAN_POINT('',(30.8472140012126,-2.56684722431573,15.7235432561772));
#65492=CARTESIAN_POINT('Origin',(30.8472140012126,-2.56684722431573,15.7235432561772));
#65493=CARTESIAN_POINT('Origin',(30.5934521435037,-2.76640753481496,15.7235432561772));
#65494=CARTESIAN_POINT('',(30.618805305313,-2.63126513885325,15.7235432561772));
#65495=CARTESIAN_POINT('Origin',(30.6323195449092,-2.63380045503418,15.7235432561772));
#65496=CARTESIAN_POINT('',(30.6432098110989,-2.62540613538822,15.7235432561772));
#65497=CARTESIAN_POINT('Origin',(30.6432098110989,-2.62540613538822,15.7235432561772));
#65498=CARTESIAN_POINT('Origin',(30.3745728950037,-2.80444134216402,15.7235432561772));
#65499=CARTESIAN_POINT('',(30.410451051658,-2.67170473125697,15.7235432561772));
#65500=CARTESIAN_POINT('Origin',(30.4237247127487,-2.67529254692239,15.7235432561772));
#65501=CARTESIAN_POINT('',(30.4352400186108,-2.66777854459992,15.7235432561772));
#65502=CARTESIAN_POINT('Origin',(30.4352400186108,-2.66777854459992,15.7235432561772));
#65503=CARTESIAN_POINT('Origin',(30.1533842800478,-2.82518483606726,15.7235432561772));
#65504=CARTESIAN_POINT('',(30.1995662307806,-2.69567237556051,15.7235432561772));
#65505=CARTESIAN_POINT('Origin',(30.2125174768313,-2.70029057063379,15.7235432561772));
#65506=CARTESIAN_POINT('',(30.224586826676,-2.69370321195777,15.7235432561772));
#65507=CARTESIAN_POINT('Origin',(30.224586826676,-2.69370321195777,15.7235432561772));
#65508=CARTESIAN_POINT('Origin',(29.93125,-2.82851012598686,15.7235432561772));
#65509=CARTESIAN_POINT('',(29.987451017728,-2.70302030326669,15.7235432561772));
#65510=CARTESIAN_POINT('Origin',(30.,-2.70864040503949,15.7235432561772));
#65511=CARTESIAN_POINT('',(30.012548982272,-2.70302030326669,15.7235432561772));
#65512=CARTESIAN_POINT('Origin',(30.012548982272,-2.70302030326669,15.7235432561772));
#65513=CARTESIAN_POINT('Origin',(29.7095395865638,-2.81439671040468,15.7235432561772));
#65514=CARTESIAN_POINT('',(29.775413173324,-2.69370321195777,15.7235432561772));
#65515=CARTESIAN_POINT('Origin',(29.7874825231687,-2.70029057063378,15.7235432561772));
#65516=CARTESIAN_POINT('',(29.8004337692193,-2.6956723755605,15.7235432561772));
#65517=CARTESIAN_POINT('Origin',(29.8004337692193,-2.6956723755605,15.7235432561772));
#65518=CARTESIAN_POINT('Origin',(29.4896199581644,-2.78293160322098,15.7235432561772));
#65519=CARTESIAN_POINT('',(29.5647599813891,-2.66777854459992,15.7235432561772));
#65520=CARTESIAN_POINT('Origin',(29.5762752872513,-2.67529254692239,15.7235432561772));
#65521=CARTESIAN_POINT('',(29.589548948342,-2.67170473125696,15.7235432561772));
#65522=CARTESIAN_POINT('Origin',(29.589548948342,-2.67170473125696,15.7235432561772));
#65523=CARTESIAN_POINT('Origin',(29.2728469924415,-2.73430879728476,15.7235432561772));
#65524=CARTESIAN_POINT('',(29.3567901889011,-2.62540613538822,15.7235432561772));
#65525=CARTESIAN_POINT('Origin',(29.3676804550907,-2.63380045503417,15.7235432561772));
#65526=CARTESIAN_POINT('',(29.3811946946869,-2.63126513885324,15.7235432561772));
#65527=CARTESIAN_POINT('Origin',(29.3811946946869,-2.63126513885324,15.7235432561772));
#65528=CARTESIAN_POINT('Origin',(29.0605571668131,-2.66882806836334,15.7235432561772));
#65529=CARTESIAN_POINT('',(29.1527859987874,-2.56684722431572,15.7235432561772));
#65530=CARTESIAN_POINT('Origin',(29.1629840831921,-2.57607010751314,15.7235432561772));
#65531=CARTESIAN_POINT('',(29.1766555815127,-2.57460292188404,15.7235432561772));
#65532=CARTESIAN_POINT('Origin',(29.1766555815127,-2.57460292188404,15.7235432561772));
#65533=CARTESIAN_POINT('Origin',(28.8540593186477,-2.58689312692507,15.7235432561772));
#65534=CARTESIAN_POINT('',(28.9540051647184,-2.49246284654199,15.7235432561772));
#65535=CARTESIAN_POINT('Origin',(28.9634481927567,-2.50245743114906,15.7235432561772));
#65536=CARTESIAN_POINT('',(28.9771926604683,-2.50206742175908,15.7235432561772));
#65537=CARTESIAN_POINT('Origin',(28.9771926604683,-2.50206742175908,15.7235432561772));
#65538=CARTESIAN_POINT('Origin',(28.6546265758469,-2.48900912913005,15.7235432561772));
#65539=CARTESIAN_POINT('',(28.7616732366375,-2.40271160649133,15.7235432561772));
#65540=CARTESIAN_POINT('Origin',(28.7703029889014,-2.4134162725704,15.7235432561772));
#65541=CARTESIAN_POINT('',(28.7840356867901,-2.41410584395713,15.7235432561772));
#65542=CARTESIAN_POINT('Origin',(28.7840356867901,-2.41410584395713,15.7235432561772));
#65543=CARTESIAN_POINT('Origin',(28.463488507588,-2.37577956237441,15.7235432561772));
#65544=CARTESIAN_POINT('',(28.5769760048382,-2.29814685040397,15.7235432561772));
#65545=CARTESIAN_POINT('Origin',(28.5847392760352,-2.30949560012899,15.7235432561772));
#65546=CARTESIAN_POINT('',(28.5983755374519,-2.31126050085552,15.7235432561772));
#65547=CARTESIAN_POINT('Origin',(28.5983755374519,-2.31126050085552,15.7235432561772));
#65548=CARTESIAN_POINT('Origin',(28.2818235436217,-2.24790252458987,15.7235432561772));
#65549=CARTESIAN_POINT('',(28.4010521891725,-2.17941325477249,15.7235432561772));
#65550=CARTESIAN_POINT('Origin',(28.4079011161542,-2.19133611932757,15.7235432561772));
#65551=CARTESIAN_POINT('',(28.4213568690129,-2.19416546819403,15.7235432561772));
#65552=CARTESIAN_POINT('Origin',(28.4213568690129,-2.19416546819403,15.7235432561772));
#65553=CARTESIAN_POINT('Origin',(28.1107517088606,-2.10616642023779,15.7235432561772));
#65554=CARTESIAN_POINT('',(28.2349864184647,-2.04724285169689,15.7235432561772));
#65555=CARTESIAN_POINT('Origin',(28.2408787753188,-2.0596663226573,15.7235432561772));
#65556=CARTESIAN_POINT('',(28.2540710604284,-2.06354267578707,15.7235432561772));
#65557=CARTESIAN_POINT('Origin',(28.2540710604284,-2.06354267578707,15.7235432561772));
#65558=CARTESIAN_POINT('Origin',(27.9513277180533,-1.95144509953353,15.7235432561772));
#65559=CARTESIAN_POINT('',(28.0798025434136,-1.90245051566325,15.7235432561772));
#65560=CARTESIAN_POINT('Origin',(28.0847020018007,-1.91529799819928,15.7235432561772));
#65561=CARTESIAN_POINT('',(28.0975494843367,-1.92019745658631,15.7235432561772));
#65562=CARTESIAN_POINT('Origin',(28.0975494843367,-1.92019745658631,15.7235432561772));
#65563=CARTESIAN_POINT('Origin',(27.8045344731168,-1.78469247086931,15.7235432561772));
#65564=CARTESIAN_POINT('',(27.9364573242129,-1.74592893957155,15.7235432561772));
#65565=CARTESIAN_POINT('Origin',(27.9403336773427,-1.75912122468116,15.7235432561772));
#65566=CARTESIAN_POINT('',(27.9527571483031,-1.76501358153525,15.7235432561772));
#65567=CARTESIAN_POINT('Origin',(27.9527571483031,-1.76501358153525,15.7235432561772));
#65568=CARTESIAN_POINT('Origin',(27.6712770032199,-1.6069366196517,15.7235432561772));
#65569=CARTESIAN_POINT('',(27.8058345318059,-1.5786431309871,15.7235432561772));
#65570=CARTESIAN_POINT('Origin',(27.8086638806724,-1.59209888384571,15.7235432561772));
#65571=CARTESIAN_POINT('',(27.8205867452275,-1.59894781082744,15.7235432561772));
#65572=CARTESIAN_POINT('Origin',(27.8205867452275,-1.59894781082744,15.7235432561772));
#65573=CARTESIAN_POINT('Origin',(27.5523768849771,-1.4192734698133,15.7235432561772));
#65574=CARTESIAN_POINT('',(27.6887394991444,-1.40162446254801,15.7235432561772));
#65575=CARTESIAN_POINT('Origin',(27.690504399871,-1.41526072396474,15.7235432561772));
#65576=CARTESIAN_POINT('',(27.701853149596,-1.42302399516179,15.7235432561772));
#65577=CARTESIAN_POINT('Origin',(27.701853149596,-1.42302399516179,15.7235432561772));
#65578=CARTESIAN_POINT('Origin',(27.4485671771557,-1.22286002707717,15.7235432561772));
#65579=CARTESIAN_POINT('',(27.5858941560428,-1.21596431320988,15.7235432561772));
#65580=CARTESIAN_POINT('Origin',(27.5865837274296,-1.22969701109859,15.7235432561772));
#65581=CARTESIAN_POINT('',(27.5972883935086,-1.23832676336246,15.7235432561772));
#65582=CARTESIAN_POINT('Origin',(27.5972883935086,-1.23832676336246,15.7235432561772));
#65583=CARTESIAN_POINT('Origin',(27.3604879011247,-1.01890724563189,15.7235432561772));
#65584=CARTESIAN_POINT('',(27.4979325782409,-1.02280733953164,15.7235432561772));
#65585=CARTESIAN_POINT('Origin',(27.4975425688509,-1.03655180724326,15.7235432561772));
#65586=CARTESIAN_POINT('',(27.507537153458,-1.04599483528157,15.7235432561772));
#65587=CARTESIAN_POINT('Origin',(27.507537153458,-1.04599483528157,15.7235432561772));
#65588=CARTESIAN_POINT('Origin',(27.2886820949101,-0.808672562196254,15.7235432561772));
#65589=CARTESIAN_POINT('',(27.4253970781159,-0.823344418487241,15.7235432561772));
#65590=CARTESIAN_POINT('Origin',(27.4239298924868,-0.837015916807826,15.7235432561772));
#65591=CARTESIAN_POINT('',(27.4331527756843,-0.847214001212589,15.7235432561772));
#65592=CARTESIAN_POINT('Origin',(27.4331527756843,-0.847214001212589,15.7235432561772));
#65593=CARTESIAN_POINT('Origin',(27.233592465185,-0.593452143503757,15.7235432561772));
#65594=CARTESIAN_POINT('',(27.3687348611467,-0.618805305313063,15.7235432561772));
#65595=CARTESIAN_POINT('Origin',(27.3661995449658,-0.632319544909233,15.7235432561772));
#65596=CARTESIAN_POINT('',(27.3745938646118,-0.643209811098888,15.7235432561772));
#65597=CARTESIAN_POINT('Origin',(27.3745938646118,-0.643209811098888,15.7235432561772));
#65598=CARTESIAN_POINT('Origin',(27.195558657836,-0.374572895003696,15.7235432561772));
#65599=CARTESIAN_POINT('',(27.328295268743,-0.410451051657984,15.7235432561772));
#65600=CARTESIAN_POINT('Origin',(27.3247074530776,-0.423724712748689,15.7235432561772));
#65601=CARTESIAN_POINT('',(27.3322214554001,-0.435240018610796,15.7235432561772));
#65602=CARTESIAN_POINT('Origin',(27.3322214554001,-0.435240018610796,15.7235432561772));
#65603=CARTESIAN_POINT('Origin',(27.1748151639327,-0.153384280047813,15.7235432561772));
#65604=CARTESIAN_POINT('',(27.3043276244395,-0.199566230780611,15.7235432561772));
#65605=CARTESIAN_POINT('Origin',(27.2997094293662,-0.212517476831286,15.7235432561772));
#65606=CARTESIAN_POINT('',(27.3062967880422,-0.224586826675978,15.7235432561772));
#65607=CARTESIAN_POINT('Origin',(27.3062967880422,-0.224586826675978,15.7235432561772));
#65608=CARTESIAN_POINT('Origin',(27.1714898740131,0.068750000000016,15.7235432561772));
#65609=CARTESIAN_POINT('Origin',(27.2969796967333,-0.0125489822720016,15.7235432561772));
#65610=CARTESIAN_POINT('Origin',(27.1856032895953,0.29046041343615,15.7235432561772));
#65611=CARTESIAN_POINT('Origin',(27.3043276244395,0.199566230780642,15.7235432561772));
#65612=CARTESIAN_POINT('Origin',(27.217068396779,0.510380041835561,15.7235432561772));
#65613=CARTESIAN_POINT('Origin',(27.328295268743,0.410451051658016,15.7235432561772));
#65614=CARTESIAN_POINT('Origin',(27.2656912027152,0.727153007558468,15.7235432561772));
#65615=CARTESIAN_POINT('Origin',(27.3687348611468,0.618805305313091,15.7235432561772));
#65616=CARTESIAN_POINT('Origin',(27.3311719316367,0.939442833186866,15.7235432561772));
#65617=CARTESIAN_POINT('Origin',(27.4253970781159,0.823344418487269,15.7235432561772));
#65618=CARTESIAN_POINT('Origin',(27.4131068730749,1.14594068135223,15.7235432561772));
#65619=CARTESIAN_POINT('Origin',(27.4979325782409,1.02280733953167,15.7235432561772));
#75324=UNCERTAINTY_MEASURE_WITH_UNIT(LENGTH_MEASURE(0.01),#75337,
'DISTANCE_ACCURACY_VALUE',
'Maximum model space distance between geometric entities at asserted c
onnectivities');
#75326=UNCERTAINTY_MEASURE_WITH_UNIT(LENGTH_MEASURE(0.01),#75337,
'DISTANCE_ACCURACY_VALUE',
'Maximum model space distance between geometric entities at asserted c
onnectivities');
#75334=(
GEOMETRIC_REPRESENTATION_CONTEXT(3)
GLOBAL_UNCERTAINTY_ASSIGNED_CONTEXT((#75324))
GLOBAL_UNIT_ASSIGNED_CONTEXT((#75337,#75339,#75340))
REPRESENTATION_CONTEXT('','3D')
);
#75336=(
GEOMETRIC_REPRESENTATION_CONTEXT(3)
GLOBAL_UNCERTAINTY_ASSIGNED_CONTEXT((#75326))
GLOBAL_UNIT_ASSIGNED_CONTEXT((#75337,#75339,#75340))
REPRESENTATION_CONTEXT('','3D')
);
#75337=(
LENGTH_UNIT()
NAMED_UNIT(*)
SI_UNIT(.MILLI.,.METRE.)
);
#75339=(
NAMED_UNIT(*)
PLANE_ANGLE_UNIT()
SI_UNIT($,.RADIAN.)
);
#75340=(
NAMED_UNIT(*)
SI_UNIT($,.STERADIAN.)
SOLID_ANGLE_UNIT()
);
#75348=SHAPE_DEFINITION_REPRESENTATION(#75357,#75374);
#75357=PRODUCT_DEFINITION_SHAPE('',$,#75384);
#75374=SHAPE_REPRESENTATION('',(#33577),#75334);
#75376=PRODUCT_DEFINITION_CONTEXT('part definition',#75405,'design');
#75384=PRODUCT_DEFINITION('Screw_02','Screw_02',#75393,#75376);
#75393=PRODUCT_DEFINITION_FORMATION('',$,#75414);
#75405=APPLICATION_CONTEXT(
'Core Data for Automotive Mechanical Design Process');
#75406=PRODUCT_CONTEXT('part definition',#75405,'mechanical');
#75414=PRODUCT('Screw_02','Screw_02',$,(#75406));
#75419=PRESENTATION_STYLE_ASSIGNMENT((#75423));
#75423=SURFACE_STYLE_USAGE(.BOTH.,#75427);
#75427=SURFACE_SIDE_STYLE('',(#75431));
#75431=SURFACE_STYLE_FILL_AREA(#75435);
#75435=FILL_AREA_STYLE('Opaque(86,86,86)',(#75439));
#75439=FILL_AREA_STYLE_COLOUR('Opaque(86,86,86)',#75443);
#75443=COLOUR_RGB('Opaque(86,86,86)', 0.08235294, 0.09019608, 0.10196078);
ENDSEC;
END-ISO-10303-21;
